ISO-10303-21;
HEADER;
/* Generated by software containing ST-Developer
 * from STEP Tools, Inc. (www.steptools.com) 
 */

FILE_DESCRIPTION(
/* description */ (''),
/* implementation_level */ '2;1');

FILE_NAME(
/* name */ 'Screw.step',
/* time_stamp */ '2026-10-05T16:20:14-07:00',
/* author */ (''),
/* organization */ (''),
/* preprocessor_version */ 'ST-DEVELOPER v20.2',
/* originating_system */ 'Autodesk Translation Framework v15.15.0.0',
/* authorisation */ '');

FILE_SCHEMA (('AUTOMOTIVE_DESIGN { 1 0 10303 214 3 1 1 }'));
ENDSEC;

DATA;
#10=MECHANICAL_DESIGN_GEOMETRIC_PRESENTATION_REPRESENTATION('',(#251),#23577);
#51=CONICAL_SURFACE('',#4468,5.14028464662889,1.31156275926766);
#52=CONICAL_SURFACE('',#4470,6.05319927020769,0.239535482048054);
#53=B_SPLINE_SURFACE_WITH_KNOTS('',3,3,((#19950,#19951,#19952,#19953,#19954,
#19955,#19956,#19957,#19958,#19959,#19960,#19961,#19962,#19963,#19964,#19965,
#19966,#19967,#19968,#19969,#19970,#19971,#19972,#19973,#19974,#19975,#19976,
#19977,#19978,#19979,#19980,#19981,#19982,#19983,#19984,#19985,#19986,#19987,
#19988,#19989,#19990,#19991,#19992,#19993,#19994,#19995,#19996,#19997,#19998,
#19999,#20000,#20001,#20002,#20003,#20004,#20005,#20006,#20007,#20008,#20009,
#20010,#20011,#20012,#20013,#20014,#20015,#20016,#20017,#20018,#20019,#20020,
#20021,#20022,#20023,#20024,#20025,#20026,#20027,#20028,#20029,#20030,#20031,
#20032,#20033,#20034,#20035,#20036,#20037,#20038,#20039,#20040,#20041,#20042,
#20043,#20044,#20045,#20046,#20047,#20048,#20049,#20050,#20051,#20052,#20053,
#20054,#20055,#20056,#20057,#20058,#20059,#20060,#20061,#20062,#20063,#20064,
#20065,#20066,#20067,#20068,#20069,#20070,#20071,#20072,#20073,#20074,#20075,
#20076,#20077,#20078,#20079,#20080,#20081,#20082,#20083,#20084,#20085,#20086,
#20087,#20088,#20089,#20090,#20091,#20092,#20093,#20094,#20095,#20096),
(#20097,#20098,#20099,#20100,#20101,#20102,#20103,#20104,#20105,#20106,
#20107,#20108,#20109,#20110,#20111,#20112,#20113,#20114,#20115,#20116,#20117,
#20118,#20119,#20120,#20121,#20122,#20123,#20124,#20125,#20126,#20127,#20128,
#20129,#20130,#20131,#20132,#20133,#20134,#20135,#20136,#20137,#20138,#20139,
#20140,#20141,#20142,#20143,#20144,#20145,#20146,#20147,#20148,#20149,#20150,
#20151,#20152,#20153,#20154,#20155,#20156,#20157,#20158,#20159,#20160,#20161,
#20162,#20163,#20164,#20165,#20166,#20167,#20168,#20169,#20170,#20171,#20172,
#20173,#20174,#20175,#20176,#20177,#20178,#20179,#20180,#20181,#20182,#20183,
#20184,#20185,#20186,#20187,#20188,#20189,#20190,#20191,#20192,#20193,#20194,
#20195,#20196,#20197,#20198,#20199,#20200,#20201,#20202,#20203,#20204,#20205,
#20206,#20207,#20208,#20209,#20210,#20211,#20212,#20213,#20214,#20215,#20216,
#20217,#20218,#20219,#20220,#20221,#20222,#20223,#20224,#20225,#20226,#20227,
#20228,#20229,#20230,#20231,#20232,#20233,#20234,#20235,#20236,#20237,#20238,
#20239,#20240,#20241,#20242,#20243),(#20244,#20245,#20246,#20247,#20248,
#20249,#20250,#20251,#20252,#20253,#20254,#20255,#20256,#20257,#20258,#20259,
#20260,#20261,#20262,#20263,#20264,#20265,#20266,#20267,#20268,#20269,#20270,
#20271,#20272,#20273,#20274,#20275,#20276,#20277,#20278,#20279,#20280,#20281,
#20282,#20283,#20284,#20285,#20286,#20287,#20288,#20289,#20290,#20291,#20292,
#20293,#20294,#20295,#20296,#20297,#20298,#20299,#20300,#20301,#20302,#20303,
#20304,#20305,#20306,#20307,#20308,#20309,#20310,#20311,#20312,#20313,#20314,
#20315,#20316,#20317,#20318,#20319,#20320,#20321,#20322,#20323,#20324,#20325,
#20326,#20327,#20328,#20329,#20330,#20331,#20332,#20333,#20334,#20335,#20336,
#20337,#20338,#20339,#20340,#20341,#20342,#20343,#20344,#20345,#20346,#20347,
#20348,#20349,#20350,#20351,#20352,#20353,#20354,#20355,#20356,#20357,#20358,
#20359,#20360,#20361,#20362,#20363,#20364,#20365,#20366,#20367,#20368,#20369,
#20370,#20371,#20372,#20373,#20374,#20375,#20376,#20377,#20378,#20379,#20380,
#20381,#20382,#20383,#20384,#20385,#20386,#20387,#20388,#20389,#20390),
(#20391,#20392,#20393,#20394,#20395,#20396,#20397,#20398,#20399,#20400,
#20401,#20402,#20403,#20404,#20405,#20406,#20407,#20408,#20409,#20410,#20411,
#20412,#20413,#20414,#20415,#20416,#20417,#20418,#20419,#20420,#20421,#20422,
#20423,#20424,#20425,#20426,#20427,#20428,#20429,#20430,#20431,#20432,#20433,
#20434,#20435,#20436,#20437,#20438,#20439,#20440,#20441,#20442,#20443,#20444,
#20445,#20446,#20447,#20448,#20449,#20450,#20451,#20452,#20453,#20454,#20455,
#20456,#20457,#20458,#20459,#20460,#20461,#20462,#20463,#20464,#20465,#20466,
#20467,#20468,#20469,#20470,#20471,#20472,#20473,#20474,#20475,#20476,#20477,
#20478,#20479,#20480,#20481,#20482,#20483,#20484,#20485,#20486,#20487,#20488,
#20489,#20490,#20491,#20492,#20493,#20494,#20495,#20496,#20497,#20498,#20499,
#20500,#20501,#20502,#20503,#20504,#20505,#20506,#20507,#20508,#20509,#20510,
#20511,#20512,#20513,#20514,#20515,#20516,#20517,#20518,#20519,#20520,#20521,
#20522,#20523,#20524,#20525,#20526,#20527,#20528,#20529,#20530,#20531,#20532,
#20533,#20534,#20535,#20536,#20537)),.UNSPECIFIED.,.F.,.F.,.F.,(4,4),(4,
1,1,1,1,1,1,1,1,1,1,1,1,1,1,1,1,1,1,1,1,1,1,1,1,1,1,1,1,1,1,1,1,1,1,1,1,
1,1,1,1,1,1,1,1,1,1,1,1,1,1,1,1,1,1,1,1,1,1,1,1,1,1,1,1,1,1,1,1,1,1,1,1,
1,1,1,1,1,1,1,1,1,1,1,1,1,1,1,1,1,1,1,1,1,1,1,1,1,1,1,1,1,1,1,1,1,1,1,1,
1,1,1,1,1,1,1,1,1,1,1,1,1,1,1,1,1,1,1,1,1,1,1,1,1,1,1,1,1,1,1,1,1,1,1,4),
(-0.000407634560164902,0.0529903850324167),(8.30815772716265,9.30425680398324,
10.3003558808038,11.2964549576244,12.292554034445,13.2886531112656,14.2847521880862,
15.2808512649068,16.2769503417274,17.273049418548,18.2691484953686,19.2652475721892,
20.2613466490097,21.2574457258303,22.2535448026509,23.2496438794715,24.2457429562921,
25.2418420331127,26.2379411099333,27.2340401867539,28.2301392635745,29.2262383403951,
30.2223374172156,31.2184364940362,32.2145355708568,33.2106346476774,34.206733724498,
35.2028328013186,36.1989318781392,37.1950309549598,38.1911300317804,39.187229108601,
40.1833281854216,41.1794272622421,42.1755263390627,43.1716254158833,44.1677244927039,
45.1638235695245,46.1599226463451,47.1560217231657,48.1521207999863,49.1482198768069,
50.1443189536275,51.1404180304481,52.1365171072686,53.1326161840892,54.1287152609098,
55.1248143377304,56.120913414551,57.1170124913716,58.1131115681922,59.1092106450128,
60.1053097218334,61.101408798654,62.0975078754745,63.0936069522951,64.0897060291157,
65.0858051059363,66.0819041827569,67.0780032595775,68.0741023363981,69.0702014132187,
70.0663004900393,71.0623995668599,72.0584986436805,73.0545977205011,74.0506967973216,
75.0467958741422,76.0428949509628,77.0389940277834,78.035093104604,79.0311921814246,
80.0272912582452,81.0233903350658,82.0194894118864,83.015588488707,84.0116875655276,
85.0077866423481,86.0038857191687,86.9999847959893,87.9960838728099,88.9921829496305,
89.9882820264511,90.9843811032717,91.9804801800923,92.9765792569129,93.9726783337335,
94.968777410554,95.9648764873746,96.9609755641952,97.9570746410158,98.9531737178364,
99.949272794657,100.945371871478,101.941470948298,102.937570025119,103.933669101939,
104.92976817876,105.925867255581,106.921966332401,107.918065409222,108.914164486042,
109.910263562863,110.906362639683,111.902461716504,112.898560793325,113.894659870145,
114.890758946966,115.886858023786,116.882957100607,117.879056177428,118.875155254248,
119.871254331069,120.867353407889,121.86345248471,122.859551561531,123.855650638351,
124.851749715172,125.847848791992,126.843947868813,127.840046945634,128.836146022454,
129.832245099275,130.828344176095,131.824443252916,132.820542329736,133.816641406557,
134.812740483378,135.808839560198,136.804938637019,137.801037713839,138.79713679066,
139.793235867481,140.789334944301,141.785434021122,142.781533097942,143.777632174763,
144.773731251584,145.769830328404,146.765929405225,147.762028482045,148.758127558866,
149.754226635687,150.750325712507,151.746832423888),.UNSPECIFIED.);
#54=B_SPLINE_SURFACE_WITH_KNOTS('',3,3,((#20716,#20717,#20718,#20719,#20720,
#20721,#20722,#20723,#20724,#20725,#20726,#20727,#20728,#20729,#20730,#20731,
#20732,#20733,#20734,#20735,#20736,#20737,#20738,#20739,#20740,#20741,#20742,
#20743,#20744,#20745,#20746,#20747,#20748,#20749,#20750,#20751,#20752,#20753,
#20754,#20755,#20756,#20757,#20758,#20759,#20760,#20761,#20762,#20763,#20764,
#20765,#20766,#20767,#20768,#20769,#20770,#20771,#20772,#20773,#20774,#20775,
#20776,#20777,#20778,#20779,#20780,#20781,#20782,#20783,#20784,#20785,#20786,
#20787,#20788,#20789,#20790,#20791,#20792,#20793,#20794,#20795,#20796,#20797,
#20798,#20799,#20800,#20801,#20802,#20803,#20804,#20805,#20806,#20807,#20808,
#20809,#20810,#20811,#20812,#20813,#20814,#20815,#20816,#20817,#20818,#20819,
#20820,#20821,#20822,#20823,#20824,#20825,#20826,#20827,#20828,#20829,#20830,
#20831,#20832,#20833,#20834,#20835,#20836,#20837,#20838,#20839,#20840,#20841,
#20842,#20843,#20844,#20845,#20846,#20847,#20848,#20849,#20850,#20851,#20852,
#20853,#20854,#20855,#20856,#20857,#20858,#20859,#20860,#20861,#20862),
(#20863,#20864,#20865,#20866,#20867,#20868,#20869,#20870,#20871,#20872,
#20873,#20874,#20875,#20876,#20877,#20878,#20879,#20880,#20881,#20882,#20883,
#20884,#20885,#20886,#20887,#20888,#20889,#20890,#20891,#20892,#20893,#20894,
#20895,#20896,#20897,#20898,#20899,#20900,#20901,#20902,#20903,#20904,#20905,
#20906,#20907,#20908,#20909,#20910,#20911,#20912,#20913,#20914,#20915,#20916,
#20917,#20918,#20919,#20920,#20921,#20922,#20923,#20924,#20925,#20926,#20927,
#20928,#20929,#20930,#20931,#20932,#20933,#20934,#20935,#20936,#20937,#20938,
#20939,#20940,#20941,#20942,#20943,#20944,#20945,#20946,#20947,#20948,#20949,
#20950,#20951,#20952,#20953,#20954,#20955,#20956,#20957,#20958,#20959,#20960,
#20961,#20962,#20963,#20964,#20965,#20966,#20967,#20968,#20969,#20970,#20971,
#20972,#20973,#20974,#20975,#20976,#20977,#20978,#20979,#20980,#20981,#20982,
#20983,#20984,#20985,#20986,#20987,#20988,#20989,#20990,#20991,#20992,#20993,
#20994,#20995,#20996,#20997,#20998,#20999,#21000,#21001,#21002,#21003,#21004,
#21005,#21006,#21007,#21008,#21009),(#21010,#21011,#21012,#21013,#21014,
#21015,#21016,#21017,#21018,#21019,#21020,#21021,#21022,#21023,#21024,#21025,
#21026,#21027,#21028,#21029,#21030,#21031,#21032,#21033,#21034,#21035,#21036,
#21037,#21038,#21039,#21040,#21041,#21042,#21043,#21044,#21045,#21046,#21047,
#21048,#21049,#21050,#21051,#21052,#21053,#21054,#21055,#21056,#21057,#21058,
#21059,#21060,#21061,#21062,#21063,#21064,#21065,#21066,#21067,#21068,#21069,
#21070,#21071,#21072,#21073,#21074,#21075,#21076,#21077,#21078,#21079,#21080,
#21081,#21082,#21083,#21084,#21085,#21086,#21087,#21088,#21089,#21090,#21091,
#21092,#21093,#21094,#21095,#21096,#21097,#21098,#21099,#21100,#21101,#21102,
#21103,#21104,#21105,#21106,#21107,#21108,#21109,#21110,#21111,#21112,#21113,
#21114,#21115,#21116,#21117,#21118,#21119,#21120,#21121,#21122,#21123,#21124,
#21125,#21126,#21127,#21128,#21129,#21130,#21131,#21132,#21133,#21134,#21135,
#21136,#21137,#21138,#21139,#21140,#21141,#21142,#21143,#21144,#21145,#21146,
#21147,#21148,#21149,#21150,#21151,#21152,#21153,#21154,#21155,#21156),
(#21157,#21158,#21159,#21160,#21161,#21162,#21163,#21164,#21165,#21166,
#21167,#21168,#21169,#21170,#21171,#21172,#21173,#21174,#21175,#21176,#21177,
#21178,#21179,#21180,#21181,#21182,#21183,#21184,#21185,#21186,#21187,#21188,
#21189,#21190,#21191,#21192,#21193,#21194,#21195,#21196,#21197,#21198,#21199,
#21200,#21201,#21202,#21203,#21204,#21205,#21206,#21207,#21208,#21209,#21210,
#21211,#21212,#21213,#21214,#21215,#21216,#21217,#21218,#21219,#21220,#21221,
#21222,#21223,#21224,#21225,#21226,#21227,#21228,#21229,#21230,#21231,#21232,
#21233,#21234,#21235,#21236,#21237,#21238,#21239,#21240,#21241,#21242,#21243,
#21244,#21245,#21246,#21247,#21248,#21249,#21250,#21251,#21252,#21253,#21254,
#21255,#21256,#21257,#21258,#21259,#21260,#21261,#21262,#21263,#21264,#21265,
#21266,#21267,#21268,#21269,#21270,#21271,#21272,#21273,#21274,#21275,#21276,
#21277,#21278,#21279,#21280,#21281,#21282,#21283,#21284,#21285,#21286,#21287,
#21288,#21289,#21290,#21291,#21292,#21293,#21294,#21295,#21296,#21297,#21298,
#21299,#21300,#21301,#21302,#21303)),.UNSPECIFIED.,.F.,.F.,.F.,(4,4),(4,
1,1,1,1,1,1,1,1,1,1,1,1,1,1,1,1,1,1,1,1,1,1,1,1,1,1,1,1,1,1,1,1,1,1,1,1,
1,1,1,1,1,1,1,1,1,1,1,1,1,1,1,1,1,1,1,1,1,1,1,1,1,1,1,1,1,1,1,1,1,1,1,1,
1,1,1,1,1,1,1,1,1,1,1,1,1,1,1,1,1,1,1,1,1,1,1,1,1,1,1,1,1,1,1,1,1,1,1,1,
1,1,1,1,1,1,1,1,1,1,1,1,1,1,1,1,1,1,1,1,1,1,1,1,1,1,1,1,1,1,1,1,1,1,1,4),
(-0.000364909195550823,0.0530331194684996),(11.6159855549096,12.6124922741621,
13.6085913509826,14.6046904278032,15.6007895046238,16.5968885814444,17.592987658265,
18.5890867350856,19.5851858119062,20.5812848887268,21.5773839655474,22.573483042368,
23.5695821191886,24.5656811960091,25.5617802728297,26.5578793496503,27.5539784264709,
28.5500775032915,29.5461765801121,30.5422756569327,31.5383747337533,32.5344738105739,
33.5305728873945,34.5266719642151,35.5227710410356,36.5188701178562,37.5149691946768,
38.5110682714974,39.507167348318,40.5032664251386,41.4993655019592,42.4954645787798,
43.4915636556004,44.487662732421,45.4837618092415,46.4798608860621,47.4759599628827,
48.4720590397033,49.4681581165239,50.4642571933445,51.4603562701651,52.4564553469857,
53.4525544238063,54.4486535006269,55.4447525774475,56.4408516542681,57.4369507310886,
58.4330498079092,59.4291488847298,60.4252479615504,61.421347038371,62.4174461151916,
63.4135451920122,64.4096442688328,65.4057433456534,66.4018424224739,67.3979414992945,
68.3940405761151,69.3901396529357,70.3862387297563,71.3823378065769,72.3784368833975,
73.3745359602181,74.3706350370387,75.3667341138593,76.3628331906799,77.3589322675004,
78.355031344321,79.3511304211416,80.3472294979622,81.3433285747828,82.3394276516034,
83.335526728424,84.3316258052446,85.3277248820652,86.3238239588858,87.3199230357064,
88.316022112527,89.3121211893476,90.3082202661681,91.3043193429887,92.3004184198093,
93.2965174966299,94.2926165734505,95.2887156502711,96.2848147270917,97.2809138039123,
98.2770128807329,99.2731119575535,100.269211034374,101.265310111195,102.261409188015,
103.257508264836,104.253607341656,105.249706418477,106.245805495298,107.241904572118,
108.238003648939,109.234102725759,110.23020180258,111.226300879401,112.222399956221,
113.218499033042,114.214598109862,115.210697186683,116.206796263503,117.202895340324,
118.198994417145,119.195093493965,120.191192570786,121.187291647606,122.183390724427,
123.179489801248,124.175588878068,125.171687954889,126.167787031709,127.16388610853,
128.159985185351,129.156084262171,130.152183338992,131.148282415812,132.144381492633,
133.140480569454,134.136579646274,135.132678723095,136.128777799915,137.124876876736,
138.120975953556,139.117075030377,140.113174107198,141.109273184018,142.105372260839,
143.101471337659,144.09757041448,145.093669491301,146.089768568121,147.085867644942,
148.081966721762,149.078065798583,150.074164875404,151.070263952224,152.066363029045,
153.062462105865,154.058561182686,155.054660259507),.UNSPECIFIED.);
#71=B_SPLINE_CURVE_WITH_KNOTS('',3,(#6240,#6241,#6242,#6243,#6244,#6245,
#6246,#6247,#6248,#6249,#6250,#6251,#6252,#6253,#6254,#6255,#6256,#6257,
#6258,#6259,#6260,#6261,#6262,#6263,#6264,#6265,#6266,#6267,#6268,#6269,
#6270,#6271,#6272,#6273,#6274,#6275,#6276,#6277,#6278,#6279,#6280,#6281,
#6282,#6283,#6284,#6285,#6286,#6287,#6288,#6289,#6290,#6291,#6292,#6293,
#6294,#6295,#6296,#6297,#6298,#6299,#6300,#6301,#6302,#6303,#6304,#6305,
#6306,#6307,#6308,#6309,#6310,#6311,#6312,#6313,#6314,#6315,#6316,#6317,
#6318,#6319,#6320,#6321,#6322,#6323,#6324,#6325,#6326,#6327,#6328,#6329,
#6330,#6331,#6332,#6333,#6334,#6335,#6336,#6337,#6338,#6339,#6340,#6341,
#6342,#6343,#6344,#6345,#6346,#6347,#6348,#6349,#6350,#6351,#6352,#6353,
#6354,#6355,#6356,#6357,#6358,#6359,#6360,#6361,#6362,#6363,#6364,#6365,
#6366,#6367,#6368,#6369,#6370,#6371,#6372,#6373,#6374,#6375,#6376,#6377,
#6378,#6379,#6380,#6381,#6382,#6383,#6384,#6385,#6386,#6387,#6388,#6389,
#6390,#6391,#6392,#6393,#6394,#6395,#6396,#6397,#6398,#6399,#6400,#6401,
#6402,#6403,#6404,#6405,#6406,#6407,#6408,#6409,#6410,#6411,#6412,#6413,
#6414,#6415,#6416,#6417,#6418,#6419,#6420,#6421,#6422,#6423,#6424,#6425,
#6426,#6427,#6428,#6429,#6430,#6431,#6432,#6433,#6434,#6435,#6436,#6437,
#6438,#6439),.UNSPECIFIED.,.F.,.F.,(4,2,2,2,2,2,2,2,2,2,2,2,2,2,2,2,2,2,
2,2,2,2,2,2,2,2,2,2,2,2,2,2,2,2,2,2,2,2,2,2,2,2,2,2,2,2,2,2,2,2,2,2,2,2,
2,2,2,2,2,2,2,2,2,2,2,2,2,2,2,2,2,2,2,2,2,2,2,2,2,2,2,2,2,2,2,2,2,2,2,2,
2,2,2,2,2,2,2,2,2,4),(-1.06702706684471,-1.05497244523198,-1.01665474666674,
-0.987326289287207,-0.984035699475469,-0.982343864446482,-0.980993032046556,
-0.979376055011248,-0.976344023459278,-0.957445920983846,-0.930057126831693,
-0.891518695952568,-0.886640257936173,-0.88356711296312,-0.881145191893844,
-0.87843483697744,-0.873892042240304,-0.855680156138417,-0.817294175426114,
-0.788127006009375,-0.784831781483875,-0.78313657234584,-0.781780806435103,
-0.7801543695058,-0.777100119816486,-0.757830693945903,-0.716953969705863,
-0.692298585803861,-0.687665864689332,-0.684663723883678,-0.682243359929601,
-0.679475912798355,-0.67469009538424,-0.65298285297418,-0.608712726286249,
-0.602465225697488,-0.588551357192911,-0.585891842462912,-0.584198945364764,
-0.58285130754978,-0.581247153549654,-0.578238297610785,-0.559520102171982,
-0.531873250013637,-0.493093337940054,-0.488232136921119,-0.485176457771325,
-0.482772740578015,-0.480087609996014,-0.475599336143425,-0.457808496003499,
-0.422846915570689,-0.392139941587043,-0.387236338277925,-0.385224212063848,
-0.383846874449487,-0.382397836822678,-0.380138381095141,-0.373073528948939,
-0.361283740951099,-0.3327770569905,-0.29345629296067,-0.288559857466281,
-0.285473632302045,-0.283040273102544,-0.280315832220917,-0.275745964889562,
-0.257351578317201,-0.218119053870677,-0.190340000473415,-0.187067238723753,
-0.185383087077227,-0.184031961276504,-0.184019005104345,-0.184006411822611,
-0.183994166925342,-0.183982256675038,-0.183970668041925,-0.183959388666292,
-0.183948406811756,-0.18393771133524,-0.183927291637329,-0.183917137641101,
-0.183907239757321,-0.183897588840279,-0.183888176187753,-0.183878993503064,
-0.183870032865609,-0.182192209855574,-0.178902630457108,-0.151793757873708,
-0.107615515621311,-0.0948511658450676,-0.0906278153001035,-0.0879581350487007,
-0.0854704570227276,-0.0821641180987161,-0.0748110605994982,-0.0197428996379006,
-0.00326166647738545),.UNSPECIFIED.);
#72=B_SPLINE_CURVE_WITH_KNOTS('',3,(#6442,#6443,#6444,#6445,#6446,#6447,
#6448,#6449,#6450,#6451,#6452,#6453,#6454,#6455,#6456,#6457,#6458,#6459,
#6460,#6461,#6462,#6463,#6464,#6465,#6466,#6467,#6468,#6469,#6470,#6471,
#6472,#6473,#6474,#6475,#6476,#6477,#6478,#6479,#6480,#6481,#6482,#6483,
#6484,#6485,#6486,#6487,#6488,#6489,#6490,#6491,#6492,#6493,#6494,#6495,
#6496,#6497,#6498,#6499,#6500,#6501,#6502,#6503,#6504,#6505,#6506,#6507,
#6508,#6509,#6510,#6511,#6512,#6513,#6514,#6515,#6516,#6517,#6518,#6519,
#6520,#6521,#6522,#6523,#6524,#6525,#6526,#6527,#6528,#6529,#6530,#6531,
#6532,#6533,#6534,#6535,#6536,#6537,#6538,#6539,#6540,#6541,#6542,#6543,
#6544,#6545,#6546,#6547,#6548,#6549,#6550,#6551,#6552,#6553,#6554,#6555,
#6556,#6557,#6558,#6559,#6560,#6561,#6562,#6563,#6564,#6565),
 .UNSPECIFIED.,.F.,.F.,(4,3,3,3,3,3,3,3,3,3,3,3,3,3,3,3,3,3,3,3,3,3,3,3,
3,3,3,3,3,3,3,3,3,3,3,3,3,3,3,3,3,4),(11.6163931973415,11.7238264230327,
11.8349096544239,11.9422659925758,12.049624554327,12.157014009309,12.2644630561389,
12.3720777239813,12.479788650104,12.5876971425722,12.6124922741621,12.7163982786736,
12.8201309958735,12.9237216952729,13.0272353744651,13.1307090292524,13.2341795975609,
13.337754874388,13.4413864212204,13.5452029841441,13.6085913509826,13.7137335322645,
13.8187189715362,13.923581225803,14.0283775980985,14.1331433556847,14.2379137215731,
14.3427919619306,14.4477304036871,14.5528461722256,14.6046904278032,14.7098521616725,
14.8148608616375,14.9197517921604,15.0245801889838,15.1293812805526,15.2341902545063,
15.3391118366484,15.4440963811367,15.5492620785737,15.6007895046238,15.7079632679489),
 .UNSPECIFIED.);
#73=B_SPLINE_CURVE_WITH_KNOTS('',3,(#6570,#6571,#6572,#6573,#6574,#6575,
#6576,#6577,#6578,#6579,#6580,#6581,#6582,#6583,#6584,#6585,#6586,#6587,
#6588,#6589,#6590,#6591,#6592,#6593,#6594,#6595,#6596,#6597,#6598,#6599,
#6600,#6601,#6602,#6603,#6604,#6605,#6606,#6607,#6608,#6609,#6610,#6611,
#6612,#6613,#6614,#6615,#6616,#6617,#6618,#6619,#6620,#6621,#6622,#6623,
#6624,#6625,#6626,#6627,#6628,#6629,#6630,#6631,#6632,#6633,#6634,#6635,
#6636,#6637,#6638,#6639,#6640,#6641,#6642,#6643,#6644,#6645,#6646,#6647,
#6648,#6649,#6650,#6651,#6652,#6653,#6654,#6655,#6656,#6657,#6658,#6659,
#6660,#6661,#6662,#6663,#6664,#6665,#6666,#6667,#6668,#6669,#6670,#6671,
#6672,#6673,#6674,#6675,#6676,#6677,#6678,#6679,#6680,#6681,#6682,#6683,
#6684,#6685,#6686,#6687,#6688,#6689,#6690,#6691,#6692,#6693,#6694,#6695,
#6696,#6697,#6698,#6699,#6700,#6701,#6702,#6703,#6704,#6705,#6706,#6707,
#6708,#6709,#6710,#6711,#6712,#6713,#6714,#6715,#6716,#6717,#6718,#6719,
#6720,#6721,#6722,#6723,#6724,#6725,#6726,#6727,#6728,#6729,#6730,#6731,
#6732,#6733,#6734,#6735,#6736,#6737,#6738,#6739,#6740,#6741,#6742,#6743,
#6744,#6745,#6746,#6747,#6748,#6749,#6750,#6751,#6752,#6753,#6754,#6755,
#6756,#6757,#6758,#6759,#6760,#6761,#6762,#6763,#6764,#6765,#6766,#6767,
#6768,#6769,#6770,#6771,#6772,#6773,#6774,#6775,#6776,#6777,#6778,#6779,
#6780,#6781,#6782,#6783,#6784,#6785),.UNSPECIFIED.,.F.,.F.,(4,2,2,2,2,2,
2,2,2,2,2,2,2,2,2,2,2,2,2,2,2,2,2,2,2,2,2,2,2,2,2,2,2,2,2,2,2,2,2,2,2,2,
2,2,2,2,2,2,2,2,2,2,2,2,2,2,2,2,2,2,2,2,2,2,2,2,2,2,2,2,2,2,2,2,2,2,2,2,
2,2,2,2,2,2,2,2,2,2,2,2,2,2,2,2,2,2,2,2,2,2,2,2,2,2,2,2,2,4),(-2.32340959930946,
-2.28671636369838,-2.28248129744248,-2.27965891672853,-2.27693862878967,
-2.27452011257343,-2.27146787835447,-2.26665554316793,-2.23659007898717,
-2.21249762971968,-2.18721978508259,-2.18035006287128,-2.1786597848142,
-2.17707240687928,-2.17571851532218,-2.1739871568661,-2.17119871447672,
-2.15466375160865,-2.13944937897683,-2.10277442830581,-2.08511469724236,
-2.08063747906312,-2.07789290905577,-2.07547780793399,-2.07246298493117,
-2.06777407196391,-2.04162762789115,-1.99753434182706,-1.98238247027529,
-1.9795052533592,-1.97792113172633,-1.9765666369363,-1.97483016455707,-1.9720252427692,
-1.95510039498244,-1.9063563954152,-1.88613155885719,-1.88144786392857,
-1.878707466285,-1.87629158113081,-1.87326989701188,-1.86855889754755,-1.84168264898425,
-1.80246384200122,-1.78348742316995,-1.78045226843756,-1.77883440396489,
-1.77748286913533,-1.77579018853629,-1.77249907620905,-1.74350934759795,
-1.70496738168487,-1.68671566353333,-1.68217177739531,-1.67946232182981,
-1.6770421873822,-1.67397266025881,-1.6691026108338,-1.62996536702173,-1.60194124700158,
-1.58425036261844,-1.5812625181024,-1.5796548511277,-1.57830278235529,-1.57659803562786,
-1.57389780788538,-1.55917593961205,-1.50834421545852,-1.48781339863567,
-1.48310987743816,-1.48036526274816,-1.47795011067682,-1.47493520880341,
-1.47024613712677,-1.44415838630842,-1.40425113971119,-1.3851521755854,
-1.38211255345633,-1.38049361187249,-1.37914138825622,-1.37744816709172,
-1.37415834136411,-1.34688282072237,-1.31193012843637,-1.28899672785052,
-1.28414858328718,-1.28137166068175,-1.27895862638588,-1.27598574083246,
-1.27143654482001,-1.24862377933376,-1.20573232481638,-1.18607028815224,
-1.1830119430291,-1.18138904228055,-1.180038348652,-1.17835296608331,-1.17571358020806,
-1.16210930303577,-1.12849464709001,-1.12385634376739,-1.09076801866163,
-1.08589923643028,-1.08283140791067,-1.0804132315342,-1.07770664095782,
-1.07316925509502,-1.06702706684471),.UNSPECIFIED.);
#74=B_SPLINE_CURVE_WITH_KNOTS('',3,(#6786,#6787,#6788,#6789,#6790,#6791,
#6792,#6793,#6794,#6795),.UNSPECIFIED.,.F.,.F.,(4,1,1,1,1,1,1,4),(15.7079719615557,
16.5968885814444,17.592987658265,18.5890867350856,19.5851858119062,20.5812848887268,
21.5773839655474,21.9911426286453),.UNSPECIFIED.);
#75=B_SPLINE_CURVE_WITH_KNOTS('',3,(#6800,#6801,#6802,#6803,#6804,#6805,
#6806,#6807,#6808,#6809,#6810),.UNSPECIFIED.,.F.,.F.,(4,1,1,1,1,1,1,1,4),
(21.9911513165397,22.2535448026509,23.2496438794715,24.2457429562921,25.2418420331127,
26.2379411099333,27.2340401867539,28.2301392635745,28.2743338823081),
 .UNSPECIFIED.);
#76=B_SPLINE_CURVE_WITH_KNOTS('',3,(#6811,#6812,#6813,#6814,#6815,#6816,
#6817,#6818,#6819,#6820,#6821,#6822,#6823,#6824,#6825,#6826,#6827,#6828,
#6829,#6830,#6831,#6832,#6833,#6834,#6835,#6836,#6837,#6838,#6839,#6840,
#6841,#6842,#6843,#6844,#6845,#6846,#6847,#6848,#6849,#6850,#6851,#6852,
#6853,#6854,#6855,#6856,#6857,#6858,#6859,#6860,#6861,#6862,#6863,#6864,
#6865,#6866,#6867,#6868,#6869,#6870,#6871,#6872,#6873,#6874,#6875,#6876,
#6877,#6878,#6879,#6880,#6881,#6882,#6883,#6884,#6885,#6886,#6887,#6888,
#6889,#6890,#6891,#6892,#6893,#6894,#6895,#6896,#6897,#6898,#6899,#6900,
#6901,#6902,#6903,#6904,#6905,#6906,#6907,#6908,#6909,#6910,#6911,#6912,
#6913,#6914,#6915,#6916,#6917,#6918,#6919,#6920,#6921,#6922,#6923,#6924,
#6925,#6926,#6927,#6928,#6929,#6930,#6931,#6932,#6933,#6934,#6935,#6936,
#6937,#6938,#6939,#6940,#6941,#6942,#6943,#6944,#6945,#6946,#6947,#6948,
#6949,#6950,#6951,#6952,#6953,#6954,#6955,#6956,#6957,#6958,#6959,#6960,
#6961,#6962,#6963,#6964,#6965,#6966,#6967,#6968,#6969,#6970,#6971,#6972,
#6973,#6974,#6975,#6976,#6977,#6978,#6979,#6980,#6981,#6982,#6983,#6984,
#6985,#6986,#6987,#6988,#6989,#6990,#6991,#6992,#6993,#6994,#6995,#6996,
#6997,#6998,#6999,#7000,#7001,#7002,#7003,#7004,#7005,#7006,#7007,#7008,
#7009,#7010,#7011,#7012,#7013,#7014,#7015,#7016,#7017,#7018,#7019,#7020,
#7021,#7022,#7023,#7024),.UNSPECIFIED.,.F.,.F.,(4,2,2,2,2,2,2,2,2,2,2,2,
2,2,2,2,2,2,2,2,2,2,2,2,2,2,2,2,2,2,2,2,2,2,2,2,2,2,2,2,2,2,2,2,2,2,2,2,
2,2,2,2,2,2,2,2,2,2,2,2,2,2,2,2,2,2,2,2,2,2,2,2,2,2,2,2,2,2,2,2,2,2,2,2,
2,2,2,2,2,2,2,2,2,2,2,2,2,2,2,2,2,2,2,2,2,2,4),(-2.51309494483192,-2.50320433340691,
-2.50019787928662,-2.49785177109079,-2.49550498564395,-2.49282979160281,
-2.48843898141752,-2.47384060084744,-2.42194777797328,-2.40189155767509,
-2.39882211610243,-2.39719746300626,-2.39584663860536,-2.39416288679831,
-2.39091279089183,-2.36757483483152,-2.33376985310361,-2.31537020214508,
-2.30764205148646,-2.30341567186313,-2.30059702444992,-2.29792694834691,
-2.29552962168192,-2.29250872221,-2.28779901889248,-2.26101007604918,-2.22174029788307,
-2.20275780425738,-2.19972287803772,-2.19810522711465,-2.19675385483173,
-2.19506135474195,-2.19177069455665,-2.16461620159165,-2.1295625510239,
-2.10658487398944,-2.10173642498569,-2.09896061732351,-2.09654932345174,
-2.09357958747997,-2.08903712860248,-2.06633021779805,-2.02336650079388,
-2.00369168254696,-2.00063383957115,-1.99901142479705,-1.99766033119149,
-1.99597354539965,-1.99270954662011,-1.96844581156467,-1.94048542244649,
-1.91108748436525,-1.90401549717365,-1.90079413463281,-1.89835452747676,
-1.89604333300452,-1.89214825145016,-1.88155714034897,-1.82104861712037,
-1.80432941469198,-1.80138075665389,-1.7997813507419,-1.79842851345984,
-1.79671293895133,-1.79397714704231,-1.77852371766808,-1.76162225748251,
-1.73074318883517,-1.7082451939056,-1.70342251211113,-1.70065184694556,
-1.69823939328664,-1.69526100457241,-1.69069169413982,-1.66738212550672,
-1.62964936886666,-1.60768027718677,-1.60312219347139,-1.60121615038319,
-1.5998395703432,-1.5985329369825,-1.59626057400744,-1.58969794624879,-1.5309160670397,
-1.50897570716499,-1.50418559679285,-1.50142222147116,-1.49900938265331,
-1.49602182559183,-1.49142197040518,-1.46739752772076,-1.42560857916681,
-1.40616692047357,-1.4031163078847,-1.40149526522063,-1.40014388511311,
-1.39845494691612,-1.39518165099361,-1.36532076346427,-1.32744775589378,
-1.30935574142146,-1.30482375826102,-1.30211677582176,-1.29969595313211,
-1.29662160012855,-1.29173594442689,-1.25689120554917),.UNSPECIFIED.);
#77=B_SPLINE_CURVE_WITH_KNOTS('',3,(#7029,#7030,#7031,#7032,#7033,#7034,
#7035,#7036,#7037,#7038,#7039,#7040,#7041,#7042,#7043,#7044,#7045,#7046,
#7047,#7048,#7049,#7050,#7051,#7052,#7053,#7054,#7055,#7056,#7057,#7058,
#7059,#7060,#7061,#7062,#7063,#7064,#7065,#7066,#7067,#7068,#7069,#7070,
#7071,#7072,#7073,#7074,#7075,#7076,#7077,#7078,#7079,#7080,#7081,#7082,
#7083,#7084,#7085,#7086,#7087,#7088,#7089,#7090,#7091,#7092,#7093,#7094,
#7095,#7096,#7097,#7098,#7099,#7100,#7101,#7102,#7103,#7104,#7105,#7106,
#7107,#7108,#7109,#7110,#7111,#7112,#7113,#7114,#7115,#7116,#7117,#7118,
#7119,#7120,#7121,#7122,#7123,#7124,#7125,#7126,#7127,#7128,#7129,#7130,
#7131,#7132,#7133,#7134,#7135,#7136,#7137,#7138,#7139,#7140,#7141,#7142,
#7143,#7144,#7145,#7146,#7147,#7148,#7149,#7150,#7151,#7152,#7153,#7154,
#7155,#7156,#7157,#7158,#7159,#7160,#7161,#7162,#7163,#7164,#7165,#7166,
#7167,#7168,#7169,#7170,#7171,#7172,#7173,#7174,#7175,#7176,#7177,#7178,
#7179,#7180,#7181,#7182,#7183,#7184,#7185,#7186,#7187,#7188,#7189,#7190,
#7191,#7192,#7193,#7194,#7195,#7196,#7197,#7198,#7199,#7200,#7201,#7202,
#7203,#7204,#7205,#7206,#7207,#7208,#7209,#7210,#7211,#7212,#7213,#7214,
#7215),.UNSPECIFIED.,.F.,.F.,(4,3,3,3,3,3,3,3,3,3,3,3,3,3,3,3,3,3,3,3,3,
3,3,3,3,3,3,3,3,3,3,3,3,3,3,3,3,3,3,3,3,3,3,3,3,3,3,3,3,3,3,3,3,3,3,3,3,
3,3,3,3,3,4),(28.2743342502764,28.3785778767343,28.4845354346919,28.5885092029038,
28.6924238812719,28.7963159943847,28.9037965808873,29.0078182645905,29.1170283024928,
29.2262383403951,29.3312185781844,29.4360418397988,29.5407424118362,29.6453775156852,
29.7499826790951,29.8545933861702,29.9593145177744,30.0640970811506,30.1690605520178,
30.2223374172156,30.3273176545636,30.432140915713,30.536841487253,30.6414765905846,
30.7460817534581,30.8506924599781,30.9554135910029,31.060196153785,31.1651596240413,
31.2184364940362,31.3234167330088,31.4282399958122,31.5329405690411,31.6375756740824,
31.7421808386837,31.8467915469473,31.9515126797276,32.0562952442743,32.1612587162913,
32.2145355708568,32.3195158090238,32.4243390710114,32.5290396434136,32.6336747476218,
32.7382799113848,32.8428906188066,32.9476117507447,33.0523943144481,33.1573577856286,
33.2106346476774,33.3156148858565,33.4204381478543,33.5251387202629,33.6297738244755,
33.7343789882406,33.8389896956618,33.9437108275967,34.048493391295,34.1534568624678,
34.206733724498,34.3277897537902,34.4478095797928,34.5575191891054),
 .UNSPECIFIED.);
#78=B_SPLINE_CURVE_WITH_KNOTS('',3,(#7216,#7217,#7218,#7219,#7220,#7221,
#7222,#7223,#7224,#7225,#7226,#7227,#7228,#7229,#7230,#7231,#7232,#7233,
#7234,#7235,#7236,#7237,#7238,#7239,#7240,#7241,#7242,#7243,#7244,#7245,
#7246,#7247,#7248,#7249,#7250,#7251,#7252,#7253,#7254,#7255,#7256,#7257,
#7258,#7259,#7260,#7261,#7262,#7263,#7264,#7265,#7266,#7267,#7268,#7269,
#7270,#7271,#7272,#7273,#7274,#7275,#7276,#7277,#7278,#7279,#7280,#7281,
#7282,#7283,#7284,#7285,#7286,#7287,#7288,#7289,#7290,#7291,#7292,#7293,
#7294,#7295,#7296,#7297,#7298,#7299,#7300,#7301,#7302,#7303,#7304,#7305,
#7306,#7307,#7308,#7309,#7310,#7311,#7312,#7313,#7314,#7315,#7316,#7317,
#7318,#7319,#7320,#7321,#7322,#7323,#7324,#7325,#7326,#7327,#7328,#7329,
#7330,#7331,#7332,#7333,#7334,#7335,#7336,#7337,#7338,#7339,#7340,#7341,
#7342,#7343,#7344,#7345,#7346,#7347,#7348,#7349,#7350,#7351,#7352,#7353,
#7354,#7355,#7356,#7357,#7358,#7359,#7360,#7361,#7362,#7363,#7364,#7365,
#7366,#7367,#7368,#7369,#7370,#7371,#7372,#7373,#7374,#7375,#7376,#7377,
#7378,#7379,#7380,#7381,#7382,#7383,#7384,#7385,#7386,#7387,#7388,#7389,
#7390,#7391,#7392,#7393,#7394,#7395,#7396,#7397,#7398,#7399,#7400,#7401,
#7402,#7403,#7404,#7405,#7406,#7407,#7408,#7409,#7410,#7411,#7412,#7413,
#7414,#7415,#7416,#7417,#7418,#7419,#7420,#7421,#7422,#7423,#7424,#7425,
#7426,#7427,#7428,#7429,#7430,#7431,#7432,#7433,#7434,#7435,#7436,#7437),
 .UNSPECIFIED.,.F.,.F.,(4,2,2,2,2,2,2,2,2,2,2,2,2,2,2,2,2,2,2,2,2,2,2,2,
2,2,2,2,2,2,2,2,2,2,2,2,2,2,2,2,2,2,2,2,2,2,2,2,2,2,2,2,2,2,2,2,2,2,2,2,
2,2,2,2,2,2,2,2,2,2,2,2,2,2,2,2,2,2,2,2,2,2,2,2,2,2,2,2,2,2,2,2,2,2,2,2,
2,2,2,2,2,2,2,2,2,2,2,2,2,2,4),(-1.25689120554917,-1.25671098397983,-1.25066044802923,
-1.20948522782805,-1.20491064445208,-1.20313714588804,-1.20185997527627,
-1.2004620937551,-1.1984396770067,-1.19314793368247,-1.18522029099217,-1.15865145486666,
-1.11497401188691,-1.10749967291772,-1.1045350791722,-1.10206941300667,
-1.09953631713358,-1.09580841404871,-1.08553719558386,-1.06994272249528,
-1.03560901274684,-1.00833242892861,-1.00504044381963,-1.00334745473176,
-1.00199584896178,-1.00037812612067,-0.997343437119441,-0.97837365130018,
-0.939151505365429,-0.912314034499537,-0.90760486837056,-0.904583841567298,
-0.902168168109199,-0.899427675624065,-0.894742998744615,-0.874501760959482,
-0.82567343419625,-0.808798879247274,-0.805995983750893,-0.804260196634177,
-0.802905814611509,-0.801321299904463,-0.798442302725255,-0.783252762889681,
-0.753093879630736,-0.713432025708798,-0.708566812426657,-0.705498458347683,
-0.703078089345408,-0.700367155226849,-0.69581786263213,-0.677501968708486,
-0.638690514808245,-0.610001750157104,-0.60671002913905,-0.605017031403042,
-0.603665339561002,-0.602047419014631,-0.599012110817107,-0.580029059989649,
-0.540736854294525,-0.513972503916871,-0.509265608884649,-0.506245163496234,
-0.503829392631909,-0.501088185318222,-0.49640077874294,-0.476121567928966,
-0.427048959552658,-0.41043452728958,-0.407642254046349,-0.405909586891387,
-0.404555367457733,-0.402968399167106,-0.400078334183035,-0.384663324279011,
-0.338508660130861,-0.314557277020408,-0.309960253739445,-0.30697328265707,
-0.304560112473025,-0.301795474673092,-0.297000917839606,-0.2749969507767,
-0.245530882454,-0.214093558884376,-0.209207553265977,-0.207183881735866,
-0.20583567815469,-0.204425498993356,-0.202279294029855,-0.199752654919245,
-0.194972367863382,-0.183059314699426,-0.155048145856931,-0.115924458706309,
-0.111054912861928,-0.107985187605656,-0.105564587246349,-0.102854282099866,
-0.0983081779359894,-0.0800363803910931,-0.0266261906942104,-0.0178723290072204,
-0.0107036920865427,-0.0083518670699158,-0.00688327807733598,-0.00559729557625789,
-0.00422686291420059,-0.00239437268791312,-0.000585284694235494),
 .UNSPECIFIED.);
#79=B_SPLINE_CURVE_WITH_KNOTS('',3,(#7442,#7443,#7444,#7445,#7446,#7447,
#7448,#7449,#7450,#7451,#7452,#7453,#7454,#7455,#7456,#7457,#7458,#7459,
#7460,#7461,#7462,#7463,#7464,#7465,#7466,#7467,#7468,#7469,#7470,#7471,
#7472,#7473,#7474,#7475,#7476,#7477,#7478,#7479,#7480,#7481,#7482,#7483,
#7484,#7485,#7486,#7487,#7488,#7489,#7490,#7491,#7492,#7493,#7494,#7495,
#7496,#7497,#7498,#7499,#7500,#7501,#7502,#7503,#7504,#7505,#7506,#7507,
#7508,#7509,#7510,#7511,#7512,#7513,#7514,#7515,#7516,#7517,#7518,#7519,
#7520,#7521,#7522,#7523,#7524,#7525,#7526,#7527,#7528,#7529,#7530,#7531,
#7532,#7533,#7534,#7535,#7536,#7537,#7538,#7539,#7540,#7541,#7542,#7543,
#7544,#7545,#7546,#7547,#7548,#7549,#7550,#7551,#7552,#7553,#7554,#7555,
#7556,#7557,#7558,#7559,#7560,#7561,#7562,#7563,#7564,#7565,#7566,#7567,
#7568,#7569,#7570,#7571,#7572,#7573,#7574,#7575,#7576,#7577,#7578,#7579,
#7580,#7581,#7582,#7583,#7584,#7585,#7586,#7587,#7588,#7589,#7590,#7591,
#7592,#7593,#7594,#7595,#7596,#7597,#7598,#7599,#7600,#7601,#7602,#7603,
#7604,#7605,#7606,#7607,#7608,#7609,#7610,#7611,#7612,#7613,#7614,#7615,
#7616,#7617,#7618,#7619,#7620,#7621,#7622,#7623,#7624,#7625,#7626,#7627,
#7628,#7629,#7630,#7631,#7632,#7633,#7634,#7635,#7636,#7637,#7638,#7639,
#7640,#7641,#7642,#7643,#7644,#7645,#7646,#7647,#7648,#7649,#7650,#7651,
#7652,#7653,#7654,#7655,#7656,#7657,#7658,#7659,#7660,#7661,#7662,#7663,
#7664,#7665,#7666,#7667,#7668,#7669,#7670,#7671,#7672,#7673,#7674,#7675,
#7676,#7677,#7678,#7679,#7680,#7681,#7682,#7683,#7684,#7685,#7686,#7687,
#7688,#7689,#7690,#7691),.UNSPECIFIED.,.F.,.F.,(4,2,2,2,2,2,2,2,2,2,2,2,
2,2,2,2,2,2,2,2,2,2,2,2,2,2,2,2,2,2,2,2,2,2,2,2,2,2,2,2,2,2,2,2,2,2,2,2,
2,2,2,2,2,2,2,2,2,2,2,2,2,2,2,2,2,2,2,2,2,2,2,2,2,2,2,2,2,2,2,2,2,2,2,2,
2,2,2,2,2,2,2,2,2,2,2,2,2,2,2,2,2,2,2,2,2,2,2,2,2,2,2,2,2,2,2,2,2,2,2,2,
2,2,2,2,4),(-1.25717479450333,-1.23431056484724,-1.22975477569507,-1.22678054944049,
-1.22436841538287,-1.22159474466381,-1.21675809941997,-1.19401259331354,
-1.16021307921353,-1.13148317515821,-1.12819157215222,-1.12649863706517,
-1.12514699650765,-1.12352913894593,-1.12049395237826,-1.10151179584398,
-1.06222206626641,-1.03545762467368,-1.03075087072106,-1.0277305290092,
-1.02531484952289,-1.02257375499927,-1.0178865640463,-0.997608684184581,
-0.948541670039921,-0.931923802857341,-0.929131466211711,-0.927398814363777,
-0.926044642690412,-0.924457771968533,-0.921567989602578,-0.906157170600152,
-0.860033563716474,-0.836052505565535,-0.831454332862117,-0.828467069765009,
-0.82605396160448,-0.8232897216895,-0.818496693530489,-0.796516560014088,
-0.737326863349453,-0.731073448412038,-0.728843814010007,-0.727545450200212,
-0.726163481855453,-0.724227296142887,-0.719488270966462,-0.695702774494737,
-0.679155461596489,-0.640743746252026,-0.633293557539204,-0.630251683469711,
-0.627991266980409,-0.625516506249222,-0.622089123662714,-0.613827449226716,
-0.602185789962517,-0.56790593347784,-0.53632536965187,-0.531426598993216,
-0.529407892772127,-0.528024368104393,-0.526574326407731,-0.524306823481104,
-0.517162211647707,-0.505172314606505,-0.477240323994236,-0.438142731879105,
-0.433271125601501,-0.430200515287726,-0.427779475435338,-0.425068948024601,
-0.420523118782819,-0.402261897213763,-0.363691817302333,-0.334681513384031,
-0.33138893403705,-0.3296955492682,-0.328343577946666,-0.326725358185739,
-0.323689582622493,-0.304707168327515,-0.264848431712814,-0.238617051112021,
-0.233916717716315,-0.230897945074816,-0.22848188025595,-0.228432726354342,
-0.228387434695292,-0.228345693394845,-0.228307216353647,-0.228271741174546,
-0.228239027215165,-0.228208853768559,-0.228181018386339,-0.228155335325058,
-0.228131634121797,-0.228109758296482,-0.22808956415974,-0.22807091971706,
-0.228042251455893,-0.228014073274487,-0.227986373900511,-0.225103190176611,
-0.219678869078645,-0.212818374838106,-0.197378730231605,-0.161999562734522,
-0.135487173969977,-0.132197080243353,-0.130504231846451,-0.129152288852188,
-0.127533625846504,-0.124495736849805,-0.10545142468155,-0.0645853483016401,
-0.0484315983646425,-0.0371236971762454,-0.0331271488265467,-0.0305367455272384,
-0.0282310577993952,-0.0258381911911154,-0.0226944350006336,-0.0147032960217883,
-0.000585062358029298),.UNSPECIFIED.);
#80=B_SPLINE_CURVE_WITH_KNOTS('',3,(#7692,#7693,#7694,#7695,#7696,#7697,
#7698,#7699,#7700,#7701,#7702,#7703,#7704,#7705,#7706,#7707,#7708,#7709,
#7710,#7711,#7712,#7713,#7714,#7715,#7716,#7717,#7718,#7719,#7720,#7721,
#7722,#7723,#7724,#7725,#7726,#7727,#7728,#7729,#7730,#7731,#7732,#7733,
#7734,#7735,#7736,#7737,#7738,#7739,#7740,#7741,#7742,#7743,#7744,#7745,
#7746,#7747,#7748,#7749,#7750,#7751,#7752,#7753,#7754,#7755,#7756,#7757,
#7758,#7759,#7760,#7761,#7762,#7763,#7764,#7765,#7766,#7767,#7768,#7769,
#7770,#7771,#7772,#7773,#7774,#7775,#7776,#7777,#7778,#7779,#7780,#7781,
#7782,#7783,#7784,#7785,#7786,#7787,#7788,#7789,#7790,#7791,#7792,#7793,
#7794,#7795,#7796,#7797,#7798,#7799,#7800,#7801,#7802,#7803,#7804,#7805,
#7806,#7807,#7808,#7809,#7810,#7811,#7812,#7813,#7814,#7815,#7816,#7817,
#7818,#7819,#7820,#7821,#7822,#7823,#7824,#7825,#7826,#7827,#7828,#7829,
#7830,#7831,#7832,#7833,#7834,#7835,#7836,#7837,#7838,#7839,#7840,#7841,
#7842,#7843,#7844,#7845,#7846,#7847,#7848,#7849,#7850,#7851,#7852,#7853,
#7854,#7855,#7856,#7857,#7858,#7859,#7860,#7861,#7862,#7863,#7864,#7865,
#7866,#7867,#7868,#7869,#7870,#7871,#7872,#7873,#7874,#7875,#7876,#7877,
#7878,#7879,#7880,#7881,#7882,#7883,#7884,#7885,#7886,#7887,#7888,#7889,
#7890,#7891,#7892,#7893,#7894,#7895,#7896,#7897,#7898,#7899,#7900,#7901,
#7902,#7903,#7904,#7905,#7906,#7907),.UNSPECIFIED.,.F.,.F.,(4,2,2,2,2,2,
2,2,2,2,2,2,2,2,2,2,2,2,2,2,2,2,2,2,2,2,2,2,2,2,2,2,2,2,2,2,2,2,2,2,2,2,
2,2,2,2,2,2,2,2,2,2,2,2,2,2,2,2,2,2,2,2,2,2,2,2,2,2,2,2,2,2,2,2,2,2,2,2,
2,2,2,2,2,2,2,2,2,2,2,2,2,2,2,2,2,2,2,2,2,2,2,2,2,2,2,2,2,4),(-2.5138436186102,
-2.50952290300276,-2.46075586215554,-2.43239072266,-2.4254435661833,-2.42224457440169,
-2.41980775736968,-2.41716430191943,-2.41292249225143,-2.39966904025624,
-2.34835617248966,-2.33322200277272,-2.32761287541776,-2.32478544366912,
-2.32302213034665,-2.32140586879113,-2.32139905251692,-2.32139207186411,
-2.32138492080939,-2.3213775930576,-2.32137008196787,-2.32005598096186,
-2.31839773972454,-2.31533221902634,-2.29803560248755,-2.24962156045713,
-2.22944579027585,-2.2247651855837,-2.22202540545508,-2.21960934763307,
-2.21658650274317,-2.21187186281261,-2.18489498256755,-2.1457610336291,
-2.12679838350396,-2.1237635189943,-2.12214564261047,-2.12079387038351,
-2.11910063177515,-2.11580804131143,-2.08867142589064,-2.05418327682725,
-2.03861854056218,-2.02836017125334,-2.02463372982322,-2.02210069156468,
-2.01963436290226,-2.01666809299148,-2.00918480243566,-1.96564164877097,
-1.93893477140375,-1.93098322869654,-1.92567984285703,-1.92365549682557,
-1.92225709483955,-1.92098008269896,-1.91920765554693,-1.91464082076545,
-1.87337137287138,-1.83300611226229,-1.82721059192544,-1.82423455625505,
-1.82182209420408,-1.81904930550816,-1.81434173957802,-1.79574953865952,
-1.74420812989008,-1.72819568158449,-1.7252775078336,-1.72368441638485,
-1.7223306921472,-1.72060600608063,-1.7178405800224,-1.70185817745435,-1.65222398183631,
-1.63186290377256,-1.62716987086098,-1.62442725197271,-1.62201136820524,
-1.61899227396319,-1.6142903369892,-1.58769008859952,-1.54399973624458,
-1.52890042064648,-1.52602543291397,-1.52444163189966,-1.52308691929542,
-1.52134950800907,-1.51854169815103,-1.50155026530522,-1.45284936562663,
-1.43262818781638,-1.42794430751206,-1.42520367049628,-1.42278749814761,
-1.41976535707357,-1.4150534604555,-1.38816525552912,-1.34894644173208,
-1.32996774733639,-1.32693213429148,-1.32531401923095,-1.32396214122059,
-1.32226888777097,-1.31897660759628,-1.29158969906332,-1.25739797810809,
-1.25725532263633),.UNSPECIFIED.);
#81=B_SPLINE_CURVE_WITH_KNOTS('',3,(#7912,#7913,#7914,#7915,#7916,#7917,
#7918,#7919,#7920,#7921,#7922,#7923,#7924,#7925,#7926,#7927,#7928,#7929,
#7930,#7931,#7932,#7933,#7934,#7935,#7936,#7937,#7938,#7939,#7940,#7941,
#7942,#7943,#7944,#7945,#7946,#7947,#7948,#7949,#7950,#7951,#7952,#7953,
#7954,#7955,#7956,#7957,#7958,#7959,#7960,#7961,#7962,#7963,#7964,#7965,
#7966,#7967,#7968,#7969,#7970,#7971,#7972,#7973,#7974,#7975,#7976,#7977,
#7978,#7979,#7980,#7981,#7982,#7983,#7984,#7985,#7986,#7987,#7988,#7989,
#7990,#7991,#7992,#7993,#7994,#7995,#7996,#7997,#7998,#7999,#8000,#8001,
#8002,#8003,#8004,#8005,#8006,#8007,#8008,#8009,#8010,#8011,#8012,#8013,
#8014,#8015,#8016,#8017,#8018,#8019,#8020,#8021,#8022,#8023,#8024,#8025,
#8026,#8027,#8028,#8029,#8030,#8031,#8032,#8033,#8034,#8035,#8036,#8037,
#8038,#8039,#8040,#8041,#8042,#8043,#8044,#8045,#8046,#8047,#8048,#8049,
#8050,#8051,#8052,#8053,#8054,#8055,#8056,#8057,#8058,#8059,#8060,#8061,
#8062,#8063,#8064,#8065,#8066,#8067,#8068,#8069,#8070,#8071,#8072,#8073,
#8074,#8075,#8076,#8077,#8078,#8079,#8080,#8081,#8082,#8083,#8084,#8085,
#8086,#8087,#8088,#8089,#8090,#8091,#8092,#8093,#8094,#8095,#8096,#8097,
#8098,#8099,#8100,#8101,#8102,#8103,#8104,#8105,#8106,#8107,#8108,#8109,
#8110,#8111,#8112,#8113,#8114,#8115,#8116,#8117,#8118,#8119,#8120,#8121,
#8122,#8123,#8124,#8125,#8126,#8127,#8128,#8129,#8130,#8131,#8132,#8133,
#8134,#8135,#8136,#8137,#8138,#8139,#8140,#8141,#8142,#8143,#8144,#8145,
#8146,#8147,#8148,#8149),.UNSPECIFIED.,.F.,.F.,(4,2,2,2,2,2,2,2,2,2,2,2,
2,2,2,2,2,2,2,2,2,2,2,2,2,2,2,2,2,2,2,2,2,2,2,2,2,2,2,2,2,2,2,2,2,2,2,2,
2,2,2,2,2,2,2,2,2,2,2,2,2,2,2,2,2,2,2,2,2,2,2,2,2,2,2,2,2,2,2,2,2,2,2,2,
2,2,2,2,2,2,2,2,2,2,2,2,2,2,2,2,2,2,2,2,2,2,2,2,2,2,2,2,2,2,2,2,2,2,4),
(-2.51335624080557,-2.506478946999,-2.48359052154761,-2.46127006800987,
-2.43234350190882,-2.42532888506851,-2.42211819499271,-2.41968037468292,
-2.41704350343578,-2.41282902361346,-2.39979778345691,-2.34825978506285,
-2.33311207445996,-2.32750032497869,-2.32467225188235,-2.32290888658861,
-2.32129271795892,-2.32128423243568,-2.32127743880788,-2.32127047540276,
-2.3212633359424,-2.32125601385886,-2.32124850222344,-2.32124079375284,
-2.32123288076894,-2.32122475516387,-2.32121640839591,-2.32120783146814,
-2.32119901485306,-2.32118994846965,-2.32118062165022,-2.3211710230933,
-2.3198578342817,-2.31815829415088,-2.31490885758603,-2.28581119154219,
-2.24735536733383,-2.22912577229372,-2.22458385700287,-2.22187497383776,
-2.21945496987617,-2.21638508520208,-2.21151340680533,-2.17243313090189,
-2.14453309376102,-2.1325095296761,-2.12535245094867,-2.12308413885026,
-2.12163435644588,-2.12025172756361,-2.11823533165146,-2.11334718851118,
-2.08325711360966,-2.05836301572525,-2.03336328455782,-2.02684808899443,
-2.02373054819745,-2.02130502030909,-2.01862274469822,-2.01420229989519,
-1.99932106227157,-1.95523663019295,-1.93038506804559,-1.92554583230165,
-1.923593857263,-1.92220945667648,-1.92073500747957,-1.9183553192337,-1.9109674070567,
-1.87029614475397,-1.84470225126122,-1.83026840771902,-1.82605510739743,
-1.823418252238,-1.82097995530959,-1.81782230715817,-1.81116430095981,-1.7588676691359,
-1.72935922744648,-1.72579391406116,-1.72406810981814,-1.72271465288763,
-1.72112320264002,-1.71829083394295,-1.70568188525691,-1.66138249721186,
-1.63528057508497,-1.62862012767713,-1.62547485602977,-1.62304568967479,
-1.62037742570763,-1.61602133933637,-1.60176155277982,-1.54555753571123,
-1.5291376692443,-1.52620177945079,-1.52460506070798,-1.52325193894913,
-1.52153272906904,-1.51878495980244,-1.50309684492989,-1.45319251212588,
-1.4327944978104,-1.42809965828995,-1.42535695329302,-1.42294157832999,
-1.41992389058856,-1.41522563737345,-1.38871405515121,-1.34916894689295,
-1.33013466670157,-1.32709759769582,-1.32547935957664,-1.32412775977318,
-1.32243533346523,-1.31914604045768,-1.29256993657596,-1.25731654093721,
-1.25717479450333),.UNSPECIFIED.);
#82=B_SPLINE_CURVE_WITH_KNOTS('',3,(#8150,#8151,#8152,#8153,#8154,#8155,
#8156,#8157,#8158,#8159,#8160,#8161,#8162,#8163,#8164,#8165,#8166,#8167,
#8168,#8169,#8170,#8171,#8172,#8173,#8174,#8175,#8176,#8177,#8178,#8179,
#8180,#8181,#8182,#8183,#8184,#8185,#8186,#8187,#8188,#8189,#8190,#8191,
#8192,#8193,#8194,#8195,#8196,#8197,#8198,#8199,#8200,#8201,#8202,#8203,
#8204,#8205,#8206,#8207,#8208,#8209,#8210,#8211,#8212,#8213,#8214,#8215,
#8216,#8217,#8218,#8219,#8220,#8221,#8222,#8223,#8224,#8225,#8226,#8227,
#8228,#8229,#8230,#8231,#8232,#8233,#8234,#8235,#8236,#8237,#8238,#8239,
#8240,#8241,#8242,#8243,#8244,#8245,#8246,#8247,#8248,#8249,#8250,#8251,
#8252,#8253,#8254,#8255,#8256,#8257,#8258,#8259,#8260,#8261,#8262,#8263,
#8264,#8265,#8266,#8267,#8268,#8269,#8270,#8271,#8272,#8273,#8274,#8275,
#8276,#8277,#8278,#8279,#8280,#8281,#8282,#8283,#8284,#8285,#8286,#8287,
#8288,#8289,#8290,#8291,#8292,#8293,#8294,#8295,#8296,#8297,#8298,#8299,
#8300,#8301,#8302,#8303,#8304,#8305,#8306,#8307,#8308,#8309,#8310,#8311,
#8312,#8313,#8314,#8315,#8316,#8317,#8318,#8319,#8320,#8321,#8322,#8323,
#8324,#8325,#8326,#8327,#8328,#8329,#8330,#8331,#8332,#8333,#8334,#8335,
#8336,#8337,#8338,#8339,#8340,#8341,#8342,#8343,#8344,#8345,#8346,#8347,
#8348,#8349,#8350,#8351,#8352,#8353,#8354,#8355,#8356,#8357,#8358,#8359,
#8360,#8361,#8362,#8363,#8364,#8365,#8366,#8367,#8368,#8369,#8370,#8371,
#8372,#8373,#8374,#8375,#8376,#8377,#8378,#8379,#8380,#8381,#8382,#8383,
#8384,#8385,#8386,#8387,#8388,#8389,#8390,#8391,#8392,#8393,#8394,#8395,
#8396,#8397),.UNSPECIFIED.,.F.,.F.,(4,2,2,2,2,2,2,2,2,2,2,2,2,2,2,2,2,2,
2,2,2,2,2,2,2,2,2,2,2,2,2,2,2,2,2,2,2,2,2,2,2,2,2,2,2,2,2,2,2,2,2,2,2,2,
2,2,2,2,2,2,2,2,2,2,2,2,2,2,2,2,2,2,2,2,2,2,2,2,2,2,2,2,2,2,2,2,2,2,2,2,
2,2,2,2,2,2,2,2,2,2,2,2,2,2,2,2,2,2,2,2,2,2,2,2,2,2,2,2,2,2,2,2,2,4),(-1.25725532263633,
-1.23414987783727,-1.229582938354,-1.22660499029235,-1.22419218275367,-1.22142032694857,
-1.21659355295292,-1.19403638234211,-1.16356267873069,-1.14684193795938,
-1.13086079136935,-1.1280953441515,-1.12637067869447,-1.1250169843593,-1.12342393274782,
-1.12050586488755,-1.10449267839333,-1.05290595323384,-1.03438806215691,
-1.02968593302645,-1.02691437014545,-1.02450176742656,-1.02152400798811,
-1.01572012717816,-0.975097572081584,-0.934084235610777,-0.929497593314563,
-0.927722029214994,-0.92644416513048,-0.925046445025526,-0.923025794801693,
-0.917747318444877,-0.90984680205646,-0.883443089779648,-0.839524782096024,
-0.832156197130007,-0.829158726567774,-0.826909172443318,-0.824424342985893,
-0.820941795960919,-0.812336419873437,-0.767823796079561,-0.735297838688778,
-0.730395453104543,-0.728376191473371,-0.72699259471416,-0.725542786094121,
-0.723276191185997,-0.716138950189172,-0.704166476090038,-0.67621647774181,
-0.637112767106812,-0.632241676356427,-0.62917127796705,-0.626750334629781,
-0.62403984157517,-0.619493893030351,-0.601229605733001,-0.562645117989373,
-0.53365581852347,-0.530363377467649,-0.528670057209901,-0.527318133825508,
-0.525699967166895,-0.522664279732112,-0.503681980369015,-0.464405504947726,
-0.437611653226557,-0.432903093952549,-0.429881872289105,-0.427465667883303,
-0.424724169948025,-0.420036768738303,-0.399766309704602,-0.350766018860153,
-0.33406139897186,-0.331265007398607,-0.32953095378834,-0.32817641867556,
-0.326589973665461,-0.32370309643189,-0.308361968464629,-0.26281376606529,
-0.238262921183173,-0.23361333728499,-0.230610029093004,-0.228195242692369,
-0.228148430478243,-0.228105290782643,-0.228065527609278,-0.228028869431055,
-0.227995067192375,-0.227963892453147,-0.227935135657683,-0.227908604541952,
-0.227884122668304,-0.227861528076439,-0.227840672040996,-0.227821417961429,
-0.227803640321601,-0.227775150263939,-0.227747146325044,-0.224871621810508,
-0.219483355561745,-0.212679848683744,-0.197426353486088,-0.162035331886598,
-0.135232805453285,-0.131941228664079,-0.130248061056178,-0.128896102313303,
-0.12727770576582,-0.124241083327297,-0.105233847404728,-0.0640561896920884,
-0.0479072784389079,-0.0368063663789557,-0.0328382139608077,-0.0305122514720755,
-0.0281761756576672,-0.0258175242526361,-0.022775380510453,-0.0147912373815069,
-0.000585061145730822),.UNSPECIFIED.);
#83=B_SPLINE_CURVE_WITH_KNOTS('',3,(#8402,#8403,#8404,#8405,#8406,#8407,
#8408,#8409,#8410,#8411,#8412,#8413,#8414,#8415,#8416,#8417,#8418,#8419,
#8420,#8421,#8422,#8423,#8424,#8425,#8426,#8427,#8428,#8429,#8430,#8431,
#8432,#8433,#8434,#8435,#8436,#8437,#8438,#8439,#8440,#8441,#8442,#8443,
#8444,#8445,#8446,#8447,#8448,#8449,#8450,#8451,#8452,#8453,#8454,#8455,
#8456,#8457,#8458,#8459,#8460,#8461,#8462,#8463,#8464,#8465,#8466,#8467,
#8468,#8469,#8470,#8471,#8472,#8473,#8474,#8475,#8476,#8477,#8478,#8479,
#8480,#8481,#8482,#8483,#8484,#8485,#8486,#8487,#8488,#8489,#8490,#8491,
#8492,#8493,#8494,#8495,#8496,#8497,#8498,#8499,#8500,#8501,#8502,#8503,
#8504,#8505,#8506,#8507,#8508,#8509,#8510,#8511,#8512,#8513,#8514,#8515,
#8516,#8517,#8518,#8519,#8520,#8521,#8522,#8523,#8524,#8525,#8526,#8527,
#8528,#8529,#8530,#8531,#8532,#8533,#8534,#8535,#8536,#8537,#8538,#8539,
#8540,#8541,#8542,#8543,#8544,#8545,#8546,#8547,#8548,#8549,#8550,#8551,
#8552,#8553,#8554,#8555,#8556,#8557,#8558,#8559,#8560,#8561,#8562,#8563,
#8564,#8565,#8566,#8567,#8568,#8569,#8570,#8571,#8572,#8573,#8574,#8575,
#8576,#8577,#8578,#8579,#8580,#8581,#8582,#8583,#8584,#8585,#8586,#8587,
#8588,#8589,#8590,#8591,#8592,#8593,#8594,#8595,#8596,#8597,#8598,#8599,
#8600,#8601,#8602,#8603,#8604,#8605,#8606,#8607,#8608,#8609,#8610,#8611,
#8612,#8613,#8614,#8615,#8616,#8617),.UNSPECIFIED.,.F.,.F.,(4,2,2,2,2,2,
2,2,2,2,2,2,2,2,2,2,2,2,2,2,2,2,2,2,2,2,2,2,2,2,2,2,2,2,2,2,2,2,2,2,2,2,
2,2,2,2,2,2,2,2,2,2,2,2,2,2,2,2,2,2,2,2,2,2,2,2,2,2,2,2,2,2,2,2,2,2,2,2,
2,2,2,2,2,2,2,2,2,2,2,2,2,2,2,2,2,2,2,2,2,2,2,2,2,2,2,2,2,4),(-1.25706550838262,
-1.25688504802724,-1.22123092182879,-1.20728198578521,-1.20462145682404,
-1.20292864050153,-1.20157693858103,-1.19995882124868,-1.19692264692035,
-1.17791534092071,-1.13848753000333,-1.11187309040359,-1.10717132592824,
-1.10415241997231,-1.10173675366566,-1.09899445318844,-1.09430215089612,
-1.07394897361652,-1.02437941311237,-1.00829779650752,-1.00552810482319,
-1.00380220346361,-1.0024484755008,-1.0008564788184,-0.997943117849524,
-0.982031177150865,-0.931454519873525,-0.911951694111017,-0.907181187104882,
-0.904394051993041,-0.901982833889149,-0.899025790607165,-0.893323025750843,
-0.855748344084509,-0.814652098577032,-0.807711750656776,-0.805388647467649,
-0.804071835323865,-0.802700272531822,-0.800825870699864,-0.796454357758817,
-0.776269068168181,-0.725858543838252,-0.711806103004129,-0.707471542862481,
-0.70480766740214,-0.70237671926059,-0.699220907939881,-0.692506507140974,
-0.66598923864767,-0.633486721974839,-0.610250071281972,-0.607000259638474,
-0.605316231189555,-0.603964846583364,-0.602339073773635,-0.599266716608962,
-0.579150978200645,-0.534395181408312,-0.513715621137475,-0.508864325751391,
-0.50605879206878,-0.503648773141945,-0.500714655762829,-0.495123115488161,
-0.450593245270213,-0.413397349567453,-0.408621352095307,-0.406819822084488,
-0.405535135100852,-0.404143462590276,-0.402153841902686,-0.39707811517086,
-0.389580256879378,-0.365476514118443,-0.318300598583093,-0.311023999784254,
-0.307800461103658,-0.30535117500284,-0.302741091976463,-0.298652509683195,
-0.28542925721175,-0.237782995101438,-0.211885060370233,-0.208603818969469,
-0.206912965422761,-0.20558617619989,-0.204013310889401,-0.202307704268895,
-0.199621085582844,-0.194404664338341,-0.180842960677011,-0.136438658626752,
-0.11534775604208,-0.110467976958645,-0.107655845400156,-0.105269056898189,
-0.102352661960632,-0.0968471246601189,-0.0541927809219825,-0.0182779878114133,
-0.0109890940378711,-0.00862216554045305,-0.00715023066165515,-0.00586260574610939,
-0.00449433631278169,-0.00256109927198567,-0.000585266250537942),
 .UNSPECIFIED.);
#84=B_SPLINE_CURVE_WITH_KNOTS('',3,(#8618,#8619,#8620,#8621,#8622,#8623,
#8624,#8625,#8626,#8627,#8628,#8629,#8630,#8631,#8632,#8633,#8634,#8635,
#8636,#8637,#8638,#8639,#8640,#8641,#8642,#8643,#8644,#8645,#8646,#8647,
#8648,#8649,#8650,#8651,#8652,#8653,#8654,#8655,#8656,#8657,#8658,#8659,
#8660,#8661,#8662,#8663,#8664,#8665,#8666,#8667,#8668,#8669,#8670,#8671,
#8672,#8673,#8674,#8675,#8676,#8677,#8678,#8679,#8680,#8681,#8682,#8683,
#8684,#8685,#8686,#8687,#8688,#8689,#8690,#8691,#8692,#8693,#8694,#8695,
#8696,#8697,#8698,#8699,#8700,#8701,#8702,#8703,#8704,#8705,#8706,#8707,
#8708,#8709,#8710,#8711,#8712,#8713,#8714,#8715,#8716,#8717,#8718,#8719,
#8720,#8721,#8722,#8723,#8724,#8725,#8726,#8727,#8728,#8729,#8730,#8731,
#8732,#8733,#8734,#8735,#8736,#8737,#8738,#8739,#8740,#8741,#8742,#8743,
#8744,#8745,#8746,#8747,#8748,#8749,#8750,#8751,#8752,#8753,#8754,#8755,
#8756,#8757,#8758,#8759,#8760,#8761,#8762,#8763,#8764,#8765,#8766,#8767,
#8768,#8769,#8770,#8771,#8772,#8773,#8774,#8775,#8776,#8777,#8778,#8779,
#8780,#8781,#8782,#8783,#8784,#8785,#8786,#8787,#8788,#8789,#8790,#8791,
#8792,#8793,#8794,#8795,#8796,#8797,#8798,#8799,#8800,#8801,#8802,#8803,
#8804),.UNSPECIFIED.,.F.,.F.,(4,3,3,3,3,3,3,3,3,3,3,3,3,3,3,3,3,3,3,3,3,
3,3,3,3,3,3,3,3,3,3,3,3,3,3,3,3,3,3,3,3,3,3,3,3,3,3,3,3,3,3,3,3,3,3,3,3,
3,3,3,3,3,4),(47.1238898042299,47.2435633757992,47.3643071377152,47.4759599628827,
47.5809402011763,47.6857634632907,47.7904640358196,47.8950991401544,47.9997043040436,
48.1043150115907,48.2090361436527,48.3138187074791,48.41878217878,48.4720590397033,
48.5770392779971,48.6818625401117,48.7865631126407,48.8911982169756,48.9958033808649,
49.1004140884122,49.2051352204743,49.3099177843008,49.4148812556019,49.4681581165239,
49.5731383548177,49.6779616169323,49.7826621894614,49.8872972937963,49.9919024576857,
50.0965131652331,50.2012342972952,50.3060168611217,50.4109803324229,50.4642571933445,
50.5692374316383,50.6740606937529,50.7787612662819,50.8833963706168,50.9880015345061,
51.0926122420534,51.1973333741155,51.3021159379419,51.407079409243,51.4603562701651,
51.5653365084589,51.6701597705735,51.7748603431025,51.8794954474374,51.9841006113267,
52.088711318874,52.1934324509361,52.2982150147626,52.4031784860637,52.4564553469857,
52.5606956544191,52.666493039488,52.7704553584402,52.8743554984829,52.9782300106044,
53.0854411916958,53.189437381338,53.298256058154,53.40707473497),
 .UNSPECIFIED.);
#85=B_SPLINE_CURVE_WITH_KNOTS('',3,(#8809,#8810,#8811,#8812,#8813,#8814,
#8815,#8816,#8817,#8818,#8819,#8820,#8821,#8822,#8823,#8824,#8825,#8826,
#8827,#8828,#8829,#8830,#8831,#8832,#8833,#8834,#8835,#8836,#8837,#8838,
#8839,#8840,#8841,#8842,#8843,#8844,#8845,#8846,#8847,#8848,#8849,#8850,
#8851,#8852,#8853,#8854,#8855,#8856,#8857,#8858,#8859,#8860,#8861,#8862,
#8863,#8864,#8865,#8866,#8867,#8868,#8869,#8870,#8871,#8872,#8873,#8874,
#8875,#8876,#8877,#8878,#8879,#8880,#8881,#8882,#8883,#8884,#8885,#8886,
#8887,#8888,#8889,#8890,#8891,#8892,#8893,#8894,#8895,#8896,#8897,#8898,
#8899,#8900,#8901,#8902,#8903,#8904,#8905,#8906,#8907,#8908,#8909,#8910,
#8911,#8912,#8913,#8914,#8915,#8916,#8917,#8918,#8919,#8920,#8921,#8922,
#8923,#8924,#8925,#8926,#8927,#8928,#8929,#8930,#8931,#8932,#8933,#8934,
#8935,#8936,#8937,#8938,#8939,#8940,#8941,#8942,#8943,#8944,#8945,#8946,
#8947,#8948,#8949,#8950,#8951,#8952,#8953,#8954,#8955,#8956,#8957,#8958,
#8959,#8960,#8961,#8962,#8963,#8964,#8965,#8966,#8967,#8968,#8969,#8970,
#8971,#8972,#8973,#8974,#8975,#8976,#8977,#8978,#8979,#8980,#8981,#8982,
#8983,#8984,#8985,#8986,#8987,#8988,#8989,#8990,#8991,#8992,#8993,#8994,
#8995,#8996,#8997,#8998,#8999,#9000,#9001,#9002,#9003,#9004,#9005,#9006,
#9007,#9008,#9009,#9010,#9011,#9012,#9013,#9014,#9015,#9016,#9017,#9018,
#9019,#9020,#9021,#9022,#9023,#9024,#9025,#9026,#9027,#9028),
 .UNSPECIFIED.,.F.,.F.,(4,2,2,2,2,2,2,2,2,2,2,2,2,2,2,2,2,2,2,2,2,2,2,2,
2,2,2,2,2,2,2,2,2,2,2,2,2,2,2,2,2,2,2,2,2,2,2,2,2,2,2,2,2,2,2,2,2,2,2,2,
2,2,2,2,2,2,2,2,2,2,2,2,2,2,2,2,2,2,2,2,2,2,2,2,2,2,2,2,2,2,2,2,2,2,2,2,
2,2,2,2,2,2,2,2,2,2,2,2,2,4),(-2.51349872763998,-2.5038851842131,-2.50087187825048,
-2.4985231050743,-2.49617779550293,-2.49350610377327,-2.48913397617121,
-2.47470867605817,-2.45518971606659,-2.40488695271871,-2.40027525480988,
-2.39836039088578,-2.39698244129476,-2.39567861831703,-2.39341999995963,
-2.38695602689522,-2.34546637603089,-2.31962086310329,-2.30999334617576,
-2.3050613691288,-2.30090026821975,-2.29898551606501,-2.29662411660384,
-2.29381428540162,-2.28894295004069,-2.26813771429483,-2.2234871187881,
-2.20339961855757,-2.20032831136248,-2.19870289031664,-2.1973516768625,
-2.19566771573073,-2.19241762492591,-2.16912071081335,-2.16177742884842,
-2.13115401214413,-2.11533855978587,-2.10496072596096,-2.10121826726596,
-2.09868216334679,-2.09621881385362,-2.09326330676,-2.08584647377472,-2.04087132675203,
-2.01521083977102,-2.00743751507438,-2.00222330775971,-2.00021257853642,
-1.99881697401559,-1.99753726925047,-1.99575417297682,-1.99111527092585,
-1.95126522272148,-1.9096554005371,-1.90382236422733,-1.90083894774715,
-1.8984262730994,-1.89565959200985,-1.89097769849647,-1.87266464531903,
-1.82083654755321,-1.80479767641897,-1.80187859615659,-1.80028543744887,
-1.79893191816085,-1.79720782907602,-1.79444399628042,-1.77849206266062,
-1.76247170689171,-1.76105128892689,-1.72601142173876,-1.71423173734209,
-1.70589529056457,-1.70245605230094,-1.69997940556005,-1.69772181257994,
-1.69411696980672,-1.68735166626761,-1.64455970117892,-1.60965831690555,
-1.603999217502,-1.60192293026968,-1.60051407345145,-1.59924714932525,-1.59718066984107,
-1.59199466371079,-1.53151400501854,-1.50944673885689,-1.504648833987,-1.50188358061218,
-1.49947064558119,-1.49648496376324,-1.49189177919711,-1.46803029563411,
-1.42608797642757,-1.40661575565723,-1.40356387669026,-1.40194246027129,
-1.40059094293453,-1.39890205083461,-1.39562946330555,-1.36564386652456,
-1.32786087722053,-1.30978966882121,-1.30525893783051,-1.30255204688415,
-1.3001308949269,-1.29705556295359,-1.29216722416761,-1.25706550838262),
 .UNSPECIFIED.);
#86=B_SPLINE_CURVE_WITH_KNOTS('',3,(#9029,#9030,#9031,#9032,#9033,#9034,
#9035,#9036,#9037,#9038,#9039),.UNSPECIFIED.,.F.,.F.,(4,1,1,1,1,1,1,1,4),
(53.4070751110265,53.4525544238063,54.4486535006269,55.4447525774475,56.4408516542681,
57.4369507310886,58.4330498079092,59.4291488847298,59.6902577852515),
 .UNSPECIFIED.);
#87=B_SPLINE_CURVE_WITH_KNOTS('',3,(#9044,#9045,#9046,#9047,#9048,#9049,
#9050,#9051,#9052,#9053),.UNSPECIFIED.,.F.,.F.,(4,1,1,1,1,1,1,4),(59.6902663011146,
60.1053097218334,61.101408798654,62.0975078754745,63.0936069522951,64.0897060291157,
65.0858051059363,65.973437039268),.UNSPECIFIED.);
#88=B_SPLINE_CURVE_WITH_KNOTS('',3,(#9054,#9055,#9056,#9057,#9058,#9059,
#9060,#9061,#9062,#9063,#9064,#9065,#9066,#9067,#9068,#9069,#9070,#9071,
#9072,#9073,#9074,#9075,#9076,#9077,#9078,#9079,#9080,#9081,#9082,#9083,
#9084,#9085,#9086,#9087,#9088,#9089,#9090,#9091,#9092,#9093,#9094,#9095,
#9096,#9097,#9098,#9099,#9100,#9101,#9102,#9103,#9104,#9105,#9106,#9107,
#9108,#9109,#9110,#9111,#9112,#9113,#9114,#9115,#9116,#9117,#9118,#9119,
#9120,#9121,#9122,#9123,#9124,#9125,#9126,#9127,#9128,#9129,#9130,#9131,
#9132,#9133,#9134,#9135,#9136,#9137,#9138,#9139,#9140,#9141,#9142,#9143,
#9144,#9145,#9146,#9147,#9148,#9149,#9150,#9151,#9152,#9153,#9154,#9155,
#9156,#9157,#9158,#9159,#9160,#9161,#9162,#9163,#9164,#9165,#9166,#9167,
#9168,#9169,#9170,#9171,#9172,#9173,#9174,#9175,#9176,#9177,#9178,#9179,
#9180,#9181,#9182,#9183,#9184,#9185,#9186,#9187,#9188,#9189,#9190,#9191,
#9192,#9193,#9194,#9195,#9196,#9197,#9198,#9199,#9200,#9201,#9202,#9203,
#9204,#9205,#9206,#9207,#9208,#9209,#9210,#9211,#9212,#9213,#9214,#9215,
#9216,#9217,#9218,#9219,#9220,#9221,#9222,#9223,#9224,#9225,#9226,#9227,
#9228,#9229,#9230,#9231,#9232,#9233,#9234,#9235,#9236,#9237,#9238,#9239,
#9240,#9241,#9242,#9243,#9244,#9245,#9246,#9247,#9248,#9249,#9250,#9251,
#9252,#9253,#9254,#9255,#9256,#9257,#9258,#9259,#9260,#9261,#9262,#9263,
#9264,#9265,#9266,#9267,#9268,#9269,#9270,#9271,#9272,#9273,#9274,#9275,
#9276,#9277,#9278,#9279),.UNSPECIFIED.,.F.,.F.,(4,2,2,2,2,2,2,2,2,2,2,2,
2,2,2,2,2,2,2,2,2,2,2,2,2,2,2,2,2,2,2,2,2,2,2,2,2,2,2,2,2,2,2,2,2,2,2,2,
2,2,2,2,2,2,2,2,2,2,2,2,2,2,2,2,2,2,2,2,2,2,2,2,2,2,2,2,2,2,2,2,2,2,2,2,
2,2,2,2,2,2,2,2,2,2,2,2,2,2,2,2,2,2,2,2,2,2,2,2,2,2,2,2,4),(-2.51352086227721,
-2.47656604450951,-2.47233342613999,-2.46951209352325,-2.46679256411087,
-2.46437402259144,-2.46132081360216,-2.4565050707433,-2.42631519722904,
-2.40240525096532,-2.37761212775579,-2.37031263472917,-2.36859248794638,
-2.36698412358358,-2.36563209473153,-2.36392815619268,-2.36123053290713,
-2.34655872265476,-2.34296884314504,-2.33830237269572,-2.29943217346383,
-2.28363969071847,-2.27667239285055,-2.2711949630713,-2.26825333037283,
-2.26584332268692,-2.26304479523154,-2.25822306675709,-2.23800150479595,
-2.19151157927723,-2.17252446097555,-2.16948910335028,-2.16787126559159,
-2.16651970165235,-2.16482694511829,-2.16153592950984,-2.13288259767781,
-2.09408099352259,-2.07576862879241,-2.07121991123292,-2.06850923027962,
-2.06608902921062,-2.06302080957817,-2.05815560792853,-2.01847891987679,
-1.98830481936321,-1.9731090428728,-1.97022979630961,-1.96864529408586,
-1.96729100790699,-1.96555546778813,-1.96275323033051,-1.94588839017909,
-1.89708562636036,-1.87685173620764,-1.8721677758771,-1.86942751000864,
-1.86701191746648,-1.86399083526381,-1.85928123748612,-1.83243483132589,
-1.79319280498197,-1.77421271403723,-1.7711775920826,-1.76955980174001,
-1.7682082317662,-1.76651541031422,-1.76322410318252,-1.73418596032668,
-1.69568827106528,-1.6774471371647,-1.67290377555124,-1.67019426410786,
-1.66777384515526,-1.66470363304381,-1.65983183381601,-1.62072905144766,
-1.59278533129058,-1.57499486754214,-1.57200297501951,-1.57039434634236,
-1.56904221983833,-1.56733831583323,-1.56464103750746,-1.54997917822018,
-1.5463993725626,-1.53299504820674,-1.50292419740552,-1.48708567683488,
-1.47669680090119,-1.47295279218317,-1.4704163309107,-1.46795316188431,
-1.46499850548168,-1.45758726248084,-1.41255296291875,-1.38693046528234,
-1.37916363718097,-1.37395266080893,-1.37194239682505,-1.37054686165185,
-1.36926701888645,-1.367483463603,-1.36284150830577,-1.32307426153321,-1.2942618662616,
-1.28398035138986,-1.27646816161009,-1.27316789283731,-1.27071554117611,
-1.2684262432894,-1.2652685295823,-1.2571219133552),.UNSPECIFIED.);
#89=B_SPLINE_CURVE_WITH_KNOTS('',3,(#9284,#9285,#9286,#9287,#9288,#9289,
#9290,#9291,#9292,#9293,#9294,#9295,#9296,#9297,#9298,#9299,#9300,#9301,
#9302,#9303,#9304,#9305,#9306,#9307,#9308,#9309,#9310,#9311,#9312,#9313,
#9314,#9315,#9316,#9317,#9318,#9319,#9320,#9321,#9322,#9323,#9324,#9325,
#9326,#9327,#9328,#9329,#9330,#9331,#9332,#9333,#9334,#9335,#9336,#9337,
#9338,#9339,#9340,#9341,#9342,#9343,#9344,#9345,#9346,#9347,#9348,#9349,
#9350,#9351,#9352,#9353,#9354,#9355,#9356,#9357,#9358,#9359,#9360,#9361,
#9362,#9363,#9364,#9365,#9366,#9367,#9368,#9369,#9370,#9371,#9372,#9373,
#9374,#9375,#9376,#9377,#9378,#9379,#9380,#9381,#9382,#9383,#9384,#9385,
#9386,#9387,#9388,#9389,#9390,#9391,#9392,#9393,#9394,#9395,#9396,#9397,
#9398,#9399,#9400,#9401,#9402,#9403,#9404,#9405,#9406,#9407,#9408,#9409,
#9410,#9411,#9412,#9413,#9414,#9415,#9416,#9417,#9418,#9419,#9420,#9421,
#9422,#9423,#9424,#9425,#9426,#9427,#9428,#9429,#9430,#9431,#9432,#9433,
#9434,#9435,#9436,#9437,#9438,#9439,#9440,#9441,#9442,#9443,#9444,#9445,
#9446,#9447,#9448,#9449,#9450,#9451,#9452,#9453,#9454,#9455,#9456,#9457,
#9458,#9459,#9460,#9461,#9462,#9463,#9464,#9465,#9466,#9467,#9468,#9469,
#9470,#9471,#9472,#9473,#9474,#9475,#9476,#9477,#9478,#9479,#9480,#9481,
#9482,#9483,#9484,#9485,#9486,#9487,#9488,#9489,#9490,#9491,#9492,#9493,
#9494,#9495,#9496,#9497,#9498,#9499,#9500,#9501,#9502,#9503,#9504,#9505,
#9506,#9507,#9508,#9509,#9510,#9511,#9512,#9513,#9514,#9515,#9516,#9517,
#9518,#9519,#9520,#9521,#9522,#9523,#9524,#9525,#9526,#9527,#9528,#9529,
#9530,#9531,#9532,#9533,#9534,#9535,#9536,#9537,#9538,#9539,#9540,#9541,
#9542,#9543,#9544,#9545,#9546,#9547,#9548,#9549,#9550,#9551,#9552,#9553,
#9554,#9555,#9556,#9557),.UNSPECIFIED.,.F.,.F.,(4,2,2,2,2,2,2,2,2,2,2,2,
2,2,2,2,2,2,2,2,2,2,2,2,2,2,2,2,2,2,2,2,2,2,2,2,2,2,2,2,2,2,2,2,2,2,2,2,
2,2,2,2,2,2,2,2,2,2,2,2,2,2,2,2,2,2,2,2,2,2,2,2,2,2,2,2,2,2,2,2,2,2,2,2,
2,2,2,2,2,2,2,2,2,2,2,2,2,2,2,2,2,2,2,2,2,2,2,2,2,2,2,2,2,2,2,2,2,2,2,2,
2,2,2,2,2,2,2,2,2,2,2,2,2,2,2,2,4),(-1.25687291994263,-1.25670044137422,
-1.22544272579206,-1.22054547491201,-1.21852746533694,-1.2171444413607,
-1.21569494768325,-1.21342834269509,-1.20628690034842,-1.19430270378767,
-1.16637957239355,-1.1272958187117,-1.12242603417447,-1.11935656334443,
-1.1169364164464,-1.11422688304229,-1.10968270712158,-1.09142792654451,
-1.05287083613732,-1.02387276977237,-1.02058140541397,-1.01888864499246,
-1.01753717185539,-1.01591954804797,-1.0128848895838,-0.993909426007681,
-0.954648925525729,-0.92786077125015,-0.923153668773008,-0.920133419639802,
-0.917718017279809,-0.914977455455784,-0.91029171989732,-0.890029594984095,
-0.841056064952028,-0.824345691015182,-0.821549760239923,-0.819816143281373,
-0.818462048361667,-0.816876234199523,-0.813990793073848,-0.798664597752717,
-0.753209356851707,-0.728538124125303,-0.723910903087646,-0.720914951280207,
-0.718501465016874,-0.715744045447738,-0.71098135724583,-0.689502978810967,
-0.629652331870388,-0.623486184077388,-0.621268664025271,-0.619972782684903,
-0.618589440555912,-0.616644844393399,-0.611853223269203,-0.587515708314427,
-0.584515966709155,-0.53344665596035,-0.52579868490047,-0.522723442859434,
-0.520455039664869,-0.517987806235039,-0.514600566467615,-0.506579705696247,
-0.495380669811647,-0.443561108261493,-0.439734942708405,-0.425651776109235,
-0.422983953027209,-0.421288851084714,-0.419936951411302,-0.418320536155404,
-0.415292749882273,-0.396532325504097,-0.369078749641853,-0.330553627612335,
-0.325677216474872,-0.322605315627897,-0.320184342686376,-0.317475021703886,
-0.312933929526981,-0.294731283787524,-0.256405134860613,-0.227070359910657,
-0.223791774650741,-0.222101486607004,-0.22074977124105,-0.220743834240699,
-0.220737976367287,-0.220732196409144,-0.220726493202849,-0.220720865602647,
-0.220715312474501,-0.220709832678287,-0.220704425161169,-0.220699088817152,
-0.22069382257323,-0.220688625428385,-0.220683496311316,-0.220678434224712,
-0.220673438206272,-0.22066850725514,-0.220663640428295,-0.220658836797703,
-0.220654095435096,-0.220649415408777,-0.220644795845114,-0.220640235867172,
-0.220635734603853,-0.220631291185153,-0.220626904800747,-0.220622574635532,
-0.220618299871072,-0.220613792946687,-0.218962971059349,-0.21573595159757,
-0.211521887709934,-0.16736328941224,-0.131391570959872,-0.126493097899004,
-0.123414585989652,-0.120992935052489,-0.118287569900292,-0.113764372938564,
-0.0957953825526273,-0.0481363765774753,-0.0369810098464935,-0.0267619539712843,
-0.0241129107165841,-0.0225631833115297,-0.0212349036940288,-0.0199043365304187,
-0.0181638814832782,-0.0153923964553053,-0.000584983637756737),
 .UNSPECIFIED.);
#90=B_SPLINE_CURVE_WITH_KNOTS('',3,(#9558,#9559,#9560,#9561,#9562,#9563,
#9564,#9565,#9566,#9567,#9568,#9569,#9570,#9571,#9572,#9573,#9574,#9575,
#9576,#9577,#9578,#9579,#9580,#9581,#9582,#9583,#9584,#9585,#9586,#9587,
#9588,#9589,#9590,#9591,#9592,#9593,#9594,#9595,#9596,#9597,#9598,#9599,
#9600,#9601,#9602,#9603,#9604,#9605,#9606,#9607,#9608,#9609,#9610,#9611,
#9612,#9613,#9614,#9615,#9616,#9617,#9618,#9619,#9620,#9621,#9622,#9623,
#9624,#9625,#9626,#9627,#9628,#9629,#9630,#9631,#9632,#9633,#9634,#9635,
#9636,#9637,#9638,#9639,#9640,#9641,#9642,#9643,#9644,#9645,#9646,#9647,
#9648,#9649,#9650,#9651,#9652,#9653,#9654,#9655,#9656,#9657,#9658,#9659,
#9660,#9661,#9662,#9663,#9664,#9665,#9666,#9667,#9668,#9669,#9670,#9671,
#9672,#9673,#9674,#9675,#9676,#9677,#9678,#9679,#9680,#9681,#9682,#9683,
#9684,#9685,#9686,#9687,#9688,#9689,#9690,#9691,#9692,#9693,#9694,#9695,
#9696,#9697,#9698,#9699,#9700,#9701,#9702,#9703,#9704,#9705,#9706,#9707,
#9708,#9709,#9710,#9711,#9712,#9713,#9714,#9715,#9716,#9717,#9718,#9719,
#9720,#9721,#9722,#9723,#9724,#9725,#9726,#9727,#9728,#9729,#9730,#9731,
#9732,#9733,#9734,#9735,#9736,#9737,#9738,#9739,#9740,#9741,#9742,#9743,
#9744,#9745,#9746,#9747,#9748,#9749,#9750,#9751,#9752,#9753,#9754,#9755,
#9756,#9757,#9758,#9759,#9760,#9761,#9762,#9763,#9764,#9765),
 .UNSPECIFIED.,.F.,.F.,(4,2,2,2,2,2,2,2,2,2,2,2,2,2,2,2,2,2,2,2,2,2,2,2,
2,2,2,2,2,2,2,2,2,2,2,2,2,2,2,2,2,2,2,2,2,2,2,2,2,2,2,2,2,2,2,2,2,2,2,2,
2,2,2,2,2,2,2,2,2,2,2,2,2,2,2,2,2,2,2,2,2,2,2,2,2,2,2,2,2,2,2,2,2,2,2,2,
2,2,2,2,2,2,2,4),(-1.2571219133552,-1.21585553434398,-1.17958221126086,
-1.17476866209243,-1.17296230431759,-1.17167636964021,-1.17028582140703,
-1.16830187538236,-1.16326227083586,-1.15583524974168,-1.13211852174542,
-1.08436975214487,-1.07785825667516,-1.07432096280615,-1.07185080152282,
-1.06932293844234,-1.06562104986835,-1.05553889594932,-1.04033699297451,
-1.00515383303319,-0.978078340918164,-0.974786502194116,-0.973093479460995,
-0.97174178701376,-0.97012388889707,-0.967088684103669,-0.948108602481126,
-0.908833085805069,-0.88205019072271,-0.8773426556386,-0.87432201651327,
-0.871906230061974,-0.869165154845333,-0.86447834789892,-0.844208227024231,
-0.795195708412977,-0.778516233458754,-0.775721247055763,-0.773987767334826,
-0.772633485086136,-0.771047108886636,-0.768159788433407,-0.75280187722704,
-0.707107100110468,-0.682675194869783,-0.678057519106133,-0.675064228541182,
-0.672650590105053,-0.669890488739537,-0.665116772060569,-0.643464742236623,
-0.595369446933154,-0.579266712389494,-0.576496088483726,-0.57476989686073,
-0.573416133958902,-0.571824321383452,-0.56891186755737,-0.553020281595855,
-0.502643427113485,-0.482943300007431,-0.478159281736766,-0.475369040543534,
-0.472958012697656,-0.470004843301442,-0.464321067347851,-0.421209691770432,
-0.382683277144806,-0.377955139881056,-0.376159748323764,-0.374876674193312,
-0.373483608914664,-0.371486814726044,-0.366364850758388,-0.358775871990412,
-0.334166487798117,-0.287728646418363,-0.280398527354053,-0.277456601328946,
-0.274996434646347,-0.27245521803386,-0.268689335682666,-0.258140745358293,
-0.2419635344494,-0.21501066525948,-0.183744437376953,-0.178839697497763,
-0.176820155866155,-0.17543659513459,-0.174016170921965,-0.171906577870583,
-0.169370041189546,-0.164563130168757,-0.152552384296939,-0.127153904817075,
-0.089000505522226,-0.081538242306694,-0.078494506707217,-0.0762338150673216,
-0.0737598363842677,-0.0703355368811069,-0.0620911922644493,-0.0504811963099944,
-0.000709655758544155),.UNSPECIFIED.);
#91=B_SPLINE_CURVE_WITH_KNOTS('',3,(#9770,#9771,#9772,#9773,#9774,#9775,
#9776,#9777,#9778,#9779,#9780,#9781,#9782,#9783,#9784,#9785,#9786,#9787,
#9788,#9789,#9790,#9791,#9792,#9793,#9794,#9795,#9796,#9797,#9798,#9799,
#9800,#9801,#9802,#9803,#9804,#9805,#9806,#9807,#9808,#9809,#9810,#9811,
#9812,#9813,#9814,#9815,#9816,#9817,#9818,#9819,#9820,#9821,#9822,#9823,
#9824,#9825,#9826,#9827,#9828,#9829,#9830,#9831,#9832,#9833,#9834,#9835,
#9836,#9837,#9838,#9839,#9840,#9841,#9842,#9843,#9844,#9845,#9846,#9847,
#9848,#9849,#9850,#9851,#9852,#9853,#9854,#9855,#9856,#9857,#9858,#9859,
#9860,#9861,#9862,#9863,#9864,#9865,#9866,#9867,#9868,#9869,#9870,#9871,
#9872,#9873,#9874,#9875,#9876,#9877,#9878,#9879,#9880,#9881,#9882,#9883,
#9884,#9885,#9886,#9887,#9888,#9889,#9890,#9891,#9892,#9893,#9894,#9895,
#9896,#9897,#9898,#9899,#9900,#9901,#9902,#9903,#9904,#9905,#9906,#9907,
#9908,#9909,#9910,#9911,#9912,#9913,#9914,#9915,#9916,#9917,#9918,#9919,
#9920,#9921,#9922,#9923,#9924,#9925,#9926,#9927,#9928,#9929,#9930,#9931,
#9932,#9933,#9934,#9935,#9936,#9937,#9938,#9939,#9940,#9941,#9942,#9943,
#9944,#9945,#9946,#9947,#9948,#9949,#9950,#9951,#9952,#9953,#9954,#9955,
#9956,#9957,#9958,#9959,#9960,#9961,#9962,#9963,#9964,#9965,#9966,#9967,
#9968,#9969,#9970,#9971,#9972,#9973,#9974,#9975,#9976,#9977,#9978,#9979,
#9980,#9981),.UNSPECIFIED.,.F.,.F.,(4,2,2,2,2,2,2,2,2,2,2,2,2,2,2,2,2,2,
2,2,2,2,2,2,2,2,2,2,2,2,2,2,2,2,2,2,2,2,2,2,2,2,2,2,2,2,2,2,2,2,2,2,2,2,
2,2,2,2,2,2,2,2,2,2,2,2,2,2,2,2,2,2,2,2,2,2,2,2,2,2,2,2,2,2,2,2,2,2,2,2,
2,2,2,2,2,2,2,2,2,2,2,2,2,2,2,4),(-2.51291706895655,-2.51217911276532,-2.51063689552374,
-2.50794325041847,-2.50342063117696,-2.48648490772758,-2.47445369401095,
-2.45120443821324,-2.42765797896785,-2.42026315675441,-2.41524076903387,
-2.41325986478204,-2.41187019828096,-2.41058406938235,-2.40877608965551,
-2.40394754532802,-2.36812421218677,-2.33662758073177,-2.32025626196319,
-2.31586426301344,-2.31358460684056,-2.31122446939816,-2.3084046314995,
-2.30333115754943,-2.27796143210425,-2.23315363221779,-2.21790935496887,
-2.2150280563601,-2.21344325340457,-2.21208922638083,-2.21035468420121,
-2.20755533770113,-2.19075354860527,-2.14190215917196,-2.12166273652728,
-2.1169789055173,-2.11423892095307,-2.11182370065366,-2.10880324812348,
-2.10409495063136,-2.07727006120171,-2.03801802718977,-2.01903793102046,
-2.01600315993614,-2.01438558761069,-2.01303421787631,-2.0113416699841,
-2.00805096034691,-1.97910582934848,-1.94054369442165,-1.92228873755923,
-1.91774479976322,-1.91503541459223,-1.91261540171038,-1.90954610355304,
-1.90467655375541,-1.86554768152715,-1.83752767537584,-1.81984233534287,
-1.81685483750885,-1.81524728711971,-1.81389530275413,-1.81219061018443,
-1.8094902995344,-1.79476215056747,-1.74396224471499,-1.72344061151146,
-1.71873842379443,-1.71599445773844,-1.71357979721617,-1.71056540439297,
-1.70587692922607,-1.67968717862693,-1.6356440025421,-1.62050060664471,
-1.61762425451455,-1.61604052395961,-1.61468638491076,-1.61295037187428,
-1.61014609782504,-1.59322291945917,-1.54448364740929,-1.52426141513679,
-1.51957873469804,-1.51683901057391,-1.5144237704685,-1.5114029637783,-1.50669347457347,
-1.47983348713225,-1.44061332355789,-1.42163894350217,-1.41860438167521,
-1.41698685879972,-1.41563549413268,-1.41394290704103,-1.41065198991999,
-1.38341844914667,-1.34842121518167,-1.33324218259898,-1.32317072898436,
-1.31947086396263,-1.31694381191842,-1.31447400006986,-1.31093643446459,
-1.30442234628972,-1.25687291994263),.UNSPECIFIED.);
#92=B_SPLINE_CURVE_WITH_KNOTS('',3,(#9983,#9984,#9985,#9986),
 .UNSPECIFIED.,.F.,.F.,(4,4),(-0.000709655758544155,-0.000586166170592014),
 .UNSPECIFIED.);
#93=B_SPLINE_CURVE_WITH_KNOTS('',3,(#9987,#9988,#9989,#9990,#9991,#9992,
#9993,#9994,#9995,#9996,#9997,#9998,#9999,#10000,#10001,#10002,#10003,#10004,
#10005,#10006,#10007,#10008,#10009,#10010,#10011,#10012,#10013,#10014,#10015,
#10016,#10017,#10018,#10019,#10020,#10021,#10022,#10023,#10024,#10025,#10026,
#10027,#10028,#10029,#10030,#10031,#10032,#10033,#10034,#10035,#10036,#10037,
#10038,#10039,#10040,#10041,#10042,#10043,#10044,#10045,#10046,#10047,#10048,
#10049,#10050,#10051,#10052,#10053,#10054,#10055,#10056,#10057,#10058,#10059,
#10060,#10061,#10062,#10063,#10064,#10065,#10066,#10067,#10068,#10069,#10070,
#10071,#10072,#10073,#10074,#10075,#10076,#10077,#10078,#10079,#10080,#10081,
#10082,#10083,#10084,#10085,#10086,#10087,#10088,#10089,#10090,#10091,#10092,
#10093,#10094,#10095,#10096,#10097,#10098,#10099,#10100,#10101,#10102,#10103,
#10104,#10105,#10106,#10107,#10108,#10109,#10110,#10111,#10112,#10113,#10114,
#10115,#10116,#10117,#10118,#10119,#10120,#10121,#10122,#10123,#10124,#10125,
#10126,#10127,#10128,#10129,#10130,#10131,#10132,#10133,#10134,#10135,#10136,
#10137,#10138,#10139,#10140,#10141,#10142,#10143,#10144,#10145,#10146,#10147,
#10148,#10149,#10150,#10151,#10152,#10153,#10154,#10155,#10156,#10157,#10158,
#10159,#10160,#10161,#10162,#10163,#10164,#10165,#10166,#10167,#10168,#10169,
#10170,#10171,#10172,#10173,#10174,#10175,#10176,#10177,#10178,#10179,#10180,
#10181,#10182,#10183,#10184,#10185,#10186,#10187,#10188,#10189,#10190,#10191,
#10192,#10193,#10194,#10195,#10196,#10197,#10198,#10199,#10200,#10201,#10202,
#10203,#10204,#10205,#10206,#10207,#10208,#10209,#10210,#10211,#10212,#10213,
#10214,#10215,#10216,#10217,#10218,#10219,#10220,#10221,#10222,#10223,#10224,
#10225,#10226,#10227,#10228,#10229,#10230,#10231,#10232,#10233,#10234,#10235,
#10236,#10237,#10238,#10239,#10240,#10241,#10242,#10243,#10244,#10245,#10246,
#10247,#10248,#10249,#10250,#10251,#10252,#10253,#10254,#10255,#10256),
 .UNSPECIFIED.,.F.,.F.,(4,2,2,2,2,2,2,2,2,2,2,2,2,2,2,2,2,2,2,2,2,2,2,2,
2,2,2,2,2,2,2,2,2,2,2,2,2,2,2,2,2,2,2,2,2,2,2,2,2,2,2,2,2,2,2,2,2,2,2,2,
2,2,2,2,2,2,2,2,2,2,2,2,2,2,2,2,2,2,2,2,2,2,2,2,2,2,2,2,2,2,2,2,2,2,2,2,
2,2,2,2,2,2,2,2,2,2,2,2,2,2,2,2,2,2,2,2,2,2,2,2,2,2,2,2,2,2,2,2,2,2,2,2,
2,2,4),(-2.51330268493464,-2.49556538564027,-2.49290201701533,-2.49120615253485,
-2.4898904663098,-2.48853737825745,-2.4869430300399,-2.48409762702869,-2.47128896680276,
-2.4594856886688,-2.41535605773799,-2.39751294833082,-2.39300046458648,
-2.39029794958568,-2.38787661178151,-2.38479543541319,-2.37988650000792,
-2.34346083290876,-2.29973097890562,-2.2955324927909,-2.29231687940625,
-2.29066783875272,-2.29066333181592,-2.29065904753134,-2.29065470789311,
-2.29065031212376,-2.29064585936457,-2.29064134876928,-2.29063677950006,
-2.29063215069075,-2.2906274614583,-2.29062271091419,-2.29061789813152,
-2.29061302220024,-2.29060808215181,-2.29060307702415,-2.29059800585755,
-2.29059286764328,-2.29058766135885,-2.29058238598007,-2.29057704046294,
-2.29057162376439,-2.29056613477796,-2.29056057237955,-2.29055493547149,
-2.28920394315063,-2.28752444821789,-2.28429479280678,-2.26299202177995,
-2.21815865601418,-2.19859242037314,-2.19395368985072,-2.19122342722089,
-2.18880662601149,-2.18577070035647,-2.18101189096847,-2.15267573831262,
-2.10132969685269,-2.09673666984598,-2.09325352969231,-2.09154386244977,
-2.09032098791343,-2.08876905430401,-2.08610960623211,-2.07576791518943,
-2.03742639767992,-2.01267364675829,-1.99854453057771,-1.99436137395314,
-1.99173088340836,-1.98928993708555,-1.9861167451348,-1.97938067267917,
-1.92770112872361,-1.89770629831308,-1.89412719200211,-1.89239855426219,
-1.89104472591207,-1.88945499836791,-1.88663076507916,-1.87414733007131,
-1.86582787793111,-1.82729010527406,-1.80980727117441,-1.8023400237277,
-1.79648929718897,-1.79350214854313,-1.7910890279511,-1.78832465873778,
-1.78365345231183,-1.76548722313976,-1.75741552951203,-1.71264751446029,
-1.69740586177275,-1.69452411190569,-1.69293895079597,-1.69158454927969,
-1.68984943899942,-1.68704900584593,-1.67023467053815,-1.62137744018325,
-1.60113366444254,-1.59644863952822,-1.59370792931997,-1.59129205293021,
-1.58827075816209,-1.58356110556567,-1.55672662334708,-1.51746606820367,
-1.49848120852406,-1.49544562871142,-1.49382762115934,-1.49247588538718,
-1.49078287596293,-1.48749126010249,-1.45852444750407,-1.41996282294013,
-1.40170550035024,-1.39716052662444,-1.39445045047062,-1.39202977465648,
-1.38895957347952,-1.38408846633085,-1.34495437080746,-1.31694045752379,
-1.29923291579913,-1.29624393479665,-1.29463580566202,-1.29328346506894,
-1.29157848856973,-1.28887803285747,-1.27415762286202,-1.27008168493941,
-1.25730851664327,-1.25713482558798),.UNSPECIFIED.);
#94=B_SPLINE_CURVE_WITH_KNOTS('',3,(#10261,#10262,#10263,#10264,#10265,
#10266,#10267,#10268,#10269,#10270,#10271,#10272,#10273,#10274,#10275,#10276,
#10277,#10278,#10279,#10280,#10281,#10282,#10283,#10284,#10285,#10286,#10287,
#10288,#10289,#10290,#10291,#10292,#10293,#10294,#10295,#10296,#10297,#10298,
#10299,#10300,#10301,#10302,#10303,#10304,#10305,#10306,#10307,#10308,#10309,
#10310,#10311,#10312,#10313,#10314,#10315,#10316,#10317,#10318,#10319,#10320,
#10321,#10322,#10323,#10324,#10325,#10326,#10327,#10328,#10329,#10330,#10331,
#10332,#10333,#10334,#10335,#10336,#10337,#10338,#10339,#10340,#10341,#10342,
#10343,#10344,#10345,#10346,#10347,#10348,#10349,#10350,#10351,#10352,#10353,
#10354,#10355,#10356,#10357,#10358,#10359,#10360,#10361,#10362,#10363,#10364,
#10365,#10366,#10367,#10368,#10369,#10370,#10371,#10372,#10373,#10374,#10375,
#10376,#10377,#10378,#10379,#10380,#10381,#10382,#10383,#10384,#10385,#10386,
#10387,#10388,#10389,#10390,#10391,#10392,#10393,#10394,#10395,#10396,#10397,
#10398,#10399,#10400,#10401,#10402,#10403,#10404,#10405,#10406,#10407,#10408,
#10409,#10410,#10411,#10412,#10413,#10414,#10415,#10416,#10417,#10418,#10419,
#10420,#10421,#10422,#10423,#10424,#10425,#10426,#10427,#10428,#10429,#10430,
#10431,#10432,#10433,#10434,#10435,#10436,#10437,#10438,#10439,#10440,#10441,
#10442,#10443,#10444,#10445,#10446,#10447,#10448,#10449,#10450,#10451,#10452,
#10453,#10454,#10455,#10456,#10457,#10458,#10459,#10460,#10461,#10462,#10463,
#10464,#10465,#10466,#10467,#10468,#10469,#10470),.UNSPECIFIED.,.F.,.F.,
(4,2,2,2,2,2,2,2,2,2,2,2,2,2,2,2,2,2,2,2,2,2,2,2,2,2,2,2,2,2,2,2,2,2,2,
2,2,2,2,2,2,2,2,2,2,2,2,2,2,2,2,2,2,2,2,2,2,2,2,2,2,2,2,2,2,2,2,2,2,2,2,
2,2,2,2,2,2,2,2,2,2,2,2,2,2,2,2,2,2,2,2,2,2,2,2,2,2,2,2,2,2,2,2,2,4),(-1.25709415659235,
-1.20640776434646,-1.19949059973977,-1.19633157902701,-1.19389272663439,
-1.19125577253466,-1.18704341112428,-1.17262444675379,-1.14707136650296,
-1.1065532048592,-1.0989463085716,-1.09653949245647,-1.09505883103481,-1.09367705061084,
-1.09174094581927,-1.08700122647073,-1.06320431902338,-1.0468965029411,
-1.00825510778017,-1.00081720987613,-0.997777743550822,-0.99551817125555,
-0.993043409768709,-0.989614315921719,-0.981340028934202,-0.96967436851556,
-0.935260274475562,-0.903870373890439,-0.898972581023899,-0.896954239251892,
-0.895570951648383,-0.894121145694341,-0.891853989000944,-0.884710282026987,
-0.872721694792077,-0.844795173472053,-0.805704450672145,-0.80083364696165,
-0.797763547326173,-0.795342913126938,-0.79263284301255,-0.788087788236677,
-0.769829787890545,-0.731266848868859,-0.702260562142043,-0.698968534151507,
-0.697275433236117,-0.695923688692776,-0.69430574055331,-0.691270475048001,
-0.672291268862101,-0.633023266047516,-0.606229308241835,-0.601521245865389,
-0.598500385783588,-0.596084498009793,-0.593343388847281,-0.588656726000295,
-0.568390739487646,-0.519408740892965,-0.502693531983316,-0.49989697825667,
-0.49816299474903,-0.496808626469107,-0.49522250722303,-0.49233654860809,
-0.477008557221062,-0.431554319187296,-0.406867501217787,-0.402238904143188,
-0.399242214145966,-0.39682823271113,-0.394070355926535,-0.389307154268813,
-0.367831769146908,-0.308068269781723,-0.301817978401269,-0.299588658040684,
-0.298290284251489,-0.296908136839533,-0.294971429070456,-0.290229799167671,
-0.266419438403095,-0.259752200029668,-0.210724612084919,-0.203759203931526,
-0.200539388065986,-0.198131362322505,-0.19587147663332,-0.192184896994095,
-0.182215643775771,-0.167247038458566,-0.134373466722911,-0.104590994909892,
-0.101295954150854,-0.0996020247622997,-0.0982500068753463,-0.0966321943319972,
-0.0935984249278762,-0.0746754017447715,-0.029992239982236,-0.00898602795741176,
-0.0040113896938448,-0.00182984320022838,-0.000585605296785841),
 .UNSPECIFIED.);
#95=B_SPLINE_CURVE_WITH_KNOTS('',3,(#10471,#10472,#10473,#10474,#10475,
#10476,#10477,#10478,#10479,#10480,#10481,#10482,#10483,#10484,#10485,#10486,
#10487,#10488,#10489,#10490,#10491,#10492,#10493,#10494,#10495,#10496,#10497,
#10498,#10499,#10500,#10501,#10502,#10503,#10504,#10505,#10506,#10507,#10508,
#10509,#10510,#10511,#10512,#10513,#10514,#10515,#10516,#10517,#10518,#10519,
#10520,#10521,#10522,#10523,#10524,#10525,#10526,#10527,#10528,#10529,#10530,
#10531,#10532,#10533,#10534,#10535,#10536,#10537,#10538,#10539,#10540,#10541,
#10542,#10543,#10544,#10545,#10546,#10547,#10548,#10549,#10550,#10551,#10552,
#10553,#10554,#10555,#10556,#10557,#10558,#10559,#10560,#10561,#10562,#10563,
#10564,#10565,#10566,#10567,#10568,#10569,#10570,#10571,#10572,#10573,#10574,
#10575,#10576,#10577,#10578,#10579,#10580,#10581,#10582,#10583,#10584,#10585,
#10586,#10587,#10588,#10589,#10590,#10591,#10592,#10593,#10594,#10595,#10596,
#10597,#10598,#10599,#10600,#10601,#10602,#10603,#10604,#10605,#10606,#10607,
#10608,#10609,#10610,#10611,#10612,#10613,#10614,#10615,#10616,#10617,#10618,
#10619,#10620,#10621,#10622,#10623,#10624,#10625,#10626,#10627,#10628,#10629,
#10630,#10631,#10632,#10633,#10634,#10635,#10636,#10637,#10638,#10639,#10640,
#10641,#10642,#10643,#10644,#10645,#10646,#10647,#10648,#10649,#10650,#10651,
#10652,#10653,#10654,#10655,#10656,#10657,#10658,#10659,#10660,#10661,#10662,
#10663,#10664,#10665,#10666,#10667,#10668,#10669,#10670,#10671,#10672,#10673,
#10674,#10675,#10676,#10677,#10678,#10679,#10680,#10681,#10682),
 .UNSPECIFIED.,.F.,.F.,(4,2,2,2,2,2,2,2,2,2,2,2,2,2,2,2,2,2,2,2,2,2,2,2,
2,2,2,2,2,2,2,2,2,2,2,2,2,2,2,2,2,2,2,2,2,2,2,2,2,2,2,2,2,2,2,2,2,2,2,2,
2,2,2,2,2,2,2,2,2,2,2,2,2,2,2,2,2,2,2,2,2,2,2,2,2,2,2,2,2,2,2,2,2,2,2,2,
2,2,2,2,2,2,2,2,2,4),(-1.25713482558798,-1.20644675376907,-1.1995293594853,
-1.19637023363597,-1.19393129996726,-1.19129425787816,-1.18708175565679,
-1.17266230639527,-1.14710836121802,-1.10658880303566,-1.09898171941286,
-1.09657483108271,-1.09509412208213,-1.09371229474114,-1.09177612057331,
-1.08703621356417,-1.06323820447604,-1.04693474455628,-1.00828721555779,
-1.00084927521382,-0.997809742935599,-0.995550104004087,-0.993075252294618,
-0.989646001541223,-0.981371177480144,-0.969704643406962,-0.935286777321501,
-0.903899327022173,-0.899001370195921,-0.896982961051145,-0.895599627333541,
-0.894149773094077,-0.891882540955324,-0.88473859671137,-0.872749611529297,
-0.844822165952047,-0.805730149644355,-0.800859183940215,-0.79778898210454,
-0.795368267259881,-0.792658106784467,-0.788112900276069,-0.769854287050508,
-0.731290039031209,-0.702282832824227,-0.698990695394506,-0.697297538120897,
-0.695945748538126,-0.694327746417834,-0.691292379434596,-0.672312529542336,
-0.633043143986475,-0.606248391037856,-0.601540175329844,-0.598519215674788,
-0.596103247498412,-0.593362046277113,-0.58867522393931,-0.568408510601516,
-0.519424527871355,-0.502709158298285,-0.499912527923449,-0.498178491595468,
-0.496824078577472,-0.495237902870162,-0.492351831340346,-0.477022981814089,
-0.431564473403236,-0.406879740383813,-0.402251111410569,-0.399254358957876,
-0.396840299974115,-0.394082304881359,-0.389318823240375,-0.367840721263265,
-0.308048120815742,-0.301820309537888,-0.299594023689091,-0.298296218232952,
-0.296913626833427,-0.294974606703214,-0.290219023402518,-0.266264641273261,
-0.26219170805801,-0.210233333209888,-0.203584032415346,-0.2004266854532,
-0.198029171265855,-0.195770583917539,-0.192007638571533,-0.181483716850691,
-0.165359799630568,-0.138322430870117,-0.107032303177929,-0.102133213625417,
-0.100114413239973,-0.0987308363359355,-0.0972807521829198,-0.0950132045020056,
-0.087868631250021,-0.0758790001103155,-0.0312122114974481,-0.00918919760743087,
-0.00408090742722382,-0.00185725317603439,-0.000585604919035816),
 .UNSPECIFIED.);
#96=B_SPLINE_CURVE_WITH_KNOTS('',3,(#10688,#10689,#10690,#10691),
 .UNSPECIFIED.,.F.,.F.,(4,4),(-0.000709656257275801,-0.000586166555388535),
 .UNSPECIFIED.);
#97=B_SPLINE_CURVE_WITH_KNOTS('',3,(#10692,#10693,#10694,#10695,#10696,
#10697,#10698,#10699,#10700,#10701,#10702,#10703,#10704,#10705,#10706,#10707,
#10708,#10709,#10710,#10711,#10712,#10713,#10714,#10715,#10716,#10717,#10718,
#10719,#10720,#10721,#10722,#10723,#10724,#10725,#10726,#10727,#10728,#10729,
#10730,#10731,#10732,#10733,#10734,#10735,#10736,#10737,#10738,#10739,#10740,
#10741,#10742,#10743,#10744,#10745,#10746,#10747,#10748,#10749,#10750,#10751,
#10752,#10753,#10754,#10755,#10756,#10757,#10758,#10759,#10760,#10761,#10762,
#10763,#10764,#10765,#10766,#10767,#10768,#10769,#10770,#10771,#10772,#10773,
#10774,#10775,#10776,#10777,#10778,#10779,#10780,#10781,#10782,#10783,#10784,
#10785,#10786,#10787,#10788,#10789,#10790,#10791,#10792,#10793,#10794,#10795,
#10796,#10797,#10798,#10799,#10800,#10801,#10802,#10803,#10804,#10805,#10806,
#10807,#10808,#10809,#10810,#10811,#10812,#10813,#10814,#10815,#10816,#10817,
#10818,#10819,#10820,#10821,#10822,#10823,#10824,#10825,#10826,#10827,#10828,
#10829,#10830,#10831,#10832,#10833,#10834,#10835,#10836,#10837,#10838,#10839,
#10840,#10841,#10842,#10843,#10844,#10845,#10846,#10847,#10848,#10849,#10850,
#10851,#10852,#10853,#10854,#10855,#10856,#10857,#10858,#10859,#10860,#10861,
#10862,#10863,#10864,#10865,#10866,#10867,#10868,#10869,#10870,#10871,#10872,
#10873,#10874,#10875,#10876,#10877,#10878,#10879,#10880,#10881,#10882,#10883,
#10884,#10885,#10886,#10887,#10888,#10889,#10890,#10891,#10892,#10893,#10894,
#10895,#10896,#10897,#10898,#10899,#10900,#10901,#10902,#10903,#10904,#10905,
#10906,#10907,#10908,#10909,#10910,#10911,#10912,#10913,#10914,#10915,#10916,
#10917,#10918,#10919,#10920,#10921,#10922,#10923,#10924,#10925,#10926,#10927,
#10928,#10929,#10930,#10931,#10932,#10933,#10934,#10935,#10936,#10937,#10938,
#10939,#10940,#10941,#10942,#10943,#10944,#10945,#10946,#10947,#10948,#10949,
#10950,#10951,#10952,#10953,#10954,#10955,#10956,#10957,#10958,#10959,#10960,
#10961,#10962,#10963,#10964,#10965,#10966,#10967,#10968,#10969,#10970,#10971,
#10972,#10973,#10974,#10975,#10976,#10977,#10978,#10979),.UNSPECIFIED.,
 .F.,.F.,(4,2,2,2,2,2,2,2,2,2,2,2,2,2,2,2,2,2,2,2,2,2,2,2,2,2,2,2,2,2,2,
2,2,2,2,2,2,2,2,2,2,2,2,2,2,2,2,2,2,2,2,2,2,2,2,2,2,2,2,2,2,2,2,2,2,2,2,
2,2,2,2,2,2,2,2,2,2,2,2,2,2,2,2,2,2,2,2,2,2,2,2,2,2,2,2,2,2,2,2,2,2,2,2,
2,2,2,2,2,2,2,2,2,2,2,2,2,2,2,2,2,2,2,2,2,2,2,2,2,2,2,2,2,2,2,2,2,2,2,2,
2,2,2,2,4),(-2.513227510422,-2.49549100342488,-2.49282775470627,-2.49113196652391,
-2.48981633945341,-2.48846331221699,-2.48686903560395,-2.48402376026985,
-2.47121567323448,-2.45941292655917,-2.41532654529159,-2.39744834645147,
-2.39293328263591,-2.39023027791097,-2.38780916465,-2.38472918193759,-2.37982397991019,
-2.34351958773065,-2.29967371101752,-2.29547121444927,-2.29225318682126,
-2.29060369057569,-2.29059918669318,-2.29059491656758,-2.29059059130032,
-2.29058621008268,-2.2905817721001,-2.29057727652477,-2.29057272250903,
-2.2905681091623,-2.29056343561767,-2.29055870099257,-2.29055390437244,
-2.29054904483257,-2.29054412142136,-2.29053913318046,-2.29053407916612,
-2.2905289583675,-2.29052376976824,-2.29051851233955,-2.2905131850438,-2.29050778680207,
-2.2905023165664,-2.29049677322567,-2.2904911556495,-2.29048546270861,-2.29047969324334,
-2.29047384609186,-2.2904679200371,-2.29046191386199,-2.29045582631849,
-2.2904496561538,-2.2904434020707,-2.28909144987658,-2.28738802560439,-2.28469198556758,
-2.27005015595464,-2.26571145215248,-2.23001093200308,-2.20224342815924,
-2.19537099996554,-2.19218615081721,-2.18975169922929,-2.18710257091817,
-2.18283345204478,-2.16934355302114,-2.11226828181438,-2.09578216400288,
-2.09284344045,-2.09124613476314,-2.08989309562249,-2.08817473138067,-2.08542970579341,
-2.06978975619767,-2.05361936028148,-2.02381675878906,-2.00796735620891,
-1.99757322460325,-1.99382843870656,-1.99129176904384,-1.98882863975991,
-1.98587432199708,-1.9784655127671,-1.93332593671369,-1.90778017751212,
-1.90002654650968,-1.89482215648459,-1.89281286038972,-1.89141748566302,
-1.89013738325237,-1.88835292768879,-1.88370483978494,-1.84410029648695,
-1.80226415702097,-1.79642417589041,-1.79343926464616,-1.7910263780879,
-1.78826054926734,-1.78358272938012,-1.76532655909163,-1.75735536328343,
-1.71259138206219,-1.69735056706792,-1.69446892929207,-1.69288382448007,
-1.69152946773313,-1.689794410528,-1.68699405482629,-1.67017989429762,-1.62132463450118,
-1.60108158385312,-1.59639671836579,-1.59365610022755,-1.59124030427927,
-1.5882191091709,-1.58350961011462,-1.5566759269351,-1.5174167529684,-1.49843253711033,
-1.49539705882048,-1.49377910527363,-1.49242741456157,-1.49073446152159,
-1.48744295515195,-1.45847707440362,-1.41991674893802,-1.40166003702122,
-1.39711521490905,-1.39440522911728,-1.39198463399448,-1.38891453513705,
-1.38404359029518,-1.34491078530148,-1.31689778684609,-1.29919084942543,
-1.29620196856318,-1.29459389314123,-1.29324159762496,-1.29153667786007,
-1.28883631183996,-1.27411638686656,-1.27004059496124,-1.2572678417837,
-1.25709415659235),.UNSPECIFIED.);
#98=B_SPLINE_CURVE_WITH_KNOTS('',3,(#10980,#10981,#10982,#10983,#10984,
#10985,#10986,#10987,#10988,#10989,#10990,#10991,#10992,#10993,#10994,#10995,
#10996,#10997,#10998,#10999,#11000,#11001,#11002,#11003,#11004,#11005,#11006,
#11007,#11008,#11009,#11010,#11011,#11012,#11013,#11014,#11015,#11016,#11017,
#11018,#11019,#11020,#11021,#11022,#11023,#11024,#11025,#11026,#11027,#11028,
#11029,#11030,#11031,#11032,#11033,#11034,#11035,#11036,#11037,#11038,#11039,
#11040,#11041,#11042,#11043,#11044,#11045,#11046,#11047,#11048,#11049,#11050,
#11051,#11052,#11053,#11054,#11055,#11056,#11057,#11058,#11059,#11060,#11061,
#11062,#11063,#11064,#11065,#11066,#11067,#11068,#11069,#11070,#11071,#11072,
#11073,#11074,#11075,#11076,#11077,#11078,#11079,#11080,#11081,#11082,#11083,
#11084,#11085,#11086,#11087,#11088,#11089,#11090,#11091,#11092,#11093,#11094,
#11095,#11096,#11097,#11098,#11099,#11100,#11101,#11102,#11103,#11104,#11105,
#11106,#11107,#11108,#11109,#11110,#11111,#11112,#11113,#11114,#11115,#11116,
#11117,#11118,#11119,#11120,#11121,#11122,#11123,#11124,#11125,#11126,#11127,
#11128,#11129,#11130,#11131,#11132,#11133,#11134,#11135,#11136,#11137,#11138,
#11139,#11140,#11141,#11142,#11143,#11144,#11145,#11146,#11147,#11148,#11149,
#11150,#11151,#11152,#11153,#11154,#11155,#11156,#11157,#11158,#11159,#11160,
#11161,#11162,#11163,#11164,#11165,#11166,#11167,#11168,#11169,#11170,#11171,
#11172,#11173,#11174,#11175,#11176,#11177,#11178,#11179,#11180,#11181,#11182,
#11183,#11184,#11185,#11186,#11187,#11188,#11189,#11190,#11191),
 .UNSPECIFIED.,.F.,.F.,(4,2,2,2,2,2,2,2,2,2,2,2,2,2,2,2,2,2,2,2,2,2,2,2,
2,2,2,2,2,2,2,2,2,2,2,2,2,2,2,2,2,2,2,2,2,2,2,2,2,2,2,2,2,2,2,2,2,2,2,2,
2,2,2,2,2,2,2,2,2,2,2,2,2,2,2,2,2,2,2,2,2,2,2,2,2,2,2,2,2,2,2,2,2,2,2,2,
2,2,2,2,2,2,2,2,2,4),(-2.51288241066526,-2.51214445501738,-2.51060224277513,
-2.50790860514932,-2.50338599726915,-2.48645030077016,-2.47441910954673,
-2.4511797341194,-2.42762592101787,-2.42022974928811,-2.41520667626236,
-2.41322566847082,-2.41183598549087,-2.41054988648136,-2.40874200974333,
-2.40391420421472,-2.36807159047678,-2.3365886990444,-2.32022151203857,
-2.31582987750348,-2.31355025120258,-2.31119011739592,-2.30837016025852,
-2.30329613694199,-2.27790866130605,-2.23311754113698,-2.21787546095408,
-2.21499427581866,-2.21340950025191,-2.21205547480733,-2.21032090648445,
-2.2075214636637,-2.19071717656399,-2.14186829819052,-2.12162929848748,
-2.11694550551634,-2.11420553445069,-2.11179032075548,-2.10876986948682,
-2.10406156036042,-2.07723599856565,-2.03798477346606,-2.01900485895288,
-2.01597010135829,-2.0143525348357,-2.01300116913392,-2.01130862524779,
-2.00801792037228,-1.97906797508171,-1.94050984249165,-1.92225585577146,
-1.91771200074851,-1.91500263889804,-1.91258263059342,-1.90951331613283,
-1.90464369616122,-1.86551689275737,-1.83750193776643,-1.8198103364135,
-1.81682260298471,-1.81521500539607,-1.81386302868469,-1.81215840570422,
-1.80945831582091,-1.79473446639502,-1.74393068086411,-1.72340855703997,
-1.71870634799361,-1.71596238252787,-1.71354773036474,-1.71053335828633,
-1.70584493530853,-1.67965802593662,-1.63561252066912,-1.62046884238219,
-1.61759248289826,-1.61600875369154,-1.61465461915812,-1.612918616231,-1.61011436681868,
-1.59319163864348,-1.54445216217191,-1.52422993928622,-1.5195472697316,
-1.51680755321848,-1.51439232056878,-1.51137152418374,-1.50666205293365,
-1.47980224716878,-1.44058212678616,-1.42160779289788,-1.41857323996224,
-1.4169557219418,-1.41560436139287,-1.41391177951697,-1.41062087268735,
-1.38338746555306,-1.34839031277509,-1.33321132179092,-1.32313989675661,
-1.31944004273002,-1.31691299832961,-1.31444319405084,-1.31090563945398,
-1.30439157194774,-1.2568423001509),.UNSPECIFIED.);
#99=B_SPLINE_CURVE_WITH_KNOTS('',3,(#11196,#11197,#11198,#11199,#11200,
#11201,#11202,#11203,#11204,#11205,#11206,#11207,#11208,#11209,#11210,#11211,
#11212,#11213,#11214,#11215,#11216,#11217,#11218,#11219,#11220,#11221,#11222,
#11223,#11224,#11225,#11226,#11227,#11228,#11229,#11230,#11231,#11232,#11233,
#11234,#11235,#11236,#11237,#11238,#11239,#11240,#11241,#11242,#11243,#11244,
#11245,#11246,#11247,#11248,#11249,#11250,#11251,#11252,#11253,#11254,#11255,
#11256,#11257,#11258,#11259,#11260,#11261,#11262,#11263,#11264,#11265,#11266,
#11267,#11268,#11269,#11270,#11271,#11272,#11273,#11274,#11275,#11276,#11277,
#11278,#11279,#11280,#11281,#11282,#11283,#11284,#11285,#11286,#11287,#11288,
#11289,#11290,#11291,#11292,#11293,#11294,#11295,#11296,#11297,#11298,#11299,
#11300,#11301,#11302,#11303,#11304,#11305,#11306,#11307,#11308,#11309,#11310,
#11311,#11312,#11313,#11314,#11315,#11316,#11317,#11318,#11319,#11320,#11321,
#11322,#11323,#11324,#11325,#11326,#11327,#11328,#11329,#11330,#11331,#11332,
#11333,#11334,#11335,#11336,#11337,#11338,#11339,#11340,#11341,#11342,#11343,
#11344,#11345,#11346,#11347,#11348,#11349,#11350,#11351,#11352,#11353,#11354,
#11355,#11356,#11357,#11358,#11359,#11360,#11361,#11362,#11363,#11364,#11365,
#11366,#11367,#11368,#11369,#11370,#11371,#11372,#11373,#11374,#11375,#11376,
#11377,#11378,#11379,#11380,#11381,#11382,#11383,#11384,#11385,#11386,#11387,
#11388,#11389,#11390,#11391,#11392,#11393,#11394,#11395,#11396,#11397,#11398,
#11399,#11400,#11401,#11402,#11403),.UNSPECIFIED.,.F.,.F.,(4,2,2,2,2,2,
2,2,2,2,2,2,2,2,2,2,2,2,2,2,2,2,2,2,2,2,2,2,2,2,2,2,2,2,2,2,2,2,2,2,2,2,
2,2,2,2,2,2,2,2,2,2,2,2,2,2,2,2,2,2,2,2,2,2,2,2,2,2,2,2,2,2,2,2,2,2,2,2,
2,2,2,2,2,2,2,2,2,2,2,2,2,2,2,2,2,2,2,2,2,2,2,2,2,4),(-1.2571395732103,
-1.21587274758227,-1.17959905046059,-1.17478545014533,-1.17297907343572,
-1.17169312534346,-1.17030256268692,-1.16831859623973,-1.16327894066679,
-1.1558518451504,-1.13213488728549,-1.08438557842686,-1.07787401689846,
-1.07433668667642,-1.07186649978398,-1.06933861031397,-1.06563668276486,
-1.05555442071088,-1.04035235318455,-1.00516879234281,-0.978093046261673,
-0.974801173174284,-0.973108132803348,-0.971756426298004,-0.970138511402003,
-0.967103275275226,-0.94812300442694,-0.908847135917745,-0.882063884310117,
-0.877356297404026,-0.874335625987243,-0.87191981433345,-0.869178711195009,
-0.864491858203241,-0.844221568498299,-0.795208829567818,-0.77852885281364,
-0.77573382360805,-0.774000321739977,-0.772646025083837,-0.77105963539429,
-0.768172298874631,-0.752814518413845,-0.707121594213327,-0.682686981858239,
-0.678069153500248,-0.675075799817945,-0.672662133857943,-0.669902026562685,
-0.665128364851073,-0.643477856951114,-0.595049789996574,-0.579250061705756,
-0.576493366971042,-0.574771355188765,-0.573417875569529,-0.571822888318959,
-0.568895703176516,-0.552678219397519,-0.498884531695963,-0.482450998923153,
-0.477874069639845,-0.47515699661495,-0.472979522737904,-0.470038419377697,
-0.464413199315306,-0.422615631294253,-0.382569438506089,-0.377922750983697,
-0.376138368740135,-0.374858215763686,-0.373462655829577,-0.371452885587081,
-0.366246055918608,-0.35848866151363,-0.332921653310087,-0.287847258389022,
-0.280436456141002,-0.277481670090351,-0.27501825796628,-0.27248141749682,
-0.268736610879544,-0.258344077884017,-0.242496420805238,-0.215202655607788,
-0.183744354591778,-0.178839674545282,-0.176820143031453,-0.175436584436919,
-0.174016157870222,-0.171906553255985,-0.169369999632317,-0.164563042519488,
-0.152552126040816,-0.127153744163367,-0.0890005180998729,-0.0815382465895854,
-0.0784945098849429,-0.0762338182520622,-0.0737598403893136,-0.0703355435282101,
-0.0620912127834048,-0.0504812419885443,-0.000709656257275801),
 .UNSPECIFIED.);
#100=B_SPLINE_CURVE_WITH_KNOTS('',3,(#11404,#11405,#11406,#11407,#11408,
#11409,#11410,#11411,#11412,#11413,#11414,#11415,#11416,#11417,#11418,#11419,
#11420,#11421,#11422,#11423,#11424,#11425,#11426,#11427,#11428,#11429,#11430,
#11431,#11432,#11433,#11434,#11435,#11436,#11437,#11438,#11439,#11440,#11441,
#11442,#11443,#11444,#11445,#11446,#11447,#11448,#11449,#11450,#11451,#11452,
#11453,#11454,#11455,#11456,#11457,#11458,#11459,#11460,#11461,#11462,#11463,
#11464,#11465,#11466,#11467,#11468,#11469,#11470,#11471,#11472,#11473,#11474,
#11475,#11476,#11477,#11478,#11479,#11480,#11481,#11482,#11483,#11484,#11485,
#11486,#11487,#11488,#11489,#11490,#11491,#11492,#11493,#11494,#11495,#11496,
#11497,#11498,#11499,#11500,#11501,#11502,#11503,#11504,#11505,#11506,#11507,
#11508,#11509,#11510,#11511,#11512,#11513,#11514,#11515,#11516,#11517,#11518,
#11519,#11520,#11521,#11522,#11523,#11524,#11525,#11526,#11527,#11528,#11529,
#11530,#11531,#11532,#11533,#11534,#11535,#11536,#11537,#11538,#11539,#11540,
#11541,#11542,#11543,#11544,#11545,#11546,#11547,#11548,#11549,#11550,#11551,
#11552,#11553,#11554,#11555,#11556,#11557,#11558,#11559,#11560,#11561,#11562,
#11563,#11564,#11565,#11566,#11567,#11568,#11569,#11570,#11571,#11572,#11573,
#11574,#11575,#11576,#11577,#11578,#11579,#11580,#11581,#11582,#11583,#11584,
#11585,#11586,#11587,#11588,#11589,#11590,#11591,#11592,#11593,#11594,#11595,
#11596,#11597,#11598,#11599,#11600,#11601,#11602,#11603,#11604,#11605,#11606,
#11607,#11608,#11609,#11610,#11611,#11612,#11613,#11614,#11615,#11616,#11617,
#11618,#11619,#11620,#11621,#11622,#11623,#11624,#11625,#11626,#11627,#11628,
#11629,#11630,#11631,#11632,#11633,#11634,#11635,#11636,#11637,#11638,#11639,
#11640,#11641,#11642,#11643,#11644,#11645,#11646,#11647,#11648,#11649,#11650,
#11651,#11652,#11653,#11654,#11655,#11656,#11657,#11658,#11659,#11660,#11661,
#11662,#11663,#11664,#11665,#11666,#11667,#11668,#11669,#11670,#11671,#11672,
#11673,#11674,#11675),.UNSPECIFIED.,.F.,.F.,(4,2,2,2,2,2,2,2,2,2,2,2,2,
2,2,2,2,2,2,2,2,2,2,2,2,2,2,2,2,2,2,2,2,2,2,2,2,2,2,2,2,2,2,2,2,2,2,2,2,
2,2,2,2,2,2,2,2,2,2,2,2,2,2,2,2,2,2,2,2,2,2,2,2,2,2,2,2,2,2,2,2,2,2,2,2,
2,2,2,2,2,2,2,2,2,2,2,2,2,2,2,2,2,2,2,2,2,2,2,2,2,2,2,2,2,2,2,2,2,2,2,2,
2,2,2,2,2,2,2,2,2,2,2,2,2,2,4),(-1.2568423001509,-1.2566698222456,-1.22541220817351,
-1.22051497282777,-1.21849696950792,-1.21711394976688,-1.21566446046196,
-1.21339786217466,-1.20625643975202,-1.19427227502351,-1.16634924188049,
-1.12726561901582,-1.12239584948917,-1.11932638806809,-1.11690624854978,
-1.11419672336264,-1.10965256110062,-1.09139783300629,-1.05284084188285,
-1.02384290342377,-1.02055154933599,-1.01885879412598,-1.01750732510715,
-1.01588970615908,-1.0128550566056,-0.993879639747066,-0.954619185808075,
-0.927831209380359,-0.923124124737194,-0.920103885873031,-0.91768849096575,
-0.914947936776402,-0.910262212208136,-0.890000098150051,-0.8410263697577,
-0.824316438153823,-0.821520532228975,-0.819786925448196,-0.818432835038808,
-0.81684702213994,-0.813961573251889,-0.798635081334897,-0.753177254540022,
-0.728508971189148,-0.723881885248253,-0.720885979558173,-0.718472503499583,
-0.715715066193194,-0.710952272498883,-0.689471978183512,-0.629594428850235,
-0.62345090106714,-0.621236501208349,-0.619941235062353,-0.618557484133402,
-0.61661059042971,-0.611804736155214,-0.587317023325035,-0.546955962271519,
-0.528573099819053,-0.523885693868055,-0.521117519767615,-0.518704625799575,
-0.515722333832088,-0.50989605779365,-0.468541453264623,-0.428356469632953,
-0.423727618598784,-0.42194576611162,-0.420666259190551,-0.419270060004242,
-0.417257134481112,-0.412029725890219,-0.404231361134605,-0.378427412343682,
-0.33368169747574,-0.326254049827473,-0.323296542279631,-0.320832392678563,
-0.318296365322415,-0.31455571753035,-0.304194204918573,-0.288411841575985,
-0.256781843283623,-0.227066115286565,-0.223790139820875,-0.222100419016791,
-0.220748735840961,-0.220742813218816,-0.220736969505651,-0.220731203506629,
-0.220725514037649,-0.220719899972107,-0.220714360174469,-0.220708893523408,
-0.220703498924682,-0.220698175293754,-0.22069292159715,-0.22068773679388,
-0.220682619843728,-0.220677569763452,-0.220672585565024,-0.220667666277393,
-0.220662810925145,-0.220658018589557,-0.220653288358301,-0.220648619309919,
-0.22064401057169,-0.220639461272971,-0.220634970523,-0.220630537475715,
-0.220626161317182,-0.220621841213998,-0.220617576367928,-0.220613071472846,
-0.218961874607189,-0.215733042849444,-0.211516000878359,-0.167272700134033,
-0.131388197292718,-0.126491494100865,-0.123413513883083,-0.120991920219225,
-0.118286243819702,-0.113761631106796,-0.0957742494569127,-0.0481363768823709,
-0.0369810077054305,-0.0267619536485706,-0.0241129102553496,-0.0225631826468939,
-0.0212349028317719,-0.0199043353833102,-0.0181638798968172,-0.0153923940619404,
-0.000584983237805827),.UNSPECIFIED.);
#101=B_SPLINE_CURVE_WITH_KNOTS('',3,(#11680,#11681,#11682,#11683,#11684,
#11685,#11686,#11687,#11688,#11689,#11690,#11691,#11692,#11693,#11694,#11695,
#11696,#11697,#11698,#11699,#11700,#11701,#11702,#11703,#11704,#11705,#11706,
#11707,#11708,#11709,#11710,#11711,#11712,#11713,#11714,#11715,#11716,#11717,
#11718,#11719,#11720,#11721,#11722,#11723,#11724,#11725,#11726,#11727,#11728,
#11729,#11730,#11731,#11732,#11733,#11734,#11735,#11736,#11737,#11738,#11739,
#11740,#11741,#11742,#11743,#11744,#11745,#11746,#11747,#11748,#11749,#11750,
#11751,#11752,#11753,#11754,#11755,#11756,#11757,#11758,#11759,#11760,#11761,
#11762,#11763,#11764,#11765,#11766,#11767,#11768,#11769,#11770,#11771,#11772,
#11773,#11774,#11775,#11776,#11777,#11778,#11779,#11780,#11781,#11782,#11783,
#11784,#11785,#11786,#11787,#11788,#11789,#11790,#11791,#11792,#11793,#11794,
#11795,#11796,#11797,#11798,#11799,#11800,#11801,#11802,#11803,#11804,#11805,
#11806,#11807,#11808,#11809,#11810,#11811,#11812,#11813,#11814,#11815,#11816,
#11817,#11818,#11819,#11820,#11821,#11822,#11823,#11824,#11825,#11826,#11827,
#11828,#11829,#11830,#11831,#11832,#11833,#11834,#11835,#11836,#11837,#11838,
#11839,#11840,#11841,#11842,#11843,#11844,#11845,#11846,#11847,#11848,#11849,
#11850,#11851,#11852,#11853,#11854,#11855,#11856,#11857,#11858,#11859,#11860,
#11861,#11862,#11863,#11864,#11865,#11866,#11867,#11868,#11869,#11870,#11871,
#11872,#11873,#11874,#11875,#11876,#11877,#11878,#11879,#11880,#11881,#11882,
#11883,#11884,#11885,#11886,#11887,#11888,#11889,#11890,#11891,#11892,#11893,
#11894,#11895,#11896,#11897,#11898,#11899,#11900,#11901,#11902,#11903,#11904,
#11905),.UNSPECIFIED.,.F.,.F.,(4,2,2,2,2,2,2,2,2,2,2,2,2,2,2,2,2,2,2,2,
2,2,2,2,2,2,2,2,2,2,2,2,2,2,2,2,2,2,2,2,2,2,2,2,2,2,2,2,2,2,2,2,2,2,2,2,
2,2,2,2,2,2,2,2,2,2,2,2,2,2,2,2,2,2,2,2,2,2,2,2,2,2,2,2,2,2,2,2,2,2,2,2,
2,2,2,2,2,2,2,2,2,2,2,2,2,2,2,2,2,2,2,2,4),(-2.5135518234981,-2.47659661189999,
-2.47236394980857,-2.46954258796683,-2.4668230303502,-2.46440446366006,
-2.46135122278182,-2.45653542941664,-2.42634523323622,-2.40243503862959,
-2.37764166219088,-2.37034208190646,-2.36862191645876,-2.36701353481963,
-2.36566149194363,-2.36395753638232,-2.36125988735885,-2.34658797162409,
-2.34299810396128,-2.33833144470471,-2.2994607991541,-2.2836681912839,-2.27670083268194,
-2.27122335335112,-2.26828169159173,-2.26587165891324,-2.26307310110431,
-2.25825131703111,-2.23802946477239,-2.19153911663431,-2.17255181116262,
-2.16951642227373,-2.16789856775074,-2.16654698975295,-2.16485421556432,
-2.16156316551322,-2.13290948589647,-2.09410750441372,-2.0757949541683,
-2.07124618961755,-2.06853548053722,-2.06611525428305,-2.06304700262955,
-2.05818175003555,-2.0185046895441,-1.98833052162263,-1.97313430702212,
-1.97025501678423,-1.96867049511841,-1.96731619519208,-1.96558064117932,
-1.96277838846072,-1.94591371543415,-1.89711011504228,-1.87687596239538,
-1.87219194986349,-1.86945165473324,-1.86703603717352,-1.86401492471449,
-1.85930528178858,-1.83245871193674,-1.79321616035522,-1.77423584936763,
-1.77120069502457,-1.769582887682,-1.76823130366523,-1.76653846484517,-1.76324712459706,
-1.73420957683203,-1.69571076542024,-1.67746927051293,-1.67292584867029,
-1.67021630620254,-1.66779586259606,-1.66472562338087,-1.65985378951481,
-1.62075026642361,-1.5928054348406,-1.5750158236052,-1.57202393976116,-1.57041530281815,
-1.56906316168771,-1.56735922955389,-1.56466188885155,-1.5499991950463,
-1.54641876152499,-1.5330158196089,-1.50294444773783,-1.48710576600214,
-1.47671678354855,-1.4729727360809,-1.4704362484655,-1.46797305379231,-1.46501836655225,
-1.45760704584601,-1.41257226268484,-1.38694949731365,-1.37918258791311,
-1.37397155702751,-1.37196127208251,-1.3705657223838,-1.3692858663284,-1.36750229257816,
-1.3628602896076,-1.32309258642019,-1.29427990913698,-1.28399829066645,
-1.27648602457344,-1.2731857217843,-1.27073334466664,-1.26844402289056,
-1.26528627603858,-1.2571395732103),.UNSPECIFIED.);
#102=B_SPLINE_CURVE_WITH_KNOTS('',3,(#11906,#11907,#11908,#11909,#11910,
#11911,#11912,#11913,#11914,#11915),.UNSPECIFIED.,.F.,.F.,(4,1,1,1,1,1,
1,4),(97.3893809475092,98.2770128807329,99.2731119575535,100.269211034374,
101.265310111195,102.261409188015,103.257508264836,103.672551685613),
 .UNSPECIFIED.);
#103=B_SPLINE_CURVE_WITH_KNOTS('',3,(#11920,#11921,#11922,#11923,#11924,
#11925,#11926,#11927,#11928,#11929,#11930),.UNSPECIFIED.,.F.,.F.,(4,1,1,
1,1,1,1,1,4),(103.672560201549,103.933669101939,104.92976817876,105.925867255581,
106.921966332401,107.918065409222,108.914164486042,109.910263562863,109.955742875643),
 .UNSPECIFIED.);
#104=B_SPLINE_CURVE_WITH_KNOTS('',3,(#11931,#11932,#11933,#11934,#11935,
#11936,#11937,#11938,#11939,#11940,#11941,#11942,#11943,#11944,#11945,#11946,
#11947,#11948,#11949,#11950,#11951,#11952,#11953,#11954,#11955,#11956,#11957,
#11958,#11959,#11960,#11961,#11962,#11963,#11964,#11965,#11966,#11967,#11968,
#11969,#11970,#11971,#11972,#11973,#11974,#11975,#11976,#11977,#11978,#11979,
#11980,#11981,#11982,#11983,#11984,#11985,#11986,#11987,#11988,#11989,#11990,
#11991,#11992,#11993,#11994,#11995,#11996,#11997,#11998,#11999,#12000,#12001,
#12002,#12003,#12004,#12005,#12006,#12007,#12008,#12009,#12010,#12011,#12012,
#12013,#12014,#12015,#12016,#12017,#12018,#12019,#12020,#12021,#12022,#12023,
#12024,#12025,#12026,#12027,#12028,#12029,#12030,#12031,#12032,#12033,#12034,
#12035,#12036,#12037,#12038,#12039,#12040,#12041,#12042,#12043,#12044,#12045,
#12046,#12047,#12048,#12049,#12050,#12051,#12052,#12053,#12054,#12055,#12056,
#12057,#12058,#12059,#12060,#12061,#12062,#12063,#12064,#12065,#12066,#12067,
#12068,#12069,#12070,#12071,#12072,#12073,#12074,#12075,#12076,#12077,#12078,
#12079,#12080,#12081,#12082,#12083,#12084,#12085,#12086,#12087,#12088,#12089,
#12090,#12091,#12092,#12093,#12094,#12095,#12096,#12097,#12098,#12099,#12100,
#12101,#12102,#12103,#12104,#12105,#12106,#12107,#12108,#12109,#12110,#12111,
#12112,#12113,#12114,#12115,#12116,#12117,#12118,#12119,#12120,#12121,#12122,
#12123,#12124,#12125,#12126,#12127,#12128,#12129,#12130,#12131,#12132,#12133,
#12134,#12135,#12136,#12137,#12138,#12139,#12140,#12141,#12142,#12143,#12144,
#12145,#12146,#12147,#12148),.UNSPECIFIED.,.F.,.F.,(4,2,2,2,2,2,2,2,2,2,
2,2,2,2,2,2,2,2,2,2,2,2,2,2,2,2,2,2,2,2,2,2,2,2,2,2,2,2,2,2,2,2,2,2,2,2,
2,2,2,2,2,2,2,2,2,2,2,2,2,2,2,2,2,2,2,2,2,2,2,2,2,2,2,2,2,2,2,2,2,2,2,2,
2,2,2,2,2,2,2,2,2,2,2,2,2,2,2,2,2,2,2,2,2,2,2,2,2,2,4),(-2.51313020307964,
-2.50351913808445,-2.50050660773422,-2.49815843919155,-2.49581373346396,
-2.49314272965445,-2.48877172810962,-2.47435014552162,-2.42228289418547,
-2.40219469446745,-2.39912406872919,-2.39749907227943,-2.3961482485783,
-2.39446481911957,-2.3912158846612,-2.36793986594067,-2.33408335644315,
-2.31567916766454,-2.30795000318622,-2.30372337978279,-2.30090475510632,
-2.29823464985763,-2.29584041929594,-2.29282152493645,-2.2881178180231,
-2.26151404940473,-2.22207530174103,-2.20306331629715,-2.20002769171616,
-2.19841003763219,-2.19705881734433,-2.19536673018494,-2.19207770441167,
-2.16537599340211,-2.13034325459464,-2.11486423377487,-2.10799250833549,
-2.1025149943886,-2.0996051560735,-2.09721954594407,-2.09440390519471,-2.0895056516581,
-2.06811523218513,-2.02397008969713,-2.00402221278937,-2.00095571201658,
-1.99933148154723,-1.99798047831947,-1.99629580463093,-1.99304157252599,
-1.96943828362305,-1.94082968756209,-1.91141036606866,-1.90433587884971,
-1.90111409058145,-1.89867444862865,-1.89636343395275,-1.8924691711515,
-1.88188348039685,-1.82137096305922,-1.80465191282259,-1.80170330066452,
-1.80010392014619,-1.79875112235557,-1.79703561297581,-1.7942999233654,
-1.77884704784025,-1.76194506009828,-1.76085454667944,-1.72582171983243,
-1.71404391167468,-1.70570869505985,-1.7022698871658,-1.69979352346803,
-1.69753617017616,-1.69393167030004,-1.68716690334331,-1.64438646555818,
-1.60948306158413,-1.60382417254802,-1.60174805580431,-1.60033934262863,
-1.59907256916522,-1.59700637548609,-1.59182127597304,-1.53134688725329,
-1.50928203603504,-1.50448466034263,-1.50171971246554,-1.4993070443035,
-1.49632169307475,-1.49172901778547,-1.46787020047601,-1.42593250836169,
-1.40646244030087,-1.40341089885887,-1.40178966175489,-1.40043829387519,
-1.39874958850897,-1.39547736270904,-1.36549513075084,-1.32771629500846,
-1.30964708016495,-1.30511684989029,-1.30241025822242,-1.29998937402529,
-1.29691438225343,-1.29202658440206,-1.25692875797613),.UNSPECIFIED.);
#105=B_SPLINE_CURVE_WITH_KNOTS('',3,(#12153,#12154,#12155,#12156,#12157,
#12158,#12159,#12160,#12161,#12162,#12163,#12164,#12165,#12166,#12167,#12168,
#12169,#12170,#12171,#12172,#12173,#12174,#12175,#12176,#12177,#12178,#12179,
#12180,#12181,#12182,#12183,#12184,#12185,#12186,#12187,#12188,#12189,#12190,
#12191,#12192,#12193,#12194,#12195,#12196,#12197,#12198,#12199,#12200,#12201,
#12202,#12203,#12204,#12205,#12206,#12207,#12208,#12209,#12210,#12211,#12212,
#12213,#12214,#12215,#12216,#12217,#12218,#12219,#12220,#12221,#12222,#12223,
#12224,#12225,#12226,#12227,#12228,#12229,#12230,#12231,#12232,#12233,#12234,
#12235,#12236,#12237,#12238,#12239,#12240,#12241,#12242,#12243,#12244,#12245,
#12246,#12247,#12248,#12249,#12250,#12251,#12252,#12253,#12254,#12255,#12256,
#12257,#12258,#12259,#12260,#12261,#12262,#12263,#12264,#12265,#12266,#12267,
#12268,#12269,#12270,#12271,#12272,#12273,#12274,#12275,#12276,#12277,#12278,
#12279,#12280,#12281,#12282,#12283,#12284,#12285,#12286,#12287,#12288,#12289,
#12290,#12291,#12292,#12293,#12294,#12295,#12296,#12297,#12298,#12299,#12300,
#12301,#12302,#12303,#12304,#12305,#12306,#12307,#12308,#12309,#12310,#12311,
#12312,#12313,#12314,#12315,#12316,#12317,#12318,#12319,#12320,#12321,#12322,
#12323,#12324,#12325,#12326,#12327,#12328,#12329,#12330,#12331,#12332,#12333,
#12334,#12335,#12336,#12337,#12338,#12339),.UNSPECIFIED.,.F.,.F.,(4,3,3,
3,3,3,3,3,3,3,3,3,3,3,3,3,3,3,3,3,3,3,3,3,3,3,3,3,3,3,3,3,3,3,3,3,3,3,3,
3,3,3,3,3,3,3,3,3,3,3,3,3,3,3,3,3,3,3,3,3,3,3,4),(109.955743251696,110.0599685937,
110.165767849448,110.269723962552,110.37362116787,110.477496011397,110.584712668469,
110.688717274338,110.79753995701,110.906362639683,111.011342877977,111.116166140091,
111.22086671262,111.325501816955,111.430106980845,111.534717688392,111.639438820454,
111.744221384281,111.849184855582,111.902461716504,112.007441954798,112.112265216913,
112.216965789442,112.321600893777,112.426206057666,112.530816765213,112.635537897276,
112.740320461102,112.845283932403,112.898560793325,113.003541031619,113.108364293734,
113.213064866263,113.317699970598,113.422305134487,113.526915842034,113.631636974096,
113.736419537923,113.841383009224,113.894659870145,113.999640108439,114.104463370553,
114.209163943082,114.313799047417,114.418404211306,114.523014918853,114.627736050915,
114.732518614742,114.837482086043,114.890758946966,114.99573918526,115.100562447374,
115.205263019903,115.309898124238,115.414503288127,115.519113995675,115.623835127737,
115.728617691563,115.833581162864,115.886858023786,116.007775537452,116.127668495559,
116.238928182439),.UNSPECIFIED.);
#106=B_SPLINE_CURVE_WITH_KNOTS('',3,(#12340,#12341,#12342,#12343,#12344,
#12345,#12346,#12347,#12348,#12349,#12350,#12351,#12352,#12353,#12354,#12355,
#12356,#12357,#12358,#12359,#12360,#12361,#12362,#12363,#12364,#12365,#12366,
#12367,#12368,#12369,#12370,#12371,#12372,#12373,#12374,#12375,#12376,#12377,
#12378,#12379,#12380,#12381,#12382,#12383,#12384,#12385,#12386,#12387,#12388,
#12389,#12390,#12391,#12392,#12393,#12394,#12395,#12396,#12397,#12398,#12399,
#12400,#12401,#12402,#12403,#12404,#12405,#12406,#12407,#12408,#12409,#12410,
#12411,#12412,#12413,#12414,#12415,#12416,#12417,#12418,#12419,#12420,#12421,
#12422,#12423,#12424,#12425,#12426,#12427,#12428,#12429,#12430,#12431,#12432,
#12433,#12434,#12435,#12436,#12437,#12438,#12439,#12440,#12441,#12442,#12443,
#12444,#12445,#12446,#12447,#12448,#12449,#12450,#12451,#12452,#12453,#12454,
#12455,#12456,#12457,#12458,#12459,#12460,#12461,#12462,#12463,#12464,#12465,
#12466,#12467,#12468,#12469,#12470,#12471,#12472,#12473,#12474,#12475,#12476,
#12477,#12478,#12479,#12480,#12481,#12482,#12483,#12484,#12485,#12486,#12487,
#12488,#12489,#12490,#12491,#12492,#12493,#12494,#12495,#12496,#12497,#12498,
#12499,#12500,#12501,#12502,#12503,#12504,#12505,#12506,#12507,#12508,#12509,
#12510,#12511,#12512,#12513,#12514,#12515,#12516,#12517,#12518,#12519,#12520,
#12521,#12522,#12523,#12524,#12525,#12526,#12527,#12528,#12529,#12530,#12531,
#12532,#12533,#12534,#12535,#12536,#12537,#12538,#12539,#12540,#12541,#12542,
#12543,#12544,#12545,#12546,#12547,#12548,#12549,#12550,#12551,#12552,#12553,
#12554,#12555,#12556,#12557,#12558,#12559),.UNSPECIFIED.,.F.,.F.,(4,2,2,
2,2,2,2,2,2,2,2,2,2,2,2,2,2,2,2,2,2,2,2,2,2,2,2,2,2,2,2,2,2,2,2,2,2,2,2,
2,2,2,2,2,2,2,2,2,2,2,2,2,2,2,2,2,2,2,2,2,2,2,2,2,2,2,2,2,2,2,2,2,2,2,2,
2,2,2,2,2,2,2,2,2,2,2,2,2,2,2,2,2,2,2,2,2,2,2,2,2,2,2,2,2,2,2,2,2,2,4),
(-1.25692875797613,-1.25674831771628,-1.22109814401454,-1.20715075077619,
-1.20449051608729,-1.20279788698641,-1.20144633454568,-1.1998283961176,
-1.1967925573605,-1.17778734641612,-1.13836384625689,-1.11175241982937,
-1.10705117788052,-1.10403260656388,-1.10161720746712,-1.09887520972168,
-1.09418342389249,-1.07383245908521,-1.02426810723142,-1.00818857747104,
-1.00541920541137,-1.00369349892358,-1.00233992095459,-1.00074809730998,
-0.997835044481727,-0.981924555709882,-0.931350460638727,-0.911852785541992,
-0.907083010806373,-0.904296230703167,-0.901885275858441,-0.898928499815264,
-0.893226073892296,-0.855647249789531,-0.814535503365626,-0.807618670692958,
-0.805298804606913,-0.803982731547137,-0.802611038654916,-0.800735047090535,
-0.796353602195302,-0.776073782845448,-0.724783548047366,-0.711541064934163,
-0.707300771921169,-0.704657775026998,-0.702221051071134,-0.699021700695893,
-0.692071862773937,-0.663679770802434,-0.628974429634597,-0.62415353701392,
-0.609670369508724,-0.6069820543422,-0.605280876782828,-0.603928896096546,
-0.602318038585365,-0.59931567660915,-0.581245868062967,-0.553504271993497,
-0.514543897039331,-0.509670307516983,-0.506599531012716,-0.504179036587773,
-0.501469825824454,-0.496927898468081,-0.478707058558699,-0.440297590914658,
-0.411082827878853,-0.40780432224785,-0.406114220230819,-0.404762732065709,
-0.403142536400415,-0.400096172631472,-0.380782076248408,-0.33964293640904,
-0.314929269570648,-0.31030005382914,-0.307303398667504,-0.304889728850224,
-0.302132517267191,-0.297371251381643,-0.275919695926451,-0.216442002964044,
-0.209960938661077,-0.20769961356291,-0.206395046823953,-0.205044563880018,
-0.203190572090568,-0.201086698355723,-0.197412573419394,-0.189274121239726,
-0.161425992263691,-0.119455369380977,-0.112076068539679,-0.109046552799285,
-0.106789281207341,-0.104312033687726,-0.10087020412236,-0.0925187169600056,
-0.0807098673079125,-0.0392913683885479,-0.0182779886034172,-0.010989094082505,
-0.00862216523462031,-0.00715023010479006,-0.00586260496413733,-0.00449433525428351,
-0.00256109856699574,-0.000585265855186645),.UNSPECIFIED.);
#107=B_SPLINE_CURVE_WITH_KNOTS('',3,(#12564,#12565,#12566,#12567,#12568,
#12569,#12570,#12571,#12572,#12573,#12574,#12575,#12576,#12577,#12578,#12579,
#12580,#12581,#12582,#12583,#12584,#12585,#12586,#12587,#12588,#12589,#12590,
#12591,#12592,#12593,#12594,#12595,#12596,#12597,#12598,#12599,#12600,#12601,
#12602,#12603,#12604,#12605,#12606,#12607,#12608,#12609,#12610,#12611,#12612,
#12613,#12614,#12615,#12616,#12617,#12618,#12619,#12620,#12621,#12622,#12623,
#12624,#12625,#12626,#12627,#12628,#12629,#12630,#12631,#12632,#12633,#12634,
#12635,#12636,#12637,#12638,#12639,#12640,#12641,#12642,#12643,#12644,#12645,
#12646,#12647,#12648,#12649,#12650,#12651,#12652,#12653,#12654,#12655,#12656,
#12657,#12658,#12659,#12660,#12661,#12662,#12663,#12664,#12665,#12666,#12667,
#12668,#12669,#12670,#12671,#12672,#12673,#12674,#12675,#12676,#12677,#12678,
#12679,#12680,#12681,#12682,#12683,#12684,#12685,#12686,#12687,#12688,#12689,
#12690,#12691,#12692,#12693,#12694,#12695,#12696,#12697,#12698,#12699,#12700,
#12701,#12702,#12703,#12704,#12705,#12706,#12707,#12708,#12709,#12710,#12711,
#12712,#12713,#12714,#12715,#12716,#12717,#12718,#12719,#12720,#12721,#12722,
#12723,#12724,#12725,#12726,#12727,#12728,#12729,#12730,#12731,#12732,#12733,
#12734,#12735,#12736,#12737,#12738,#12739,#12740,#12741,#12742,#12743,#12744,
#12745,#12746,#12747,#12748,#12749,#12750,#12751,#12752,#12753,#12754,#12755,
#12756,#12757,#12758,#12759,#12760,#12761,#12762,#12763,#12764,#12765,#12766,
#12767,#12768,#12769,#12770,#12771,#12772,#12773,#12774,#12775,#12776,#12777,
#12778,#12779,#12780,#12781,#12782,#12783,#12784,#12785,#12786,#12787,#12788,
#12789,#12790,#12791,#12792,#12793,#12794,#12795,#12796,#12797,#12798,#12799,
#12800,#12801,#12802,#12803,#12804,#12805,#12806,#12807,#12808,#12809,#12810,
#12811,#12812,#12813,#12814,#12815,#12816,#12817),.UNSPECIFIED.,.F.,.F.,
(4,2,2,2,2,2,2,2,2,2,2,2,2,2,2,2,2,2,2,2,2,2,2,2,2,2,2,2,2,2,2,2,2,2,2,
2,2,2,2,2,2,2,2,2,2,2,2,2,2,2,2,2,2,2,2,2,2,2,2,2,2,2,2,2,2,2,2,2,2,2,2,
2,2,2,2,2,2,2,2,2,2,2,2,2,2,2,2,2,2,2,2,2,2,2,2,2,2,2,2,2,2,2,2,2,2,2,2,
2,2,2,2,2,2,2,2,2,2,2,2,2,2,2,2,2,2,2,4),(-1.25721314605092,-1.23410841050774,
-1.22954161186543,-1.22656375576533,-1.22415102282358,-1.2213792528173,
-1.21655262850479,-1.1939961644514,-1.16352389726284,-1.14680516878331,
-1.13082265003821,-1.12805720747367,-1.1263325710184,-1.12497891679185,
-1.12338593268706,-1.12046804004912,-1.10445722586107,-1.05289135589093,
-1.03435531751347,-1.02965198137857,-1.02688019427728,-1.02446769410289,
-1.0214904436709,-1.01568879368394,-0.975133357582088,-0.934045095177474,
-0.929463525901543,-0.927688776187349,-0.926411150294908,-0.925013288919188,
-0.922991762752392,-0.917707210838215,-0.90979442286352,-0.883317223127766,
-0.839502033391039,-0.83203204238506,-0.82906786170256,-0.826602039218295,
-0.824068271270609,-0.820338421416605,-0.810055608898703,-0.794437841170515,
-0.760313609126218,-0.732852138489897,-0.72955954685681,-0.727866277201391,
-0.726514463180541,-0.72489650969611,-0.721861443067769,-0.702891381175583,
-0.663678137920787,-0.636819808664008,-0.632109334575591,-0.629087663546109,
-0.62667160003942,-0.623930799418827,-0.619245930790415,-0.599009663918522,
-0.550226702083068,-0.533292055105846,-0.530486400260093,-0.528749647696569,
-0.527394999157189,-0.525810737980295,-0.522933607471545,-0.507788863622081,
-0.463746243340883,-0.437564045080649,-0.43287495247255,-0.429859726370079,
-0.42744413412075,-0.424698824012465,-0.419993625127158,-0.399447804412861,
-0.348533978060796,-0.333863207189271,-0.331164830994524,-0.329460351564713,
-0.328107839038345,-0.326498826255675,-0.323506434495639,-0.305716982370102,
-0.277771298222007,-0.23869810383822,-0.233819850544559,-0.230747217691625,
-0.228325935105404,-0.228286333013025,-0.228232330027664,-0.228182580458323,
-0.228136740536762,-0.228094494714532,-0.22805555347062,-0.228019651229689,
-0.227986544399185,-0.227956009547196,-0.227927841703126,-0.227901852799441,
-0.227877870239158,-0.227855735569204,-0.22783530328297,-0.227816439721745,
-0.227787725550702,-0.227759502646055,-0.22773175972712,-0.224849511854618,
-0.219429371895256,-0.212575646028398,-0.197158165912927,-0.161712336597581,
-0.135229983426135,-0.131940067678489,-0.130247256307972,-0.128895313480881,
-0.127276615593005,-0.124238566824772,-0.105189659513025,-0.0640561891760269,
-0.0479072815185143,-0.03680636699023,-0.0328382146543954,-0.0305122524671761,
-0.0281761769943295,-0.0258175261057142,-0.0227753831788527,-0.0147912398161514,
-0.000585061531517047),.UNSPECIFIED.);
#108=B_SPLINE_CURVE_WITH_KNOTS('',3,(#12818,#12819,#12820,#12821,#12822,
#12823,#12824,#12825,#12826,#12827,#12828,#12829,#12830,#12831,#12832,#12833,
#12834,#12835,#12836,#12837,#12838,#12839,#12840,#12841,#12842,#12843,#12844,
#12845,#12846,#12847,#12848,#12849,#12850,#12851,#12852,#12853,#12854,#12855,
#12856,#12857,#12858,#12859,#12860,#12861,#12862,#12863,#12864,#12865,#12866,
#12867,#12868,#12869,#12870,#12871,#12872,#12873,#12874,#12875,#12876,#12877,
#12878,#12879,#12880,#12881,#12882,#12883,#12884,#12885,#12886,#12887,#12888,
#12889,#12890,#12891,#12892,#12893,#12894,#12895,#12896,#12897,#12898,#12899,
#12900,#12901,#12902,#12903,#12904,#12905,#12906,#12907,#12908,#12909,#12910,
#12911,#12912,#12913,#12914,#12915,#12916,#12917,#12918,#12919,#12920,#12921,
#12922,#12923,#12924,#12925,#12926,#12927,#12928,#12929,#12930,#12931,#12932,
#12933,#12934,#12935,#12936,#12937,#12938,#12939,#12940,#12941,#12942,#12943,
#12944,#12945,#12946,#12947,#12948,#12949,#12950,#12951,#12952,#12953,#12954,
#12955,#12956,#12957,#12958,#12959,#12960,#12961,#12962,#12963,#12964,#12965,
#12966,#12967,#12968,#12969,#12970,#12971,#12972,#12973,#12974,#12975,#12976,
#12977,#12978,#12979,#12980,#12981,#12982,#12983,#12984,#12985,#12986,#12987,
#12988,#12989,#12990,#12991,#12992,#12993,#12994,#12995,#12996,#12997,#12998,
#12999,#13000,#13001,#13002,#13003,#13004,#13005,#13006,#13007,#13008,#13009,
#13010,#13011,#13012,#13013,#13014,#13015,#13016,#13017,#13018,#13019,#13020,
#13021),.UNSPECIFIED.,.F.,.F.,(4,2,2,2,2,2,2,2,2,2,2,2,2,2,2,2,2,2,2,2,
2,2,2,2,2,2,2,2,2,2,2,2,2,2,2,2,2,2,2,2,2,2,2,2,2,2,2,2,2,2,2,2,2,2,2,2,
2,2,2,2,2,2,2,2,2,2,2,2,2,2,2,2,2,2,2,2,2,2,2,2,2,2,2,2,2,2,2,2,2,2,2,2,
2,2,2,2,2,2,2,2,2,4),(-2.51343961457606,-2.50700411879925,-2.46704646714677,
-2.44191814983947,-2.42765358818164,-2.42345778919562,-2.42082515830955,
-2.41838618736802,-2.41522118302671,-2.40826685724874,-2.3577464267704,
-2.32686446612291,-2.3243328698153,-2.32218244790152,-2.32077525475688,
-2.31942380913582,-2.31740253109399,-2.31252778337271,-2.28250596247546,
-2.25389848716447,-2.23801209810173,-2.2276012878937,-2.22385498020029,
-2.22131855573529,-2.21885663492621,-2.21590493207425,-2.20850901840045,
-2.16318610321753,-2.13778920524827,-2.13006249460125,-2.1248720413167,
-2.12286525313205,-2.12147068393915,-2.12019057529134,-2.11840512372588,
-2.11374736535972,-2.07434923090019,-2.03179038556258,-2.02628881881331,
-2.02337402253571,-2.02119985331399,-2.01846578883249,-2.01380830988486,
-1.99652066761897,-1.93967124548566,-1.927148752595,-1.92441890489801,-1.92286700841356,
-1.92150805206502,-1.91975329459839,-1.91682243371769,-1.89600398338736,
-1.85074725132523,-1.83110462755919,-1.8264608122908,-1.8237295249604,-1.82131301706365,
-1.81827905865397,-1.81352646531298,-1.78537809844438,-1.73396061176384,
-1.72930379017801,-1.72578290123095,-1.72406582086938,-1.72271296400863,
-1.72111488948532,-1.71825331342435,-1.70521750918886,-1.66141040381531,
-1.63529753580209,-1.6286356378767,-1.62549007546057,-1.62306085315691,
-1.62039269663943,-1.61603716976111,-1.60178291879809,-1.54557207953828,
-1.52915157310119,-1.52621563531571,-1.52461889752026,-1.52326576389771,
-1.52154654439469,-1.51879876998948,-1.50311084355116,-1.45320575481505,
-1.43280751368249,-1.42811262893877,-1.4253698985028,-1.42295450172262,
-1.41993678749009,-1.41523849450132,-1.38872675079965,-1.34918122684277,
-1.33014676584787,-1.32710966907882,-1.32549141624457,-1.32413980419056,
-1.32244736257289,-1.31915803988056,-1.2925816857723,-1.25732799229113,
-1.25718624449385),.UNSPECIFIED.);
#109=B_SPLINE_CURVE_WITH_KNOTS('',3,(#13026,#13027,#13028,#13029,#13030,
#13031,#13032,#13033,#13034,#13035,#13036,#13037,#13038,#13039,#13040,#13041,
#13042,#13043,#13044,#13045,#13046,#13047,#13048,#13049,#13050,#13051,#13052,
#13053,#13054,#13055,#13056,#13057,#13058,#13059,#13060,#13061,#13062,#13063,
#13064,#13065,#13066,#13067,#13068,#13069,#13070,#13071,#13072,#13073,#13074,
#13075,#13076,#13077,#13078,#13079,#13080,#13081,#13082,#13083,#13084,#13085,
#13086,#13087,#13088,#13089,#13090,#13091,#13092,#13093,#13094,#13095,#13096,
#13097,#13098,#13099,#13100,#13101,#13102,#13103,#13104,#13105,#13106,#13107,
#13108,#13109,#13110,#13111,#13112,#13113,#13114,#13115,#13116,#13117,#13118,
#13119,#13120,#13121,#13122,#13123,#13124,#13125,#13126,#13127,#13128,#13129,
#13130,#13131,#13132,#13133,#13134,#13135,#13136,#13137,#13138,#13139,#13140,
#13141,#13142,#13143,#13144,#13145,#13146,#13147,#13148,#13149,#13150,#13151,
#13152,#13153,#13154,#13155,#13156,#13157,#13158,#13159,#13160,#13161,#13162,
#13163,#13164,#13165,#13166,#13167,#13168,#13169,#13170,#13171,#13172,#13173,
#13174,#13175,#13176,#13177,#13178,#13179,#13180,#13181,#13182,#13183,#13184,
#13185,#13186,#13187,#13188,#13189,#13190,#13191,#13192,#13193,#13194,#13195,
#13196,#13197,#13198,#13199,#13200,#13201,#13202,#13203,#13204,#13205,#13206,
#13207,#13208,#13209,#13210,#13211,#13212,#13213,#13214,#13215,#13216,#13217,
#13218,#13219,#13220,#13221,#13222,#13223,#13224,#13225,#13226,#13227,#13228,
#13229,#13230,#13231,#13232,#13233,#13234,#13235,#13236,#13237,#13238,#13239,
#13240,#13241,#13242,#13243,#13244,#13245,#13246,#13247,#13248,#13249,#13250,
#13251,#13252,#13253,#13254,#13255,#13256,#13257,#13258,#13259,#13260,#13261,
#13262,#13263,#13264,#13265,#13266,#13267,#13268,#13269,#13270,#13271),
 .UNSPECIFIED.,.F.,.F.,(4,2,2,2,2,2,2,2,2,2,2,2,2,2,2,2,2,2,2,2,2,2,2,2,
2,2,2,2,2,2,2,2,2,2,2,2,2,2,2,2,2,2,2,2,2,2,2,2,2,2,2,2,2,2,2,2,2,2,2,2,
2,2,2,2,2,2,2,2,2,2,2,2,2,2,2,2,2,2,2,2,2,2,2,2,2,2,2,2,2,2,2,2,2,2,2,2,
2,2,2,2,2,2,2,2,2,2,2,2,2,2,2,2,2,2,2,2,2,2,2,2,2,2,4),(-2.51376700494393,
-2.50951882086084,-2.46053664590167,-2.43229343177985,-2.42536141386723,
-2.42216526669347,-2.41972891587046,-2.41708430645807,-2.41283699457617,
-2.39953623005897,-2.3482779193926,-2.33314843911664,-2.3275405111926,-2.3247135310518,
-2.32295042109657,-2.3213343143447,-2.32132749281789,-2.32132050668485,
-2.32131334996416,-2.32130601632168,-2.32129849912296,-2.32129079137716,
-2.3212828857202,-2.32127477441211,-2.32126644925545,-2.32125790162258,
-2.32124912239502,-2.3212401019345,-2.32123083004353,-2.32122129591618,
-2.32121148808407,-2.32120139439018,-2.3211910019283,-2.32118029697447,
-2.32116926491338,-2.32115789016918,-2.31984349567252,-2.31811351985876,
-2.31533018994175,-2.29892846395731,-2.24969051023426,-2.22938937032416,
-2.22470059822666,-2.22195908171957,-2.21954333138586,-2.21652329876995,
-2.21181775690181,-2.18510154620058,-2.14573515367814,-2.12673160925154,
-2.12369540429155,-2.12207727140088,-2.12072555223376,-2.11903271606401,
-2.11574187639599,-2.08903783408751,-2.05398308729099,-2.03850012440538,
-2.02828111733017,-2.02456016183992,-2.02202830466941,-2.01956117212641,
-2.01659157210825,-2.00908682867244,-1.96610903211396,-1.93898671374315,
-1.93096633619318,-1.92562881358758,-1.92359940147936,-1.9222000298252,
-1.92092412486658,-1.91915584732139,-1.91461476245716,-1.87300896983209,
-1.83293115869864,-1.82714486219935,-1.82417075856621,-1.82175849219758,
-1.81898441300576,-1.8142709855831,-1.79559517002237,-1.74414180702794,
-1.72813833009116,-1.72522063079813,-1.72362767114012,-1.72227398087562,
-1.72054923811949,-1.71778353177524,-1.70179317254349,-1.65216836746208,
-1.63180906824576,-1.62711625548801,-1.62437373778515,-1.62195792658133,
-1.61893890118004,-1.61423702909489,-1.58763525055298,-1.54394842216482,
-1.52884986736008,-1.52597498300791,-1.52439123409069,-1.523036563021,-1.52129920111356,
-1.51849146357304,-1.50150019275957,-1.45280111895708,-1.4325806137216,
-1.42789688130584,-1.42515632969725,-1.42274023196918,-1.41971818334393,
-1.41500642915766,-1.38811896574053,-1.34890143194295,-1.32992333442592,
-1.32688781554247,-1.32526975057594,-1.32391791436567,-1.32222471322663,
-1.31893253464901,-1.29154648467702,-1.25735579703317,-1.25721314605092),
 .UNSPECIFIED.);
#110=B_SPLINE_CURVE_WITH_KNOTS('',3,(#13272,#13273,#13274,#13275,#13276,
#13277,#13278,#13279,#13280,#13281,#13282,#13283,#13284,#13285,#13286,#13287,
#13288,#13289,#13290,#13291,#13292,#13293,#13294,#13295,#13296,#13297,#13298,
#13299,#13300,#13301,#13302,#13303,#13304,#13305,#13306,#13307,#13308,#13309,
#13310,#13311,#13312,#13313,#13314,#13315,#13316,#13317,#13318,#13319,#13320,
#13321,#13322,#13323,#13324,#13325,#13326,#13327,#13328,#13329,#13330,#13331,
#13332,#13333,#13334,#13335,#13336,#13337,#13338,#13339,#13340,#13341,#13342,
#13343,#13344,#13345,#13346,#13347,#13348,#13349,#13350,#13351,#13352,#13353,
#13354,#13355,#13356,#13357,#13358,#13359,#13360,#13361,#13362,#13363,#13364,
#13365,#13366,#13367,#13368,#13369,#13370,#13371,#13372,#13373,#13374,#13375,
#13376,#13377,#13378,#13379,#13380,#13381,#13382,#13383,#13384,#13385,#13386,
#13387,#13388,#13389,#13390,#13391,#13392,#13393,#13394,#13395,#13396,#13397,
#13398,#13399,#13400,#13401,#13402,#13403,#13404,#13405,#13406,#13407,#13408,
#13409,#13410,#13411,#13412,#13413,#13414,#13415,#13416,#13417,#13418,#13419,
#13420,#13421,#13422,#13423,#13424,#13425,#13426,#13427,#13428,#13429,#13430,
#13431,#13432,#13433,#13434,#13435,#13436,#13437,#13438,#13439,#13440,#13441,
#13442,#13443,#13444,#13445,#13446,#13447,#13448,#13449,#13450,#13451,#13452,
#13453,#13454,#13455,#13456,#13457,#13458,#13459,#13460,#13461,#13462,#13463,
#13464,#13465,#13466,#13467,#13468,#13469,#13470,#13471,#13472,#13473,#13474,
#13475,#13476,#13477,#13478,#13479,#13480,#13481,#13482,#13483,#13484,#13485,
#13486,#13487,#13488,#13489,#13490,#13491,#13492,#13493,#13494,#13495,#13496,
#13497,#13498,#13499,#13500,#13501,#13502,#13503,#13504,#13505,#13506,#13507,
#13508,#13509,#13510,#13511,#13512,#13513,#13514,#13515,#13516,#13517,#13518,
#13519,#13520,#13521),.UNSPECIFIED.,.F.,.F.,(4,2,2,2,2,2,2,2,2,2,2,2,2,
2,2,2,2,2,2,2,2,2,2,2,2,2,2,2,2,2,2,2,2,2,2,2,2,2,2,2,2,2,2,2,2,2,2,2,2,
2,2,2,2,2,2,2,2,2,2,2,2,2,2,2,2,2,2,2,2,2,2,2,2,2,2,2,2,2,2,2,2,2,2,2,2,
2,2,2,2,2,2,2,2,2,2,2,2,2,2,2,2,2,2,2,2,2,2,2,2,2,2,2,2,2,2,2,2,2,2,2,2,
2,2,2,4),(-1.25718624449385,-1.23432181272649,-1.22976598265445,-1.22679172956097,
-1.22437957364868,-1.22160587769723,-1.21676918817301,-1.19402346659137,
-1.16022355147993,-1.13149350969374,-1.12820187708346,-1.12650892670364,
-1.12515727389588,-1.12353940160373,-1.12050418720247,-1.10152184785097,
-1.06223169092915,-1.03546710093895,-1.03076030774855,-1.02773993970722,
-1.02532423841764,-1.02258311834827,-1.0178958816887,-0.997617768060992,
-0.948549966039133,-0.931932334454174,-0.929139988698659,-0.927407326004779,
-0.926053142434892,-0.924466253773311,-0.921576428707393,-0.906165124988586,
-0.86003828767815,-0.836059961369632,-0.831461874734936,-0.828474623678264,
-0.826061496498789,-0.823297203262125,-0.818504001719344,-0.796521450350457,
-0.737302313453606,-0.731073098457612,-0.728846768470997,-0.727549047000138,
-0.726166641106457,-0.724228035880202,-0.719474230249166,-0.695535590368005,
-0.681607867791069,-0.640673780711772,-0.633271029246933,-0.630237319787426,
-0.627978900256045,-0.625502333925371,-0.622065053941201,-0.613742655701104,
-0.601988260361855,-0.567095524959475,-0.536346540122064,-0.531432653814182,
-0.529411445941615,-0.52802743758372,-0.526578119166187,-0.524313911346372,
-0.517197597079717,-0.505275211932711,-0.477267665615142,-0.438140639031808,
-0.433270201470152,-0.430199942586518,-0.427778939241377,-0.42506820146735,
-0.420521416268441,-0.402247534360887,-0.363623639867946,-0.334681443628133,
-0.331388931026975,-0.32969556011226,-0.328343588819775,-0.326725355915732,
-0.323689520296327,-0.304705389526956,-0.264835456090722,-0.238616623466363,
-0.233916512100262,-0.230897806361875,-0.228481746398326,-0.228432602825057,
-0.228387320658029,-0.228345588083555,-0.228307119064811,-0.228271651264636,
-0.228238944092884,-0.228208776891345,-0.228180947253649,-0.228155269479728,
-0.228131573148775,-0.228109701815023,-0.228089511809844,-0.228070871169533,
-0.228042203680407,-0.228014026252729,-0.227986327617261,-0.225103123637765,
-0.219678707888599,-0.212818064639295,-0.197377933086562,-0.162000447780933,
-0.135487182985478,-0.132197083640806,-0.130504233859789,-0.129152290567674,
-0.127533628149821,-0.124495742777054,-0.105451548106014,-0.0645853488185647,
-0.0484315952897971,-0.0371236965880628,-0.0331271481493886,-0.0305367445142057,
-0.0282310564276066,-0.025838189284329,-0.0226944322401059,-0.0147032935327984,
-0.000585061972299964),.UNSPECIFIED.);
#111=B_SPLINE_CURVE_WITH_KNOTS('',3,(#13526,#13527,#13528,#13529,#13530,
#13531,#13532,#13533,#13534,#13535,#13536,#13537,#13538,#13539,#13540,#13541,
#13542,#13543,#13544,#13545,#13546,#13547,#13548,#13549,#13550,#13551,#13552,
#13553,#13554,#13555,#13556,#13557,#13558,#13559,#13560,#13561,#13562,#13563,
#13564,#13565,#13566,#13567,#13568,#13569,#13570,#13571,#13572,#13573,#13574,
#13575,#13576,#13577,#13578,#13579,#13580,#13581,#13582,#13583,#13584,#13585,
#13586,#13587,#13588,#13589,#13590,#13591,#13592,#13593,#13594,#13595,#13596,
#13597,#13598,#13599,#13600,#13601,#13602,#13603,#13604,#13605,#13606,#13607,
#13608,#13609,#13610,#13611,#13612,#13613,#13614,#13615,#13616,#13617,#13618,
#13619,#13620,#13621,#13622,#13623,#13624,#13625,#13626,#13627,#13628,#13629,
#13630,#13631,#13632,#13633,#13634,#13635,#13636,#13637,#13638,#13639,#13640,
#13641,#13642,#13643,#13644,#13645,#13646,#13647,#13648,#13649,#13650,#13651,
#13652,#13653,#13654,#13655,#13656,#13657,#13658,#13659,#13660,#13661,#13662,
#13663,#13664,#13665,#13666,#13667,#13668,#13669,#13670,#13671,#13672,#13673,
#13674,#13675,#13676,#13677,#13678,#13679,#13680,#13681,#13682,#13683,#13684,
#13685,#13686,#13687,#13688,#13689,#13690,#13691,#13692,#13693,#13694,#13695,
#13696,#13697,#13698,#13699,#13700,#13701,#13702,#13703,#13704,#13705,#13706,
#13707,#13708,#13709,#13710,#13711,#13712,#13713,#13714,#13715,#13716,#13717,
#13718,#13719,#13720,#13721,#13722,#13723,#13724,#13725,#13726,#13727,#13728,
#13729,#13730,#13731,#13732,#13733,#13734,#13735,#13736,#13737,#13738,#13739,
#13740,#13741,#13742,#13743,#13744,#13745,#13746,#13747),.UNSPECIFIED.,
 .F.,.F.,(4,2,2,2,2,2,2,2,2,2,2,2,2,2,2,2,2,2,2,2,2,2,2,2,2,2,2,2,2,2,2,
2,2,2,2,2,2,2,2,2,2,2,2,2,2,2,2,2,2,2,2,2,2,2,2,2,2,2,2,2,2,2,2,2,2,2,2,
2,2,2,2,2,2,2,2,2,2,2,2,2,2,2,2,2,2,2,2,2,2,2,2,2,2,2,2,2,2,2,2,2,2,2,2,
2,2,2,2,2,2,2,4),(-1.25689118322759,-1.25671096155556,-1.25066039709721,
-1.20948520878915,-1.20491062352101,-1.20313712487133,-1.2018599543989,
-1.20046207327059,-1.19843965751658,-1.19314791923008,-1.18522028623814,
-1.15865150577119,-1.11497398590445,-1.10749965065631,-1.10453505784319,
-1.10206939225266,-1.09953629676943,-1.09580839389071,-1.08553717371309,
-1.06994269622606,-1.03560901004996,-1.00833240958728,-1.00504042490444,
-1.00334743610044,-1.00199583059752,-1.00037810814358,-0.997343420062909,
-0.978373648568059,-0.939151580434908,-0.912314022136519,-0.907604853576636,
-0.904583826346341,-0.902168153279766,-0.899427662031066,-0.894742989255381,
-0.874501804533818,-0.825673820371346,-0.808798892153525,-0.805995981848572,
-0.804260190475218,-0.802905808354335,-0.801321297295135,-0.798442316134587,
-0.783253095478853,-0.753093923533356,-0.713432011248414,-0.708566798631958,
-0.705498445073798,-0.703078076551615,-0.700367143047883,-0.695817851683732,
-0.677501966244538,-0.638690545643279,-0.610001738098589,-0.606710017538426,
-0.605017020098656,-0.60366532853022,-0.602047408374565,-0.59901210109803,
-0.580029064381446,-0.540736935040638,-0.513972499064096,-0.509265601671788,
-0.506245155882249,-0.503829385418153,-0.501088179338337,-0.496400776833039,
-0.476121618543464,-0.427049352990098,-0.410434549023895,-0.407642260609676,
-0.40590958908575,-0.404555369560065,-0.40296840504757,-0.400078356691766,
-0.384663685343858,-0.338511767862587,-0.314557519280654,-0.309960372522951,
-0.306973363949184,-0.304560191482653,-0.301795581799726,-0.297001152618108,
-0.274999356020909,-0.245539285514575,-0.214093563464176,-0.209207554590877,
-0.207183882719002,-0.205835679281454,-0.20442550059127,-0.202279296975025,
-0.199752659737215,-0.194972377385831,-0.183059340713377,-0.155048153012684,
-0.115924457363705,-0.111054912269187,-0.107985187527713,-0.105564587606867,
-0.102854282990023,-0.0983081798209412,-0.080036388434619,-0.0266263034238271,
-0.0178723281638256,-0.0107036920365692,-0.0083518673755166,-0.00688327863526397,
-0.005597296360091,-0.00422686397429686,-0.00239437338399666,-0.000585285094892383),
 .UNSPECIFIED.);
#112=B_SPLINE_CURVE_WITH_KNOTS('',3,(#13748,#13749,#13750,#13751,#13752,
#13753,#13754,#13755,#13756,#13757,#13758,#13759,#13760,#13761,#13762,#13763,
#13764,#13765,#13766,#13767,#13768,#13769,#13770,#13771,#13772,#13773,#13774,
#13775,#13776,#13777,#13778,#13779,#13780,#13781,#13782,#13783,#13784,#13785,
#13786,#13787,#13788,#13789,#13790,#13791,#13792,#13793,#13794,#13795,#13796,
#13797,#13798,#13799,#13800,#13801,#13802,#13803,#13804,#13805,#13806,#13807,
#13808,#13809,#13810,#13811,#13812,#13813,#13814,#13815,#13816,#13817,#13818,
#13819,#13820,#13821,#13822,#13823,#13824,#13825,#13826,#13827,#13828,#13829,
#13830,#13831,#13832,#13833,#13834,#13835,#13836,#13837,#13838,#13839,#13840,
#13841,#13842,#13843,#13844,#13845,#13846,#13847,#13848,#13849,#13850,#13851,
#13852,#13853,#13854,#13855,#13856,#13857,#13858,#13859,#13860,#13861,#13862,
#13863,#13864,#13865,#13866,#13867,#13868,#13869,#13870,#13871,#13872,#13873,
#13874,#13875,#13876,#13877,#13878,#13879,#13880,#13881,#13882,#13883,#13884,
#13885,#13886,#13887,#13888,#13889,#13890,#13891,#13892,#13893,#13894,#13895,
#13896,#13897,#13898,#13899,#13900,#13901,#13902,#13903,#13904,#13905,#13906,
#13907,#13908,#13909,#13910,#13911,#13912,#13913,#13914,#13915,#13916,#13917,
#13918,#13919,#13920,#13921,#13922,#13923,#13924,#13925,#13926,#13927,#13928,
#13929,#13930,#13931,#13932,#13933,#13934),.UNSPECIFIED.,.F.,.F.,(4,3,3,
3,3,3,3,3,3,3,3,3,3,3,3,3,3,3,3,3,3,3,3,3,3,3,3,3,3,3,3,3,3,3,3,3,3,3,3,
3,3,3,3,3,3,3,3,3,3,3,3,3,3,3,3,3,3,3,3,3,3,3,4),(128.805298797564,128.925099568478,
129.04598205521,129.156084262171,129.261064500337,129.365887762324,129.470588334727,
129.575223438936,129.679828602701,129.784439310126,129.889160442068,129.993943005775,
130.098906476961,130.152183338992,130.257163577166,130.361986839159,130.466687411564,
130.571322515774,130.675927679538,130.780538386958,130.885259518893,130.990042082592,
131.095005553766,131.148282415812,131.253262654818,131.358085917647,131.46278649089,
131.567421595939,131.67202676054,131.776637468796,131.881358601558,131.98614116608,
132.091104638063,132.144381492633,132.249361729886,132.354184990962,132.458885562461,
132.563520665773,132.668125828646,132.772736535186,132.877457666261,132.98224022911,
133.08720369946,133.140480569454,133.245460807318,133.350284068991,133.454984641061,
133.559619744928,133.66422490834,133.768835615401,133.873556746968,133.978339310294,
134.083302781091,134.136579646274,134.240837463293,134.34679324743,134.45077290342,
134.554690371446,134.658582180826,134.766057569717,134.870071282027,134.979277509208,
135.088483736389),.UNSPECIFIED.);
#113=B_SPLINE_CURVE_WITH_KNOTS('',3,(#13939,#13940,#13941,#13942,#13943,
#13944,#13945,#13946,#13947,#13948,#13949,#13950,#13951,#13952,#13953,#13954,
#13955,#13956,#13957,#13958,#13959,#13960,#13961,#13962,#13963,#13964,#13965,
#13966,#13967,#13968,#13969,#13970,#13971,#13972,#13973,#13974,#13975,#13976,
#13977,#13978,#13979,#13980,#13981,#13982,#13983,#13984,#13985,#13986,#13987,
#13988,#13989,#13990,#13991,#13992,#13993,#13994,#13995,#13996,#13997,#13998,
#13999,#14000,#14001,#14002,#14003,#14004,#14005,#14006,#14007,#14008,#14009,
#14010,#14011,#14012,#14013,#14014,#14015,#14016,#14017,#14018,#14019,#14020,
#14021,#14022,#14023,#14024,#14025,#14026,#14027,#14028,#14029,#14030,#14031,
#14032,#14033,#14034,#14035,#14036,#14037,#14038,#14039,#14040,#14041,#14042,
#14043,#14044,#14045,#14046,#14047,#14048,#14049,#14050,#14051,#14052,#14053,
#14054,#14055,#14056,#14057,#14058,#14059,#14060,#14061,#14062,#14063,#14064,
#14065,#14066,#14067,#14068,#14069,#14070,#14071,#14072,#14073,#14074,#14075,
#14076,#14077,#14078,#14079,#14080,#14081,#14082,#14083,#14084,#14085,#14086,
#14087,#14088,#14089,#14090,#14091,#14092,#14093,#14094,#14095,#14096,#14097,
#14098,#14099,#14100,#14101,#14102,#14103,#14104,#14105,#14106,#14107,#14108,
#14109,#14110,#14111,#14112,#14113,#14114,#14115,#14116,#14117,#14118,#14119,
#14120,#14121,#14122,#14123,#14124,#14125,#14126,#14127,#14128,#14129,#14130,
#14131,#14132,#14133,#14134,#14135,#14136,#14137,#14138,#14139,#14140,#14141,
#14142,#14143,#14144,#14145,#14146,#14147,#14148,#14149,#14150,#14151,#14152,
#14153,#14154),.UNSPECIFIED.,.F.,.F.,(4,2,2,2,2,2,2,2,2,2,2,2,2,2,2,2,2,
2,2,2,2,2,2,2,2,2,2,2,2,2,2,2,2,2,2,2,2,2,2,2,2,2,2,2,2,2,2,2,2,2,2,2,2,
2,2,2,2,2,2,2,2,2,2,2,2,2,2,2,2,2,2,2,2,2,2,2,2,2,2,2,2,2,2,2,2,2,2,2,2,
2,2,2,2,2,2,2,2,2,2,2,2,2,2,2,2,2,2,4),(-2.51320253931066,-2.50287632153621,
-2.49999269476239,-2.49768312658147,-2.49527430426203,-2.49248391015901,
-2.48769450544466,-2.46995109143646,-2.41385089511168,-2.40138555260747,
-2.39865980979826,-2.39710905312572,-2.39575014213638,-2.39399434132568,
-2.39105963924904,-2.37011592718344,-2.32497597339052,-2.31202115044277,
-2.30594668884389,-2.30236945828159,-2.29915574431846,-2.29675025966136,
-2.29446571714883,-2.29132511509424,-2.28499056260217,-2.23521259837668,
-2.21280395406171,-2.2056232296417,-2.20071066851767,-2.19874696748224,
-2.19736042941638,-2.1960700367412,-2.19387907785268,-2.18788906555115,
-2.14596862640986,-2.12000346906759,-2.10543782419957,-2.10121181716219,
-2.09857235025286,-2.09613525094372,-2.09298424032767,-2.08610817894176,
-2.03489016843594,-2.00454813616068,-2.00096030321405,-1.99923022322779,
-1.99787659622532,-1.99628865941446,-1.9934712508542,-1.98108139745902,
-1.97261243845498,-1.94070155955165,-1.91112041297461,-1.9040264532269,
-1.9008011001887,-1.89836090062067,-1.89605094328751,-1.89216230855972,
-1.88161578612324,-1.82105219406479,-1.80432961429153,-1.80138081352482,
-1.79978137729434,-1.79842854286192,-1.79671300830993,-1.79397734817377,
-1.77852667008295,-1.76161031874187,-1.73073990436008,-1.70824485623651,
-1.7034223418343,-1.70065171337826,-1.69823925683315,-1.69526081975989,
-1.69069135061393,-1.66737809906642,-1.62964720303596,-1.60767997776593,
-1.60312208474202,-1.60121607385071,-1.5998394994061,-1.59853285677504,
-1.59626044615774,-1.58969746879012,-1.5309160032488,-1.50897567696896,
-1.50418556920118,-1.50142219478823,-1.49900935641869,-1.4960217994714,
-1.49142194363728,-1.46739747270714,-1.42560854830984,-1.40616689497807,
-1.40311628300498,-1.40149524066759,-1.40014386083638,-1.39845492301067,
-1.39518162790263,-1.36532069691864,-1.3274477220626,-1.30935571615107,
-1.30482373422545,-1.30211675239783,-1.29969593018133,-1.29662157768381,
-1.291735922612,-1.25689118322759),.UNSPECIFIED.);
#114=B_SPLINE_CURVE_WITH_KNOTS('',3,(#14155,#14156,#14157,#14158,#14159,
#14160,#14161,#14162,#14163,#14164,#14165),.UNSPECIFIED.,.F.,.F.,(4,1,1,
1,1,1,1,1,4),(135.088484104361,135.132678723095,136.128777799915,137.124876876736,
138.120975953556,139.117075030377,140.113174107198,141.109273184018,141.371666670261),
 .UNSPECIFIED.);
#115=B_SPLINE_CURVE_WITH_KNOTS('',3,(#14170,#14171,#14172,#14173,#14174,
#14175,#14176,#14177,#14178,#14179),.UNSPECIFIED.,.F.,.F.,(4,1,1,1,1,1,
1,4),(141.371675358084,141.785434021122,142.781533097942,143.777632174763,
144.773731251584,145.769830328404,146.765929405225,147.654846025158),
 .UNSPECIFIED.);
#116=B_SPLINE_CURVE_WITH_KNOTS('',3,(#14180,#14181,#14182,#14183,#14184,
#14185,#14186,#14187,#14188,#14189,#14190,#14191,#14192,#14193,#14194,#14195,
#14196,#14197,#14198,#14199,#14200,#14201,#14202,#14203,#14204,#14205,#14206,
#14207,#14208,#14209,#14210,#14211,#14212,#14213,#14214,#14215,#14216,#14217,
#14218,#14219,#14220,#14221,#14222,#14223,#14224,#14225,#14226,#14227,#14228,
#14229,#14230,#14231,#14232,#14233,#14234,#14235,#14236,#14237,#14238,#14239,
#14240,#14241,#14242,#14243,#14244,#14245,#14246,#14247,#14248,#14249,#14250,
#14251,#14252,#14253,#14254,#14255,#14256,#14257,#14258,#14259,#14260,#14261,
#14262,#14263,#14264,#14265,#14266,#14267,#14268,#14269,#14270,#14271,#14272,
#14273,#14274,#14275,#14276,#14277,#14278,#14279,#14280,#14281,#14282,#14283,
#14284,#14285,#14286,#14287,#14288,#14289,#14290,#14291,#14292,#14293,#14294,
#14295,#14296,#14297,#14298,#14299,#14300,#14301,#14302,#14303,#14304,#14305,
#14306,#14307,#14308,#14309,#14310,#14311,#14312,#14313,#14314,#14315,#14316,
#14317,#14318,#14319,#14320,#14321,#14322,#14323,#14324,#14325,#14326,#14327,
#14328,#14329,#14330,#14331,#14332,#14333,#14334,#14335,#14336,#14337,#14338,
#14339,#14340,#14341,#14342,#14343,#14344,#14345,#14346,#14347,#14348,#14349,
#14350,#14351,#14352,#14353,#14354,#14355,#14356,#14357,#14358,#14359,#14360,
#14361,#14362,#14363,#14364,#14365,#14366,#14367,#14368,#14369,#14370,#14371,
#14372,#14373,#14374,#14375,#14376,#14377,#14378,#14379,#14380,#14381,#14382,
#14383,#14384,#14385,#14386,#14387,#14388,#14389,#14390,#14391,#14392,#14393,
#14394,#14395),.UNSPECIFIED.,.F.,.F.,(4,2,2,2,2,2,2,2,2,2,2,2,2,2,2,2,2,
2,2,2,2,2,2,2,2,2,2,2,2,2,2,2,2,2,2,2,2,2,2,2,2,2,2,2,2,2,2,2,2,2,2,2,2,
2,2,2,2,2,2,2,2,2,2,2,2,2,2,2,2,2,2,2,2,2,2,2,2,2,2,2,2,2,2,2,2,2,2,2,2,
2,2,2,2,2,2,2,2,2,2,2,2,2,2,2,2,2,2,4),(1.06702749696459,1.07316969738846,
1.07770707088996,1.08041365887283,1.08283183593376,1.08589966942507,1.09076846782211,
1.12385846889157,1.12849512758101,1.16210969520842,1.17571395237882,1.17835333713161,
1.18003871940382,1.1813894128234,1.1830123133441,1.18607065916365,1.2057327472199,
1.24862446758751,1.27143689203918,1.27598607150705,1.27895895115665,1.28137198390553,
1.28414890832231,1.28899706537762,1.31193072570234,1.34688441869337,1.37415864223013,
1.37744846191372,1.37914168114933,1.380493904015,1.38211284568512,1.38515246994505,
1.40425152330437,1.44415930257887,1.47024636851639,1.47493545036338,1.47795035489268,
1.48036550659463,1.48311011817824,1.4878136273382,1.50834427377816,1.55917481256092,
1.57389788217752,1.57659816947687,1.57830293406867,1.5796550035686,1.58126265552273,
1.58425043047079,1.60193953394739,1.62996503109149,1.66910279698706,1.67397282135017,
1.67704234054098,1.67946247365302,1.68217193286552,1.68671583748078,1.70496781130397,
1.74351087911226,1.77249917222258,1.77579028169015,1.77748296143559,1.77883449587214,
1.78045236022482,1.783487515892,1.80246398554958,1.84168311021497,1.86855896815675,
1.87326995269718,1.87629163171949,1.87870751567614,1.88144791505473,1.88613162066953,
1.90635663748937,1.95510184909357,1.97202534686489,1.97483021351245,1.97656666905203,
1.97792116205628,1.97950529482133,1.98238256472473,1.99753552905286,2.04163702341759,
2.06777405660442,2.07246296105816,2.07547778094528,2.07789288109646,2.08063745165059,
2.08511467473775,2.10277438643751,2.13944932480042,2.15466361930623,2.17119862678294,
2.17398707032581,2.17571842884612,2.17707232002611,2.1786596970405,2.18034997397262,
2.18721968582645,2.21249752401594,2.23658996480899,2.26665540963193,2.27146774281066,
2.27451997590356,2.27693849132688,2.27965877848377,2.28248115842509,2.28671622365621,
2.32340943786923),.UNSPECIFIED.);
#117=B_SPLINE_CURVE_WITH_KNOTS('',3,(#14399,#14400,#14401,#14402,#14403,
#14404),.UNSPECIFIED.,.F.,.F.,(4,1,1,4),(-4.09157007060747,-3.98439630728236,
-2.98829723046177,-2.06697924613302),.UNSPECIFIED.);
#118=B_SPLINE_CURVE_WITH_KNOTS('',3,(#14408,#14409,#14410,#14411,#14412),
 .UNSPECIFIED.,.F.,.F.,(4,1,4),(0.,0.996099076820589,1.11662023360659),
 .UNSPECIFIED.);
#119=B_SPLINE_CURVE_WITH_KNOTS('',3,(#14414,#14415,#14416,#14417,#14418,
#14419,#14420,#14421,#14422,#14423,#14424,#14425,#14426,#14427,#14428,#14429,
#14430,#14431,#14432,#14433,#14434,#14435,#14436,#14437,#14438,#14439,#14440,
#14441,#14442,#14443,#14444,#14445,#14446,#14447,#14448,#14449,#14450,#14451,
#14452,#14453,#14454,#14455,#14456,#14457,#14458,#14459,#14460,#14461,#14462,
#14463,#14464,#14465,#14466,#14467,#14468,#14469,#14470,#14471,#14472,#14473,
#14474,#14475,#14476,#14477,#14478,#14479,#14480,#14481,#14482,#14483,#14484,
#14485,#14486,#14487,#14488,#14489,#14490,#14491,#14492,#14493,#14494,#14495,
#14496,#14497,#14498,#14499,#14500,#14501,#14502,#14503,#14504,#14505,#14506,
#14507,#14508,#14509,#14510,#14511,#14512,#14513,#14514,#14515,#14516,#14517,
#14518,#14519,#14520,#14521,#14522,#14523,#14524,#14525,#14526,#14527,#14528,
#14529,#14530,#14531,#14532,#14533,#14534,#14535,#14536,#14537,#14538,#14539,
#14540,#14541,#14542,#14543,#14544,#14545,#14546,#14547,#14548,#14549,#14550,
#14551,#14552,#14553,#14554,#14555,#14556,#14557,#14558,#14559,#14560,#14561,
#14562,#14563,#14564,#14565,#14566,#14567,#14568,#14569,#14570,#14571,#14572,
#14573,#14574,#14575,#14576,#14577,#14578,#14579,#14580,#14581,#14582,#14583,
#14584,#14585,#14586,#14587,#14588,#14589,#14590,#14591,#14592,#14593,#14594,
#14595,#14596,#14597,#14598,#14599,#14600,#14601,#14602,#14603),
 .UNSPECIFIED.,.F.,.F.,(4,3,3,3,3,3,3,3,3,3,3,3,3,3,3,3,3,3,3,3,3,3,3,3,
3,3,3,3,3,3,3,3,3,3,3,3,3,3,3,3,3,3,3,3,3,3,3,3,3,3,3,3,3,3,3,3,3,3,3,3,
3,3,3,4),(1.11662023360659,1.21395960073087,1.31123941984466,1.40835533084337,
1.50542414661334,1.6024785085988,1.69990841985939,1.79708787003672,1.89464301183895,
1.99219815364118,2.09206832018503,2.19179618714873,2.2914085980286,2.39095757425931,
2.49047334616975,2.58998610368882,2.6895942510025,2.78924740690214,2.88907827446621,
2.98829723046177,3.08818590285126,3.18793562179281,3.28757488220297,3.3871537332985,
3.48670237186321,3.58625095709643,3.6858994133622,3.78559537647605,3.88547288200059,
3.98439630728237,4.08397687852573,4.18341302704854,4.28304832168035,4.38230265605514,
4.48152333465635,4.58074095905183,4.68067956531461,4.78004053948457,4.88026796179376,
4.98049538410296,5.08024179575617,5.17984583624233,5.27943941432748,5.37886540572931,
5.4782587815898,5.57764991309518,5.67738605005227,5.7769207674125,5.87675761416802,
5.97659446092355,6.07633099881174,6.17592546866135,6.2755214772967,6.37493871517028,
6.47432366735524,6.57370671833513,6.67345342318738,6.77298099142734,6.87283726458574,
6.97269353774414,7.0813231118754,7.18967359580752,7.29755728296376,7.39980554044995),
 .UNSPECIFIED.);
#120=B_SPLINE_CURVE_WITH_KNOTS('',3,(#14605,#14606,#14607,#14608,#14609,
#14610,#14611,#14612,#14613,#14614,#14615,#14616,#14617,#14618,#14619,#14620,
#14621,#14622,#14623,#14624,#14625,#14626,#14627,#14628,#14629,#14630,#14631,
#14632,#14633,#14634,#14635,#14636,#14637,#14638,#14639,#14640,#14641,#14642,
#14643,#14644,#14645,#14646,#14647,#14648,#14649,#14650,#14651,#14652,#14653,
#14654,#14655,#14656,#14657,#14658,#14659,#14660,#14661,#14662,#14663,#14664,
#14665,#14666,#14667,#14668,#14669,#14670,#14671,#14672,#14673,#14674,#14675,
#14676,#14677,#14678,#14679,#14680,#14681,#14682,#14683,#14684,#14685,#14686,
#14687,#14688,#14689,#14690,#14691,#14692,#14693,#14694,#14695,#14696,#14697,
#14698,#14699,#14700,#14701,#14702,#14703,#14704,#14705,#14706,#14707,#14708,
#14709,#14710,#14711,#14712,#14713,#14714,#14715,#14716,#14717,#14718,#14719,
#14720,#14721,#14722,#14723,#14724,#14725,#14726,#14727,#14728,#14729,#14730,
#14731,#14732,#14733,#14734,#14735,#14736,#14737,#14738,#14739,#14740,#14741,
#14742,#14743,#14744,#14745,#14746,#14747,#14748,#14749,#14750,#14751,#14752,
#14753,#14754,#14755,#14756,#14757,#14758,#14759,#14760,#14761,#14762,#14763,
#14764,#14765,#14766,#14767,#14768,#14769,#14770,#14771,#14772,#14773,#14774,
#14775,#14776,#14777,#14778,#14779,#14780,#14781,#14782,#14783,#14784,#14785,
#14786,#14787,#14788,#14789,#14790,#14791,#14792,#14793,#14794,#14795,#14796,
#14797),.UNSPECIFIED.,.F.,.F.,(4,3,3,3,3,3,3,3,3,3,3,3,3,3,3,3,3,3,3,3,
3,3,3,3,3,3,3,3,3,3,3,3,3,3,3,3,3,3,3,3,3,3,3,3,3,3,3,3,3,3,3,3,3,3,3,3,
3,3,3,3,3,3,3,3,4),(7.39980554078617,7.50127500453455,7.60280606280058,
7.70450719814795,7.80630059718374,7.90830478263615,7.96879261456473,8.06851462888085,
8.16809417032358,8.2676938604563,8.36709529233758,8.4664641421303,8.56583081537116,
8.6655960343747,8.76510671312207,8.8649992022537,8.96489169138532,9.06461014674377,
9.16418613953539,9.2637867181192,9.36318465387135,9.46255003542686,9.5619132732633,
9.66168264699895,9.7611900068315,9.8610903875187,9.96099076820591,10.0607041961592,
10.160275061418,10.259876909369,10.3592695113978,10.4586294932631,10.5579872726214,
10.6577629157227,10.7572647278683,10.8571772864474,10.9570898450265,11.0568071226611,
11.1563818918839,11.2559827706293,11.3553793797902,11.4547433987415,11.554105239685,
11.6538761602255,11.7533820527727,11.8532854873099,11.9531889218471,12.0529053877899,
12.1524793419243,12.2520804240172,12.3514762160153,12.4508394188827,12.5502004459571,
12.6499723341348,12.7494774266543,12.849382712661,12.9492879986677,13.0479544690933,
13.146491070714,13.2449296699801,13.3433020143127,13.4416647231121,13.5400212760094,
13.6384443379891,13.6829908479658),.UNSPECIFIED.);
#121=B_SPLINE_CURVE_WITH_KNOTS('',3,(#14799,#14800,#14801,#14802,#14803,
#14804,#14805,#14806,#14807,#14808,#14809,#14810,#14811,#14812,#14813,#14814,
#14815,#14816,#14817,#14818,#14819,#14820,#14821,#14822,#14823,#14824,#14825,
#14826,#14827,#14828,#14829,#14830,#14831,#14832,#14833,#14834,#14835,#14836,
#14837,#14838,#14839,#14840,#14841,#14842,#14843,#14844,#14845,#14846,#14847,
#14848,#14849,#14850,#14851,#14852,#14853,#14854,#14855,#14856,#14857,#14858,
#14859,#14860,#14861,#14862,#14863,#14864,#14865,#14866,#14867,#14868,#14869,
#14870,#14871,#14872,#14873,#14874,#14875,#14876,#14877,#14878,#14879,#14880,
#14881,#14882,#14883,#14884,#14885,#14886,#14887,#14888,#14889,#14890,#14891,
#14892,#14893,#14894,#14895,#14896,#14897,#14898,#14899,#14900,#14901,#14902,
#14903,#14904,#14905,#14906,#14907,#14908,#14909,#14910,#14911,#14912,#14913,
#14914,#14915,#14916,#14917,#14918,#14919,#14920,#14921,#14922,#14923,#14924,
#14925,#14926,#14927,#14928,#14929,#14930,#14931,#14932,#14933,#14934,#14935,
#14936,#14937,#14938,#14939,#14940,#14941,#14942,#14943,#14944,#14945,#14946,
#14947,#14948,#14949,#14950,#14951,#14952,#14953,#14954,#14955,#14956,#14957,
#14958,#14959,#14960,#14961,#14962,#14963,#14964,#14965,#14966,#14967,#14968,
#14969,#14970,#14971,#14972,#14973,#14974,#14975,#14976,#14977,#14978,#14979,
#14980,#14981,#14982,#14983,#14984,#14985,#14986,#14987,#14988),
 .UNSPECIFIED.,.F.,.F.,(4,3,3,3,3,3,3,3,3,3,3,3,3,3,3,3,3,3,3,3,3,3,3,3,
3,3,3,3,3,3,3,3,3,3,3,3,3,3,3,3,3,3,3,3,3,3,3,3,3,3,3,3,3,3,3,3,3,3,3,3,
3,3,3,4),(13.68299084831,13.8141889618991,13.9453870754883,14.045103508525,
14.1446774250973,14.2442785159987,14.3436742593052,14.4430374093747,14.5423983795991,
14.6421703227765,14.7416753490146,14.8415807506617,14.9414861523089,15.0412024277253,
15.1407761854903,15.2403773159452,15.3397728987519,15.4391358880464,15.5384966974423,
15.6382688303641,15.7377736972944,15.8376794632119,15.9375852291294,16.037301438858,
16.1368751293062,16.2364762763867,16.3358717883985,16.4352347057417,16.5345954421242,
16.6343676580806,16.7338724501227,16.8337783780363,16.93368430595,17.0334005966038,
17.1329743692339,17.232575495926,17.3319710925712,17.4313340952835,17.5306949176561,
17.6304670339347,17.7299719126177,17.8298776476941,17.9297833827706,18.0294996453416,
18.1290733896206,18.2286745233669,18.3280700912204,18.4274330650398,18.5267938584577,
18.6265660087411,18.7260708586147,18.8259766591029,18.9258824595912,19.0255987158882,
19.1251724537,19.224773589039,19.324169150001,19.4235321167842,19.5228929030299,
19.6226650613754,19.7221699038144,19.8220757201131,19.9219815364118,19.9661761551453),
 .UNSPECIFIED.);
#122=B_SPLINE_CURVE_WITH_KNOTS('',3,(#14990,#14991,#14992,#14993,#14994,
#14995,#14996,#14997,#14998,#14999,#15000,#15001,#15002,#15003,#15004,#15005,
#15006,#15007,#15008,#15009,#15010,#15011,#15012,#15013,#15014,#15015,#15016,
#15017,#15018,#15019,#15020,#15021,#15022,#15023,#15024,#15025,#15026,#15027,
#15028,#15029,#15030,#15031,#15032,#15033,#15034,#15035,#15036,#15037,#15038,
#15039,#15040,#15041,#15042,#15043,#15044,#15045,#15046,#15047,#15048,#15049,
#15050,#15051,#15052,#15053,#15054,#15055,#15056,#15057,#15058,#15059,#15060,
#15061,#15062,#15063,#15064,#15065,#15066,#15067,#15068,#15069,#15070,#15071,
#15072,#15073,#15074,#15075,#15076,#15077,#15078,#15079,#15080,#15081,#15082,
#15083,#15084,#15085,#15086,#15087,#15088,#15089,#15090,#15091,#15092,#15093,
#15094,#15095,#15096,#15097,#15098,#15099,#15100,#15101,#15102,#15103,#15104,
#15105,#15106,#15107,#15108,#15109,#15110,#15111,#15112,#15113,#15114,#15115,
#15116,#15117,#15118,#15119,#15120,#15121,#15122,#15123,#15124,#15125,#15126,
#15127,#15128,#15129,#15130,#15131,#15132,#15133,#15134,#15135,#15136,#15137,
#15138,#15139,#15140,#15141,#15142,#15143,#15144,#15145,#15146,#15147,#15148,
#15149,#15150,#15151,#15152,#15153,#15154,#15155,#15156,#15157,#15158,#15159,
#15160,#15161,#15162,#15163,#15164,#15165,#15166,#15167,#15168,#15169,#15170,
#15171,#15172,#15173,#15174,#15175,#15176,#15177,#15178,#15179),
 .UNSPECIFIED.,.F.,.F.,(4,3,3,3,3,3,3,3,3,3,3,3,3,3,3,3,3,3,3,3,3,3,3,3,
3,3,3,3,3,3,3,3,3,3,3,3,3,3,3,3,3,3,3,3,3,3,3,3,3,3,3,3,3,3,3,3,3,3,3,3,
3,3,3,4),(19.9661761554348,20.0651927431259,20.1640704476281,20.2628396467232,
20.3615508043941,20.4602352289878,20.5589241933452,20.6577132657921,20.756556096028,
20.855566502222,20.9180806132324,21.0177968761178,21.1173706206501,21.2169717543255,
21.3163673222812,21.4157302961454,21.5150910895504,21.614863239676,21.7143680893936,
21.8142738897233,21.914179690053,22.0138959525192,22.1134696966111,22.2130708303939,
22.3124663978608,22.4118293712188,22.5111901641008,22.610962314794,22.710467163953,
22.8103729654133,22.9102787668736,23.0099950308829,23.1095687765443,23.209169909938,
23.308565479027,23.4079284540233,23.5072892485576,23.6070613973418,23.7065662481709,
23.8064720459326,23.9063778436942,24.0060941069383,24.1056678518254,24.2052689854116,
24.3046645537096,24.4040275279105,24.5033883216461,24.6031604713633,24.702665321393,
24.8025711209539,24.9024769205148,25.0021931837702,25.1017669286672,25.2013680622507,
25.300763630553,25.4001266047564,25.4994873984927,25.5992595482034,25.6987643982292,
25.7986701977823,25.8985759973354,26.0135619711779,26.131461597519,26.2493612238602),
 .UNSPECIFIED.);
#123=B_SPLINE_CURVE_WITH_KNOTS('',3,(#15181,#15182,#15183,#15184,#15185,
#15186,#15187,#15188,#15189,#15190),.UNSPECIFIED.,.F.,.F.,(4,1,1,1,1,1,
1,4),(26.2493614623249,26.8946750741559,27.8907741509765,28.8868732277971,
29.8829723046177,30.8790713814383,31.8751704582589,32.5325467695045),
 .UNSPECIFIED.);
#124=B_SPLINE_CURVE_WITH_KNOTS('',3,(#15192,#15193,#15194,#15195,#15196,
#15197,#15198,#15199,#15200,#15201),.UNSPECIFIED.,.F.,.F.,(4,1,1,1,1,1,
1,4),(32.5325467695045,32.8712695350795,33.8673686119001,34.8634676887207,
35.8595667655413,36.8556658423619,37.8517649191825,38.8157320766841),
 .UNSPECIFIED.);
#125=B_SPLINE_CURVE_WITH_KNOTS('',3,(#15203,#15204,#15205,#15206,#15207,
#15208,#15209,#15210,#15211,#15212,#15213),.UNSPECIFIED.,.F.,.F.,(4,1,1,
1,1,1,1,1,4),(38.8157320766841,38.847863996003,39.8439630728236,40.8400621496442,
41.8361612264648,42.8322603032854,43.828359380106,44.8244584569266,45.0989135531719),
 .UNSPECIFIED.);
#126=B_SPLINE_CURVE_WITH_KNOTS('',3,(#15215,#15216,#15217,#15218,#15219,
#15220,#15221,#15222,#15223,#15224,#15225,#15226,#15227,#15228,#15229,#15230,
#15231,#15232,#15233,#15234,#15235,#15236,#15237,#15238,#15239,#15240,#15241,
#15242,#15243,#15244,#15245,#15246,#15247,#15248,#15249,#15250,#15251,#15252,
#15253,#15254,#15255,#15256,#15257,#15258,#15259,#15260,#15261,#15262,#15263,
#15264,#15265,#15266,#15267,#15268,#15269,#15270,#15271,#15272,#15273,#15274,
#15275,#15276,#15277,#15278,#15279,#15280,#15281,#15282,#15283,#15284,#15285,
#15286,#15287,#15288,#15289,#15290,#15291,#15292,#15293,#15294,#15295,#15296,
#15297,#15298,#15299,#15300,#15301,#15302,#15303,#15304,#15305,#15306,#15307,
#15308,#15309,#15310,#15311,#15312,#15313,#15314,#15315,#15316,#15317,#15318,
#15319,#15320,#15321,#15322,#15323,#15324,#15325,#15326,#15327,#15328,#15329,
#15330,#15331,#15332,#15333,#15334,#15335,#15336,#15337,#15338,#15339,#15340,
#15341,#15342,#15343,#15344,#15345,#15346,#15347,#15348,#15349,#15350,#15351,
#15352,#15353,#15354,#15355,#15356,#15357,#15358,#15359,#15360,#15361,#15362,
#15363,#15364,#15365,#15366,#15367,#15368,#15369,#15370,#15371,#15372,#15373,
#15374,#15375,#15376,#15377,#15378,#15379,#15380,#15381,#15382,#15383,#15384,
#15385,#15386,#15387,#15388,#15389,#15390,#15391,#15392,#15393,#15394,#15395,
#15396,#15397,#15398,#15399,#15400,#15401,#15402,#15403,#15404,#15405,#15406,
#15407),.UNSPECIFIED.,.F.,.F.,(4,3,3,3,3,3,3,3,3,3,3,3,3,3,3,3,3,3,3,3,
3,3,3,3,3,3,3,3,3,3,3,3,3,3,3,3,3,3,3,3,3,3,3,3,3,3,3,3,3,3,3,3,3,3,3,3,
3,3,3,3,3,3,3,3,4),(45.0989173838637,45.1974554529775,45.295945096918,45.3944178160819,
45.4929050849441,45.5914993213688,45.6901566383898,45.7889738889615,45.8205575337472,
45.9202737971117,46.0198475421196,46.1194486756756,46.218844244094,46.318207218415,
46.41756801227,46.5173401618445,46.6168450119913,46.7167508112796,46.8166566105678,
46.9163728739322,47.0159466189399,47.115547752496,47.2149433209143,47.3143062952352,
47.41366708909,47.5134392386646,47.6129440888115,47.7128498880999,47.8127556873883,
47.9124719507529,48.0120456957608,48.1116468293169,48.2110423977352,48.3104053720562,
48.4097661659113,48.5095383154857,48.6090431656326,48.7089489649208,48.8088547642089,
48.9085710275734,49.0081447725815,49.1077459061375,49.2071414745558,49.3065044488767,
49.4058652427315,49.505637392306,49.605142242453,49.7050480417412,49.8049538410295,
49.904670104394,50.0042438494017,50.1038449829578,50.2032405513761,50.3026035256972,
50.4019643195525,50.5017364691269,50.601241319274,50.701147118562,50.8010529178501,
50.9027101568192,51.0042053443703,51.1055352600135,51.2067678706425,51.3079249204948,
51.3821026910433),.UNSPECIFIED.);
#127=B_SPLINE_CURVE_WITH_KNOTS('',3,(#15409,#15410,#15411,#15412,#15413,
#15414,#15415,#15416,#15417,#15418,#15419,#15420,#15421,#15422,#15423,#15424,
#15425,#15426,#15427,#15428,#15429,#15430,#15431,#15432,#15433,#15434,#15435,
#15436,#15437,#15438,#15439,#15440,#15441,#15442,#15443,#15444,#15445,#15446,
#15447,#15448,#15449,#15450,#15451,#15452,#15453,#15454,#15455,#15456,#15457,
#15458,#15459,#15460,#15461,#15462,#15463,#15464,#15465,#15466,#15467,#15468,
#15469,#15470,#15471,#15472,#15473,#15474,#15475,#15476,#15477,#15478,#15479,
#15480,#15481,#15482,#15483,#15484,#15485,#15486,#15487,#15488,#15489,#15490,
#15491,#15492,#15493,#15494,#15495,#15496,#15497,#15498,#15499,#15500,#15501,
#15502,#15503,#15504,#15505,#15506,#15507,#15508,#15509,#15510,#15511,#15512,
#15513,#15514,#15515,#15516,#15517,#15518,#15519,#15520,#15521,#15522,#15523,
#15524,#15525,#15526,#15527,#15528,#15529,#15530,#15531,#15532,#15533,#15534,
#15535,#15536,#15537,#15538,#15539,#15540,#15541,#15542,#15543,#15544,#15545,
#15546,#15547,#15548,#15549,#15550,#15551,#15552,#15553,#15554,#15555,#15556,
#15557,#15558,#15559,#15560,#15561,#15562,#15563,#15564,#15565,#15566,#15567,
#15568,#15569,#15570,#15571,#15572,#15573,#15574,#15575,#15576,#15577,#15578,
#15579,#15580,#15581,#15582,#15583,#15584,#15585,#15586,#15587,#15588,#15589,
#15590,#15591,#15592,#15593,#15594,#15595,#15596,#15597,#15598),
 .UNSPECIFIED.,.F.,.F.,(4,3,3,3,3,3,3,3,3,3,3,3,3,3,3,3,3,3,3,3,3,3,3,3,
3,3,3,3,3,3,3,3,3,3,3,3,3,3,3,3,3,3,3,3,3,3,3,3,3,3,3,3,3,3,3,3,3,3,3,3,
3,3,3,4),(51.3821026914169,51.4908012816284,51.5998205885544,51.709326319515,
51.7971519946707,51.8968682580351,51.9964420030431,52.0960431365991,52.1954387050175,
52.2948016793383,52.3941624731934,52.4939346227679,52.5934394729148,52.693345272203,
52.7932510714913,52.8929673348557,52.9925410798636,53.0921422134197,53.191537781838,
53.290900756159,53.390261550014,53.4900336995885,53.5895385497354,53.6894443490237,
53.7893501483119,53.8890664116764,53.9886401566842,54.0882412902402,54.1876368586586,
54.2869998329795,54.3863606268345,54.486132776409,54.5856376265559,54.6855434258442,
54.7854492251325,54.885165488497,54.9847392335048,55.0843403670609,55.1837359354792,
55.2830989098002,55.3824597036552,55.4822318532297,55.5817367033766,55.6816425026649,
55.7815483019531,55.8812645653176,55.9808383103254,56.0804394438814,56.1798350122998,
56.2791979866208,56.3785587804758,56.4783309300503,56.5778357801972,56.6777415794854,
56.7776473787737,56.8760648306049,56.9747177265293,57.0728810226054,57.1709850818081,
57.2690618349296,57.3681183756972,57.4662860871674,57.5657870425837,57.665287998),
 .UNSPECIFIED.);
#128=B_SPLINE_CURVE_WITH_KNOTS('',3,(#15600,#15601,#15602,#15603,#15604,
#15605,#15606,#15607,#15608,#15609,#15610,#15611,#15612,#15613,#15614,#15615,
#15616,#15617,#15618,#15619,#15620,#15621,#15622,#15623,#15624,#15625,#15626,
#15627,#15628,#15629,#15630,#15631,#15632,#15633,#15634,#15635,#15636,#15637,
#15638,#15639,#15640,#15641,#15642,#15643,#15644,#15645,#15646,#15647,#15648,
#15649,#15650,#15651,#15652,#15653,#15654,#15655,#15656,#15657,#15658,#15659,
#15660,#15661,#15662,#15663,#15664,#15665,#15666,#15667,#15668,#15669,#15670,
#15671,#15672,#15673,#15674,#15675,#15676,#15677,#15678,#15679,#15680,#15681,
#15682,#15683,#15684,#15685,#15686,#15687,#15688,#15689,#15690,#15691,#15692,
#15693,#15694,#15695,#15696,#15697,#15698,#15699,#15700,#15701,#15702,#15703,
#15704,#15705,#15706,#15707,#15708,#15709,#15710,#15711,#15712,#15713,#15714,
#15715,#15716,#15717,#15718,#15719,#15720,#15721,#15722,#15723,#15724,#15725,
#15726,#15727,#15728,#15729,#15730,#15731,#15732,#15733,#15734,#15735,#15736,
#15737,#15738,#15739,#15740,#15741,#15742,#15743,#15744,#15745,#15746,#15747,
#15748,#15749,#15750,#15751,#15752,#15753,#15754,#15755,#15756,#15757,#15758,
#15759,#15760,#15761,#15762,#15763,#15764,#15765,#15766,#15767,#15768,#15769,
#15770,#15771,#15772,#15773,#15774,#15775,#15776,#15777,#15778,#15779,#15780,
#15781,#15782,#15783,#15784,#15785,#15786,#15787,#15788,#15789),
 .UNSPECIFIED.,.F.,.F.,(4,3,3,3,3,3,3,3,3,3,3,3,3,3,3,3,3,3,3,3,3,3,3,3,
3,3,3,3,3,3,3,3,3,3,3,3,3,3,3,3,3,3,3,3,3,3,3,3,3,3,3,3,3,3,3,3,3,3,3,3,
3,3,3,4),(57.6652879982229,57.7737464555943,57.8734627189586,57.9730364639664,
58.0726375975224,58.1720331659406,58.2713961402615,58.3707569341163,58.470529083691,
58.5700339338378,58.6699397331264,58.7698455324149,58.8695617957793,58.9691355407871,
59.0687366743432,59.1681322427615,59.2674952170824,59.3668560109375,59.4666281605119,
59.5661330106589,59.6660388099471,59.7659446092354,59.8656608725999,59.9652346176078,
60.0648357511638,60.1642313195822,60.2635942939031,60.3629550877582,60.4627272373327,
60.5622320874796,60.6621378867678,60.762043686056,60.8617599494205,60.9613336944283,
61.0609348279844,61.1603303964027,61.2596933707237,61.3590541645787,61.4588263141532,
61.5583311643001,61.6582369635884,61.7581427628766,61.8578590262411,61.9574327712489,
62.0570339048049,62.1564294732233,62.2557924475442,62.3551532413992,62.4549253909737,
62.5544302411206,62.6543360404089,62.7542418396972,62.8539581030616,62.9535318480695,
63.0531329816256,63.1525285500439,63.2518915243648,63.3512523182199,63.4510244677944,
63.5505293179413,63.6504351172296,63.7503409165178,63.8932777478165,63.9484733054025),
 .UNSPECIFIED.);
#129=B_SPLINE_CURVE_WITH_KNOTS('',3,(#15791,#15792,#15793,#15794,#15795,
#15796,#15797,#15798,#15799,#15800,#15801,#15802,#15803,#15804,#15805,#15806,
#15807,#15808,#15809,#15810,#15811,#15812,#15813,#15814,#15815,#15816,#15817,
#15818,#15819,#15820,#15821,#15822,#15823,#15824,#15825,#15826,#15827,#15828,
#15829,#15830,#15831,#15832,#15833,#15834,#15835,#15836,#15837,#15838,#15839,
#15840,#15841,#15842,#15843,#15844,#15845,#15846,#15847,#15848,#15849,#15850,
#15851,#15852,#15853,#15854,#15855,#15856,#15857,#15858,#15859,#15860,#15861,
#15862,#15863,#15864,#15865,#15866,#15867,#15868,#15869,#15870,#15871,#15872,
#15873,#15874,#15875,#15876,#15877,#15878,#15879,#15880,#15881,#15882,#15883,
#15884,#15885,#15886,#15887,#15888,#15889,#15890,#15891,#15892,#15893,#15894,
#15895,#15896,#15897,#15898,#15899,#15900,#15901,#15902,#15903,#15904,#15905,
#15906,#15907,#15908,#15909,#15910,#15911,#15912,#15913,#15914,#15915,#15916,
#15917,#15918,#15919,#15920,#15921,#15922,#15923,#15924,#15925,#15926,#15927,
#15928,#15929,#15930,#15931,#15932,#15933,#15934,#15935,#15936,#15937,#15938,
#15939,#15940,#15941,#15942,#15943,#15944,#15945,#15946,#15947,#15948,#15949,
#15950,#15951,#15952,#15953,#15954,#15955,#15956,#15957,#15958,#15959,#15960,
#15961,#15962,#15963,#15964,#15965,#15966,#15967,#15968,#15969,#15970,#15971,
#15972,#15973,#15974,#15975,#15976,#15977,#15978,#15979,#15980),
 .UNSPECIFIED.,.F.,.F.,(4,3,3,3,3,3,3,3,3,3,3,3,3,3,3,3,3,3,3,3,3,3,3,3,
3,3,3,3,3,3,3,3,3,3,3,3,3,3,3,3,3,3,3,3,3,3,3,3,3,3,3,3,3,3,3,3,3,3,3,3,
3,3,3,4),(63.9484733057394,64.0482191416893,64.1462266027633,64.2441857239191,
64.3421285416433,64.4432064045671,64.5412711684761,64.6438555809072,64.7464399933384,
64.8461562567029,64.9457300017107,65.0453311352667,65.1447267036851,65.2440896780061,
65.3434504718611,65.4432226214356,65.5427274715825,65.6426332708707,65.742539070159,
65.8422553335236,65.9418290785314,66.0414302120874,66.1408257805058,66.2401887548268,
66.3395495486819,66.4393216982563,66.5388265484033,66.6387323476914,66.7386381469796,
66.8383544103442,66.9379281553521,67.0375292889081,67.1369248573264,67.2362878316474,
67.3356486255025,67.4354207750769,67.5349256252239,67.634831424512,67.7347372238002,
67.8344534871647,67.9340272321724,68.0336283657284,68.1330239341468,68.2323869084678,
68.3317477023228,68.4315198518973,68.5310247020442,68.6309305013325,68.7308363006208,
68.8305525639852,68.930126308993,69.029727442549,69.1291230109673,69.2284859852882,
69.3278467791429,69.4276189287175,69.5271237788644,69.6270295781529,69.7269353774414,
69.8314472135698,69.9356740013037,70.0397314369953,70.1435751012175,70.2316586125821),
 .UNSPECIFIED.);
#130=B_SPLINE_CURVE_WITH_KNOTS('',3,(#15982,#15983,#15984,#15985,#15986,
#15987,#15988,#15989,#15990,#15991),.UNSPECIFIED.,.F.,.F.,(4,1,1,1,1,1,
1,4),(70.2316591231073,70.7230344542619,71.7191335310825,72.7152326079031,
73.7113316847237,74.7074307615443,75.7035298383649,76.5148439197617),
 .UNSPECIFIED.);
#131=B_SPLINE_CURVE_WITH_KNOTS('',3,(#15993,#15994,#15995,#15996,#15997,
#15998,#15999,#16000,#16001,#16002,#16003),.UNSPECIFIED.,.F.,.F.,(4,1,1,
1,1,1,1,1,4),(76.5148439197617,76.6996289151855,77.6957279920061,78.6918270688267,
79.6879261456473,80.6840252224679,81.6801242992884,82.676223376109,82.7980292269413),
 .UNSPECIFIED.);
#132=B_SPLINE_CURVE_WITH_KNOTS('',3,(#16005,#16006,#16007,#16008,#16009,
#16010,#16011,#16012,#16013,#16014),.UNSPECIFIED.,.F.,.F.,(4,1,1,1,1,1,
1,4),(82.7980292269413,83.6723224529296,84.6684215297502,85.6645206065708,
86.6606196833914,87.656718760212,88.6528178370326,89.0812093748789),
 .UNSPECIFIED.);
#133=B_SPLINE_CURVE_WITH_KNOTS('',3,(#16016,#16017,#16018,#16019,#16020,
#16021,#16022,#16023,#16024,#16025,#16026,#16027,#16028,#16029,#16030,#16031,
#16032,#16033,#16034,#16035,#16036,#16037,#16038,#16039,#16040,#16041,#16042,
#16043,#16044,#16045,#16046,#16047,#16048,#16049,#16050,#16051,#16052,#16053,
#16054,#16055,#16056,#16057,#16058,#16059,#16060,#16061,#16062,#16063,#16064,
#16065,#16066,#16067,#16068,#16069,#16070,#16071,#16072,#16073,#16074,#16075,
#16076,#16077,#16078,#16079,#16080,#16081,#16082,#16083,#16084,#16085,#16086,
#16087,#16088,#16089,#16090,#16091,#16092,#16093,#16094,#16095,#16096,#16097,
#16098,#16099,#16100,#16101,#16102,#16103,#16104,#16105,#16106,#16107,#16108,
#16109,#16110,#16111,#16112,#16113,#16114,#16115,#16116,#16117,#16118,#16119,
#16120,#16121,#16122,#16123,#16124,#16125,#16126,#16127,#16128,#16129,#16130,
#16131,#16132,#16133,#16134,#16135,#16136,#16137,#16138,#16139,#16140,#16141,
#16142,#16143,#16144,#16145,#16146,#16147,#16148,#16149,#16150,#16151,#16152,
#16153,#16154,#16155,#16156,#16157,#16158,#16159,#16160,#16161,#16162,#16163,
#16164,#16165,#16166,#16167,#16168,#16169,#16170,#16171,#16172,#16173,#16174,
#16175,#16176,#16177,#16178,#16179,#16180,#16181,#16182,#16183,#16184,#16185,
#16186,#16187,#16188,#16189,#16190,#16191,#16192,#16193,#16194,#16195,#16196,
#16197,#16198,#16199,#16200,#16201,#16202,#16203,#16204,#16205,#16206,#16207,
#16208),.UNSPECIFIED.,.F.,.F.,(4,3,3,3,3,3,3,3,3,3,3,3,3,3,3,3,3,3,3,3,
3,3,3,3,3,3,3,3,3,3,3,3,3,3,3,3,3,3,3,3,3,3,3,3,3,3,3,3,3,3,3,3,3,3,3,3,
3,3,3,3,3,3,3,3,4),(89.0812145341209,89.1827415934861,89.2843318214027,
89.3860935755736,89.4879486441807,89.5900145312011,89.6489169138532,89.7486331772176,
89.8482069222256,89.9478080557816,90.0472036241999,90.1465665985208,90.245927392376,
90.3456995419504,90.4452043920974,90.5451101913856,90.6450159906738,90.7447322540383,
90.844305999046,90.9439071326021,91.0433027010204,91.1426656753412,91.2420264691962,
91.3417986187707,91.4413034689177,91.541209268206,91.6411150674944,91.7408313308589,
91.8404050758667,91.9400062094227,92.039401777841,92.1387647521618,92.238125546017,
92.3378976955914,92.4374025457384,92.5373083450266,92.6372141443149,92.7369304076793,
92.8365041526871,92.9361052862431,93.0355008546614,93.1348638289824,93.2342246228377,
93.3339967724121,93.433501622559,93.5334074218472,93.6333132211355,93.7330294844999,
93.8326032295079,93.9322043630639,94.0315999314824,94.1309629058033,94.230323699658,
94.3300958492325,94.4296006993794,94.5295064986678,94.6294122979561,94.7280662758581,
94.8265905097541,94.9250168787457,95.0233771428202,95.1217282720921,95.2200733769884,
95.3184859041702,95.3643998413005),.UNSPECIFIED.);
#134=B_SPLINE_CURVE_WITH_KNOTS('',3,(#16210,#16211,#16212,#16213,#16214,
#16215,#16216,#16217,#16218,#16219,#16220,#16221,#16222,#16223,#16224,#16225,
#16226,#16227,#16228,#16229,#16230,#16231,#16232,#16233,#16234,#16235,#16236,
#16237,#16238,#16239,#16240,#16241,#16242,#16243,#16244,#16245,#16246,#16247,
#16248,#16249,#16250,#16251,#16252,#16253,#16254,#16255,#16256,#16257,#16258,
#16259,#16260,#16261,#16262,#16263,#16264,#16265,#16266,#16267,#16268,#16269,
#16270,#16271,#16272,#16273,#16274,#16275,#16276,#16277,#16278,#16279,#16280,
#16281,#16282,#16283,#16284,#16285,#16286,#16287,#16288,#16289,#16290,#16291,
#16292,#16293,#16294,#16295,#16296,#16297,#16298,#16299,#16300,#16301,#16302,
#16303,#16304,#16305,#16306,#16307,#16308,#16309,#16310,#16311,#16312,#16313,
#16314,#16315,#16316,#16317,#16318,#16319,#16320,#16321,#16322,#16323,#16324,
#16325,#16326,#16327,#16328,#16329,#16330,#16331,#16332,#16333,#16334,#16335,
#16336,#16337,#16338,#16339,#16340,#16341,#16342,#16343,#16344,#16345,#16346,
#16347,#16348,#16349,#16350,#16351,#16352,#16353,#16354,#16355,#16356,#16357,
#16358,#16359,#16360,#16361,#16362,#16363,#16364,#16365,#16366,#16367,#16368,
#16369,#16370,#16371,#16372,#16373,#16374,#16375,#16376,#16377,#16378,#16379,
#16380,#16381,#16382,#16383,#16384,#16385,#16386,#16387,#16388,#16389,#16390,
#16391,#16392,#16393,#16394,#16395,#16396,#16397,#16398,#16399),
 .UNSPECIFIED.,.F.,.F.,(4,3,3,3,3,3,3,3,3,3,3,3,3,3,3,3,3,3,3,3,3,3,3,3,
3,3,3,3,3,3,3,3,3,3,3,3,3,3,3,3,3,3,3,3,3,3,3,3,3,3,3,3,3,3,3,3,3,3,3,3,
3,3,3,4),(95.364399841631,95.4949556082039,95.6255113747767,95.7252276381412,
95.824801383149,95.924402516705,96.0237980851234,96.1231610594444,96.2225218532995,
96.3222940028739,96.4217988530209,96.5217046523091,96.6216104515973,96.7213267149618,
96.8209004599697,96.9205015935257,97.0198971619441,97.119260136265,97.21862093012,
97.3183930796945,97.4178979298414,97.5178037291297,97.6177095284179,97.7174257917823,
97.8169995367902,97.9166006703463,98.0159962387646,98.1153592130855,98.2147200069405,
98.314492156515,98.413997006662,98.5139028059502,98.6138086052385,98.7135248686029,
98.8130986136108,98.9126997471668,99.0120953155852,99.1114582899061,99.2108190837611,
99.3105912333356,99.4100960834825,99.5100018827708,99.6099076820591,99.7096239454237,
99.8091976904318,99.9087988239878,100.008194392406,100.107557366727,100.206918160583,
100.306690310157,100.406195160304,100.506100959592,100.60600675888,100.705723022244,
100.805296767252,100.904897900808,101.004293469226,101.103656443547,101.203017237402,
101.302789386976,101.402294237123,101.502200036412,101.6021058357,101.64758514848),
 .UNSPECIFIED.);
#135=B_SPLINE_CURVE_WITH_KNOTS('',3,(#16401,#16402,#16403,#16404,#16405,
#16406,#16407,#16408,#16409,#16410,#16411,#16412,#16413,#16414,#16415,#16416,
#16417,#16418,#16419,#16420,#16421,#16422,#16423,#16424,#16425,#16426,#16427,
#16428,#16429,#16430,#16431,#16432,#16433,#16434,#16435,#16436,#16437,#16438,
#16439,#16440,#16441,#16442,#16443,#16444,#16445,#16446,#16447,#16448,#16449,
#16450,#16451,#16452,#16453,#16454,#16455,#16456,#16457,#16458,#16459,#16460,
#16461,#16462,#16463,#16464,#16465,#16466,#16467,#16468,#16469,#16470,#16471,
#16472,#16473,#16474,#16475,#16476,#16477,#16478,#16479,#16480,#16481,#16482,
#16483,#16484,#16485,#16486,#16487,#16488,#16489,#16490,#16491,#16492,#16493,
#16494,#16495,#16496,#16497,#16498,#16499,#16500,#16501,#16502,#16503,#16504,
#16505,#16506,#16507,#16508,#16509,#16510,#16511,#16512,#16513,#16514,#16515,
#16516,#16517,#16518,#16519,#16520,#16521,#16522,#16523,#16524,#16525,#16526,
#16527,#16528,#16529,#16530,#16531,#16532,#16533,#16534,#16535,#16536,#16537,
#16538,#16539,#16540,#16541,#16542,#16543,#16544,#16545,#16546,#16547,#16548,
#16549,#16550,#16551,#16552,#16553,#16554,#16555,#16556,#16557,#16558,#16559,
#16560,#16561,#16562,#16563,#16564,#16565,#16566,#16567,#16568,#16569,#16570,
#16571,#16572,#16573,#16574,#16575,#16576,#16577,#16578,#16579,#16580,#16581,
#16582,#16583,#16584,#16585,#16586,#16587,#16588,#16589,#16590),
 .UNSPECIFIED.,.F.,.F.,(4,3,3,3,3,3,3,3,3,3,3,3,3,3,3,3,3,3,3,3,3,3,3,3,
3,3,3,3,3,3,3,3,3,3,3,3,3,3,3,3,3,3,3,3,3,3,3,3,3,3,3,3,3,3,3,3,3,3,3,3,
3,3,3,4),(101.647585148776,101.746584368854,101.845444892809,101.944197198785,
102.042891669239,102.141559630776,102.240232374683,102.339005330467,102.43783229681,
102.536826449131,102.598204912521,102.697921175885,102.797494920893,102.897096054449,
102.996491622867,103.095854597188,103.195215391042,103.294987540617,103.394492390764,
103.494398190052,103.594303989341,103.694020252705,103.793593997713,103.893195131269,
103.992590699688,104.091953674009,104.191314467864,104.291086617438,104.390591467585,
104.490497266874,104.590403066162,104.690119329527,104.789693074535,104.889294208091,
104.98868977651,105.088052750831,105.187413544686,105.28718569426,105.386690544408,
105.486596343695,105.586502142983,105.686218406347,105.785792151355,105.885393284911,
105.984788853329,106.08415182765,106.183512621505,106.283284771079,106.382789621226,
106.482695420514,106.582601219803,106.682317483167,106.781891228175,106.881492361731,
106.980887930149,107.08025090447,107.179611698324,107.279383847899,107.378888698046,
107.478794497335,107.578700296624,107.693554700363,107.812162458578,107.930770216793),
 .UNSPECIFIED.);
#136=B_SPLINE_CURVE_WITH_KNOTS('',3,(#16592,#16593,#16594,#16595,#16596,
#16597,#16598,#16599,#16600,#16601),.UNSPECIFIED.,.F.,.F.,(4,1,1,1,1,1,
1,4),(107.93077045566,108.574799373444,109.570898450265,110.566997527086,
111.563096603906,112.559195680727,113.555294757547,114.213955762839),
 .UNSPECIFIED.);
#137=B_SPLINE_CURVE_WITH_KNOTS('',3,(#16603,#16604,#16605,#16606,#16607,
#16608,#16609,#16610,#16611,#16612),.UNSPECIFIED.,.F.,.F.,(4,1,1,1,1,1,
1,4),(114.213955762839,114.551393834368,115.547492911189,116.543591988009,
117.53969106483,118.53579014165,119.531889218471,120.497141070019),
 .UNSPECIFIED.);
#138=B_SPLINE_CURVE_WITH_KNOTS('',3,(#16614,#16615,#16616,#16617,#16618,
#16619,#16620,#16621,#16622,#16623,#16624,#16625),.UNSPECIFIED.,.F.,.F.,
(4,2,1,1,1,1,1,1,4),(120.497141070019,120.527988295291,121.524087372112,
122.520186448933,123.516285525753,124.512384602574,125.508483679394,126.504582756215,
126.780322445093),.UNSPECIFIED.);
#139=B_SPLINE_CURVE_WITH_KNOTS('',3,(#16627,#16628,#16629,#16630,#16631,
#16632,#16633,#16634,#16635,#16636,#16637,#16638,#16639,#16640,#16641,#16642,
#16643,#16644,#16645,#16646,#16647,#16648,#16649,#16650,#16651,#16652,#16653,
#16654,#16655,#16656,#16657,#16658,#16659,#16660,#16661,#16662,#16663,#16664,
#16665,#16666,#16667,#16668,#16669,#16670,#16671,#16672,#16673,#16674,#16675,
#16676,#16677,#16678,#16679,#16680,#16681,#16682,#16683,#16684,#16685,#16686,
#16687,#16688,#16689,#16690,#16691,#16692,#16693,#16694,#16695,#16696,#16697,
#16698,#16699,#16700,#16701,#16702,#16703,#16704,#16705,#16706,#16707,#16708,
#16709,#16710,#16711,#16712,#16713,#16714,#16715,#16716,#16717,#16718,#16719,
#16720,#16721,#16722,#16723,#16724,#16725,#16726,#16727,#16728,#16729,#16730,
#16731,#16732,#16733,#16734,#16735,#16736,#16737,#16738,#16739,#16740,#16741,
#16742,#16743,#16744,#16745,#16746,#16747,#16748,#16749,#16750,#16751,#16752,
#16753,#16754,#16755,#16756,#16757,#16758,#16759,#16760,#16761,#16762,#16763,
#16764,#16765,#16766,#16767,#16768,#16769,#16770,#16771,#16772,#16773,#16774,
#16775,#16776,#16777,#16778,#16779,#16780,#16781,#16782,#16783,#16784,#16785,
#16786,#16787,#16788,#16789,#16790,#16791,#16792,#16793,#16794,#16795,#16796,
#16797,#16798,#16799,#16800,#16801,#16802,#16803,#16804,#16805,#16806,#16807,
#16808,#16809,#16810,#16811,#16812,#16813,#16814,#16815,#16816,#16817,#16818,
#16819),.UNSPECIFIED.,.F.,.F.,(4,3,3,3,3,3,3,3,3,3,3,3,3,3,3,3,3,3,3,3,
3,3,3,3,3,3,3,3,3,3,3,3,3,3,3,3,3,3,3,3,3,3,3,3,3,3,3,3,3,3,3,3,3,3,3,3,
3,3,3,3,3,3,3,3,4),(126.780326377198,126.878877284594,126.977380400159,
127.075867207474,127.17436916484,127.272978540219,127.371651503393,127.470484131865,
127.500681833036,127.600398113995,127.699971876108,127.799573005326,127.898968589554,
127.998331579165,128.097692387774,128.197464518294,128.296969381748,128.396875145802,
128.496780909856,128.596497347317,128.696071267361,128.795672357275,128.895068101716,
128.994431252039,129.093792221636,129.193564162896,129.293069186359,129.392974586518,
129.492879986677,129.592595825653,129.692169146105,129.791770385779,129.891165532297,
129.990528086646,130.089888463013,130.189661113134,130.289165556068,130.389072309782,
130.488979063497,130.588695574014,130.688269563117,130.787870635267,130.887266438695,
130.986629644111,131.085990664859,131.185762533724,131.285267598285,131.385172869301,
131.485078140318,131.584795431877,131.684370212025,131.783971087664,131.883367700396,
131.982731720144,132.082093559111,132.181864473618,132.281370357431,132.381273787285,
132.481177217139,132.582792401507,132.68424603593,132.785535467147,132.886728202003,
132.98784686251,133.063511684378),.UNSPECIFIED.);
#140=B_SPLINE_CURVE_WITH_KNOTS('',3,(#16821,#16822,#16823,#16824,#16825,
#16826,#16827,#16828,#16829,#16830,#16831,#16832,#16833,#16834,#16835,#16836,
#16837,#16838,#16839,#16840,#16841,#16842,#16843,#16844,#16845,#16846,#16847,
#16848,#16849,#16850,#16851,#16852,#16853,#16854,#16855,#16856,#16857,#16858,
#16859,#16860,#16861,#16862,#16863,#16864,#16865,#16866,#16867,#16868,#16869,
#16870,#16871,#16872,#16873,#16874,#16875,#16876,#16877,#16878,#16879,#16880,
#16881,#16882,#16883,#16884,#16885,#16886,#16887,#16888,#16889,#16890,#16891,
#16892,#16893,#16894,#16895,#16896,#16897,#16898,#16899,#16900,#16901,#16902,
#16903,#16904,#16905,#16906,#16907,#16908,#16909,#16910,#16911,#16912,#16913,
#16914,#16915,#16916,#16917,#16918,#16919,#16920,#16921,#16922,#16923,#16924,
#16925,#16926,#16927,#16928,#16929,#16930,#16931,#16932,#16933,#16934,#16935,
#16936,#16937,#16938,#16939,#16940,#16941,#16942,#16943,#16944,#16945,#16946,
#16947,#16948,#16949,#16950,#16951,#16952,#16953,#16954,#16955,#16956,#16957,
#16958,#16959,#16960,#16961,#16962,#16963,#16964,#16965,#16966,#16967,#16968,
#16969,#16970,#16971,#16972,#16973,#16974,#16975,#16976,#16977,#16978,#16979,
#16980,#16981,#16982,#16983,#16984,#16985,#16986,#16987,#16988,#16989,#16990,
#16991,#16992,#16993,#16994,#16995,#16996,#16997,#16998,#16999,#17000,#17001,
#17002,#17003,#17004,#17005,#17006,#17007,#17008,#17009,#17010),
 .UNSPECIFIED.,.F.,.F.,(4,3,3,3,3,3,3,3,3,3,3,3,3,3,3,3,3,3,3,3,3,3,3,3,
3,3,3,3,3,3,3,3,3,3,3,3,3,3,3,3,3,3,3,3,3,3,3,3,3,3,3,3,3,3,3,3,3,3,3,3,
3,3,3,4),(133.063511684756,133.172291812194,133.281396986747,133.390991808195,
133.477276293959,133.576995093555,133.6765713564,133.776171858198,133.875569882223,
133.974935283458,134.074298472429,134.174067697017,134.27357484093,134.373475105855,
134.47337537078,134.573097363914,134.672676888739,134.772276583596,134.871678010046,
134.971046858628,135.070413534876,135.170178763057,135.269689455091,135.369581951345,
135.4694744476,135.569169653751,135.668722304918,135.768328707356,135.867703245832,
135.967045260529,136.066385192976,136.166182275837,136.265666715005,136.365620119713,
136.465573524421,136.565312640281,136.664909132444,136.764504566044,136.863922464818,
136.963307564101,137.062690248756,137.162435836878,137.261961787792,137.361817194517,
137.461672601242,137.561418059226,137.661021351614,137.76061514242,137.860040889361,
137.959434210848,138.058825477927,138.158562027961,138.258097343667,138.357934510865,
138.457771678062,138.556066971266,138.654895723802,138.752936329977,138.850917784218,
138.948872116646,139.048328335374,139.146375338602,139.24653616508,139.346696991558),
 .UNSPECIFIED.);
#141=B_SPLINE_CURVE_WITH_KNOTS('',3,(#17012,#17013,#17014,#17015,#17016,
#17017),.UNSPECIFIED.,.F.,.F.,(4,1,1,4),(139.346696991558,139.453870754883,
140.449969831703,141.371287863237),.UNSPECIFIED.);
#142=B_SPLINE_CURVE_WITH_KNOTS('',3,(#17021,#17022,#17023,#17024,#17025),
 .UNSPECIFIED.,.F.,.F.,(4,1,4),(-143.438267062165,-142.442167985344,-142.321646828558),
 .UNSPECIFIED.);
#143=B_SPLINE_CURVE_WITH_KNOTS('',3,(#17027,#17028,#17029,#17030,#17031,
#17032,#17033,#17034,#17035,#17036,#17037,#17038,#17039,#17040,#17041,#17042,
#17043,#17044,#17045,#17046,#17047,#17048,#17049,#17050,#17051,#17052,#17053,
#17054,#17055,#17056,#17057,#17058,#17059,#17060,#17061,#17062,#17063,#17064,
#17065,#17066,#17067,#17068,#17069,#17070,#17071,#17072,#17073,#17074,#17075,
#17076,#17077,#17078,#17079,#17080,#17081,#17082,#17083,#17084,#17085,#17086,
#17087,#17088,#17089,#17090,#17091,#17092,#17093,#17094,#17095,#17096,#17097,
#17098,#17099,#17100,#17101,#17102,#17103,#17104,#17105,#17106,#17107,#17108,
#17109,#17110,#17111,#17112,#17113,#17114,#17115,#17116,#17117,#17118,#17119,
#17120,#17121,#17122,#17123,#17124,#17125,#17126,#17127,#17128,#17129,#17130,
#17131,#17132,#17133,#17134,#17135,#17136,#17137,#17138,#17139,#17140,#17141,
#17142,#17143,#17144,#17145,#17146,#17147,#17148,#17149,#17150,#17151,#17152,
#17153,#17154,#17155,#17156,#17157,#17158,#17159,#17160,#17161,#17162,#17163,
#17164,#17165,#17166,#17167,#17168,#17169,#17170,#17171,#17172,#17173,#17174,
#17175,#17176,#17177,#17178,#17179,#17180,#17181,#17182,#17183,#17184,#17185,
#17186,#17187,#17188,#17189,#17190,#17191,#17192,#17193,#17194,#17195,#17196,
#17197,#17198,#17199,#17200,#17201,#17202,#17203,#17204,#17205,#17206,#17207,
#17208,#17209,#17210,#17211,#17212,#17213,#17214,#17215,#17216),
 .UNSPECIFIED.,.F.,.F.,(4,3,3,3,3,3,3,3,3,3,3,3,3,3,3,3,3,3,3,3,3,3,3,3,
3,3,3,3,3,3,3,3,3,3,3,3,3,3,3,3,3,3,3,3,3,3,3,3,3,3,3,3,3,3,3,3,3,3,3,3,
3,3,3,4),(-142.321646828558,-142.224307303066,-142.127027503749,-142.029911432816,
-141.932842456695,-141.835787934027,-141.738358177651,-141.641178566955,
-141.543623737739,-141.446068908524,-141.346198822403,-141.246471036733,
-141.146858708073,-141.047309814581,-140.947794125809,-140.848281451711,
-140.748673387673,-140.6490203151,-140.549189529954,-140.449969831703,-140.350081173411,
-140.25033146897,-140.150692223606,-140.051113387881,-139.95156476499,-139.852016195714,
-139.752367755746,-139.652671809141,-139.552794320295,-139.453870754883,
-139.354290146588,-139.254853960499,-139.155218675195,-139.055964302264,
-138.956743584816,-138.857525921331,-138.757587360514,-138.658226347041,
-138.557999012552,-138.457771678062,-138.358025282948,-138.258421259161,
-138.158827676921,-138.059401702484,-137.960008343651,-137.860617229212,
-137.760881072219,-137.661346371846,-137.561509486544,-137.461672601242,
-137.361936067032,-137.262341600965,-137.162745591397,-137.06332835753,
-136.963943409428,-136.864560362603,-136.764813653057,-136.665286089106,
-136.565429806764,-136.465573524421,-136.356943941667,-136.24859344887,
-136.140709752633,-136.038461521715),.UNSPECIFIED.);
#144=B_SPLINE_CURVE_WITH_KNOTS('',3,(#17218,#17219,#17220,#17221,#17222,
#17223,#17224,#17225,#17226,#17227,#17228,#17229,#17230,#17231,#17232,#17233,
#17234,#17235,#17236,#17237,#17238,#17239,#17240,#17241,#17242,#17243,#17244,
#17245,#17246,#17247,#17248,#17249,#17250,#17251,#17252,#17253,#17254,#17255,
#17256,#17257,#17258,#17259,#17260,#17261,#17262,#17263,#17264,#17265,#17266,
#17267,#17268,#17269,#17270,#17271,#17272,#17273,#17274,#17275,#17276,#17277,
#17278,#17279,#17280,#17281,#17282,#17283,#17284,#17285,#17286,#17287,#17288,
#17289,#17290,#17291,#17292,#17293,#17294,#17295,#17296,#17297,#17298,#17299,
#17300,#17301,#17302,#17303,#17304,#17305,#17306,#17307,#17308,#17309,#17310,
#17311,#17312,#17313,#17314,#17315,#17316,#17317,#17318,#17319,#17320,#17321,
#17322,#17323,#17324,#17325,#17326,#17327,#17328,#17329,#17330,#17331,#17332,
#17333,#17334,#17335,#17336,#17337,#17338,#17339,#17340,#17341,#17342,#17343,
#17344,#17345,#17346,#17347,#17348,#17349,#17350,#17351,#17352,#17353,#17354,
#17355,#17356,#17357,#17358,#17359,#17360,#17361,#17362,#17363,#17364,#17365,
#17366,#17367,#17368,#17369,#17370,#17371,#17372,#17373,#17374,#17375,#17376,
#17377,#17378,#17379,#17380,#17381,#17382,#17383,#17384,#17385,#17386,#17387,
#17388,#17389,#17390,#17391,#17392,#17393,#17394,#17395,#17396,#17397,#17398,
#17399,#17400,#17401,#17402,#17403,#17404,#17405,#17406,#17407,#17408,#17409,
#17410),.UNSPECIFIED.,.F.,.F.,(4,3,3,3,3,3,3,3,3,3,3,3,3,3,3,3,3,3,3,3,
3,3,3,3,3,3,3,3,3,3,3,3,3,3,3,3,3,3,3,3,3,3,3,3,3,3,3,3,3,3,3,3,3,3,3,3,
3,3,3,3,3,3,3,3,4),(-136.038461521379,-135.936992047935,-135.835460979858,
-135.733759834605,-135.631966425612,-135.52996223022,-135.4694744476,-135.369752436872,
-135.270172899054,-135.17057320802,-135.071171779823,-134.971802933729,
-134.872436264197,-134.772671040843,-134.673160365789,-134.573267868285,
-134.47337537078,-134.373656915975,-134.274080923756,-134.174480345031,
-134.075082409895,-133.97571702897,-133.876353791779,-133.776584417324,
-133.677077058164,-133.577176676062,-133.477276293959,-133.377562864481,
-133.277991997674,-133.178390150107,-133.078997546483,-132.979637563009,
-132.880279782029,-132.780504140807,-132.681002327027,-132.581089772083,
-132.481177217139,-132.381459940243,-132.281885171767,-132.182284292836,
-132.082887684435,-131.983523666248,-131.884161826071,-131.784390904633,
-131.68488501285,-131.584981576584,-131.485078140318,-131.385361674423,
-131.285787720339,-131.186186638234,-131.086790846293,-130.987427643486,
-130.888066616474,-130.788294728229,-130.688789635777,-130.588884349637,
-130.488979063497,-130.390312592852,-130.291775991008,-130.193337391515,
-130.094965046952,-129.996602337919,-129.898245784786,-129.799822722568,
-129.755276214199),.UNSPECIFIED.);
#145=B_SPLINE_CURVE_WITH_KNOTS('',3,(#17412,#17413,#17414,#17415,#17416,
#17417,#17418,#17419,#17420,#17421,#17422,#17423,#17424,#17425,#17426,#17427,
#17428,#17429,#17430,#17431,#17432,#17433,#17434,#17435,#17436,#17437,#17438,
#17439,#17440,#17441,#17442,#17443,#17444,#17445,#17446,#17447,#17448,#17449,
#17450,#17451,#17452,#17453,#17454,#17455,#17456,#17457,#17458,#17459,#17460,
#17461,#17462,#17463,#17464,#17465,#17466,#17467,#17468,#17469,#17470,#17471,
#17472,#17473,#17474,#17475,#17476,#17477,#17478,#17479,#17480,#17481,#17482,
#17483,#17484,#17485,#17486,#17487,#17488,#17489,#17490,#17491,#17492,#17493,
#17494,#17495,#17496,#17497,#17498,#17499,#17500,#17501,#17502,#17503,#17504,
#17505,#17506,#17507,#17508,#17509,#17510,#17511,#17512,#17513,#17514,#17515,
#17516,#17517,#17518,#17519,#17520,#17521,#17522,#17523,#17524,#17525,#17526,
#17527,#17528,#17529,#17530,#17531,#17532,#17533,#17534,#17535,#17536,#17537,
#17538,#17539,#17540,#17541,#17542,#17543,#17544,#17545,#17546,#17547,#17548,
#17549,#17550,#17551,#17552,#17553,#17554,#17555,#17556,#17557,#17558,#17559,
#17560,#17561,#17562,#17563,#17564,#17565,#17566,#17567,#17568,#17569,#17570,
#17571,#17572,#17573,#17574,#17575,#17576,#17577,#17578,#17579,#17580,#17581,
#17582,#17583,#17584,#17585,#17586,#17587,#17588,#17589,#17590,#17591,#17592,
#17593,#17594,#17595,#17596,#17597,#17598,#17599,#17600,#17601),
 .UNSPECIFIED.,.F.,.F.,(4,3,3,3,3,3,3,3,3,3,3,3,3,3,3,3,3,3,3,3,3,3,3,3,
3,3,3,3,3,3,3,3,3,3,3,3,3,3,3,3,3,3,3,3,3,3,3,3,3,3,3,3,3,3,3,3,3,3,3,3,
3,3,3,4),(-129.755276213855,-129.624078100266,-129.492879986677,-129.393163553783,
-129.293589637355,-129.193988546418,-129.094592803258,-128.995229653337,
-128.895868683261,-128.79609673991,-128.696591713821,-128.596686311838,
-128.496780909856,-128.397064634437,-128.29749087667,-128.197889746215,
-128.098494163407,-127.999131174112,-127.899770364715,-127.799998231795,
-127.700493364865,-127.600587598951,-127.500681833036,-127.400965623265,
-127.301391932773,-127.201790785703,-127.102395273646,-127.003032356258,
-126.903671619829,-126.803899403926,-126.704394611837,-126.604488684026,
-126.504582756215,-126.404866465587,-126.305292692984,-126.205691566285,
-126.106295969667,-126.006932966982,-125.907572144637,-125.807800028326,
-125.70829514967,-125.608389414532,-125.508483679394,-125.408767416821,
-125.309193672539,-125.209592538794,-125.110196970938,-125.010833997116,
-124.911473203696,-124.811701053416,-124.71219620354,-124.612290403057,
-124.512384602574,-124.41266834627,-124.313094608452,-124.213493473115,
-124.114097912145,-124.014734945355,-123.915374159102,-123.815602000765,
-123.716097158319,-123.616191342036,-123.516285525753,-123.47209090702),
 .UNSPECIFIED.);
#146=B_SPLINE_CURVE_WITH_KNOTS('',3,(#17603,#17604,#17605,#17606,#17607,
#17608,#17609,#17610,#17611,#17612,#17613,#17614,#17615,#17616,#17617,#17618,
#17619,#17620,#17621,#17622,#17623,#17624,#17625,#17626,#17627,#17628,#17629,
#17630,#17631,#17632,#17633,#17634,#17635,#17636,#17637,#17638,#17639,#17640,
#17641,#17642,#17643,#17644,#17645,#17646,#17647,#17648,#17649,#17650,#17651,
#17652,#17653,#17654,#17655,#17656,#17657,#17658,#17659,#17660,#17661,#17662,
#17663,#17664,#17665,#17666,#17667,#17668,#17669,#17670,#17671,#17672,#17673,
#17674,#17675,#17676,#17677,#17678,#17679,#17680,#17681,#17682,#17683,#17684,
#17685,#17686,#17687,#17688,#17689,#17690,#17691,#17692,#17693,#17694,#17695,
#17696,#17697,#17698,#17699,#17700,#17701,#17702,#17703,#17704,#17705,#17706,
#17707,#17708,#17709,#17710,#17711,#17712,#17713,#17714,#17715,#17716,#17717,
#17718,#17719,#17720,#17721,#17722,#17723,#17724,#17725,#17726,#17727,#17728,
#17729,#17730,#17731,#17732,#17733,#17734,#17735,#17736,#17737,#17738,#17739,
#17740,#17741,#17742,#17743,#17744,#17745,#17746,#17747,#17748,#17749,#17750,
#17751,#17752,#17753,#17754,#17755,#17756,#17757,#17758,#17759,#17760,#17761,
#17762,#17763,#17764,#17765,#17766,#17767,#17768,#17769,#17770,#17771,#17772,
#17773,#17774,#17775,#17776,#17777,#17778,#17779,#17780,#17781,#17782,#17783,
#17784,#17785,#17786,#17787,#17788,#17789,#17790,#17791,#17792),
 .UNSPECIFIED.,.F.,.F.,(4,3,3,3,3,3,3,3,3,3,3,3,3,3,3,3,3,3,3,3,3,3,3,3,
3,3,3,3,3,3,3,3,3,3,3,3,3,3,3,3,3,3,3,3,3,3,3,3,3,3,3,3,3,3,3,3,3,3,3,3,
3,3,3,4),(-123.47209090673,-123.373074319044,-123.274196614546,-123.175427415456,
-123.07671625779,-122.978031833201,-122.879342868848,-122.780553796406,
-122.681710966175,-122.582700559986,-122.520186448933,-122.420470186047,
-122.320896441513,-122.221295307838,-122.121899739882,-122.022536766017,
-121.923175972611,-121.823403822486,-121.723898972768,-121.62399317244,
-121.524087372112,-121.424371109645,-121.324797365551,-121.225196231769,
-121.125800664301,-121.026437690942,-120.927076898058,-120.827304747366,
-120.727799898206,-120.627894096749,-120.527988295291,-120.428272031283,
-120.328698285622,-120.229097152228,-120.129701583141,-120.030338608145,
-119.930977813612,-119.831205664827,-119.731700813999,-119.631795016235,
-119.531889218471,-119.432172955226,-119.332599210339,-119.232998076753,
-119.133602508455,-119.034239534254,-118.934878740518,-118.835106590801,
-118.735601740771,-118.63569594121,-118.53579014165,-118.436073878395,-118.336500133498,
-118.236898999915,-118.137503431612,-118.038140457409,-117.938779663673,
-117.839007513962,-117.739502663937,-117.639596864383,-117.53969106483,
-117.424705090993,-117.306805464647,-117.188905838301),.UNSPECIFIED.);
#147=B_SPLINE_CURVE_WITH_KNOTS('',3,(#17794,#17795,#17796,#17797,#17798,
#17799,#17800,#17801,#17802,#17803),.UNSPECIFIED.,.F.,.F.,(4,1,1,1,1,1,
1,4),(-117.18890559984,-116.543591988009,-115.547492911189,-114.551393834368,
-113.555294757547,-112.559195680727,-111.563096603906,-110.905720292661),
 .UNSPECIFIED.);
#148=B_SPLINE_CURVE_WITH_KNOTS('',3,(#17805,#17806,#17807,#17808,#17809,
#17810,#17811,#17812,#17813,#17814),.UNSPECIFIED.,.F.,.F.,(4,1,1,1,1,1,
1,4),(-110.905720292661,-110.566997527086,-109.570898450265,-108.574799373444,
-107.578700296624,-106.582601219803,-105.586502142983,-104.622534985481),
 .UNSPECIFIED.);
#149=B_SPLINE_CURVE_WITH_KNOTS('',3,(#17816,#17817,#17818,#17819,#17820,
#17821,#17822,#17823,#17824,#17825,#17826),.UNSPECIFIED.,.F.,.F.,(4,1,1,
1,1,1,1,1,4),(-104.622534985481,-104.590403066162,-103.594303989341,-102.598204912521,
-101.6021058357,-100.60600675888,-99.6099076820591,-98.6138086052385,-98.3393535088609),
 .UNSPECIFIED.);
#150=B_SPLINE_CURVE_WITH_KNOTS('',3,(#17828,#17829,#17830,#17831,#17832,
#17833,#17834,#17835,#17836,#17837,#17838,#17839,#17840,#17841,#17842,#17843,
#17844,#17845,#17846,#17847,#17848,#17849,#17850,#17851,#17852,#17853,#17854,
#17855,#17856,#17857,#17858,#17859,#17860,#17861,#17862,#17863,#17864,#17865,
#17866,#17867,#17868,#17869,#17870,#17871,#17872,#17873,#17874,#17875,#17876,
#17877,#17878,#17879,#17880,#17881,#17882,#17883,#17884,#17885,#17886,#17887,
#17888,#17889,#17890,#17891,#17892,#17893,#17894,#17895,#17896,#17897,#17898,
#17899,#17900,#17901,#17902,#17903,#17904,#17905,#17906,#17907,#17908,#17909,
#17910,#17911,#17912,#17913,#17914,#17915,#17916,#17917,#17918,#17919,#17920,
#17921,#17922,#17923,#17924,#17925,#17926,#17927,#17928,#17929,#17930,#17931,
#17932,#17933,#17934,#17935,#17936,#17937,#17938,#17939,#17940,#17941,#17942,
#17943,#17944,#17945,#17946,#17947,#17948,#17949,#17950,#17951,#17952,#17953,
#17954,#17955,#17956,#17957,#17958,#17959,#17960,#17961,#17962,#17963,#17964,
#17965,#17966,#17967,#17968,#17969,#17970,#17971,#17972,#17973,#17974,#17975,
#17976,#17977,#17978,#17979,#17980,#17981,#17982,#17983,#17984,#17985,#17986,
#17987,#17988,#17989,#17990,#17991,#17992,#17993,#17994,#17995,#17996,#17997,
#17998,#17999,#18000,#18001,#18002,#18003,#18004,#18005,#18006,#18007,#18008,
#18009,#18010,#18011,#18012,#18013,#18014,#18015,#18016,#18017,#18018,#18019,
#18020),.UNSPECIFIED.,.F.,.F.,(4,3,3,3,3,3,3,3,3,3,3,3,3,3,3,3,3,3,3,3,
3,3,3,3,3,3,3,3,3,3,3,3,3,3,3,3,3,3,3,3,3,3,3,3,3,3,3,3,3,3,3,3,3,3,3,3,
3,3,3,3,3,3,3,3,4),(-98.3393496783013,-98.2408116091876,-98.142321965247,
-98.0438492460831,-97.9453619772209,-97.8467677407963,-97.7481104237754,
-97.6492931732037,-97.6177095284179,-97.5179932650533,-97.4184195200453,
-97.3188183864893,-97.219422818071,-97.1200598437499,-97.0206990498948,
-96.9209269003204,-96.8214220501735,-96.7215162508854,-96.6216104515973,
-96.5218941882327,-96.4223204432247,-96.3227193096687,-96.2233237412504,
-96.1239607669294,-96.0245999730744,-95.9248278235,-95.8253229733531,-95.7254171740649,
-95.6255113747767,-95.5257951114123,-95.4262213664045,-95.3266202328485,
-95.2272246644301,-95.1278616901092,-95.0285008962541,-94.9287287466796,
-94.8292238965327,-94.7293180972444,-94.6294122979561,-94.5296960345917,
-94.4301222895839,-94.3305211560279,-94.2311255876095,-94.1317626132885,
-94.0324018194335,-93.932629669859,-93.8331248197122,-93.7332190204238,
-93.6333132211355,-93.5335969577712,-93.4340232127631,-93.3344220792071,
-93.2350265107889,-93.1356635364681,-93.0363027426131,-92.9365305930386,
-92.8370257428917,-92.7371199436033,-92.6372141443149,-92.5355569053459,
-92.4340617177943,-92.3327318021511,-92.2314991915218,-92.1303421416695,
-92.0561643711217),.UNSPECIFIED.);
#151=B_SPLINE_CURVE_WITH_KNOTS('',3,(#18022,#18023,#18024,#18025,#18026,
#18027,#18028,#18029,#18030,#18031,#18032,#18033,#18034,#18035,#18036,#18037,
#18038,#18039,#18040,#18041,#18042,#18043,#18044,#18045,#18046,#18047,#18048,
#18049,#18050,#18051,#18052,#18053,#18054,#18055,#18056,#18057,#18058,#18059,
#18060,#18061,#18062,#18063,#18064,#18065,#18066,#18067,#18068,#18069,#18070,
#18071,#18072,#18073,#18074,#18075,#18076,#18077,#18078,#18079,#18080,#18081,
#18082,#18083,#18084,#18085,#18086,#18087,#18088,#18089,#18090,#18091,#18092,
#18093,#18094,#18095,#18096,#18097,#18098,#18099,#18100,#18101,#18102,#18103,
#18104,#18105,#18106,#18107,#18108,#18109,#18110,#18111,#18112,#18113,#18114,
#18115,#18116,#18117,#18118,#18119,#18120,#18121,#18122,#18123,#18124,#18125,
#18126,#18127,#18128,#18129,#18130,#18131,#18132,#18133,#18134,#18135,#18136,
#18137,#18138,#18139,#18140,#18141,#18142,#18143,#18144,#18145,#18146,#18147,
#18148,#18149,#18150,#18151,#18152,#18153,#18154,#18155,#18156,#18157,#18158,
#18159,#18160,#18161,#18162,#18163,#18164,#18165,#18166,#18167,#18168,#18169,
#18170,#18171,#18172,#18173,#18174,#18175,#18176,#18177,#18178,#18179,#18180,
#18181,#18182,#18183,#18184,#18185,#18186,#18187,#18188,#18189,#18190,#18191,
#18192,#18193,#18194,#18195,#18196,#18197,#18198,#18199,#18200,#18201,#18202,
#18203,#18204,#18205,#18206,#18207,#18208,#18209,#18210,#18211),
 .UNSPECIFIED.,.F.,.F.,(4,3,3,3,3,3,3,3,3,3,3,3,3,3,3,3,3,3,3,3,3,3,3,3,
3,3,3,3,3,3,3,3,3,3,3,3,3,3,3,3,3,3,3,3,3,3,3,3,3,3,3,3,3,3,3,3,3,3,3,3,
3,3,3,4),(-92.0561643707481,-91.9474657805367,-91.8384464736106,-91.7289407426503,
-91.6411150674944,-91.5413988041299,-91.441825059122,-91.342223925566,-91.2428283571476,
-91.1434653828266,-91.0441045889715,-90.9443324393971,-90.8448275892501,
-90.744921789962,-90.6450159906738,-90.5452997273093,-90.4457259823015,
-90.3461248487454,-90.2467292803271,-90.1473663060061,-90.0480055121511,
-89.9482333625766,-89.8487285124297,-89.7488227131414,-89.6489169138532,
-89.5492006504887,-89.4496269054809,-89.3500257719249,-89.2506302035065,
-89.1512672291856,-89.0519064353306,-88.9521342857561,-88.8526294356091,
-88.7527236363209,-88.6528178370326,-88.5531015736681,-88.4535278286602,
-88.3539266951042,-88.2545311266858,-88.1551681523649,-88.0558073585099,
-87.9560352089354,-87.8565303587885,-87.7566245595002,-87.656718760212,
-87.5570024968475,-87.4574287518397,-87.3578276182837,-87.2584320498653,
-87.1590690755444,-87.0597082816894,-86.9599361321149,-86.860431281968,
-86.7605254826797,-86.6606196833914,-86.5622022315602,-86.4635493356358,
-86.3653860395597,-86.267281980357,-86.1692052272356,-86.070148686468,-85.9719809749976,
-85.8724800195813,-85.772979064165),.UNSPECIFIED.);
#152=B_SPLINE_CURVE_WITH_KNOTS('',3,(#18213,#18214,#18215,#18216,#18217,
#18218,#18219,#18220,#18221,#18222,#18223,#18224,#18225,#18226,#18227,#18228,
#18229,#18230,#18231,#18232,#18233,#18234,#18235,#18236,#18237,#18238,#18239,
#18240,#18241,#18242,#18243,#18244,#18245,#18246,#18247,#18248,#18249,#18250,
#18251,#18252,#18253,#18254,#18255,#18256,#18257,#18258,#18259,#18260,#18261,
#18262,#18263,#18264,#18265,#18266,#18267,#18268,#18269,#18270,#18271,#18272,
#18273,#18274,#18275,#18276,#18277,#18278,#18279,#18280,#18281,#18282,#18283,
#18284,#18285,#18286,#18287,#18288,#18289,#18290,#18291,#18292,#18293,#18294,
#18295,#18296,#18297,#18298,#18299,#18300,#18301,#18302,#18303,#18304,#18305,
#18306,#18307,#18308,#18309,#18310,#18311,#18312,#18313,#18314,#18315,#18316,
#18317,#18318,#18319,#18320,#18321,#18322,#18323,#18324,#18325,#18326,#18327,
#18328,#18329,#18330,#18331,#18332,#18333,#18334,#18335,#18336,#18337,#18338,
#18339,#18340,#18341,#18342,#18343,#18344,#18345,#18346,#18347,#18348,#18349,
#18350,#18351,#18352,#18353,#18354,#18355,#18356,#18357,#18358,#18359,#18360,
#18361,#18362,#18363,#18364,#18365,#18366,#18367,#18368,#18369,#18370,#18371,
#18372,#18373,#18374,#18375,#18376,#18377,#18378,#18379,#18380,#18381,#18382,
#18383,#18384,#18385,#18386,#18387,#18388,#18389,#18390,#18391,#18392,#18393,
#18394,#18395,#18396,#18397,#18398,#18399,#18400,#18401,#18402),
 .UNSPECIFIED.,.F.,.F.,(4,3,3,3,3,3,3,3,3,3,3,3,3,3,3,3,3,3,3,3,3,3,3,3,
3,3,3,3,3,3,3,3,3,3,3,3,3,3,3,3,3,3,3,3,3,3,3,3,3,3,3,3,3,3,3,3,3,3,3,3,
3,3,3,4),(-85.7729790639421,-85.6645206065708,-85.5648043432062,-85.4652305981982,
-85.3656294646422,-85.2662338962237,-85.1668709219025,-85.0675101280473,
-84.9677379784731,-84.8682331283259,-84.7683273290381,-84.6684215297502,
-84.5687052663858,-84.4691315213779,-84.3695303878219,-84.2701348194036,
-84.1707718450827,-84.0714110512278,-83.9716389016532,-83.8721340515064,
-83.772228252218,-83.6723224529296,-83.5726061895651,-83.4730324445573,
-83.3734313110012,-83.2740357425829,-83.1746727682619,-83.0753119744069,
-82.9755398248324,-82.8760349746855,-82.7761291753972,-82.676223376109,
-82.5765071127445,-82.4769333677366,-82.3773322341806,-82.2779366657622,
-82.1785736914413,-82.0792128975862,-81.9794407480118,-81.8799358978648,
-81.7800300985766,-81.6801242992884,-81.580408035924,-81.4808342909161,
-81.3812331573601,-81.2818375889418,-81.1824746146209,-81.0831138207659,
-80.9833416711914,-80.8838368210445,-80.7839310217562,-80.6840252224679,
-80.5843089591034,-80.4847352140955,-80.3851340805394,-80.2857385121211,
-80.1863755378002,-80.0870147439451,-79.9872425943706,-79.8877377442237,
-79.7878319449355,-79.6879261456473,-79.5449893143448,-79.4897937567626),
 .UNSPECIFIED.);
#153=B_SPLINE_CURVE_WITH_KNOTS('',3,(#18404,#18405,#18406,#18407,#18408,
#18409,#18410,#18411,#18412,#18413,#18414,#18415,#18416,#18417,#18418,#18419,
#18420,#18421,#18422,#18423,#18424,#18425,#18426,#18427,#18428,#18429,#18430,
#18431,#18432,#18433,#18434,#18435,#18436,#18437,#18438,#18439,#18440,#18441,
#18442,#18443,#18444,#18445,#18446,#18447,#18448,#18449,#18450,#18451,#18452,
#18453,#18454,#18455,#18456,#18457,#18458,#18459,#18460,#18461,#18462,#18463,
#18464,#18465,#18466,#18467,#18468,#18469,#18470,#18471,#18472,#18473,#18474,
#18475,#18476,#18477,#18478,#18479,#18480,#18481,#18482,#18483,#18484,#18485,
#18486,#18487,#18488,#18489,#18490,#18491,#18492,#18493,#18494,#18495,#18496,
#18497,#18498,#18499,#18500,#18501,#18502,#18503,#18504,#18505,#18506,#18507,
#18508,#18509,#18510,#18511,#18512,#18513,#18514,#18515,#18516,#18517,#18518,
#18519,#18520,#18521,#18522,#18523,#18524,#18525,#18526,#18527,#18528,#18529,
#18530,#18531,#18532,#18533,#18534,#18535,#18536,#18537,#18538,#18539,#18540,
#18541,#18542,#18543,#18544,#18545,#18546,#18547,#18548,#18549,#18550,#18551,
#18552,#18553,#18554,#18555,#18556,#18557,#18558,#18559,#18560,#18561,#18562,
#18563,#18564,#18565,#18566,#18567,#18568,#18569,#18570,#18571,#18572,#18573,
#18574,#18575,#18576,#18577,#18578,#18579,#18580,#18581,#18582,#18583,#18584,
#18585,#18586,#18587,#18588,#18589,#18590,#18591,#18592,#18593),
 .UNSPECIFIED.,.F.,.F.,(4,3,3,3,3,3,3,3,3,3,3,3,3,3,3,3,3,3,3,3,3,3,3,3,
3,3,3,3,3,3,3,3,3,3,3,3,3,3,3,3,3,3,3,3,3,3,3,3,3,3,3,3,3,3,3,3,3,3,3,3,
3,3,3,4),(-79.4897937564256,-79.3900479204758,-79.2920404594018,-79.1940813382461,
-79.0961385205218,-78.995060657598,-78.896995893689,-78.7944114812578,-78.6918270688267,
-78.5921108054622,-78.4925370604542,-78.3929359268982,-78.2935403584798,
-78.194177384159,-78.0948165903039,-77.9950444407295,-77.8955395905825,
-77.7956337912943,-77.6957279920061,-77.5960117286416,-77.4964379836338,
-77.3968368500778,-77.2974412816595,-77.1980783073386,-77.0987175134835,
-76.998945363909,-76.8994405137621,-76.7995347144738,-76.6996289151855,
-76.599912651821,-76.5003389068132,-76.4007377732572,-76.3013422048388,
-76.2019792305179,-76.1026184366628,-76.0028462870883,-75.9033414369415,
-75.8034356376532,-75.7035298383649,-75.6038135750004,-75.5042398299924,
-75.4046386964364,-75.3052431280181,-75.2058801536972,-75.1065193598425,
-75.0067472102679,-74.9072423601209,-74.8073365608326,-74.7074307615443,
-74.6077144981799,-74.5081407531721,-74.408539619616,-74.3091440511978,
-74.209781076877,-74.1104202830217,-74.0106481334472,-73.9111432833001,
-73.8112374840119,-73.7113316847237,-73.6068198485953,-73.5025930608617,
-73.3985356251701,-73.294691960948,-73.206608449583),.UNSPECIFIED.);
#154=B_SPLINE_CURVE_WITH_KNOTS('',3,(#18595,#18596,#18597,#18598,#18599,
#18600,#18601,#18602,#18603,#18604),.UNSPECIFIED.,.F.,.F.,(4,1,1,1,1,1,
1,4),(-73.2066079390623,-72.7152326079031,-71.7191335310825,-70.7230344542619,
-69.7269353774414,-68.7308363006208,-67.7347372238002,-66.9234231424034),
 .UNSPECIFIED.);
#155=B_SPLINE_CURVE_WITH_KNOTS('',3,(#18606,#18607,#18608,#18609,#18610,
#18611,#18612,#18613,#18614,#18615,#18616),.UNSPECIFIED.,.F.,.F.,(4,1,1,
1,1,1,1,1,4),(-66.9234231424034,-66.7386381469796,-65.742539070159,-64.7464399933384,
-63.7503409165178,-62.7542418396972,-61.7581427628766,-60.762043686056,
-60.6402378352238),.UNSPECIFIED.);
#156=B_SPLINE_CURVE_WITH_KNOTS('',3,(#18618,#18619,#18620,#18621,#18622,
#18623,#18624,#18625,#18626,#18627),.UNSPECIFIED.,.F.,.F.,(4,1,1,1,1,1,
1,4),(-60.6402378352238,-59.7659446092355,-58.7698455324149,-57.7737464555943,
-56.7776473787737,-55.7815483019531,-54.7854492251325,-54.3570576872367),
 .UNSPECIFIED.);
#157=B_SPLINE_CURVE_WITH_KNOTS('',3,(#18629,#18630,#18631,#18632,#18633,
#18634,#18635,#18636,#18637,#18638,#18639,#18640,#18641,#18642,#18643,#18644,
#18645,#18646,#18647,#18648,#18649,#18650,#18651,#18652,#18653,#18654,#18655,
#18656,#18657,#18658,#18659,#18660,#18661,#18662,#18663,#18664,#18665,#18666,
#18667,#18668,#18669,#18670,#18671,#18672,#18673,#18674,#18675,#18676,#18677,
#18678,#18679,#18680,#18681,#18682,#18683,#18684,#18685,#18686,#18687,#18688,
#18689,#18690,#18691,#18692,#18693,#18694,#18695,#18696,#18697,#18698,#18699,
#18700,#18701,#18702,#18703,#18704,#18705,#18706,#18707,#18708,#18709,#18710,
#18711,#18712,#18713,#18714,#18715,#18716,#18717,#18718,#18719,#18720,#18721,
#18722,#18723,#18724,#18725,#18726,#18727,#18728,#18729,#18730,#18731,#18732,
#18733,#18734,#18735,#18736,#18737,#18738,#18739,#18740,#18741,#18742,#18743,
#18744,#18745,#18746,#18747,#18748,#18749,#18750,#18751,#18752,#18753,#18754,
#18755,#18756,#18757,#18758,#18759,#18760,#18761,#18762,#18763,#18764,#18765,
#18766,#18767,#18768,#18769,#18770,#18771,#18772,#18773,#18774,#18775,#18776,
#18777,#18778,#18779,#18780,#18781,#18782,#18783,#18784,#18785,#18786,#18787,
#18788,#18789,#18790,#18791,#18792,#18793,#18794,#18795,#18796,#18797,#18798,
#18799,#18800,#18801,#18802,#18803,#18804,#18805,#18806,#18807,#18808,#18809,
#18810,#18811,#18812,#18813,#18814,#18815,#18816,#18817,#18818,#18819,#18820,
#18821),.UNSPECIFIED.,.F.,.F.,(4,3,3,3,3,3,3,3,3,3,3,3,3,3,3,3,3,3,3,3,
3,3,3,3,3,3,3,3,3,3,3,3,3,3,3,3,3,3,3,3,3,3,3,3,3,3,3,3,3,3,3,3,3,3,3,3,
3,3,3,3,3,3,3,3,4),(-54.3570525280442,-54.2555254686791,-54.1539352407624,
-54.0521734865916,-53.9503184179844,-53.8482525309639,-53.7893501483119,
-53.6896338849475,-53.5900601399395,-53.4904590063835,-53.3910634379651,
-53.2917004636443,-53.1923396697892,-53.0925675202148,-52.9930626700678,
-52.8931568707795,-52.7932510714913,-52.6935348081268,-52.5939610631188,
-52.4943599295628,-52.3949643611444,-52.2956013868235,-52.1962405929686,
-52.0964684433942,-51.9969635932472,-51.8970577939589,-51.7971519946707,
-51.6974357313063,-51.5978619862985,-51.4982608527425,-51.3988652843241,
-51.2995023100033,-51.2001415161481,-51.1003693665736,-51.0008645164266,
-50.9009587171384,-50.8010529178501,-50.7013366544856,-50.6017629094778,
-50.5021617759218,-50.4027662075034,-50.3034032331824,-50.2040424393273,
-50.1042702897528,-50.0047654396059,-49.9048596403177,-49.8049538410295,
-49.705237577665,-49.6056638326575,-49.5060626991014,-49.4066671306832,
-49.3073041563622,-49.2079433625071,-49.1081712129326,-49.0086663627857,
-48.9087605634973,-48.8088547642089,-48.710200786307,-48.611676552411,-48.5132501834196,
-48.4148899193455,-48.3165387900736,-48.2181936851774,-48.1197811579957,
-48.0738672208646),.UNSPECIFIED.);
#158=B_SPLINE_CURVE_WITH_KNOTS('',3,(#18823,#18824,#18825,#18826,#18827,
#18828,#18829,#18830,#18831,#18832,#18833,#18834,#18835,#18836,#18837,#18838,
#18839,#18840,#18841,#18842,#18843,#18844,#18845,#18846,#18847,#18848,#18849,
#18850,#18851,#18852,#18853,#18854,#18855,#18856,#18857,#18858,#18859,#18860,
#18861,#18862,#18863,#18864,#18865,#18866,#18867,#18868,#18869,#18870,#18871,
#18872,#18873,#18874,#18875,#18876,#18877,#18878,#18879,#18880,#18881,#18882,
#18883,#18884,#18885,#18886,#18887,#18888,#18889,#18890,#18891,#18892,#18893,
#18894,#18895,#18896,#18897,#18898,#18899,#18900,#18901,#18902,#18903,#18904,
#18905,#18906,#18907,#18908,#18909,#18910,#18911,#18912,#18913,#18914,#18915,
#18916,#18917,#18918,#18919,#18920,#18921,#18922,#18923,#18924,#18925,#18926,
#18927,#18928,#18929,#18930,#18931,#18932,#18933,#18934,#18935,#18936,#18937,
#18938,#18939,#18940,#18941,#18942,#18943,#18944,#18945,#18946,#18947,#18948,
#18949,#18950,#18951,#18952,#18953,#18954,#18955,#18956,#18957,#18958,#18959,
#18960,#18961,#18962,#18963,#18964,#18965,#18966,#18967,#18968,#18969,#18970,
#18971,#18972,#18973,#18974,#18975,#18976,#18977,#18978,#18979,#18980,#18981,
#18982,#18983,#18984,#18985,#18986,#18987,#18988,#18989,#18990,#18991,#18992,
#18993,#18994,#18995,#18996,#18997,#18998,#18999,#19000,#19001,#19002,#19003,
#19004,#19005,#19006,#19007,#19008,#19009,#19010,#19011,#19012),
 .UNSPECIFIED.,.F.,.F.,(4,3,3,3,3,3,3,3,3,3,3,3,3,3,3,3,3,3,3,3,3,3,3,3,
3,3,3,3,3,3,3,3,3,3,3,3,3,3,3,3,3,3,3,3,3,3,3,3,3,3,3,3,3,3,3,3,3,3,3,3,
3,3,3,4),(-48.0738672205341,-47.9433114539612,-47.8127556873884,-47.7130394240239,
-47.613465679016,-47.51386454546,-47.4144689770416,-47.3151060027206,-47.2157452088656,
-47.1159730592911,-47.0164682091442,-46.916562409856,-46.8166566105678,
-46.7169403472033,-46.6173666021954,-46.5177654686394,-46.418369900221,
-46.3190069259001,-46.2196461320451,-46.1198739824706,-46.0203691323237,
-45.9204633330354,-45.8205575337472,-45.7208412703827,-45.6212675253749,
-45.5216663918188,-45.4222708234005,-45.3229078490796,-45.2235470552246,
-45.1237749056501,-45.0242700555032,-44.9243642562149,-44.8244584569266,
-44.7247421935621,-44.6251684485543,-44.5255673149982,-44.4261717465799,
-44.326808772259,-44.2274479784039,-44.1276758288294,-44.0281709786825,
-43.9282651793943,-43.828359380106,-43.7286431167415,-43.6290693717336,
-43.5294682381776,-43.4300726697592,-43.3307096954383,-43.2313489015833,
-43.1315767520088,-43.0320719018619,-42.9321661025737,-42.8322603032854,
-42.7325440399209,-42.6329702949131,-42.533369161357,-42.4339735929387,
-42.3346106186178,-42.2352498247627,-42.1354776751882,-42.0359728250413,
-41.936067025753,-41.8361612264648,-41.790681913685),.UNSPECIFIED.);
#159=B_SPLINE_CURVE_WITH_KNOTS('',3,(#19014,#19015,#19016,#19017,#19018,
#19019,#19020,#19021,#19022,#19023,#19024,#19025,#19026,#19027,#19028,#19029,
#19030,#19031,#19032,#19033,#19034,#19035,#19036,#19037,#19038,#19039,#19040,
#19041,#19042,#19043,#19044,#19045,#19046,#19047,#19048,#19049,#19050,#19051,
#19052,#19053,#19054,#19055,#19056,#19057,#19058,#19059,#19060,#19061,#19062,
#19063,#19064,#19065,#19066,#19067,#19068,#19069,#19070,#19071,#19072,#19073,
#19074,#19075,#19076,#19077,#19078,#19079,#19080,#19081,#19082,#19083,#19084,
#19085,#19086,#19087,#19088,#19089,#19090,#19091,#19092,#19093,#19094,#19095,
#19096,#19097,#19098,#19099,#19100,#19101,#19102,#19103,#19104,#19105,#19106,
#19107,#19108,#19109,#19110,#19111,#19112,#19113,#19114,#19115,#19116,#19117,
#19118,#19119,#19120,#19121,#19122,#19123,#19124,#19125,#19126,#19127,#19128,
#19129,#19130,#19131,#19132,#19133,#19134,#19135,#19136,#19137,#19138,#19139,
#19140,#19141,#19142,#19143,#19144,#19145,#19146,#19147,#19148,#19149,#19150,
#19151,#19152,#19153,#19154,#19155,#19156,#19157,#19158,#19159,#19160,#19161,
#19162,#19163,#19164,#19165,#19166,#19167,#19168,#19169,#19170,#19171,#19172,
#19173,#19174,#19175,#19176,#19177,#19178,#19179,#19180,#19181,#19182,#19183,
#19184,#19185,#19186,#19187,#19188,#19189,#19190,#19191,#19192,#19193,#19194,
#19195,#19196,#19197,#19198,#19199,#19200,#19201,#19202,#19203),
 .UNSPECIFIED.,.F.,.F.,(4,3,3,3,3,3,3,3,3,3,3,3,3,3,3,3,3,3,3,3,3,3,3,3,
3,3,3,3,3,3,3,3,3,3,3,3,3,3,3,3,3,3,3,3,3,3,3,3,3,3,3,3,3,3,3,3,3,3,3,3,
3,3,3,4),(-41.790681913389,-41.6916826933112,-41.5928221693564,-41.4940698633804,
-41.3953753929266,-41.2967074313893,-41.198034687483,-41.0992617316987,
-41.0004347653562,-40.9014406130349,-40.8400621496442,-40.7403458862797,
-40.640772141272,-40.5411710077159,-40.4417754392976,-40.3424124649767,
-40.2430516711217,-40.1432795215472,-40.0437746714003,-39.9438688721119,
-39.8439630728236,-39.7442468094591,-39.6446730644513,-39.5450719308952,
-39.4456763624769,-39.346313388156,-39.246952594301,-39.1471804447265,-39.0476755945796,
-38.9477697952913,-38.847863996003,-38.7481477326385,-38.648573987631,-38.5489728540749,
-38.4495772856566,-38.3502143113355,-38.2508535174804,-38.1510813679059,
-38.051576517759,-37.9516707184707,-37.8517649191824,-37.752048655818,-37.6524749108102,
-37.5528737772542,-37.4534782088358,-37.3541152345149,-37.2547544406597,
-37.1549822910853,-37.0554774409384,-36.9555716416501,-36.8556658423619,
-36.7559495789976,-36.6563758339897,-36.5567747004336,-36.4573791320155,
-36.3580161576947,-36.2586553638398,-36.1588832142652,-36.0593783641184,
-35.9594725648298,-35.8595667655413,-35.7447123618031,-35.6261046035863,
-35.5074968453696),.UNSPECIFIED.);
#160=B_SPLINE_CURVE_WITH_KNOTS('',3,(#19205,#19206,#19207,#19208,#19209,
#19210,#19211,#19212,#19213,#19214),.UNSPECIFIED.,.F.,.F.,(4,1,1,1,1,1,
1,4),(-35.5074966065054,-34.8634676887207,-33.8673686119001,-32.8712695350795,
-31.8751704582589,-30.8790713814383,-29.8829723046177,-29.2243112993258),
 .UNSPECIFIED.);
#161=B_SPLINE_CURVE_WITH_KNOTS('',3,(#19216,#19217,#19218,#19219,#19220,
#19221,#19222,#19223,#19224,#19225),.UNSPECIFIED.,.F.,.F.,(4,1,1,1,1,1,
1,4),(-29.2243112993258,-28.8868732277971,-27.8907741509765,-26.894675074156,
-25.8985759973354,-24.9024769205148,-23.9063778436942,-22.9411259921462),
 .UNSPECIFIED.);
#162=B_SPLINE_CURVE_WITH_KNOTS('',3,(#19227,#19228,#19229,#19230,#19231,
#19232,#19233,#19234,#19235,#19236,#19237),.UNSPECIFIED.,.F.,.F.,(4,1,1,
1,1,1,1,1,4),(-22.9411259921462,-22.9102787668736,-21.914179690053,-20.9180806132324,
-19.9219815364118,-18.9258824595912,-17.9297833827706,-16.93368430595,-16.6579446169396),
 .UNSPECIFIED.);
#163=B_SPLINE_CURVE_WITH_KNOTS('',3,(#19239,#19240,#19241,#19242,#19243,
#19244,#19245,#19246,#19247,#19248,#19249,#19250,#19251,#19252,#19253,#19254,
#19255,#19256,#19257,#19258,#19259,#19260,#19261,#19262,#19263,#19264,#19265,
#19266,#19267,#19268,#19269,#19270,#19271,#19272,#19273,#19274,#19275,#19276,
#19277,#19278,#19279,#19280,#19281,#19282,#19283,#19284,#19285,#19286,#19287,
#19288,#19289,#19290,#19291,#19292,#19293,#19294,#19295,#19296,#19297,#19298,
#19299,#19300,#19301,#19302,#19303,#19304,#19305,#19306,#19307,#19308,#19309,
#19310,#19311,#19312,#19313,#19314,#19315,#19316,#19317,#19318,#19319,#19320,
#19321,#19322,#19323,#19324,#19325,#19326,#19327,#19328,#19329,#19330,#19331,
#19332,#19333,#19334,#19335,#19336,#19337,#19338,#19339,#19340,#19341,#19342,
#19343,#19344,#19345,#19346,#19347,#19348,#19349,#19350,#19351,#19352,#19353,
#19354,#19355,#19356,#19357,#19358,#19359,#19360,#19361,#19362,#19363,#19364,
#19365,#19366,#19367,#19368,#19369,#19370,#19371,#19372,#19373,#19374,#19375,
#19376,#19377,#19378,#19379,#19380,#19381,#19382,#19383,#19384,#19385,#19386,
#19387,#19388,#19389,#19390,#19391,#19392,#19393,#19394,#19395,#19396,#19397,
#19398,#19399,#19400,#19401,#19402,#19403,#19404,#19405,#19406,#19407,#19408,
#19409,#19410,#19411,#19412,#19413,#19414,#19415,#19416,#19417,#19418,#19419,
#19420,#19421,#19422,#19423,#19424,#19425,#19426,#19427,#19428,#19429,#19430,
#19431),.UNSPECIFIED.,.F.,.F.,(4,3,3,3,3,3,3,3,3,3,3,3,3,3,3,3,3,3,3,3,
3,3,3,3,3,3,3,3,3,3,3,3,3,3,3,3,3,3,3,3,3,3,3,3,3,3,3,3,3,3,3,3,3,3,3,3,
3,3,3,3,3,3,3,3,4),(-16.6579406849666,-16.5593897775357,-16.4608866619369,
-16.3623998545879,-16.2638978971885,-16.1652885217759,-16.0666155585702,
-15.9677829300662,-15.9375852291295,-15.8378689481712,-15.7382951860584,
-15.6386940568397,-15.5392984726109,-15.4399354829983,-15.3405746743875,
-15.2408025438679,-15.1412976804118,-15.0413919163603,-14.9414861523089,
-14.8417697149956,-14.7421957951011,-14.6425947051495,-14.5431989608577,
-14.4438358106844,-14.3444748412367,-14.2447028997996,-14.1451978764835,
-14.0452924759859,-13.9453870754883,-13.8456712362277,-13.7460979154923,
-13.6464966758892,-13.5471015290883,-13.4477389744586,-13.3483785978117,
-13.2486059480257,-13.1491015048194,-13.0491947517435,-12.9492879986677,
-12.8495714882222,-12.7499974991886,-12.650396427021,-12.5510006236563,
-12.4516374183018,-12.3522763976134,-12.2525045286719,-12.1529994641636,
-12.0530941930054,-11.9531889218471,-11.8534716310433,-11.7538968516564,
-11.6542959758276,-11.5548993638604,-11.4555353448774,-11.356173506674,
-11.2564025912621,-11.1568967082028,-11.0569932766146,-10.9570898450265,
-10.8554746586855,-10.754021022291,-10.6527315891179,-10.5515388523147,
-10.4504201898901,-10.3747553777871),.UNSPECIFIED.);
#164=B_SPLINE_CURVE_WITH_KNOTS('',3,(#19432,#19433,#19434,#19435,#19436,
#19437,#19438,#19439,#19440,#19441,#19442,#19443,#19444,#19445,#19446,#19447,
#19448,#19449,#19450,#19451,#19452,#19453,#19454,#19455,#19456,#19457,#19458,
#19459,#19460,#19461,#19462,#19463,#19464,#19465,#19466,#19467,#19468,#19469,
#19470,#19471,#19472,#19473,#19474,#19475,#19476,#19477,#19478,#19479,#19480,
#19481,#19482,#19483,#19484,#19485,#19486,#19487,#19488,#19489,#19490,#19491,
#19492,#19493,#19494,#19495,#19496,#19497,#19498,#19499,#19500,#19501,#19502,
#19503,#19504,#19505,#19506,#19507,#19508,#19509,#19510,#19511,#19512,#19513,
#19514,#19515,#19516,#19517,#19518,#19519,#19520,#19521,#19522,#19523,#19524,
#19525,#19526,#19527,#19528,#19529,#19530,#19531,#19532,#19533,#19534,#19535,
#19536,#19537,#19538,#19539,#19540,#19541,#19542,#19543,#19544,#19545,#19546,
#19547,#19548,#19549,#19550,#19551,#19552,#19553,#19554,#19555,#19556,#19557,
#19558,#19559,#19560,#19561,#19562,#19563,#19564,#19565,#19566,#19567,#19568,
#19569,#19570,#19571,#19572,#19573,#19574,#19575,#19576,#19577,#19578,#19579,
#19580,#19581,#19582,#19583,#19584,#19585,#19586,#19587,#19588,#19589,#19590,
#19591,#19592,#19593,#19594,#19595,#19596,#19597,#19598,#19599,#19600,#19601,
#19602,#19603,#19604,#19605,#19606,#19607,#19608,#19609,#19610,#19611,#19612,
#19613,#19614,#19615,#19616,#19617,#19618,#19619,#19620,#19621),
 .UNSPECIFIED.,.F.,.F.,(4,3,3,3,3,3,3,3,3,3,3,3,3,3,3,3,3,3,3,3,3,3,3,3,
3,3,3,3,3,3,3,3,3,3,3,3,3,3,3,3,3,3,3,3,3,3,3,3,3,3,3,3,3,3,3,3,3,3,3,3,
3,3,3,4),(-10.3747553774094,-10.2659752484022,-10.1568700723105,-10.0472752494143,
-9.96099076820591,-9.86127196929943,-9.7616957071339,-9.66209520516533,
-9.56269718179088,-9.46333178119533,-9.36396859284967,-9.26419936748358,
-9.16469222415936,-9.06479195777234,-8.96489169138532,-8.86516970189676,
-8.76559018074002,-8.66599048496811,-8.56658906221728,-8.46722021733717,
-8.36785354478904,-8.26808831223296,-8.16857762385655,-8.06868511921064,
-7.96879261456473,-7.8690973998874,-7.76954474017978,-7.66993833987533,
-7.5705637928849,-7.47122176970325,-7.37188182881078,-7.27208475604412,
-7.17260030861201,-7.07264692317808,-6.97269353774414,-6.87295442623608,
-6.77335793838362,-6.67376250370111,-6.57434460910662,-6.47495951394585,
-6.37557683335036,-6.27583124024365,-6.17630529319603,-6.07644987705978,
-5.97659446092354,-5.87684901969211,-5.77724574417183,-5.67765194916322,
-5.57822621924204,-5.47883291479406,-5.37944166475022,-5.2797050945884,
-5.18016979573384,-5.0803325899184,-4.98049538410295,-4.88220005204375,
-4.78337130436421,-4.68533065927096,-4.58734916614617,-4.48939479490125,
-4.38993861382781,-4.29189157221189,-4.19173082140968,-4.09157007060747),
 .UNSPECIFIED.);
#165=B_SPLINE_CURVE_WITH_KNOTS('',3,(#19624,#19625,#19626,#19627,#19628,
#19629,#19630,#19631,#19632,#19633,#19634,#19635,#19636,#19637,#19638,#19639,
#19640,#19641,#19642,#19643,#19644,#19645,#19646,#19647,#19648,#19649,#19650,
#19651,#19652,#19653,#19654,#19655,#19656,#19657,#19658,#19659,#19660,#19661,
#19662,#19663,#19664,#19665,#19666,#19667,#19668,#19669,#19670,#19671,#19672,
#19673,#19674,#19675,#19676,#19677,#19678,#19679,#19680,#19681,#19682,#19683,
#19684,#19685,#19686,#19687,#19688,#19689,#19690,#19691,#19692,#19693,#19694,
#19695,#19696,#19697,#19698,#19699,#19700,#19701,#19702,#19703,#19704,#19705,
#19706,#19707,#19708,#19709,#19710,#19711,#19712,#19713,#19714,#19715,#19716,
#19717,#19718,#19719,#19720,#19721,#19722,#19723,#19724,#19725,#19726,#19727,
#19728,#19729,#19730,#19731,#19732,#19733,#19734,#19735,#19736,#19737,#19738,
#19739,#19740,#19741,#19742,#19743,#19744,#19745,#19746,#19747,#19748,#19749,
#19750,#19751,#19752,#19753,#19754,#19755,#19756,#19757,#19758,#19759,#19760,
#19761,#19762,#19763,#19764,#19765,#19766,#19767,#19768,#19769,#19770,#19771,
#19772,#19773,#19774,#19775,#19776,#19777,#19778,#19779,#19780,#19781,#19782,
#19783,#19784,#19785,#19786,#19787,#19788,#19789,#19790,#19791,#19792,#19793,
#19794,#19795,#19796,#19797,#19798,#19799,#19800,#19801,#19802,#19803,#19804,
#19805,#19806,#19807,#19808,#19809,#19810,#19811,#19812,#19813,#19814,#19815,
#19816,#19817,#19818,#19819,#19820,#19821,#19822,#19823),.UNSPECIFIED.,
 .F.,.F.,(4,2,2,2,2,2,2,2,2,2,2,2,2,2,2,2,2,2,2,2,2,2,2,2,2,2,2,2,2,2,2,
2,2,2,2,2,2,2,2,2,2,2,2,2,2,2,2,2,2,2,2,2,2,2,2,2,2,2,2,2,2,2,2,2,2,2,2,
2,2,2,2,2,2,2,2,2,2,2,2,2,2,2,2,2,2,2,2,2,2,2,2,2,2,2,2,2,2,2,2,4),(0.00326162500843006,
0.0197447762864837,0.0748215617595025,0.082167278784108,0.0854722927311191,
0.0879597576891903,0.0906299556293424,0.0948557198684813,0.107639883892953,
0.151800459018261,0.178902896427261,0.182192364140908,0.18387015633938,
0.183879116759064,0.183888299241087,0.183897711707281,0.183907362460959,
0.183917260204829,0.183927414073413,0.183937833665262,0.183948529061159,
0.183959510853069,0.18397079019248,0.18398237881444,0.183994289087449,0.184006534032961,
0.184019127396874,0.184032083688368,0.185383199046984,0.187067363254308,
0.190340194813029,0.218062962634009,0.257340175901016,0.275744767436072,
0.280315400158962,0.2830400089683,0.285473338279774,0.288559280984999,0.293454778705634,
0.332862991654633,0.361103634370691,0.373011519743452,0.380126153845839,
0.382391447113787,0.383841767871193,0.385218283606201,0.387225981320361,
0.392102170469598,0.421882741364194,0.457578467176283,0.475570096991801,
0.480073813086898,0.482762335967425,0.485165431345914,0.488215332912887,
0.493057333654311,0.53194547082417,0.559769077621238,0.57825267981081,0.581253242296325,
0.582855641916501,0.584203409276343,0.585898403562848,0.58856480988963,
0.602607510633657,0.608628735611976,0.652983968945658,0.674690687177921,
0.679476468698024,0.682243905683431,0.684664267023071,0.687666412674625,
0.692299156560563,0.71695516502572,0.757831396980101,0.777100723342141,
0.780154965497359,0.781781398879197,0.78313716291058,0.784832370830203,
0.788127593165175,0.817294661810435,0.855680716458636,0.873892619328436,
0.878435414468737,0.881145769002038,0.883567689344995,0.886640832883721,
0.891519267651087,0.930057646863374,0.957446404750408,0.976344496235866,
0.979376527435769,0.980993504510696,0.982344337096749,0.984036172650702,
0.987326764415839,1.01665603120223,1.05497305173704,1.06702749696459),
 .UNSPECIFIED.);
#166=B_SPLINE_CURVE_WITH_KNOTS('',3,(#19826,#19827,#19828,#19829,#19830,
#19831,#19832,#19833,#19834,#19835,#19836,#19837,#19838,#19839,#19840,#19841,
#19842,#19843,#19844,#19845,#19846,#19847,#19848,#19849,#19850,#19851,#19852,
#19853,#19854,#19855,#19856,#19857,#19858,#19859,#19860,#19861,#19862,#19863,
#19864,#19865,#19866,#19867,#19868,#19869,#19870,#19871,#19872,#19873,#19874,
#19875,#19876,#19877,#19878,#19879,#19880,#19881,#19882,#19883,#19884,#19885,
#19886,#19887,#19888,#19889,#19890,#19891,#19892,#19893,#19894,#19895,#19896,
#19897,#19898,#19899,#19900,#19901,#19902,#19903,#19904,#19905,#19906,#19907,
#19908,#19909,#19910,#19911,#19912,#19913,#19914,#19915,#19916,#19917,#19918,
#19919,#19920,#19921,#19922,#19923,#19924,#19925,#19926,#19927,#19928,#19929,
#19930,#19931,#19932,#19933,#19934,#19935,#19936,#19937,#19938,#19939,#19940,
#19941,#19942,#19943,#19944,#19945,#19946,#19947,#19948,#19949),
 .UNSPECIFIED.,.F.,.F.,(4,3,3,3,3,3,3,3,3,3,3,3,3,3,3,3,3,3,3,3,3,3,3,3,
3,3,3,3,3,3,3,3,3,3,3,3,3,3,3,3,3,4),(147.65485471872,147.762028482045,
147.86721043816,147.972234768624,148.077134483648,148.181967416618,148.286768802862,
148.391573832499,148.496485101084,148.601455688331,148.706601951883,148.758127558866,
148.863259229857,148.968236566764,149.073094308716,149.177888396139,149.282654092532,
149.387426619453,149.492310360179,149.597256212211,149.702382262756,149.754226635687,
149.858063290691,149.961742205202,150.065302377591,150.168799882304,150.272271688643,
150.375754725542,150.47936423613,150.583042333312,150.686924471371,150.750325712507,
150.858239782028,150.96926290794,151.076819947692,151.184275590721,151.291658671096,
151.398997929083,151.506351328449,151.613712019336,151.721144432213,151.746424789328),
 .UNSPECIFIED.);
#167=B_SPLINE_CURVE_WITH_KNOTS('',3,(#20538,#20539,#20540,#20541,#20542,
#20543,#20544,#20545,#20546,#20547,#20548,#20549,#20550,#20551,#20552,#20553,
#20554,#20555,#20556,#20557,#20558,#20559,#20560,#20561,#20562,#20563,#20564,
#20565,#20566,#20567,#20568,#20569,#20570,#20571,#20572,#20573,#20574,#20575,
#20576,#20577,#20578,#20579,#20580,#20581,#20582,#20583,#20584,#20585,#20586,
#20587,#20588,#20589,#20590,#20591,#20592,#20593,#20594,#20595,#20596,#20597,
#20598,#20599,#20600,#20601,#20602,#20603,#20604,#20605,#20606,#20607,#20608,
#20609,#20610,#20611,#20612,#20613,#20614,#20615,#20616,#20617,#20618,#20619,
#20620,#20621,#20622,#20623,#20624,#20625),.UNSPECIFIED.,.F.,.F.,(4,3,3,
3,3,3,3,3,3,3,3,3,3,3,3,3,3,3,3,3,3,3,3,3,3,3,3,3,3,4),(0.,0.0182760710704149,
0.0437675064709697,0.0695752992456494,0.0922813564527724,0.0963438741865412,
0.121479543983109,0.146526999164012,0.170952555575599,0.182419474302491,
0.186963208615901,0.211099004300551,0.234533760957442,0.251900460808682,
0.26514437268587,0.271415138183839,0.275123593425889,0.298667119795758,
0.322419773257956,0.345934625047122,0.351073300043322,0.35531942417871,
0.359377579094087,0.382316439597603,0.402792093527263,0.408417580703764,
0.413280341911519,0.435488471747807,0.457053381724928,0.463803050843696),
 .UNSPECIFIED.);
#168=B_SPLINE_CURVE_WITH_KNOTS('',3,(#20627,#20628,#20629,#20630,#20631,
#20632,#20633,#20634,#20635,#20636,#20637,#20638,#20639,#20640,#20641,#20642,
#20643,#20644,#20645,#20646,#20647,#20648,#20649,#20650,#20651,#20652,#20653,
#20654,#20655,#20656,#20657,#20658,#20659,#20660,#20661,#20662,#20663,#20664,
#20665,#20666,#20667,#20668,#20669,#20670,#20671,#20672,#20673,#20674,#20675,
#20676,#20677,#20678,#20679,#20680,#20681,#20682,#20683,#20684,#20685,#20686,
#20687,#20688,#20689,#20690,#20691,#20692,#20693,#20694,#20695,#20696,#20697,
#20698,#20699,#20700,#20701,#20702,#20703,#20704,#20705,#20706,#20707,#20708,
#20709,#20710,#20711),.UNSPECIFIED.,.F.,.F.,(4,3,3,3,3,3,3,3,3,3,3,3,3,
3,3,3,3,3,3,3,3,3,3,3,3,3,3,3,4),(-0.463803050843718,-0.448740022185204,
-0.42691444385268,-0.414669408555542,-0.410232646093364,-0.387935224132788,
-0.365010556573471,-0.359638840893696,-0.355551191051294,-0.351346727838988,
-0.327878176942996,-0.304134002765552,-0.280552762497995,-0.273242198114603,
-0.268716587605523,-0.244288506390758,-0.235180056184415,-0.211343912259743,
-0.187507768335072,-0.183690135280684,-0.15932822702224,-0.134515626743572,
-0.109408117315328,-0.0938532048355855,-0.0899591209447907,-0.0642123177659208,
-0.0384373539397261,-0.0132154939304623,-1.37208636376373E-15),
 .UNSPECIFIED.);
#169=B_SPLINE_CURVE_WITH_KNOTS('',3,(#20712,#20713,#20714,#20715),
 .UNSPECIFIED.,.F.,.F.,(4,4),(-0.0135998802120258,0.),.UNSPECIFIED.);
#170=B_SPLINE_CURVE_WITH_KNOTS('',3,(#21305,#21306,#21307,#21308,#21309,
#21310,#21311,#21312,#21313,#21314,#21315,#21316,#21317,#21318,#21319,#21320,
#21321,#21322,#21323,#21324,#21325,#21326,#21327,#21328,#21329,#21330,#21331,
#21332,#21333,#21334,#21335,#21336,#21337,#21338,#21339,#21340,#21341,#21342,
#21343,#21344,#21345,#21346,#21347,#21348,#21349,#21350,#21351,#21352,#21353,
#21354,#21355,#21356,#21357,#21358,#21359,#21360,#21361,#21362,#21363,#21364,
#21365,#21366,#21367,#21368,#21369,#21370,#21371,#21372,#21373,#21374,#21375,
#21376,#21377,#21378,#21379,#21380,#21381,#21382,#21383,#21384,#21385,#21386,
#21387,#21388,#21389,#21390,#21391,#21392,#21393,#21394,#21395),
 .UNSPECIFIED.,.F.,.F.,(4,3,3,3,3,3,3,3,3,3,3,3,3,3,3,3,3,3,3,3,3,3,3,3,
3,3,3,3,3,3,4),(0.,0.0150138269319462,0.036520890660569,0.0587157842271369,
0.0697076727300594,0.0762008005980358,0.0816663983792169,0.104427855536438,
0.127790613405416,0.151113577304524,0.159780223723126,0.163861468767013,
0.187890149415679,0.211826173958714,0.227871101166216,0.242490967649561,
0.246618252277857,0.250650056860218,0.27416492806894,0.29836373674207,0.323030301871278,
0.329929523699832,0.335709402506641,0.339916278287732,0.365088975678724,
0.390432981304092,0.397923686724778,0.402696895452255,0.428440535010322,
0.453950365417961,0.461788964899747),.UNSPECIFIED.);
#171=B_SPLINE_CURVE_WITH_KNOTS('',3,(#21396,#21397,#21398,#21399),
 .UNSPECIFIED.,.F.,.F.,(4,4),(0.,0.0135996993161776),.UNSPECIFIED.);
#172=B_SPLINE_CURVE_WITH_KNOTS('',3,(#21400,#21401,#21402,#21403,#21404,
#21405,#21406,#21407,#21408,#21409,#21410,#21411,#21412,#21413,#21414,#21415,
#21416,#21417,#21418,#21419,#21420,#21421,#21422,#21423,#21424,#21425,#21426,
#21427,#21428,#21429,#21430,#21431,#21432,#21433,#21434,#21435,#21436,#21437,
#21438,#21439,#21440,#21441,#21442,#21443,#21444,#21445,#21446,#21447,#21448,
#21449,#21450,#21451,#21452,#21453,#21454,#21455,#21456,#21457,#21458,#21459,
#21460,#21461,#21462,#21463,#21464,#21465,#21466,#21467,#21468,#21469,#21470,
#21471,#21472,#21473,#21474,#21475,#21476,#21477,#21478,#21479,#21480,#21481,
#21482,#21483,#21484,#21485,#21486,#21487,#21488,#21489,#21490),
 .UNSPECIFIED.,.F.,.F.,(4,3,3,3,3,3,3,3,3,3,3,3,3,3,3,3,3,3,3,3,3,3,3,3,
3,3,3,3,3,3,4),(-0.461788964899773,-0.443595824964341,-0.417881602474246,
-0.405040573218592,-0.399033269720178,-0.394779666370722,-0.369467283426724,
-0.344172275666879,-0.340434254998593,-0.335819056172879,-0.331683328772696,
-0.306946125658135,-0.282481738829071,-0.258728029909401,-0.251428002001961,
-0.247028273677602,-0.243317649896853,-0.219840949155418,-0.211223388199231,
-0.187163181376808,-0.163852594642498,-0.158770548393032,-0.135417929772648,
-0.112049986589736,-0.0891501996726069,-0.0803321462983234,-0.076617754044123,
-0.0541541414655251,-0.0320539914425208,-0.0106610814724787,0.),
 .UNSPECIFIED.);
#233=SHAPE_REPRESENTATION_RELATIONSHIP('SRR','None',#23616,#242);
#242=ADVANCED_BREP_SHAPE_REPRESENTATION('',(#260),#23572);
#251=STYLED_ITEM('',(#23667),#260);
#260=MANIFOLD_SOLID_BREP('Body1',#4161);
#283=FACE_BOUND('',#755,.T.);
#350=PLANE('',#4465);
#351=PLANE('',#4466);
#352=PLANE('',#4472);
#483=FACE_OUTER_BOUND('',#727,.T.);
#484=FACE_OUTER_BOUND('',#728,.T.);
#485=FACE_OUTER_BOUND('',#729,.T.);
#486=FACE_OUTER_BOUND('',#730,.T.);
#487=FACE_OUTER_BOUND('',#731,.T.);
#488=FACE_OUTER_BOUND('',#732,.T.);
#489=FACE_OUTER_BOUND('',#733,.T.);
#490=FACE_OUTER_BOUND('',#734,.T.);
#491=FACE_OUTER_BOUND('',#735,.T.);
#492=FACE_OUTER_BOUND('',#736,.T.);
#493=FACE_OUTER_BOUND('',#737,.T.);
#494=FACE_OUTER_BOUND('',#738,.T.);
#495=FACE_OUTER_BOUND('',#739,.T.);
#496=FACE_OUTER_BOUND('',#740,.T.);
#497=FACE_OUTER_BOUND('',#741,.T.);
#498=FACE_OUTER_BOUND('',#742,.T.);
#499=FACE_OUTER_BOUND('',#743,.T.);
#500=FACE_OUTER_BOUND('',#744,.T.);
#501=FACE_OUTER_BOUND('',#745,.T.);
#502=FACE_OUTER_BOUND('',#746,.T.);
#503=FACE_OUTER_BOUND('',#747,.T.);
#504=FACE_OUTER_BOUND('',#748,.T.);
#505=FACE_OUTER_BOUND('',#749,.T.);
#506=FACE_OUTER_BOUND('',#750,.T.);
#507=FACE_OUTER_BOUND('',#751,.T.);
#508=FACE_OUTER_BOUND('',#752,.T.);
#509=FACE_OUTER_BOUND('',#753,.T.);
#510=FACE_OUTER_BOUND('',#754,.T.);
#511=FACE_OUTER_BOUND('',#756,.T.);
#512=FACE_OUTER_BOUND('',#757,.T.);
#513=FACE_OUTER_BOUND('',#758,.T.);
#727=EDGE_LOOP('',(#3079,#3080,#3081,#3082));
#728=EDGE_LOOP('',(#3083,#3084,#3085,#3086));
#729=EDGE_LOOP('',(#3087,#3088,#3089,#3090));
#730=EDGE_LOOP('',(#3091,#3092,#3093,#3094));
#731=EDGE_LOOP('',(#3095,#3096,#3097,#3098));
#732=EDGE_LOOP('',(#3099,#3100,#3101,#3102));
#733=EDGE_LOOP('',(#3103,#3104,#3105,#3106));
#734=EDGE_LOOP('',(#3107,#3108,#3109,#3110));
#735=EDGE_LOOP('',(#3111,#3112,#3113,#3114));
#736=EDGE_LOOP('',(#3115,#3116,#3117,#3118));
#737=EDGE_LOOP('',(#3119,#3120,#3121,#3122,#3123));
#738=EDGE_LOOP('',(#3124,#3125,#3126,#3127));
#739=EDGE_LOOP('',(#3128,#3129,#3130,#3131,#3132));
#740=EDGE_LOOP('',(#3133,#3134,#3135,#3136));
#741=EDGE_LOOP('',(#3137,#3138,#3139,#3140));
#742=EDGE_LOOP('',(#3141,#3142,#3143,#3144));
#743=EDGE_LOOP('',(#3145,#3146,#3147,#3148));
#744=EDGE_LOOP('',(#3149,#3150,#3151,#3152));
#745=EDGE_LOOP('',(#3153,#3154,#3155,#3156));
#746=EDGE_LOOP('',(#3157,#3158,#3159,#3160));
#747=EDGE_LOOP('',(#3161,#3162,#3163,#3164));
#748=EDGE_LOOP('',(#3165,#3166,#3167,#3168));
#749=EDGE_LOOP('',(#3169,#3170,#3171,#3172,#3173,#3174,#3175,#3176,#3177,
#3178,#3179,#3180,#3181,#3182,#3183,#3184,#3185,#3186,#3187,#3188,#3189,
#3190,#3191,#3192,#3193,#3194,#3195,#3196,#3197,#3198,#3199,#3200,#3201,
#3202,#3203,#3204,#3205,#3206,#3207,#3208,#3209,#3210,#3211,#3212,#3213,
#3214,#3215,#3216,#3217,#3218));
#750=EDGE_LOOP('',(#3219,#3220,#3221,#3222));
#751=EDGE_LOOP('',(#3223,#3224,#3225,#3226,#3227,#3228,#3229,#3230,#3231,
#3232,#3233,#3234,#3235,#3236,#3237,#3238,#3239,#3240,#3241,#3242,#3243,
#3244,#3245,#3246,#3247,#3248,#3249,#3250,#3251,#3252,#3253,#3254,#3255,
#3256,#3257,#3258,#3259,#3260,#3261,#3262,#3263,#3264,#3265,#3266,#3267,
#3268,#3269,#3270,#3271,#3272,#3273));
#752=EDGE_LOOP('',(#3274,#3275,#3276,#3277,#3278,#3279,#3280,#3281,#3282,
#3283,#3284,#3285,#3286,#3287,#3288,#3289,#3290,#3291,#3292,#3293,#3294,
#3295,#3296,#3297,#3298,#3299,#3300,#3301,#3302,#3303,#3304,#3305,#3306,
#3307,#3308,#3309,#3310,#3311,#3312,#3313,#3314,#3315,#3316,#3317,#3318,
#3319,#3320,#3321,#3322,#3323,#3324));
#753=EDGE_LOOP('',(#3325,#3326,#3327,#3328,#3329));
#754=EDGE_LOOP('',(#3330));
#755=EDGE_LOOP('',(#3331,#3332,#3333,#3334,#3335));
#756=EDGE_LOOP('',(#3336,#3337,#3338,#3339));
#757=EDGE_LOOP('',(#3340,#3341,#3342,#3343));
#758=EDGE_LOOP('',(#3344));
#1026=LINE('',#6238,#1311);
#1027=LINE('',#6569,#1312);
#1028=LINE('',#6799,#1313);
#1029=LINE('',#7028,#1314);
#1030=LINE('',#7441,#1315);
#1031=LINE('',#7911,#1316);
#1032=LINE('',#8401,#1317);
#1033=LINE('',#8808,#1318);
#1034=LINE('',#9043,#1319);
#1035=LINE('',#9283,#1320);
#1036=LINE('',#9769,#1321);
#1037=LINE('',#10260,#1322);
#1038=LINE('',#10686,#1323);
#1039=LINE('',#11195,#1324);
#1040=LINE('',#11679,#1325);
#1041=LINE('',#11919,#1326);
#1042=LINE('',#12152,#1327);
#1043=LINE('',#12563,#1328);
#1044=LINE('',#13025,#1329);
#1045=LINE('',#13525,#1330);
#1046=LINE('',#13938,#1331);
#1047=LINE('',#14169,#1332);
#1048=LINE('',#21498,#1333);
#1049=LINE('',#21501,#1334);
#1311=VECTOR('',#5161,1.99475);
#1312=VECTOR('',#5166,1.99475);
#1313=VECTOR('',#5169,1.99475);
#1314=VECTOR('',#5172,1.99475);
#1315=VECTOR('',#5175,1.99475);
#1316=VECTOR('',#5178,1.99475);
#1317=VECTOR('',#5181,1.99475);
#1318=VECTOR('',#5184,1.99475);
#1319=VECTOR('',#5187,1.99475);
#1320=VECTOR('',#5190,1.99475);
#1321=VECTOR('',#5193,1.99475);
#1322=VECTOR('',#5196,1.99475);
#1323=VECTOR('',#5199,1.99475);
#1324=VECTOR('',#5202,1.99475);
#1325=VECTOR('',#5205,1.99475);
#1326=VECTOR('',#5208,1.99475);
#1327=VECTOR('',#5211,1.99475);
#1328=VECTOR('',#5214,1.99475);
#1329=VECTOR('',#5217,1.99475);
#1330=VECTOR('',#5220,1.99475);
#1331=VECTOR('',#5223,1.99475);
#1332=VECTOR('',#5226,1.99475);
#1333=VECTOR('',#5247,5.14028464662889);
#1334=VECTOR('',#5250,6.05319927020769);
#1527=CIRCLE('',#4438,1.99475);
#1528=CIRCLE('',#4461,2.4505);
#1529=CIRCLE('',#4462,2.4505);
#1530=CIRCLE('',#4464,1.99475);
#1531=CIRCLE('',#4467,3.24975268099691);
#1532=CIRCLE('',#4469,7.03081661226087);
#1533=CIRCLE('',#4471,5.0755819281545);
#1774=VERTEX_POINT('',#6236);
#1775=VERTEX_POINT('',#6237);
#1776=VERTEX_POINT('',#6239);
#1777=VERTEX_POINT('',#6440);
#1778=VERTEX_POINT('',#6567);
#1779=VERTEX_POINT('',#6568);
#1780=VERTEX_POINT('',#6797);
#1781=VERTEX_POINT('',#6798);
#1782=VERTEX_POINT('',#7026);
#1783=VERTEX_POINT('',#7027);
#1784=VERTEX_POINT('',#7439);
#1785=VERTEX_POINT('',#7440);
#1786=VERTEX_POINT('',#7909);
#1787=VERTEX_POINT('',#7910);
#1788=VERTEX_POINT('',#8399);
#1789=VERTEX_POINT('',#8400);
#1790=VERTEX_POINT('',#8806);
#1791=VERTEX_POINT('',#8807);
#1792=VERTEX_POINT('',#9041);
#1793=VERTEX_POINT('',#9042);
#1794=VERTEX_POINT('',#9281);
#1795=VERTEX_POINT('',#9282);
#1796=VERTEX_POINT('',#9767);
#1797=VERTEX_POINT('',#9768);
#1798=VERTEX_POINT('',#9982);
#1799=VERTEX_POINT('',#10258);
#1800=VERTEX_POINT('',#10259);
#1801=VERTEX_POINT('',#10684);
#1802=VERTEX_POINT('',#10685);
#1803=VERTEX_POINT('',#10687);
#1804=VERTEX_POINT('',#11193);
#1805=VERTEX_POINT('',#11194);
#1806=VERTEX_POINT('',#11677);
#1807=VERTEX_POINT('',#11678);
#1808=VERTEX_POINT('',#11917);
#1809=VERTEX_POINT('',#11918);
#1810=VERTEX_POINT('',#12150);
#1811=VERTEX_POINT('',#12151);
#1812=VERTEX_POINT('',#12561);
#1813=VERTEX_POINT('',#12562);
#1814=VERTEX_POINT('',#13023);
#1815=VERTEX_POINT('',#13024);
#1816=VERTEX_POINT('',#13523);
#1817=VERTEX_POINT('',#13524);
#1818=VERTEX_POINT('',#13936);
#1819=VERTEX_POINT('',#13937);
#1820=VERTEX_POINT('',#14167);
#1821=VERTEX_POINT('',#14168);
#1822=VERTEX_POINT('',#14397);
#1823=VERTEX_POINT('',#14398);
#1824=VERTEX_POINT('',#14405);
#1825=VERTEX_POINT('',#14407);
#1826=VERTEX_POINT('',#14413);
#1827=VERTEX_POINT('',#14604);
#1828=VERTEX_POINT('',#14798);
#1829=VERTEX_POINT('',#14989);
#1830=VERTEX_POINT('',#15180);
#1831=VERTEX_POINT('',#15191);
#1832=VERTEX_POINT('',#15202);
#1833=VERTEX_POINT('',#15214);
#1834=VERTEX_POINT('',#15408);
#1835=VERTEX_POINT('',#15599);
#1836=VERTEX_POINT('',#15790);
#1837=VERTEX_POINT('',#15981);
#1838=VERTEX_POINT('',#15992);
#1839=VERTEX_POINT('',#16004);
#1840=VERTEX_POINT('',#16015);
#1841=VERTEX_POINT('',#16209);
#1842=VERTEX_POINT('',#16400);
#1843=VERTEX_POINT('',#16591);
#1844=VERTEX_POINT('',#16602);
#1845=VERTEX_POINT('',#16613);
#1846=VERTEX_POINT('',#16626);
#1847=VERTEX_POINT('',#16820);
#1848=VERTEX_POINT('',#17011);
#1849=VERTEX_POINT('',#17018);
#1850=VERTEX_POINT('',#17020);
#1851=VERTEX_POINT('',#17026);
#1852=VERTEX_POINT('',#17217);
#1853=VERTEX_POINT('',#17411);
#1854=VERTEX_POINT('',#17602);
#1855=VERTEX_POINT('',#17793);
#1856=VERTEX_POINT('',#17804);
#1857=VERTEX_POINT('',#17815);
#1858=VERTEX_POINT('',#17827);
#1859=VERTEX_POINT('',#18021);
#1860=VERTEX_POINT('',#18212);
#1861=VERTEX_POINT('',#18403);
#1862=VERTEX_POINT('',#18594);
#1863=VERTEX_POINT('',#18605);
#1864=VERTEX_POINT('',#18617);
#1865=VERTEX_POINT('',#18628);
#1866=VERTEX_POINT('',#18822);
#1867=VERTEX_POINT('',#19013);
#1868=VERTEX_POINT('',#19204);
#1869=VERTEX_POINT('',#19215);
#1870=VERTEX_POINT('',#19226);
#1871=VERTEX_POINT('',#19238);
#1872=VERTEX_POINT('',#19623);
#1873=VERTEX_POINT('',#19824);
#1874=VERTEX_POINT('',#20626);
#1875=VERTEX_POINT('',#21304);
#1876=VERTEX_POINT('',#21493);
#1877=VERTEX_POINT('',#21496);
#1878=VERTEX_POINT('',#21500);
#2256=EDGE_CURVE('',#1774,#1775,#1026,.T.);
#2257=EDGE_CURVE('',#1776,#1774,#71,.F.);
#2258=EDGE_CURVE('',#1777,#1776,#1527,.T.);
#2259=EDGE_CURVE('',#1777,#1775,#72,.T.);
#2260=EDGE_CURVE('',#1778,#1779,#1027,.T.);
#2261=EDGE_CURVE('',#1774,#1778,#73,.F.);
#2262=EDGE_CURVE('',#1775,#1779,#74,.T.);
#2263=EDGE_CURVE('',#1780,#1781,#1028,.T.);
#2264=EDGE_CURVE('',#1778,#1780,#75,.T.);
#2265=EDGE_CURVE('',#1779,#1781,#76,.T.);
#2266=EDGE_CURVE('',#1782,#1783,#1029,.T.);
#2267=EDGE_CURVE('',#1780,#1782,#77,.T.);
#2268=EDGE_CURVE('',#1781,#1783,#78,.T.);
#2269=EDGE_CURVE('',#1784,#1785,#1030,.T.);
#2270=EDGE_CURVE('',#1782,#1784,#79,.F.);
#2271=EDGE_CURVE('',#1783,#1785,#80,.T.);
#2272=EDGE_CURVE('',#1786,#1787,#1031,.T.);
#2273=EDGE_CURVE('',#1784,#1786,#81,.F.);
#2274=EDGE_CURVE('',#1785,#1787,#82,.T.);
#2275=EDGE_CURVE('',#1788,#1789,#1032,.T.);
#2276=EDGE_CURVE('',#1786,#1788,#83,.F.);
#2277=EDGE_CURVE('',#1787,#1789,#84,.T.);
#2278=EDGE_CURVE('',#1790,#1791,#1033,.T.);
#2279=EDGE_CURVE('',#1788,#1790,#85,.F.);
#2280=EDGE_CURVE('',#1789,#1791,#86,.T.);
#2281=EDGE_CURVE('',#1792,#1793,#1034,.T.);
#2282=EDGE_CURVE('',#1790,#1792,#87,.T.);
#2283=EDGE_CURVE('',#1791,#1793,#88,.T.);
#2284=EDGE_CURVE('',#1794,#1795,#1035,.T.);
#2285=EDGE_CURVE('',#1792,#1794,#89,.F.);
#2286=EDGE_CURVE('',#1793,#1795,#90,.T.);
#2287=EDGE_CURVE('',#1796,#1797,#1036,.T.);
#2288=EDGE_CURVE('',#1794,#1796,#91,.F.);
#2289=EDGE_CURVE('',#1795,#1798,#92,.T.);
#2290=EDGE_CURVE('',#1798,#1797,#93,.T.);
#2291=EDGE_CURVE('',#1799,#1800,#1037,.T.);
#2292=EDGE_CURVE('',#1796,#1799,#94,.F.);
#2293=EDGE_CURVE('',#1797,#1800,#95,.T.);
#2294=EDGE_CURVE('',#1801,#1802,#1038,.T.);
#2295=EDGE_CURVE('',#1803,#1801,#96,.F.);
#2296=EDGE_CURVE('',#1799,#1803,#97,.F.);
#2297=EDGE_CURVE('',#1800,#1802,#98,.T.);
#2298=EDGE_CURVE('',#1804,#1805,#1039,.T.);
#2299=EDGE_CURVE('',#1801,#1804,#99,.F.);
#2300=EDGE_CURVE('',#1802,#1805,#100,.T.);
#2301=EDGE_CURVE('',#1806,#1807,#1040,.T.);
#2302=EDGE_CURVE('',#1804,#1806,#101,.F.);
#2303=EDGE_CURVE('',#1805,#1807,#102,.T.);
#2304=EDGE_CURVE('',#1808,#1809,#1041,.T.);
#2305=EDGE_CURVE('',#1806,#1808,#103,.T.);
#2306=EDGE_CURVE('',#1807,#1809,#104,.T.);
#2307=EDGE_CURVE('',#1810,#1811,#1042,.T.);
#2308=EDGE_CURVE('',#1808,#1810,#105,.T.);
#2309=EDGE_CURVE('',#1809,#1811,#106,.T.);
#2310=EDGE_CURVE('',#1812,#1813,#1043,.T.);
#2311=EDGE_CURVE('',#1810,#1812,#107,.F.);
#2312=EDGE_CURVE('',#1811,#1813,#108,.T.);
#2313=EDGE_CURVE('',#1814,#1815,#1044,.T.);
#2314=EDGE_CURVE('',#1812,#1814,#109,.F.);
#2315=EDGE_CURVE('',#1813,#1815,#110,.T.);
#2316=EDGE_CURVE('',#1816,#1817,#1045,.T.);
#2317=EDGE_CURVE('',#1814,#1816,#111,.F.);
#2318=EDGE_CURVE('',#1815,#1817,#112,.T.);
#2319=EDGE_CURVE('',#1818,#1819,#1046,.T.);
#2320=EDGE_CURVE('',#1816,#1818,#113,.F.);
#2321=EDGE_CURVE('',#1817,#1819,#114,.T.);
#2322=EDGE_CURVE('',#1820,#1821,#1047,.T.);
#2323=EDGE_CURVE('',#1818,#1820,#115,.T.);
#2324=EDGE_CURVE('',#1819,#1821,#116,.F.);
#2325=EDGE_CURVE('',#1822,#1823,#117,.T.);
#2326=EDGE_CURVE('',#1824,#1823,#1528,.T.);
#2327=EDGE_CURVE('',#1824,#1825,#118,.T.);
#2328=EDGE_CURVE('',#1825,#1826,#119,.T.);
#2329=EDGE_CURVE('',#1826,#1827,#120,.T.);
#2330=EDGE_CURVE('',#1827,#1828,#121,.T.);
#2331=EDGE_CURVE('',#1828,#1829,#122,.T.);
#2332=EDGE_CURVE('',#1829,#1830,#123,.T.);
#2333=EDGE_CURVE('',#1830,#1831,#124,.T.);
#2334=EDGE_CURVE('',#1831,#1832,#125,.T.);
#2335=EDGE_CURVE('',#1832,#1833,#126,.T.);
#2336=EDGE_CURVE('',#1833,#1834,#127,.T.);
#2337=EDGE_CURVE('',#1834,#1835,#128,.T.);
#2338=EDGE_CURVE('',#1835,#1836,#129,.T.);
#2339=EDGE_CURVE('',#1836,#1837,#130,.T.);
#2340=EDGE_CURVE('',#1837,#1838,#131,.T.);
#2341=EDGE_CURVE('',#1838,#1839,#132,.T.);
#2342=EDGE_CURVE('',#1839,#1840,#133,.T.);
#2343=EDGE_CURVE('',#1840,#1841,#134,.T.);
#2344=EDGE_CURVE('',#1841,#1842,#135,.T.);
#2345=EDGE_CURVE('',#1842,#1843,#136,.T.);
#2346=EDGE_CURVE('',#1843,#1844,#137,.T.);
#2347=EDGE_CURVE('',#1844,#1845,#138,.T.);
#2348=EDGE_CURVE('',#1845,#1846,#139,.T.);
#2349=EDGE_CURVE('',#1846,#1847,#140,.T.);
#2350=EDGE_CURVE('',#1847,#1848,#141,.T.);
#2351=EDGE_CURVE('',#1849,#1848,#1529,.F.);
#2352=EDGE_CURVE('',#1849,#1850,#142,.T.);
#2353=EDGE_CURVE('',#1850,#1851,#143,.T.);
#2354=EDGE_CURVE('',#1851,#1852,#144,.T.);
#2355=EDGE_CURVE('',#1852,#1853,#145,.T.);
#2356=EDGE_CURVE('',#1853,#1854,#146,.T.);
#2357=EDGE_CURVE('',#1854,#1855,#147,.T.);
#2358=EDGE_CURVE('',#1855,#1856,#148,.T.);
#2359=EDGE_CURVE('',#1856,#1857,#149,.T.);
#2360=EDGE_CURVE('',#1857,#1858,#150,.T.);
#2361=EDGE_CURVE('',#1858,#1859,#151,.T.);
#2362=EDGE_CURVE('',#1859,#1860,#152,.T.);
#2363=EDGE_CURVE('',#1860,#1861,#153,.T.);
#2364=EDGE_CURVE('',#1861,#1862,#154,.T.);
#2365=EDGE_CURVE('',#1862,#1863,#155,.T.);
#2366=EDGE_CURVE('',#1863,#1864,#156,.T.);
#2367=EDGE_CURVE('',#1864,#1865,#157,.T.);
#2368=EDGE_CURVE('',#1865,#1866,#158,.T.);
#2369=EDGE_CURVE('',#1866,#1867,#159,.T.);
#2370=EDGE_CURVE('',#1867,#1868,#160,.T.);
#2371=EDGE_CURVE('',#1868,#1869,#161,.T.);
#2372=EDGE_CURVE('',#1869,#1870,#162,.T.);
#2373=EDGE_CURVE('',#1870,#1871,#163,.T.);
#2374=EDGE_CURVE('',#1871,#1822,#164,.T.);
#2375=EDGE_CURVE('',#1821,#1872,#165,.F.);
#2376=EDGE_CURVE('',#1873,#1872,#1530,.T.);
#2377=EDGE_CURVE('',#1820,#1873,#166,.T.);
#2378=EDGE_CURVE('',#1848,#1873,#167,.T.);
#2379=EDGE_CURVE('',#1874,#1824,#168,.T.);
#2380=EDGE_CURVE('',#1874,#1776,#169,.T.);
#2381=EDGE_CURVE('',#1875,#1849,#170,.T.);
#2382=EDGE_CURVE('',#1872,#1875,#171,.T.);
#2383=EDGE_CURVE('',#1823,#1777,#172,.T.);
#2384=EDGE_CURVE('',#1876,#1876,#1531,.T.);
#2385=EDGE_CURVE('',#1877,#1877,#1532,.T.);
#2386=EDGE_CURVE('',#1877,#1876,#1048,.T.);
#2387=EDGE_CURVE('',#1877,#1878,#1049,.T.);
#2388=EDGE_CURVE('',#1878,#1878,#1533,.T.);
#3079=ORIENTED_EDGE('',*,*,#2256,.F.);
#3080=ORIENTED_EDGE('',*,*,#2257,.F.);
#3081=ORIENTED_EDGE('',*,*,#2258,.F.);
#3082=ORIENTED_EDGE('',*,*,#2259,.T.);
#3083=ORIENTED_EDGE('',*,*,#2260,.F.);
#3084=ORIENTED_EDGE('',*,*,#2261,.F.);
#3085=ORIENTED_EDGE('',*,*,#2256,.T.);
#3086=ORIENTED_EDGE('',*,*,#2262,.T.);
#3087=ORIENTED_EDGE('',*,*,#2263,.F.);
#3088=ORIENTED_EDGE('',*,*,#2264,.F.);
#3089=ORIENTED_EDGE('',*,*,#2260,.T.);
#3090=ORIENTED_EDGE('',*,*,#2265,.T.);
#3091=ORIENTED_EDGE('',*,*,#2266,.F.);
#3092=ORIENTED_EDGE('',*,*,#2267,.F.);
#3093=ORIENTED_EDGE('',*,*,#2263,.T.);
#3094=ORIENTED_EDGE('',*,*,#2268,.T.);
#3095=ORIENTED_EDGE('',*,*,#2269,.F.);
#3096=ORIENTED_EDGE('',*,*,#2270,.F.);
#3097=ORIENTED_EDGE('',*,*,#2266,.T.);
#3098=ORIENTED_EDGE('',*,*,#2271,.T.);
#3099=ORIENTED_EDGE('',*,*,#2272,.F.);
#3100=ORIENTED_EDGE('',*,*,#2273,.F.);
#3101=ORIENTED_EDGE('',*,*,#2269,.T.);
#3102=ORIENTED_EDGE('',*,*,#2274,.T.);
#3103=ORIENTED_EDGE('',*,*,#2275,.F.);
#3104=ORIENTED_EDGE('',*,*,#2276,.F.);
#3105=ORIENTED_EDGE('',*,*,#2272,.T.);
#3106=ORIENTED_EDGE('',*,*,#2277,.T.);
#3107=ORIENTED_EDGE('',*,*,#2278,.F.);
#3108=ORIENTED_EDGE('',*,*,#2279,.F.);
#3109=ORIENTED_EDGE('',*,*,#2275,.T.);
#3110=ORIENTED_EDGE('',*,*,#2280,.T.);
#3111=ORIENTED_EDGE('',*,*,#2281,.F.);
#3112=ORIENTED_EDGE('',*,*,#2282,.F.);
#3113=ORIENTED_EDGE('',*,*,#2278,.T.);
#3114=ORIENTED_EDGE('',*,*,#2283,.T.);
#3115=ORIENTED_EDGE('',*,*,#2284,.F.);
#3116=ORIENTED_EDGE('',*,*,#2285,.F.);
#3117=ORIENTED_EDGE('',*,*,#2281,.T.);
#3118=ORIENTED_EDGE('',*,*,#2286,.T.);
#3119=ORIENTED_EDGE('',*,*,#2287,.F.);
#3120=ORIENTED_EDGE('',*,*,#2288,.F.);
#3121=ORIENTED_EDGE('',*,*,#2284,.T.);
#3122=ORIENTED_EDGE('',*,*,#2289,.T.);
#3123=ORIENTED_EDGE('',*,*,#2290,.T.);
#3124=ORIENTED_EDGE('',*,*,#2291,.F.);
#3125=ORIENTED_EDGE('',*,*,#2292,.F.);
#3126=ORIENTED_EDGE('',*,*,#2287,.T.);
#3127=ORIENTED_EDGE('',*,*,#2293,.T.);
#3128=ORIENTED_EDGE('',*,*,#2294,.F.);
#3129=ORIENTED_EDGE('',*,*,#2295,.F.);
#3130=ORIENTED_EDGE('',*,*,#2296,.F.);
#3131=ORIENTED_EDGE('',*,*,#2291,.T.);
#3132=ORIENTED_EDGE('',*,*,#2297,.T.);
#3133=ORIENTED_EDGE('',*,*,#2298,.F.);
#3134=ORIENTED_EDGE('',*,*,#2299,.F.);
#3135=ORIENTED_EDGE('',*,*,#2294,.T.);
#3136=ORIENTED_EDGE('',*,*,#2300,.T.);
#3137=ORIENTED_EDGE('',*,*,#2301,.F.);
#3138=ORIENTED_EDGE('',*,*,#2302,.F.);
#3139=ORIENTED_EDGE('',*,*,#2298,.T.);
#3140=ORIENTED_EDGE('',*,*,#2303,.T.);
#3141=ORIENTED_EDGE('',*,*,#2304,.F.);
#3142=ORIENTED_EDGE('',*,*,#2305,.F.);
#3143=ORIENTED_EDGE('',*,*,#2301,.T.);
#3144=ORIENTED_EDGE('',*,*,#2306,.T.);
#3145=ORIENTED_EDGE('',*,*,#2307,.F.);
#3146=ORIENTED_EDGE('',*,*,#2308,.F.);
#3147=ORIENTED_EDGE('',*,*,#2304,.T.);
#3148=ORIENTED_EDGE('',*,*,#2309,.T.);
#3149=ORIENTED_EDGE('',*,*,#2310,.F.);
#3150=ORIENTED_EDGE('',*,*,#2311,.F.);
#3151=ORIENTED_EDGE('',*,*,#2307,.T.);
#3152=ORIENTED_EDGE('',*,*,#2312,.T.);
#3153=ORIENTED_EDGE('',*,*,#2313,.F.);
#3154=ORIENTED_EDGE('',*,*,#2314,.F.);
#3155=ORIENTED_EDGE('',*,*,#2310,.T.);
#3156=ORIENTED_EDGE('',*,*,#2315,.T.);
#3157=ORIENTED_EDGE('',*,*,#2316,.F.);
#3158=ORIENTED_EDGE('',*,*,#2317,.F.);
#3159=ORIENTED_EDGE('',*,*,#2313,.T.);
#3160=ORIENTED_EDGE('',*,*,#2318,.T.);
#3161=ORIENTED_EDGE('',*,*,#2319,.F.);
#3162=ORIENTED_EDGE('',*,*,#2320,.F.);
#3163=ORIENTED_EDGE('',*,*,#2316,.T.);
#3164=ORIENTED_EDGE('',*,*,#2321,.T.);
#3165=ORIENTED_EDGE('',*,*,#2322,.F.);
#3166=ORIENTED_EDGE('',*,*,#2323,.F.);
#3167=ORIENTED_EDGE('',*,*,#2319,.T.);
#3168=ORIENTED_EDGE('',*,*,#2324,.T.);
#3169=ORIENTED_EDGE('',*,*,#2325,.T.);
#3170=ORIENTED_EDGE('',*,*,#2326,.F.);
#3171=ORIENTED_EDGE('',*,*,#2327,.T.);
#3172=ORIENTED_EDGE('',*,*,#2328,.T.);
#3173=ORIENTED_EDGE('',*,*,#2329,.T.);
#3174=ORIENTED_EDGE('',*,*,#2330,.T.);
#3175=ORIENTED_EDGE('',*,*,#2331,.T.);
#3176=ORIENTED_EDGE('',*,*,#2332,.T.);
#3177=ORIENTED_EDGE('',*,*,#2333,.T.);
#3178=ORIENTED_EDGE('',*,*,#2334,.T.);
#3179=ORIENTED_EDGE('',*,*,#2335,.T.);
#3180=ORIENTED_EDGE('',*,*,#2336,.T.);
#3181=ORIENTED_EDGE('',*,*,#2337,.T.);
#3182=ORIENTED_EDGE('',*,*,#2338,.T.);
#3183=ORIENTED_EDGE('',*,*,#2339,.T.);
#3184=ORIENTED_EDGE('',*,*,#2340,.T.);
#3185=ORIENTED_EDGE('',*,*,#2341,.T.);
#3186=ORIENTED_EDGE('',*,*,#2342,.T.);
#3187=ORIENTED_EDGE('',*,*,#2343,.T.);
#3188=ORIENTED_EDGE('',*,*,#2344,.T.);
#3189=ORIENTED_EDGE('',*,*,#2345,.T.);
#3190=ORIENTED_EDGE('',*,*,#2346,.T.);
#3191=ORIENTED_EDGE('',*,*,#2347,.T.);
#3192=ORIENTED_EDGE('',*,*,#2348,.T.);
#3193=ORIENTED_EDGE('',*,*,#2349,.T.);
#3194=ORIENTED_EDGE('',*,*,#2350,.T.);
#3195=ORIENTED_EDGE('',*,*,#2351,.F.);
#3196=ORIENTED_EDGE('',*,*,#2352,.T.);
#3197=ORIENTED_EDGE('',*,*,#2353,.T.);
#3198=ORIENTED_EDGE('',*,*,#2354,.T.);
#3199=ORIENTED_EDGE('',*,*,#2355,.T.);
#3200=ORIENTED_EDGE('',*,*,#2356,.T.);
#3201=ORIENTED_EDGE('',*,*,#2357,.T.);
#3202=ORIENTED_EDGE('',*,*,#2358,.T.);
#3203=ORIENTED_EDGE('',*,*,#2359,.T.);
#3204=ORIENTED_EDGE('',*,*,#2360,.T.);
#3205=ORIENTED_EDGE('',*,*,#2361,.T.);
#3206=ORIENTED_EDGE('',*,*,#2362,.T.);
#3207=ORIENTED_EDGE('',*,*,#2363,.T.);
#3208=ORIENTED_EDGE('',*,*,#2364,.T.);
#3209=ORIENTED_EDGE('',*,*,#2365,.T.);
#3210=ORIENTED_EDGE('',*,*,#2366,.T.);
#3211=ORIENTED_EDGE('',*,*,#2367,.T.);
#3212=ORIENTED_EDGE('',*,*,#2368,.T.);
#3213=ORIENTED_EDGE('',*,*,#2369,.T.);
#3214=ORIENTED_EDGE('',*,*,#2370,.T.);
#3215=ORIENTED_EDGE('',*,*,#2371,.T.);
#3216=ORIENTED_EDGE('',*,*,#2372,.T.);
#3217=ORIENTED_EDGE('',*,*,#2373,.T.);
#3218=ORIENTED_EDGE('',*,*,#2374,.T.);
#3219=ORIENTED_EDGE('',*,*,#2322,.T.);
#3220=ORIENTED_EDGE('',*,*,#2375,.T.);
#3221=ORIENTED_EDGE('',*,*,#2376,.F.);
#3222=ORIENTED_EDGE('',*,*,#2377,.F.);
#3223=ORIENTED_EDGE('',*,*,#2378,.F.);
#3224=ORIENTED_EDGE('',*,*,#2350,.F.);
#3225=ORIENTED_EDGE('',*,*,#2349,.F.);
#3226=ORIENTED_EDGE('',*,*,#2348,.F.);
#3227=ORIENTED_EDGE('',*,*,#2347,.F.);
#3228=ORIENTED_EDGE('',*,*,#2346,.F.);
#3229=ORIENTED_EDGE('',*,*,#2345,.F.);
#3230=ORIENTED_EDGE('',*,*,#2344,.F.);
#3231=ORIENTED_EDGE('',*,*,#2343,.F.);
#3232=ORIENTED_EDGE('',*,*,#2342,.F.);
#3233=ORIENTED_EDGE('',*,*,#2341,.F.);
#3234=ORIENTED_EDGE('',*,*,#2340,.F.);
#3235=ORIENTED_EDGE('',*,*,#2339,.F.);
#3236=ORIENTED_EDGE('',*,*,#2338,.F.);
#3237=ORIENTED_EDGE('',*,*,#2337,.F.);
#3238=ORIENTED_EDGE('',*,*,#2336,.F.);
#3239=ORIENTED_EDGE('',*,*,#2335,.F.);
#3240=ORIENTED_EDGE('',*,*,#2334,.F.);
#3241=ORIENTED_EDGE('',*,*,#2333,.F.);
#3242=ORIENTED_EDGE('',*,*,#2332,.F.);
#3243=ORIENTED_EDGE('',*,*,#2331,.F.);
#3244=ORIENTED_EDGE('',*,*,#2330,.F.);
#3245=ORIENTED_EDGE('',*,*,#2329,.F.);
#3246=ORIENTED_EDGE('',*,*,#2328,.F.);
#3247=ORIENTED_EDGE('',*,*,#2327,.F.);
#3248=ORIENTED_EDGE('',*,*,#2379,.F.);
#3249=ORIENTED_EDGE('',*,*,#2380,.T.);
#3250=ORIENTED_EDGE('',*,*,#2257,.T.);
#3251=ORIENTED_EDGE('',*,*,#2261,.T.);
#3252=ORIENTED_EDGE('',*,*,#2264,.T.);
#3253=ORIENTED_EDGE('',*,*,#2267,.T.);
#3254=ORIENTED_EDGE('',*,*,#2270,.T.);
#3255=ORIENTED_EDGE('',*,*,#2273,.T.);
#3256=ORIENTED_EDGE('',*,*,#2276,.T.);
#3257=ORIENTED_EDGE('',*,*,#2279,.T.);
#3258=ORIENTED_EDGE('',*,*,#2282,.T.);
#3259=ORIENTED_EDGE('',*,*,#2285,.T.);
#3260=ORIENTED_EDGE('',*,*,#2288,.T.);
#3261=ORIENTED_EDGE('',*,*,#2292,.T.);
#3262=ORIENTED_EDGE('',*,*,#2296,.T.);
#3263=ORIENTED_EDGE('',*,*,#2295,.T.);
#3264=ORIENTED_EDGE('',*,*,#2299,.T.);
#3265=ORIENTED_EDGE('',*,*,#2302,.T.);
#3266=ORIENTED_EDGE('',*,*,#2305,.T.);
#3267=ORIENTED_EDGE('',*,*,#2308,.T.);
#3268=ORIENTED_EDGE('',*,*,#2311,.T.);
#3269=ORIENTED_EDGE('',*,*,#2314,.T.);
#3270=ORIENTED_EDGE('',*,*,#2317,.T.);
#3271=ORIENTED_EDGE('',*,*,#2320,.T.);
#3272=ORIENTED_EDGE('',*,*,#2323,.T.);
#3273=ORIENTED_EDGE('',*,*,#2377,.T.);
#3274=ORIENTED_EDGE('',*,*,#2381,.F.);
#3275=ORIENTED_EDGE('',*,*,#2382,.F.);
#3276=ORIENTED_EDGE('',*,*,#2375,.F.);
#3277=ORIENTED_EDGE('',*,*,#2324,.F.);
#3278=ORIENTED_EDGE('',*,*,#2321,.F.);
#3279=ORIENTED_EDGE('',*,*,#2318,.F.);
#3280=ORIENTED_EDGE('',*,*,#2315,.F.);
#3281=ORIENTED_EDGE('',*,*,#2312,.F.);
#3282=ORIENTED_EDGE('',*,*,#2309,.F.);
#3283=ORIENTED_EDGE('',*,*,#2306,.F.);
#3284=ORIENTED_EDGE('',*,*,#2303,.F.);
#3285=ORIENTED_EDGE('',*,*,#2300,.F.);
#3286=ORIENTED_EDGE('',*,*,#2297,.F.);
#3287=ORIENTED_EDGE('',*,*,#2293,.F.);
#3288=ORIENTED_EDGE('',*,*,#2290,.F.);
#3289=ORIENTED_EDGE('',*,*,#2289,.F.);
#3290=ORIENTED_EDGE('',*,*,#2286,.F.);
#3291=ORIENTED_EDGE('',*,*,#2283,.F.);
#3292=ORIENTED_EDGE('',*,*,#2280,.F.);
#3293=ORIENTED_EDGE('',*,*,#2277,.F.);
#3294=ORIENTED_EDGE('',*,*,#2274,.F.);
#3295=ORIENTED_EDGE('',*,*,#2271,.F.);
#3296=ORIENTED_EDGE('',*,*,#2268,.F.);
#3297=ORIENTED_EDGE('',*,*,#2265,.F.);
#3298=ORIENTED_EDGE('',*,*,#2262,.F.);
#3299=ORIENTED_EDGE('',*,*,#2259,.F.);
#3300=ORIENTED_EDGE('',*,*,#2383,.F.);
#3301=ORIENTED_EDGE('',*,*,#2325,.F.);
#3302=ORIENTED_EDGE('',*,*,#2374,.F.);
#3303=ORIENTED_EDGE('',*,*,#2373,.F.);
#3304=ORIENTED_EDGE('',*,*,#2372,.F.);
#3305=ORIENTED_EDGE('',*,*,#2371,.F.);
#3306=ORIENTED_EDGE('',*,*,#2370,.F.);
#3307=ORIENTED_EDGE('',*,*,#2369,.F.);
#3308=ORIENTED_EDGE('',*,*,#2368,.F.);
#3309=ORIENTED_EDGE('',*,*,#2367,.F.);
#3310=ORIENTED_EDGE('',*,*,#2366,.F.);
#3311=ORIENTED_EDGE('',*,*,#2365,.F.);
#3312=ORIENTED_EDGE('',*,*,#2364,.F.);
#3313=ORIENTED_EDGE('',*,*,#2363,.F.);
#3314=ORIENTED_EDGE('',*,*,#2362,.F.);
#3315=ORIENTED_EDGE('',*,*,#2361,.F.);
#3316=ORIENTED_EDGE('',*,*,#2360,.F.);
#3317=ORIENTED_EDGE('',*,*,#2359,.F.);
#3318=ORIENTED_EDGE('',*,*,#2358,.F.);
#3319=ORIENTED_EDGE('',*,*,#2357,.F.);
#3320=ORIENTED_EDGE('',*,*,#2356,.F.);
#3321=ORIENTED_EDGE('',*,*,#2355,.F.);
#3322=ORIENTED_EDGE('',*,*,#2354,.F.);
#3323=ORIENTED_EDGE('',*,*,#2353,.F.);
#3324=ORIENTED_EDGE('',*,*,#2352,.F.);
#3325=ORIENTED_EDGE('',*,*,#2381,.T.);
#3326=ORIENTED_EDGE('',*,*,#2351,.T.);
#3327=ORIENTED_EDGE('',*,*,#2378,.T.);
#3328=ORIENTED_EDGE('',*,*,#2376,.T.);
#3329=ORIENTED_EDGE('',*,*,#2382,.T.);
#3330=ORIENTED_EDGE('',*,*,#2384,.F.);
#3331=ORIENTED_EDGE('',*,*,#2326,.T.);
#3332=ORIENTED_EDGE('',*,*,#2383,.T.);
#3333=ORIENTED_EDGE('',*,*,#2258,.T.);
#3334=ORIENTED_EDGE('',*,*,#2380,.F.);
#3335=ORIENTED_EDGE('',*,*,#2379,.T.);
#3336=ORIENTED_EDGE('',*,*,#2385,.F.);
#3337=ORIENTED_EDGE('',*,*,#2386,.T.);
#3338=ORIENTED_EDGE('',*,*,#2384,.T.);
#3339=ORIENTED_EDGE('',*,*,#2386,.F.);
#3340=ORIENTED_EDGE('',*,*,#2385,.T.);
#3341=ORIENTED_EDGE('',*,*,#2387,.T.);
#3342=ORIENTED_EDGE('',*,*,#2388,.F.);
#3343=ORIENTED_EDGE('',*,*,#2387,.F.);
#3344=ORIENTED_EDGE('',*,*,#2388,.T.);
#3874=CYLINDRICAL_SURFACE('',#4437,1.99475);
#3875=CYLINDRICAL_SURFACE('',#4439,1.99475);
#3876=CYLINDRICAL_SURFACE('',#4440,1.99475);
#3877=CYLINDRICAL_SURFACE('',#4441,1.99475);
#3878=CYLINDRICAL_SURFACE('',#4442,1.99475);
#3879=CYLINDRICAL_SURFACE('',#4443,1.99475);
#3880=CYLINDRICAL_SURFACE('',#4444,1.99475);
#3881=CYLINDRICAL_SURFACE('',#4445,1.99475);
#3882=CYLINDRICAL_SURFACE('',#4446,1.99475);
#3883=CYLINDRICAL_SURFACE('',#4447,1.99475);
#3884=CYLINDRICAL_SURFACE('',#4448,1.99475);
#3885=CYLINDRICAL_SURFACE('',#4449,1.99475);
#3886=CYLINDRICAL_SURFACE('',#4450,1.99475);
#3887=CYLINDRICAL_SURFACE('',#4451,1.99475);
#3888=CYLINDRICAL_SURFACE('',#4452,1.99475);
#3889=CYLINDRICAL_SURFACE('',#4453,1.99475);
#3890=CYLINDRICAL_SURFACE('',#4454,1.99475);
#3891=CYLINDRICAL_SURFACE('',#4455,1.99475);
#3892=CYLINDRICAL_SURFACE('',#4456,1.99475);
#3893=CYLINDRICAL_SURFACE('',#4457,1.99475);
#3894=CYLINDRICAL_SURFACE('',#4458,1.99475);
#3895=CYLINDRICAL_SURFACE('',#4459,1.99475);
#3896=CYLINDRICAL_SURFACE('',#4460,2.4505);
#3897=CYLINDRICAL_SURFACE('',#4463,1.99475);
#4018=ADVANCED_FACE('',(#483),#3874,.T.);
#4019=ADVANCED_FACE('',(#484),#3875,.T.);
#4020=ADVANCED_FACE('',(#485),#3876,.T.);
#4021=ADVANCED_FACE('',(#486),#3877,.T.);
#4022=ADVANCED_FACE('',(#487),#3878,.T.);
#4023=ADVANCED_FACE('',(#488),#3879,.T.);
#4024=ADVANCED_FACE('',(#489),#3880,.T.);
#4025=ADVANCED_FACE('',(#490),#3881,.T.);
#4026=ADVANCED_FACE('',(#491),#3882,.T.);
#4027=ADVANCED_FACE('',(#492),#3883,.T.);
#4028=ADVANCED_FACE('',(#493),#3884,.T.);
#4029=ADVANCED_FACE('',(#494),#3885,.T.);
#4030=ADVANCED_FACE('',(#495),#3886,.T.);
#4031=ADVANCED_FACE('',(#496),#3887,.T.);
#4032=ADVANCED_FACE('',(#497),#3888,.T.);
#4033=ADVANCED_FACE('',(#498),#3889,.T.);
#4034=ADVANCED_FACE('',(#499),#3890,.T.);
#4035=ADVANCED_FACE('',(#500),#3891,.T.);
#4036=ADVANCED_FACE('',(#501),#3892,.T.);
#4037=ADVANCED_FACE('',(#502),#3893,.T.);
#4038=ADVANCED_FACE('',(#503),#3894,.T.);
#4039=ADVANCED_FACE('',(#504),#3895,.T.);
#4040=ADVANCED_FACE('',(#505),#3896,.T.);
#4041=ADVANCED_FACE('',(#506),#3897,.T.);
#4042=ADVANCED_FACE('',(#507),#53,.F.);
#4043=ADVANCED_FACE('',(#508),#54,.F.);
#4044=ADVANCED_FACE('',(#509),#350,.T.);
#4045=ADVANCED_FACE('',(#510,#283),#351,.T.);
#4046=ADVANCED_FACE('',(#511),#51,.T.);
#4047=ADVANCED_FACE('',(#512),#52,.T.);
#4048=ADVANCED_FACE('',(#513),#352,.T.);
#4161=CLOSED_SHELL('',(#4018,#4019,#4020,#4021,#4022,#4023,#4024,#4025,
#4026,#4027,#4028,#4029,#4030,#4031,#4032,#4033,#4034,#4035,#4036,#4037,
#4038,#4039,#4040,#4041,#4042,#4043,#4044,#4045,#4046,#4047,#4048));
#4436=AXIS2_PLACEMENT_3D('',#6234,#5157,#5158);
#4437=AXIS2_PLACEMENT_3D('',#6235,#5159,#5160);
#4438=AXIS2_PLACEMENT_3D('',#6441,#5162,#5163);
#4439=AXIS2_PLACEMENT_3D('',#6566,#5164,#5165);
#4440=AXIS2_PLACEMENT_3D('',#6796,#5167,#5168);
#4441=AXIS2_PLACEMENT_3D('',#7025,#5170,#5171);
#4442=AXIS2_PLACEMENT_3D('',#7438,#5173,#5174);
#4443=AXIS2_PLACEMENT_3D('',#7908,#5176,#5177);
#4444=AXIS2_PLACEMENT_3D('',#8398,#5179,#5180);
#4445=AXIS2_PLACEMENT_3D('',#8805,#5182,#5183);
#4446=AXIS2_PLACEMENT_3D('',#9040,#5185,#5186);
#4447=AXIS2_PLACEMENT_3D('',#9280,#5188,#5189);
#4448=AXIS2_PLACEMENT_3D('',#9766,#5191,#5192);
#4449=AXIS2_PLACEMENT_3D('',#10257,#5194,#5195);
#4450=AXIS2_PLACEMENT_3D('',#10683,#5197,#5198);
#4451=AXIS2_PLACEMENT_3D('',#11192,#5200,#5201);
#4452=AXIS2_PLACEMENT_3D('',#11676,#5203,#5204);
#4453=AXIS2_PLACEMENT_3D('',#11916,#5206,#5207);
#4454=AXIS2_PLACEMENT_3D('',#12149,#5209,#5210);
#4455=AXIS2_PLACEMENT_3D('',#12560,#5212,#5213);
#4456=AXIS2_PLACEMENT_3D('',#13022,#5215,#5216);
#4457=AXIS2_PLACEMENT_3D('',#13522,#5218,#5219);
#4458=AXIS2_PLACEMENT_3D('',#13935,#5221,#5222);
#4459=AXIS2_PLACEMENT_3D('',#14166,#5224,#5225);
#4460=AXIS2_PLACEMENT_3D('',#14396,#5227,#5228);
#4461=AXIS2_PLACEMENT_3D('',#14406,#5229,#5230);
#4462=AXIS2_PLACEMENT_3D('',#17019,#5231,#5232);
#4463=AXIS2_PLACEMENT_3D('',#19622,#5233,#5234);
#4464=AXIS2_PLACEMENT_3D('',#19825,#5235,#5236);
#4465=AXIS2_PLACEMENT_3D('',#21491,#5237,#5238);
#4466=AXIS2_PLACEMENT_3D('',#21492,#5239,#5240);
#4467=AXIS2_PLACEMENT_3D('',#21494,#5241,#5242);
#4468=AXIS2_PLACEMENT_3D('',#21495,#5243,#5244);
#4469=AXIS2_PLACEMENT_3D('',#21497,#5245,#5246);
#4470=AXIS2_PLACEMENT_3D('',#21499,#5248,#5249);
#4471=AXIS2_PLACEMENT_3D('',#21502,#5251,#5252);
#4472=AXIS2_PLACEMENT_3D('',#21503,#5253,#5254);
#5157=DIRECTION('axis',(0.,0.,1.));
#5158=DIRECTION('refdir',(1.,0.,0.));
#5159=DIRECTION('center_axis',(0.,0.,1.));
#5160=DIRECTION('ref_axis',(-1.,-4.17628703648668E-14,0.));
#5161=DIRECTION('',(0.,0.,-1.));
#5162=DIRECTION('center_axis',(0.,0.,-1.));
#5163=DIRECTION('ref_axis',(-1.,-4.17628703648668E-14,0.));
#5164=DIRECTION('center_axis',(0.,0.,1.));
#5165=DIRECTION('ref_axis',(-1.,-4.17628703648668E-14,0.));
#5166=DIRECTION('',(0.,0.,-1.));
#5167=DIRECTION('center_axis',(0.,0.,1.));
#5168=DIRECTION('ref_axis',(-1.,-4.17628703648668E-14,0.));
#5169=DIRECTION('',(0.,0.,-1.));
#5170=DIRECTION('center_axis',(0.,0.,1.));
#5171=DIRECTION('ref_axis',(-1.,-4.17628703648668E-14,0.));
#5172=DIRECTION('',(0.,0.,-1.));
#5173=DIRECTION('center_axis',(0.,0.,1.));
#5174=DIRECTION('ref_axis',(-1.,-4.17628703648668E-14,0.));
#5175=DIRECTION('',(0.,0.,-1.));
#5176=DIRECTION('center_axis',(0.,0.,1.));
#5177=DIRECTION('ref_axis',(-1.,-4.17628703648668E-14,0.));
#5178=DIRECTION('',(0.,0.,-1.));
#5179=DIRECTION('center_axis',(0.,0.,1.));
#5180=DIRECTION('ref_axis',(-1.,-4.17628703648668E-14,0.));
#5181=DIRECTION('',(0.,0.,-1.));
#5182=DIRECTION('center_axis',(0.,0.,1.));
#5183=DIRECTION('ref_axis',(-1.,-4.17628703648668E-14,0.));
#5184=DIRECTION('',(0.,0.,-1.));
#5185=DIRECTION('center_axis',(0.,0.,1.));
#5186=DIRECTION('ref_axis',(-1.,-4.17628703648668E-14,0.));
#5187=DIRECTION('',(0.,0.,-1.));
#5188=DIRECTION('center_axis',(0.,0.,1.));
#5189=DIRECTION('ref_axis',(-1.,-4.17628703648668E-14,0.));
#5190=DIRECTION('',(0.,0.,-1.));
#5191=DIRECTION('center_axis',(0.,0.,1.));
#5192=DIRECTION('ref_axis',(-1.,-4.17628703648668E-14,0.));
#5193=DIRECTION('',(0.,0.,-1.));
#5194=DIRECTION('center_axis',(0.,0.,1.));
#5195=DIRECTION('ref_axis',(-1.,-4.17628703648668E-14,0.));
#5196=DIRECTION('',(0.,0.,-1.));
#5197=DIRECTION('center_axis',(0.,0.,1.));
#5198=DIRECTION('ref_axis',(-1.,-4.17628703648668E-14,0.));
#5199=DIRECTION('',(0.,0.,-1.));
#5200=DIRECTION('center_axis',(0.,0.,1.));
#5201=DIRECTION('ref_axis',(-1.,-4.17628703648668E-14,0.));
#5202=DIRECTION('',(0.,0.,-1.));
#5203=DIRECTION('center_axis',(0.,0.,1.));
#5204=DIRECTION('ref_axis',(-1.,-4.17628703648668E-14,0.));
#5205=DIRECTION('',(0.,0.,-1.));
#5206=DIRECTION('center_axis',(0.,0.,1.));
#5207=DIRECTION('ref_axis',(-1.,-4.17628703648668E-14,0.));
#5208=DIRECTION('',(0.,0.,-1.));
#5209=DIRECTION('center_axis',(0.,0.,1.));
#5210=DIRECTION('ref_axis',(-1.,-4.17628703648668E-14,0.));
#5211=DIRECTION('',(0.,0.,-1.));
#5212=DIRECTION('center_axis',(0.,0.,1.));
#5213=DIRECTION('ref_axis',(-1.,-4.17628703648668E-14,0.));
#5214=DIRECTION('',(0.,0.,-1.));
#5215=DIRECTION('center_axis',(0.,0.,1.));
#5216=DIRECTION('ref_axis',(-1.,-4.17628703648668E-14,0.));
#5217=DIRECTION('',(0.,0.,-1.));
#5218=DIRECTION('center_axis',(0.,0.,1.));
#5219=DIRECTION('ref_axis',(-1.,-4.17628703648668E-14,0.));
#5220=DIRECTION('',(0.,0.,-1.));
#5221=DIRECTION('center_axis',(0.,0.,1.));
#5222=DIRECTION('ref_axis',(-1.,-4.17628703648668E-14,0.));
#5223=DIRECTION('',(0.,0.,-1.));
#5224=DIRECTION('center_axis',(0.,0.,1.));
#5225=DIRECTION('ref_axis',(-1.,-4.17628703648668E-14,0.));
#5226=DIRECTION('',(0.,0.,-1.));
#5227=DIRECTION('center_axis',(0.,0.,1.));
#5228=DIRECTION('ref_axis',(-1.,0.,0.));
#5229=DIRECTION('center_axis',(0.,0.,-1.));
#5230=DIRECTION('ref_axis',(-1.,0.,0.));
#5231=DIRECTION('center_axis',(0.,0.,-1.));
#5232=DIRECTION('ref_axis',(-1.,0.,0.));
#5233=DIRECTION('center_axis',(0.,0.,1.));
#5234=DIRECTION('ref_axis',(-1.,-4.17628703648668E-14,0.));
#5235=DIRECTION('center_axis',(0.,0.,1.));
#5236=DIRECTION('ref_axis',(-1.,-4.17628703648668E-14,0.));
#5237=DIRECTION('center_axis',(0.,0.,1.));
#5238=DIRECTION('ref_axis',(-1.,0.,0.));
#5239=DIRECTION('center_axis',(0.,0.,1.));
#5240=DIRECTION('ref_axis',(1.,0.,0.));
#5241=DIRECTION('center_axis',(0.,0.,-1.));
#5242=DIRECTION('ref_axis',(1.,0.,0.));
#5243=DIRECTION('center_axis',(0.,0.,-1.));
#5244=DIRECTION('ref_axis',(-1.,0.,0.));
#5245=DIRECTION('center_axis',(0.,0.,-1.));
#5246=DIRECTION('ref_axis',(1.,0.,0.));
#5247=DIRECTION('',(-0.966586729160533,1.18372734396476E-16,0.256339803797111));
#5248=DIRECTION('center_axis',(0.,0.,1.));
#5249=DIRECTION('ref_axis',(-1.,0.,0.));
#5250=DIRECTION('',(-0.237251396871265,-2.90549163771633E-17,-0.971448287189099));
#5251=DIRECTION('center_axis',(0.,0.,-1.));
#5252=DIRECTION('ref_axis',(1.,0.,0.));
#5253=DIRECTION('center_axis',(0.,0.,-1.));
#5254=DIRECTION('ref_axis',(-1.,0.,0.));
#6234=CARTESIAN_POINT('',(0.,0.,0.));
#6235=CARTESIAN_POINT('Origin',(5.09382715545311,0.,-6.77268258743872));
#6236=CARTESIAN_POINT('',(7.08857715545311,-1.48167178722712E-8,-4.61281584510352));
#6237=CARTESIAN_POINT('',(7.08857671412439,-0.00132690645140175,-4.77268258743872));
#6238=CARTESIAN_POINT('',(7.08857715545311,8.3550772080578E-14,-6.77268258743872));
#6239=CARTESIAN_POINT('',(6.2322442180908,1.63799699450132,-5.29363746883395));
#6240=CARTESIAN_POINT('Ctrl Pts',(7.08857715545311,-1.48167178722712E-8,
-4.61281584510352));
#6241=CARTESIAN_POINT('Ctrl Pts',(7.08857715515529,-0.0400947307971134,
-4.61544918220441));
#6242=CARTESIAN_POINT('Ctrl Pts',(7.0873683003548,-0.0801825303907697,-4.61811867810323));
#6243=CARTESIAN_POINT('Ctrl Pts',(7.07727049993181,-0.247440799661336,-4.62940828682582));
#6244=CARTESIAN_POINT('Ctrl Pts',(7.05741240048877,-0.373631769826948,-4.6383184861514));
#6245=CARTESIAN_POINT('Ctrl Pts',(7.00135287300863,-0.591512757714937,-4.65398174107726));
#6246=CARTESIAN_POINT('Ctrl Pts',(6.97014883384365,-0.684078311974067,-4.66072168793572));
#6247=CARTESIAN_POINT('Ctrl Pts',(6.92804514054676,-0.784086582838243,-4.66785393707128));
#6248=CARTESIAN_POINT('Ctrl Pts',(6.92371465678162,-0.794140498682412,-4.66856912793543));
#6249=CARTESIAN_POINT('Ctrl Pts',(6.91703252460397,-0.80930922547275,-4.66964484456109));
#6250=CARTESIAN_POINT('Ctrl Pts',(6.9147417128135,-0.814450377374438,-4.67000885662465));
#6251=CARTESIAN_POINT('Ctrl Pts',(6.91058268033754,-0.823679016097091,-4.6706611388414));
#6252=CARTESIAN_POINT('Ctrl Pts',(6.90872238990846,-0.8277699244717,-4.67094987407352));
#6253=CARTESIAN_POINT('Ctrl Pts',(6.90460481660111,-0.836744145192207,-4.67158236707836));
#6254=CARTESIAN_POINT('Ctrl Pts',(6.90234160175738,-0.841624620463466,-4.67192575795504));
#6255=CARTESIAN_POINT('Ctrl Pts',(6.89577780104207,-0.855630291153922,-4.67290969774183));
#6256=CARTESIAN_POINT('Ctrl Pts',(6.89142762871411,-0.864732255025353,-4.67354729854128));
#6257=CARTESIAN_POINT('Ctrl Pts',(6.85946477911054,-0.930325201194365,-4.67813158667197));
#6258=CARTESIAN_POINT('Ctrl Pts',(6.82926078743822,-0.985521692584171,-4.68193274237631));
#6259=CARTESIAN_POINT('Ctrl Pts',(6.74901098783228,-1.11700580624151,-4.69106971997584));
#6260=CARTESIAN_POINT('Ctrl Pts',(6.69624707153906,-1.19146436221979,-4.6963199151433));
#6261=CARTESIAN_POINT('Ctrl Pts',(6.55742275297117,-1.36138427180224,-4.70907614350377));
#6262=CARTESIAN_POINT('Ctrl Pts',(6.46689259400708,-1.45264043881999,-4.71661590767991));
#6263=CARTESIAN_POINT('Ctrl Pts',(6.3557489127286,-1.54494160516324,-4.72557527884981));
#6264=CARTESIAN_POINT('Ctrl Pts',(6.34313466569004,-1.55515973634511,-4.72658781247032));
#6265=CARTESIAN_POINT('Ctrl Pts',(6.32237361935444,-1.57156155225421,-4.72824814092839));
#6266=CARTESIAN_POINT('Ctrl Pts',(6.31430134311785,-1.57783867283577,-4.72889222466277));
#6267=CARTESIAN_POINT('Ctrl Pts',(6.29978192139657,-1.58895110203977,-4.7300482784867));
#6268=CARTESIAN_POINT('Ctrl Pts',(6.29335302089738,-1.59380996270127,-4.73055931069375));
#6269=CARTESIAN_POINT('Ctrl Pts',(6.27966772771486,-1.60402338643849,-4.73164546739798));
#6270=CARTESIAN_POINT('Ctrl Pts',(6.27240413063881,-1.60936794930186,-4.73222096407933));
#6271=CARTESIAN_POINT('Ctrl Pts',(6.25287004646879,-1.62353798533996,-4.73376616418403));
#6272=CARTESIAN_POINT('Ctrl Pts',(6.24053526541135,-1.63227341546723,-4.73473928172537));
#6273=CARTESIAN_POINT('Ctrl Pts',(6.17826093377316,-1.67532152531414,-4.73964036149228));
#6274=CARTESIAN_POINT('Ctrl Pts',(6.12688017056799,-1.70748324017133,-4.74364771664052));
#6275=CARTESIAN_POINT('Ctrl Pts',(5.96291474065865,-1.80000515005531,-4.7563320750856));
#6276=CARTESIAN_POINT('Ctrl Pts',(5.84595120515671,-1.85192722898832,-4.76525737892825));
#6277=CARTESIAN_POINT('Ctrl Pts',(5.6328247064913,-1.92299730751201,-4.78089415862207));
#6278=CARTESIAN_POINT('Ctrl Pts',(5.53867674249202,-1.9469335538999,-4.78759396831812));
#6279=CARTESIAN_POINT('Ctrl Pts',(5.43235884025432,-1.96584435240037,-4.79469128894282));
#6280=CARTESIAN_POINT('Ctrl Pts',(5.42155068496735,-1.96767502922678,-4.7954074228328));
#6281=CARTESIAN_POINT('Ctrl Pts',(5.40515987895374,-1.97031248818372,-4.79648477745489));
#6282=CARTESIAN_POINT('Ctrl Pts',(5.39958820031319,-1.97118480897772,-4.79684948487212));
#6283=CARTESIAN_POINT('Ctrl Pts',(5.38955382730705,-1.97271225507761,-4.79750349341496));
#6284=CARTESIAN_POINT('Ctrl Pts',(5.38509258255286,-1.97337587848556,-4.79779325599492));
#6285=CARTESIAN_POINT('Ctrl Pts',(5.37527424371394,-1.9748023641512,-4.79842876016531));
#6286=CARTESIAN_POINT('Ctrl Pts',(5.36991628869129,-1.97555856230869,-4.79877412811315));
#6287=CARTESIAN_POINT('Ctrl Pts',(5.3544878673316,-1.97767206833307,-4.79976467899655));
#6288=CARTESIAN_POINT('Ctrl Pts',(5.34440984664975,-1.97897426503916,-4.80040688279367));
#6289=CARTESIAN_POINT('Ctrl Pts',(5.27067772117271,-1.98792902018792,-4.80507290662605));
#6290=CARTESIAN_POINT('Ctrl Pts',(5.20669059594675,-1.99258664349983,-4.80894626086477));
#6291=CARTESIAN_POINT('Ctrl Pts',(5.00659272338178,-1.99747900392144,-4.82081444578765));
#6292=CARTESIAN_POINT('Ctrl Pts',(4.87061587215657,-1.9868849133802,-4.82855057247952));
#6293=CARTESIAN_POINT('Ctrl Pts',(4.65604088092438,-1.94784595316983,-4.84142773341889));
#6294=CARTESIAN_POINT('Ctrl Pts',(4.57630245148535,-1.92819255035695,-4.84636193642796));
#6295=CARTESIAN_POINT('Ctrl Pts',(4.48329474201247,-1.89908277104335,-4.85241289230236));
#6296=CARTESIAN_POINT('Ctrl Pts',(4.46863721086776,-1.89430797697619,-4.85337527953983));
#6297=CARTESIAN_POINT('Ctrl Pts',(4.4445753087319,-1.88615995797207,-4.85497037589027));
#6298=CARTESIAN_POINT('Ctrl Pts',(4.4351381533715,-1.88288505763404,-4.85559987359212));
#6299=CARTESIAN_POINT('Ctrl Pts',(4.41813803594403,-1.87684219652712,-4.85674108532922));
#6300=CARTESIAN_POINT('Ctrl Pts',(4.41056643845231,-1.87409903857928,-4.85725197343053));
#6301=CARTESIAN_POINT('Ctrl Pts',(4.39437370686075,-1.86812130766766,-4.85835026905944));
#6302=CARTESIAN_POINT('Ctrl Pts',(4.38575796957072,-1.86487274907785,-4.85893813033501));
#6303=CARTESIAN_POINT('Ctrl Pts',(4.36230536462303,-1.85584400518734,-4.8605480280963));
#6304=CARTESIAN_POINT('Ctrl Pts',(4.34751497817963,-1.84994573213895,-4.86157397246172));
#6305=CARTESIAN_POINT('Ctrl Pts',(4.26604076303032,-1.81631847830108,-4.86728609052941));
#6306=CARTESIAN_POINT('Ctrl Pts',(4.20083769700026,-1.78516408602775,-4.87208670876007));
#6307=CARTESIAN_POINT('Ctrl Pts',(4.00824617895935,-1.6799480055716,-4.88697874456887));
#6308=CARTESIAN_POINT('Ctrl Pts',(3.88723954816717,-1.59525872597823,-4.89737444923679));
#6309=CARTESIAN_POINT('Ctrl Pts',(3.76106781248094,-1.4843219981909,-4.90896301151816));
#6310=CARTESIAN_POINT('Ctrl Pts',(3.74567909414366,-1.47035917679528,-4.91038982975238));
#6311=CARTESIAN_POINT('Ctrl Pts',(3.69672988504033,-1.42453087882556,-4.91496537723626));
#6312=CARTESIAN_POINT('Ctrl Pts',(3.66405652730914,-1.39173478381734,-4.91807751757299));
#6313=CARTESIAN_POINT('Ctrl Pts',(3.62652904699974,-1.35134824842086,-4.9216925637817));
#6314=CARTESIAN_POINT('Ctrl Pts',(3.62055009565997,-1.34482732703748,-4.92226980080627));
#6315=CARTESIAN_POINT('Ctrl Pts',(3.61083639125473,-1.33409057812522,-4.92320940507348));
#6316=CARTESIAN_POINT('Ctrl Pts',(3.60707583263341,-1.32989841089904,-4.92357361086162));
#6317=CARTESIAN_POINT('Ctrl Pts',(3.60035354389009,-1.32234043764107,-4.92422537471545));
#6318=CARTESIAN_POINT('Ctrl Pts',(3.597385341909,-1.3189805008644,-4.92451340917361));
#6319=CARTESIAN_POINT('Ctrl Pts',(3.5909086290735,-1.31159900364749,-4.92514243459031));
#6320=CARTESIAN_POINT('Ctrl Pts',(3.58740491633508,-1.30757335641467,-4.92548307230828));
#6321=CARTESIAN_POINT('Ctrl Pts',(3.57737584996034,-1.29595648272935,-4.92645930351697));
#6322=CARTESIAN_POINT('Ctrl Pts',(3.57089131441462,-1.28833000472427,-4.92709196714809));
#6323=CARTESIAN_POINT('Ctrl Pts',(3.52448166516577,-1.23290742648859,-4.93163328279849));
#6324=CARTESIAN_POINT('Ctrl Pts',(3.48675254618516,-1.18330844017394,-4.93539778804676));
#6325=CARTESIAN_POINT('Ctrl Pts',(3.39919089019986,-1.05626705578178,-4.9445465152989));
#6326=CARTESIAN_POINT('Ctrl Pts',(3.35228026933408,-0.97698931312293,-4.94983891668592));
#6327=CARTESIAN_POINT('Ctrl Pts',(3.25311619480361,-0.779402390041069,-4.96267537833802));
#6328=CARTESIAN_POINT('Ctrl Pts',(3.20656356209051,-0.658721982534789,-4.97025327754844));
#6329=CARTESIAN_POINT('Ctrl Pts',(3.16766022697015,-0.518816124761333,-4.97925591514562));
#6330=CARTESIAN_POINT('Ctrl Pts',(3.16351659099316,-0.503180194681899,-4.98026456673374));
#6331=CARTESIAN_POINT('Ctrl Pts',(3.15707891071831,-0.477637069939258,-4.98191719976237));
#6332=CARTESIAN_POINT('Ctrl Pts',(3.15466960846471,-0.467759485037016,-4.98255745585297));
#6333=CARTESIAN_POINT('Ctrl Pts',(3.15050021851563,-0.450079927691032,-4.98370571725798));
#6334=CARTESIAN_POINT('Ctrl Pts',(3.14871133108398,-0.442284921596935,-4.98421278243635));
#6335=CARTESIAN_POINT('Ctrl Pts',(3.14502351138985,-0.425760180928002,-4.98528948308725));
#6336=CARTESIAN_POINT('Ctrl Pts',(3.14313625776749,-0.41702804721845,-4.98585948152347));
#6337=CARTESIAN_POINT('Ctrl Pts',(3.13825134764445,-0.393667126727878,-4.9873873057125));
#6338=CARTESIAN_POINT('Ctrl Pts',(3.1353592409189,-0.379017089723568,-4.98834848135653));
#6339=CARTESIAN_POINT('Ctrl Pts',(3.12182138282397,-0.306143804023358,-4.993145722628));
#6340=CARTESIAN_POINT('Ctrl Pts',(3.11360720870425,-0.24750464213578,-4.99705805834837));
#6341=CARTESIAN_POINT('Ctrl Pts',(3.09701745954933,-0.0728196042003857,
-5.00887189309357));
#6342=CARTESIAN_POINT('Ctrl Pts',(3.09616900309937,0.0436810129057251,-5.01697136695062));
#6343=CARTESIAN_POINT('Ctrl Pts',(3.11363990879115,0.261370512183108,-5.03220192407051));
#6344=CARTESIAN_POINT('Ctrl Pts',(3.12961504059217,0.362396192732447,-5.03930375089956));
#6345=CARTESIAN_POINT('Ctrl Pts',(3.15703518181583,0.477630041467434,-5.0471582693509));
#6346=CARTESIAN_POINT('Ctrl Pts',(3.16100558520107,0.493451541969581,-5.04823098521159));
#6347=CARTESIAN_POINT('Ctrl Pts',(3.16687847548655,0.515694821989584,-5.04972933867866));
#6348=CARTESIAN_POINT('Ctrl Pts',(3.1686197812671,0.522157959002024,-5.05016353886671));
#6349=CARTESIAN_POINT('Ctrl Pts',(3.17160784005498,0.533030449615308,-5.05089184696418));
#6350=CARTESIAN_POINT('Ctrl Pts',(3.17283730196313,0.537444454071113,-5.05118693353936));
#6351=CARTESIAN_POINT('Ctrl Pts',(3.1753914786931,0.546493692024882,-5.05179063611881));
#6352=CARTESIAN_POINT('Ctrl Pts',(3.17671779487256,0.5511283898126,-5.05209915913269));
#6353=CARTESIAN_POINT('Ctrl Pts',(3.18015521981358,0.562977610470331,-5.05288632485509));
#6354=CARTESIAN_POINT('Ctrl Pts',(3.18229035364499,0.570185168845214,-5.05336360109104));
#6355=CARTESIAN_POINT('Ctrl Pts',(3.19126970718108,0.599879318977058,-5.05532422318489));
#6356=CARTESIAN_POINT('Ctrl Pts',(3.19847068057325,0.622257172053322,-5.0567882694558));
#6357=CARTESIAN_POINT('Ctrl Pts',(3.21874071946015,0.681628433729931,-5.06064926655386));
#6358=CARTESIAN_POINT('Ctrl Pts',(3.23250874331918,0.718373587059294,-5.06301445747872));
#6359=CARTESIAN_POINT('Ctrl Pts',(3.28324289446776,0.842502992402395,-5.07099527907893));
#6360=CARTESIAN_POINT('Ctrl Pts',(3.32535350892617,0.927647251040959,-5.07645855214757));
#6361=CARTESIAN_POINT('Ctrl Pts',(3.43959101262252,1.12234378590508,-5.08957745425663));
#6362=CARTESIAN_POINT('Ctrl Pts',(3.51675249593857,1.22840620137394,-5.09726287174244));
#6363=CARTESIAN_POINT('Ctrl Pts',(3.61456781561203,1.33831417118987,-5.10638892053515));
#6364=CARTESIAN_POINT('Ctrl Pts',(3.62554794010361,1.35035148636723,-5.10740536135711));
#6365=CARTESIAN_POINT('Ctrl Pts',(3.64368682446066,1.36975400418078,-5.10907245717445));
#6366=CARTESIAN_POINT('Ctrl Pts',(3.65075732207012,1.37720095165135,-5.10971939058417));
#6367=CARTESIAN_POINT('Ctrl Pts',(3.66350469653888,1.39042107874366,-5.11088079550017));
#6368=CARTESIAN_POINT('Ctrl Pts',(3.66915985602239,1.39621495318322,-5.11139432659713));
#6369=CARTESIAN_POINT('Ctrl Pts',(3.68122094243299,1.4084223145352,-5.11248606560021));
#6370=CARTESIAN_POINT('Ctrl Pts',(3.68763561171649,1.41482686821925,-5.11306464907469));
#6371=CARTESIAN_POINT('Ctrl Pts',(3.70492603614829,1.43185628105505,-5.11461887322415));
#6372=CARTESIAN_POINT('Ctrl Pts',(3.71587981704447,1.4424007211425,-5.11559795270281));
#6373=CARTESIAN_POINT('Ctrl Pts',(3.77152328685271,1.49475249209425,-5.12054497786874));
#6374=CARTESIAN_POINT('Ctrl Pts',(3.81799544058498,1.53460895886861,-5.12459343596775));
#6375=CARTESIAN_POINT('Ctrl Pts',(3.96908172653465,1.65257539009432,-5.13751048811448));
#6376=CARTESIAN_POINT('Ctrl Pts',(4.07956606839761,1.72259260882287,-5.1466369508837));
#6377=CARTESIAN_POINT('Ctrl Pts',(4.27857703879079,1.82289041387427,-5.16212226696692));
#6378=CARTESIAN_POINT('Ctrl Pts',(4.36387414234001,1.8586916851381,-5.16848442723695));
#6379=CARTESIAN_POINT('Ctrl Pts',(4.46166116029799,1.89195989236394,-5.17527070293879));
#6380=CARTESIAN_POINT('Ctrl Pts',(4.47199640601663,1.89538191702214,-5.17598174371719));
#6381=CARTESIAN_POINT('Ctrl Pts',(4.48769219062187,1.90043662213043,-5.17705165927343));
#6382=CARTESIAN_POINT('Ctrl Pts',(4.49303225058894,1.9021315502465,-5.1774139392048));
#6383=CARTESIAN_POINT('Ctrl Pts',(4.50266930301365,1.90514570544937,-5.17806453420173));
#6384=CARTESIAN_POINT('Ctrl Pts',(4.5069635931026,1.90647290175745,-5.17835329019095));
#6385=CARTESIAN_POINT('Ctrl Pts',(4.51130368123066,1.90779819853609,-5.17864398511427));
#6386=CARTESIAN_POINT('Ctrl Pts',(4.51134490418714,1.90781078498836,-5.17864674608481));
#6387=CARTESIAN_POINT('Ctrl Pts',(4.51142619629517,1.90783560272552,-5.1786521905442));
#6388=CARTESIAN_POINT('Ctrl Pts',(4.51146626542467,1.90784783408437,-5.17865487403729));
#6389=CARTESIAN_POINT('Ctrl Pts',(4.51154529592963,1.90787195593133,-5.17866016664289));
#6390=CARTESIAN_POINT('Ctrl Pts',(4.51158425730295,1.90788384649409,-5.17866277576058));
#6391=CARTESIAN_POINT('Ctrl Pts',(4.51166111600311,1.90790730031126,-5.17866792255817));
#6392=CARTESIAN_POINT('Ctrl Pts',(4.51169901329897,1.90791886362657,-5.17867046024098));
#6393=CARTESIAN_POINT('Ctrl Pts',(4.51177378521746,1.90794167578141,-5.17867546695405));
#6394=CARTESIAN_POINT('Ctrl Pts',(4.51181065982405,1.90795292468183,-5.1786779359879));
#6395=CARTESIAN_POINT('Ctrl Pts',(4.51188342566564,1.90797512019131,-5.17868280804843));
#6396=CARTESIAN_POINT('Ctrl Pts',(4.51191931687129,1.90798606685296,-5.17868521107751));
#6397=CARTESIAN_POINT('Ctrl Pts',(4.51199015315827,1.90800766942779,-5.17868995363527));
#6398=CARTESIAN_POINT('Ctrl Pts',(4.51202509823475,1.90801832539711,-5.1786922931677));
#6399=CARTESIAN_POINT('Ctrl Pts',(4.51209407772082,1.90803935757052,-5.17869691111814));
#6400=CARTESIAN_POINT('Ctrl Pts',(4.51212811210257,1.90804973382013,-5.1786991895381));
#6401=CARTESIAN_POINT('Ctrl Pts',(4.51219530386416,1.90807021697808,-5.17870368752863));
#6402=CARTESIAN_POINT('Ctrl Pts',(4.51222846122625,1.90808032393167,-5.1787059071016));
#6403=CARTESIAN_POINT('Ctrl Pts',(4.51229393094737,1.9081002784018,-5.17871028955084));
#6404=CARTESIAN_POINT('Ctrl Pts',(4.51232624330227,1.90811012596464,-5.17871245243019));
#6405=CARTESIAN_POINT('Ctrl Pts',(4.51239005356905,1.90812957110803,-5.17871672354777));
#6406=CARTESIAN_POINT('Ctrl Pts',(4.51242155143479,1.90813916871918,-5.17871883178607));
#6407=CARTESIAN_POINT('Ctrl Pts',(4.5124837616893,1.90815812291801,-5.17872299556973));
#6408=CARTESIAN_POINT('Ctrl Pts',(4.51251447408323,1.90816747954926,-5.17872505111839));
#6409=CARTESIAN_POINT('Ctrl Pts',(4.5125751410553,1.90818596034009,-5.17872911138295));
#6410=CARTESIAN_POINT('Ctrl Pts',(4.51260509563796,1.90819508454056,-5.17873111610192));
#6411=CARTESIAN_POINT('Ctrl Pts',(4.51266427340371,1.90821310863363,-5.17873507648332));
#6412=CARTESIAN_POINT('Ctrl Pts',(4.51269349656876,1.90822200855794,-5.17873703214715));
#6413=CARTESIAN_POINT('Ctrl Pts',(4.51275123664262,1.90823959186659,-5.17874089610871));
#6414=CARTESIAN_POINT('Ctrl Pts',(4.51277975355018,1.9082482752856,-5.17874280440882));
#6415=CARTESIAN_POINT('Ctrl Pts',(4.51814791843944,1.90988275389405,-5.17910202306494));
#6416=CARTESIAN_POINT('Ctrl Pts',(4.52349444223894,1.91148615363887,-5.17945806639703));
#6417=CARTESIAN_POINT('Ctrl Pts',(4.53934342743911,1.91616677929283,-5.18050859076488));
#6418=CARTESIAN_POINT('Ctrl Pts',(4.54986475541454,1.91918009847527,-5.18119960800947));
#6419=CARTESIAN_POINT('Ctrl Pts',(4.64731731655288,1.94622480219857,-5.1875458738251));
#6420=CARTESIAN_POINT('Ctrl Pts',(4.73577126136325,1.96442411363878,-5.19291108914789));
#6421=CARTESIAN_POINT('Ctrl Pts',(4.97084173553032,1.99637583227205,-5.20683902370581));
#6422=CARTESIAN_POINT('Ctrl Pts',(5.11825368088441,2.00001087643513,-5.21527525205736));
#6423=CARTESIAN_POINT('Ctrl Pts',(5.3070452282168,1.98377665772296,-5.22676186821689));
#6424=CARTESIAN_POINT('Ctrl Pts',(5.34923553970442,1.97878698884587,-5.22937010927931));
#6425=CARTESIAN_POINT('Ctrl Pts',(5.40512783787735,1.97035959218224,-5.23289576224414));
#6426=CARTESIAN_POINT('Ctrl Pts',(5.41900053741939,1.96811770315274,-5.23377662301283));
#6427=CARTESIAN_POINT('Ctrl Pts',(5.44160151179112,1.9642198096068,-5.23522165382061));
#6428=CARTESIAN_POINT('Ctrl Pts',(5.45034460428841,1.96265171847022,-5.23578309968515));
#6429=CARTESIAN_POINT('Ctrl Pts',(5.46721373009004,1.95950976892486,-5.23687122144608));
#6430=CARTESIAN_POINT('Ctrl Pts',(5.47534102704791,1.95794362306406,-5.23739764737598));
#6431=CARTESIAN_POINT('Ctrl Pts',(5.49424672746183,1.95417827668302,-5.23862742713321));
#6432=CARTESIAN_POINT('Ctrl Pts',(5.50501707229167,1.95194042305006,-5.23933197378369));
#6433=CARTESIAN_POINT('Ctrl Pts',(5.53967787618224,1.94443903150109,-5.24161241682866));
#6434=CARTESIAN_POINT('Ctrl Pts',(5.56348944002623,1.93882522784069,-5.24319920677025));
#6435=CARTESIAN_POINT('Ctrl Pts',(5.76469480781892,1.88746517394931,-5.25678539002971));
#6436=CARTESIAN_POINT('Ctrl Pts',(5.93508144129706,1.81792512317405,-5.26959192125343));
#6437=CARTESIAN_POINT('Ctrl Pts',(6.14096963814191,1.69868297205753,-5.28613388575147));
#6438=CARTESIAN_POINT('Ctrl Pts',(6.18724241698336,1.66927349769524,-5.28992086259104));
#6439=CARTESIAN_POINT('Ctrl Pts',(6.2322442180908,1.63799699450132,-5.29363746883395));
#6440=CARTESIAN_POINT('',(3.93347817078403,1.62253437445172,-5.29363746883395));
#6441=CARTESIAN_POINT('Origin',(5.09382715545311,0.,-5.29363746883395));
#6442=CARTESIAN_POINT('Ctrl Pts',(3.93347817078403,1.62253437445172,-5.29363746883395));
#6443=CARTESIAN_POINT('Ctrl Pts',(3.8753734702366,1.5809810296682,-5.28907786112167));
#6444=CARTESIAN_POINT('Ctrl Pts',(3.81946032609053,1.53627216112948,-5.28451825340938));
#6445=CARTESIAN_POINT('Ctrl Pts',(3.76608398691568,1.48866572503776,-5.2799586456971));
#6446=CARTESIAN_POINT('Ctrl Pts',(3.71089420556803,1.43944187718194,-5.27524412693162));
#6447=CARTESIAN_POINT('Ctrl Pts',(3.65841713885386,1.38712029687635,-5.27052960816615));
#6448=CARTESIAN_POINT('Ctrl Pts',(3.60899742177806,1.33203161542603,-5.26581508940068));
#6449=CARTESIAN_POINT('Ctrl Pts',(3.56123575882214,1.27879118444419,-5.26125874489691));
#6450=CARTESIAN_POINT('Ctrl Pts',(3.51632984488522,1.22296676941307,-5.25670240039315));
#6451=CARTESIAN_POINT('Ctrl Pts',(3.47455215491635,1.16489314322674,-5.25214605588938));
#6452=CARTESIAN_POINT('Ctrl Pts',(3.4327735996344,1.10681831420061,-5.24758961701313));
#6453=CARTESIAN_POINT('Ctrl Pts',(3.39412366375182,1.04649455185753,-5.24303317813688));
#6454=CARTESIAN_POINT('Ctrl Pts',(3.35883245938466,0.984287034921393,-5.23847673926063));
#6455=CARTESIAN_POINT('Ctrl Pts',(3.32353109970894,0.922061617306017,-5.23391898923494));
#6456=CARTESIAN_POINT('Ctrl Pts',(3.29159061787254,0.857951764582268,-5.22936123920926));
#6457=CARTESIAN_POINT('Ctrl Pts',(3.26319532059391,0.792347554864684,-5.22480348918357));
#6458=CARTESIAN_POINT('Ctrl Pts',(3.23478426638423,0.726706940491822,-5.22024321000131));
#6459=CARTESIAN_POINT('Ctrl Pts',(3.20992248861641,0.659570739210518,-5.21568293081904));
#6460=CARTESIAN_POINT('Ctrl Pts',(3.18874577409805,0.591348030278524,-5.21112265163678));
#6461=CARTESIAN_POINT('Ctrl Pts',(3.16753641797883,0.523020163465085,-5.20655534328043));
#6462=CARTESIAN_POINT('Ctrl Pts',(3.15002359695028,0.453602882957732,-5.20198803492408));
#6463=CARTESIAN_POINT('Ctrl Pts',(3.13629280128157,0.38351898875835,-5.19742072656773));
#6464=CARTESIAN_POINT('Ctrl Pts',(3.12254972380403,0.313372406495415,-5.19284933288308));
#6465=CARTESIAN_POINT('Ctrl Pts',(3.11259547387306,0.242558474210875,-5.18827793919843));
#6466=CARTESIAN_POINT('Ctrl Pts',(3.10646377784675,0.171506174375812,-5.18370654551377));
#6467=CARTESIAN_POINT('Ctrl Pts',(3.1003208348948,0.100323548456682,-5.179126766853));
#6468=CARTESIAN_POINT('Ctrl Pts',(3.09801445824188,0.0289021375374889,-5.17454698819222));
#6469=CARTESIAN_POINT('Ctrl Pts',(3.09952631099107,-0.0423285279449318,
-5.16996720953145));
#6470=CARTESIAN_POINT('Ctrl Pts',(3.09987370336958,-0.0586958562568392,
-5.16891487146288));
#6471=CARTESIAN_POINT('Ctrl Pts',(3.10042247643775,-0.0750531374033765,
-5.16786253339431));
#6472=CARTESIAN_POINT('Ctrl Pts',(3.10117202283689,-0.0913952129941374,
-5.16681019532573));
#6473=CARTESIAN_POINT('Ctrl Pts',(3.10431305765046,-0.159878002605746,-5.16240028752975));
#6474=CARTESIAN_POINT('Ctrl Pts',(3.11099626812022,-0.228362232762861,-5.15799037973377));
#6475=CARTESIAN_POINT('Ctrl Pts',(3.12122800980039,-0.296445902434433,-5.15358047193779));
#6476=CARTESIAN_POINT('Ctrl Pts',(3.13144268768317,-0.364416026828859,-5.14917791868373));
#6477=CARTESIAN_POINT('Ctrl Pts',(3.1451940865303,-0.43198642593221,-5.14477536542967));
#6478=CARTESIAN_POINT('Ctrl Pts',(3.16243659052121,-0.498756501904512,-5.14037281217561));
#6479=CARTESIAN_POINT('Ctrl Pts',(3.17965548824249,-0.56543516467969,-5.13597628634421));
#6480=CARTESIAN_POINT('Ctrl Pts',(3.20035587887727,-0.631315197845588,-5.1315797605128));
#6481=CARTESIAN_POINT('Ctrl Pts',(3.22444081749529,-0.696004512885265,-5.12718323468139));
#6482=CARTESIAN_POINT('Ctrl Pts',(3.24850784884,-0.760645731093032,-5.12278997768911));
#6483=CARTESIAN_POINT('Ctrl Pts',(3.27595426613844,-0.824097518387005,-5.11839672069683));
#6484=CARTESIAN_POINT('Ctrl Pts',(3.3066332883872,-0.885982868921297,-5.11400346370455));
#6485=CARTESIAN_POINT('Ctrl Pts',(3.33730044834284,-0.947844290982176,-5.10961190540077));
#6486=CARTESIAN_POINT('Ctrl Pts',(3.37119751199032,-1.00814002943846,-5.10522034709698));
#6487=CARTESIAN_POINT('Ctrl Pts',(3.40813033188671,-1.06651478260648,-5.1008287887932));
#6488=CARTESIAN_POINT('Ctrl Pts',(3.44506205012717,-1.12488779453478,-5.09643736148364));
#6489=CARTESIAN_POINT('Ctrl Pts',(3.48502907526759,-1.18133951304622,-5.09204593417409));
#6490=CARTESIAN_POINT('Ctrl Pts',(3.52779326149865,-1.23554255510922,-5.08765450686453));
#6491=CARTESIAN_POINT('Ctrl Pts',(3.57060072355836,-1.28980044871432,-5.08325863558743));
#6492=CARTESIAN_POINT('Ctrl Pts',(3.61621068605795,-1.34180472978312,-5.07886276431032));
#6493=CARTESIAN_POINT('Ctrl Pts',(3.66434462067253,-1.39126102700295,-5.07446689303322));
#6494=CARTESIAN_POINT('Ctrl Pts',(3.7125047053187,-1.44074419266277,-5.07006863358292));
#6495=CARTESIAN_POINT('Ctrl Pts',(3.7631911220563,-1.48767628083195,-5.06567037413261));
#6496=CARTESIAN_POINT('Ctrl Pts',(3.81609053451927,-1.53180177895985,-5.06127211468231));
#6497=CARTESIAN_POINT('Ctrl Pts',(3.86908438967676,-1.57600605548522,-5.05686600290521));
#6498=CARTESIAN_POINT('Ctrl Pts',(3.92429872536512,-1.61739344136932,-5.05245989112812));
#6499=CARTESIAN_POINT('Ctrl Pts',(3.98139012068197,-1.6557510097142,-5.04805377935102));
#6500=CARTESIAN_POINT('Ctrl Pts',(4.01624901224758,-1.67917139221202,-5.04536349350652));
#6501=CARTESIAN_POINT('Ctrl Pts',(4.05180715926841,-1.70146311100992,-5.04267320766202));
#6502=CARTESIAN_POINT('Ctrl Pts',(4.08798226477829,-1.72258631667715,-5.03998292181752));
#6503=CARTESIAN_POINT('Ctrl Pts',(4.14798585362447,-1.75762334366313,-5.03552054904992));
#6504=CARTESIAN_POINT('Ctrl Pts',(4.20993801918174,-1.78958901750203,-5.03105817628233));
#6505=CARTESIAN_POINT('Ctrl Pts',(4.27349218707037,-1.8182623853967,-5.02659580351474));
#6506=CARTESIAN_POINT('Ctrl Pts',(4.33695161079536,-1.84689300811272,-5.02214008308466));
#6507=CARTESIAN_POINT('Ctrl Pts',(4.40200785542346,-1.87224086854705,-5.01768436265459));
#6508=CARTESIAN_POINT('Ctrl Pts',(4.46828841563392,-1.89413010310417,-5.01322864222452));
#6509=CARTESIAN_POINT('Ctrl Pts',(4.53449120533457,-1.9159936538571,-5.00877814992844));
#6510=CARTESIAN_POINT('Ctrl Pts',(4.60191499636852,-1.9344064878101,-5.00432765763235));
#6511=CARTESIAN_POINT('Ctrl Pts',(4.67016754203147,-1.94924090210918,-4.99987716533626));
#6512=CARTESIAN_POINT('Ctrl Pts',(4.73837720656159,-1.96406599636777,-4.99542946915788));
#6513=CARTESIAN_POINT('Ctrl Pts',(4.80741411742909,-1.97531702834745,-4.9909817729795));
#6514=CARTESIAN_POINT('Ctrl Pts',(4.87687255648581,-1.98291660553008,-4.98653407680112));
#6515=CARTESIAN_POINT('Ctrl Pts',(4.94631070428743,-1.9905139626087,-4.98208767995136));
#6516=CARTESIAN_POINT('Ctrl Pts',(5.01616965151141,-1.99446192986204,-4.9776412831016));
#6517=CARTESIAN_POINT('Ctrl Pts',(5.08603695885747,-1.99473478822048,-4.97319488625183));
#6518=CARTESIAN_POINT('Ctrl Pts',(5.15590733943729,-1.99500765858106,-4.96874829381965));
#6519=CARTESIAN_POINT('Ctrl Pts',(5.22578559346422,-1.99160509957665,-4.96430170138747));
#6520=CARTESIAN_POINT('Ctrl Pts',(5.29525943375409,-1.98455350135956,-4.95985510895529));
#6521=CARTESIAN_POINT('Ctrl Pts',(5.36480480623327,-1.97749464262172,-4.95540393818844));
#6522=CARTESIAN_POINT('Ctrl Pts',(5.43394444802563,-1.96677929490471,-4.95095276742159));
#6523=CARTESIAN_POINT('Ctrl Pts',(5.50227230557564,-1.952485626539,-4.94650159665474));
#6524=CARTESIAN_POINT('Ctrl Pts',(5.5706393841556,-1.93818375343198,-4.94204787086117));
#6525=CARTESIAN_POINT('Ctrl Pts',(5.63819327947979,-1.92029959530799,-4.93759414506759));
#6526=CARTESIAN_POINT('Ctrl Pts',(5.70454189775908,-1.89896157571188,-4.93314041927402));
#6527=CARTESIAN_POINT('Ctrl Pts',(5.77100263307362,-1.87758749876361,-4.92867916749807));
#6528=CARTESIAN_POINT('Ctrl Pts',(5.83625357025589,-1.85274808319428,-4.92421791572212));
#6529=CARTESIAN_POINT('Ctrl Pts',(5.89992218843671,-1.82462005916278,-4.91975666394617));
#6530=CARTESIAN_POINT('Ctrl Pts',(5.93132425264772,-1.81074700769718,-4.91755632540055));
#6531=CARTESIAN_POINT('Ctrl Pts',(5.96234177917846,-1.79607469034805,-4.91535598685492));
#6532=CARTESIAN_POINT('Ctrl Pts',(5.99293249024594,-1.78062830468548,-4.9131556483093));
#6533=CARTESIAN_POINT('Ctrl Pts',(6.05498318767251,-1.74929660399475,-4.90869244570412));
#6534=CARTESIAN_POINT('Ctrl Pts',(6.11551123781745,-1.7146584687059,-4.90422924309895));
#6535=CARTESIAN_POINT('Ctrl Pts',(6.17414294624894,-1.67688561167934,-4.89976604049377));
#6536=CARTESIAN_POINT('Ctrl Pts',(6.23268933239712,-1.63916772262991,-4.89530933284921));
#6537=CARTESIAN_POINT('Ctrl Pts',(6.28934444840992,-1.59832442910512,-4.89085262520466));
#6538=CARTESIAN_POINT('Ctrl Pts',(6.34375847328421,-1.55457365962665,-4.8863959175601));
#6539=CARTESIAN_POINT('Ctrl Pts',(6.39811147169727,-1.5108719575466,-4.88194420820591));
#6540=CARTESIAN_POINT('Ctrl Pts',(6.45022799340618,-1.46426956035437,-4.87749249885171));
#6541=CARTESIAN_POINT('Ctrl Pts',(6.49978800489005,-1.41502708537701,-4.87304078949752));
#6542=CARTESIAN_POINT('Ctrl Pts',(6.5493184697692,-1.36581396769599,-4.86859173415596));
#6543=CARTESIAN_POINT('Ctrl Pts',(6.59629510362083,-1.31396423782261,-4.8641426788144));
#6544=CARTESIAN_POINT('Ctrl Pts',(6.64043287929411,-1.25977708245636,-4.85969362347284));
#6545=CARTESIAN_POINT('Ctrl Pts',(6.68455915814744,-1.20560404152971,-4.85524572700229));
#6546=CARTESIAN_POINT('Ctrl Pts',(6.72584773954907,-1.14909516160501,-4.85079783053173));
#6547=CARTESIAN_POINT('Ctrl Pts',(6.76405340047442,-1.0905832627278,-4.84634993406117));
#6548=CARTESIAN_POINT('Ctrl Pts',(6.80226193495501,-1.03206696300607,-4.8419017030518));
#6549=CARTESIAN_POINT('Ctrl Pts',(6.83738682424129,-0.971547754435772,-4.83745347204244));
#6550=CARTESIAN_POINT('Ctrl Pts',(6.86922673464641,-0.909386549658754,-4.83300524103307));
#6551=CARTESIAN_POINT('Ctrl Pts',(6.90110085428473,-0.847158558037083,-4.82855223078375));
#6552=CARTESIAN_POINT('Ctrl Pts',(6.92968272841109,-0.783285483644192,-4.82409922053443));
#6553=CARTESIAN_POINT('Ctrl Pts',(6.95481791846453,-0.718151058264328,-4.81964621028511));
#6554=CARTESIAN_POINT('Ctrl Pts',(6.97996819188313,-0.652977546395753,-4.81519052783083));
#6555=CARTESIAN_POINT('Ctrl Pts',(7.00166751287834,-0.586541640042753,-4.81073484537655));
#6556=CARTESIAN_POINT('Ctrl Pts',(7.01981125049916,-0.519242552310239,-4.80627916292227));
#6557=CARTESIAN_POINT('Ctrl Pts',(7.03798629550514,-0.451827338644638,-4.80181579209805));
#6558=CARTESIAN_POINT('Ctrl Pts',(7.05259340871707,-0.38354644677953,-4.79735242127384));
#6559=CARTESIAN_POINT('Ctrl Pts',(7.06357916381499,-0.314808811907094,-4.79288905044963));
#6560=CARTESIAN_POINT('Ctrl Pts',(7.06896179044333,-0.281129832125018,-4.79070215856678));
#6561=CARTESIAN_POINT('Ctrl Pts',(7.07347584890439,-0.247341274937136,-4.78851526668393));
#6562=CARTESIAN_POINT('Ctrl Pts',(7.07711961959692,-0.213491367905988,-4.78632837480109));
#6563=CARTESIAN_POINT('Ctrl Pts',(7.08469843048945,-0.143085717889515,-4.78177977901363));
#6564=CARTESIAN_POINT('Ctrl Pts',(7.08852952589302,-0.0722653690654421,
-4.77723118322618));
#6565=CARTESIAN_POINT('Ctrl Pts',(7.08857671412439,-0.00132690645140175,
-4.77268258743872));
#6566=CARTESIAN_POINT('Origin',(5.09382715545311,0.,-6.77268258743872));
#6567=CARTESIAN_POINT('',(7.08797499842338,0.00179838134685419,-3.81459200118186));
#6568=CARTESIAN_POINT('',(7.08573545875024,-0.000892991754021077,-3.97270035107971));
#6569=CARTESIAN_POINT('',(7.08857715545311,8.3550772080578E-14,-6.77268258743872));
#6570=CARTESIAN_POINT('Ctrl Pts',(7.08857636722083,0.00177331668636056,
-3.81424619860756));
#6571=CARTESIAN_POINT('Ctrl Pts',(7.08868493718784,-0.120353688486413,-3.82134987712496));
#6572=CARTESIAN_POINT('Ctrl Pts',(7.0775782485065,-0.242220620626991,-3.82853578695394));
#6573=CARTESIAN_POINT('Ctrl Pts',(7.0528391367539,-0.376162548922293,-3.83696215330685));
#6574=CARTESIAN_POINT('Ctrl Pts',(7.0501324847327,-0.389994421885436,-3.83783843504427));
#6575=CARTESIAN_POINT('Ctrl Pts',(7.04537824197903,-0.412994111282967,-3.83930629344508));
#6576=CARTESIAN_POINT('Ctrl Pts',(7.04341203446348,-0.422178367559234,-3.83989531658134));
#6577=CARTESIAN_POINT('Ctrl Pts',(7.03942356063078,-0.440186479087877,-3.84105608047177));
#6578=CARTESIAN_POINT('Ctrl Pts',(7.03740594259745,-0.449011137968301,-3.84162766169996));
#6579=CARTESIAN_POINT('Ctrl Pts',(7.03348124127359,-0.465654764271371,-3.84271104446087));
#6580=CARTESIAN_POINT('Ctrl Pts',(7.0315867624428,-0.473476540652351,-3.84322243317116));
#6581=CARTESIAN_POINT('Ctrl Pts',(7.02719449821022,-0.491142988340545,-3.8443826542762));
#6582=CARTESIAN_POINT('Ctrl Pts',(7.02466876780043,-0.50098041756057,-3.8450323725717));
#6583=CARTESIAN_POINT('Ctrl Pts',(7.01796762726499,-0.526276941322821,-3.84671273033162));
#6584=CARTESIAN_POINT('Ctrl Pts',(7.01368106020594,-0.541705578630841,-3.84774691855927));
#6585=CARTESIAN_POINT('Ctrl Pts',(6.98127167752794,-0.653137131235577,-3.85528557673982));
#6586=CARTESIAN_POINT('Ctrl Pts',(6.94615230061261,-0.746941140064223,-3.8620174191873));
#6587=CARTESIAN_POINT('Ctrl Pts',(6.87049712102965,-0.910436155184257,-3.87441783100382));
#6588=CARTESIAN_POINT('Ctrl Pts',(6.83249001261459,-0.981071208680531,-3.88001811585327));
#6589=CARTESIAN_POINT('Ctrl Pts',(6.74611470559416,-1.12073304743609,-3.89145471180277));
#6590=CARTESIAN_POINT('Ctrl Pts',(6.69740925624548,-1.18937950939001,-3.89727782484544));
#6591=CARTESIAN_POINT('Ctrl Pts',(6.63013691080471,-1.27251805247618,-3.90442338933991));
#6592=CARTESIAN_POINT('Ctrl Pts',(6.61545624457557,-1.29003677492584,-3.90593450432855));
#6593=CARTESIAN_POINT('Ctrl Pts',(6.59679140359883,-1.31154780974618,-3.90779278355947));
#6594=CARTESIAN_POINT('Ctrl Pts',(6.59308780056581,-1.31577988595263,-3.90815851825653));
#6595=CARTESIAN_POINT('Ctrl Pts',(6.58587134929426,-1.32395603410954,-3.90886526900823));
#6596=CARTESIAN_POINT('Ctrl Pts',(6.58236064031558,-1.32790192508087,-3.90920643186956));
#6597=CARTESIAN_POINT('Ctrl Pts',(6.57582655771295,-1.33518748762305,-3.90983641143045));
#6598=CARTESIAN_POINT('Ctrl Pts',(6.57280756088526,-1.33853084252206,-3.91012552783963));
#6599=CARTESIAN_POINT('Ctrl Pts',(6.56590189791195,-1.34612655489895,-3.91078243988307));
#6600=CARTESIAN_POINT('Ctrl Pts',(6.5620081225761,-1.35037231864342,-3.91114969484924));
#6601=CARTESIAN_POINT('Ctrl Pts',(6.55179519415034,-1.36141207868538,-3.91210497481531));
#6602=CARTESIAN_POINT('Ctrl Pts',(6.54544685250411,-1.3681790499666,-3.9126908759351));
#6603=CARTESIAN_POINT('Ctrl Pts',(6.50112739431156,-1.41476533167554,-3.91672895200675));
#6604=CARTESIAN_POINT('Ctrl Pts',(6.46156648239265,-1.45304687488431,-3.92007047626247));
#6605=CARTESIAN_POINT('Ctrl Pts',(6.38265470622991,-1.52332373244278,-3.92636966106398));
#6606=CARTESIAN_POINT('Ctrl Pts',(6.34356969428608,-1.55554995555016,-3.92933438178092));
#6607=CARTESIAN_POINT('Ctrl Pts',(6.20622524192424,-1.6602709941878,-3.9393916918384));
#6608=CARTESIAN_POINT('Ctrl Pts',(6.10256740660566,-1.7252161735282,-3.94640263768227));
#6609=CARTESIAN_POINT('Ctrl Pts',(5.94116771046996,-1.80679172218707,-3.95722480054487));
#6610=CARTESIAN_POINT('Ctrl Pts',(5.88756805845946,-1.83097152842719,-3.96080133028954));
#6611=CARTESIAN_POINT('Ctrl Pts',(5.81914381043214,-1.85826943915055,-3.96538605804275));
#6612=CARTESIAN_POINT('Ctrl Pts',(5.80524382536161,-1.86363512022709,-3.96631829902992));
#6613=CARTESIAN_POINT('Ctrl Pts',(5.78272865540576,-1.87203784686826,-3.96783034836368));
#6614=CARTESIAN_POINT('Ctrl Pts',(5.77415027143917,-1.87517237344433,-3.96840691052599));
#6615=CARTESIAN_POINT('Ctrl Pts',(5.7579836003182,-1.8809541103729,-3.96949449668728));
#6616=CARTESIAN_POINT('Ctrl Pts',(5.75040022957682,-1.88361459535506,-3.97000506918895));
#6617=CARTESIAN_POINT('Ctrl Pts',(5.73331489358926,-1.88949295722637,-3.97115641524462));
#6618=CARTESIAN_POINT('Ctrl Pts',(5.72380436832726,-1.89268510530384,-3.97179802032093));
#6619=CARTESIAN_POINT('Ctrl Pts',(5.69944211943663,-1.9006581763267,-3.97344355688786));
#6620=CARTESIAN_POINT('Ctrl Pts',(5.68455786463766,-1.90533676661088,-3.97445079471311));
#6621=CARTESIAN_POINT('Ctrl Pts',(5.58632702583627,-1.93495216274059,-3.98111194071517));
#6622=CARTESIAN_POINT('Ctrl Pts',(5.50149138906808,-1.95458492288619,-3.98693566383776));
#6623=CARTESIAN_POINT('Ctrl Pts',(5.27090091917171,-1.99228165763517,-4.00292625774647));
#6624=CARTESIAN_POINT('Ctrl Pts',(5.123990446511,-1.99990687132354,-4.01331056366706));
#6625=CARTESIAN_POINT('Ctrl Pts',(4.92726552521078,-1.98842267231143,-4.02678734633476));
#6626=CARTESIAN_POINT('Ctrl Pts',(4.8770778572172,-1.98357964055613,-4.03018296403609));
#6627=CARTESIAN_POINT('Ctrl Pts',(4.81763726118323,-1.97556025633291,-4.03411413998269));
#6628=CARTESIAN_POINT('Ctrl Pts',(4.80816039167025,-1.97421217019396,-4.03473813676925));
#6629=CARTESIAN_POINT('Ctrl Pts',(4.79348107021089,-1.97201611750034,-4.03570000937651));
#6630=CARTESIAN_POINT('Ctrl Pts',(4.78827180894577,-1.97121568337227,-4.03604043474387));
#6631=CARTESIAN_POINT('Ctrl Pts',(4.77861426088005,-1.96969253993504,-4.03666978051929));
#6632=CARTESIAN_POINT('Ctrl Pts',(4.77416527832216,-1.96897540759155,-4.03695899494));
#6633=CARTESIAN_POINT('Ctrl Pts',(4.76401797969515,-1.96730446261442,-4.03761705428538));
#6634=CARTESIAN_POINT('Ctrl Pts',(4.75832135502093,-1.96634096761489,-4.03798535124291));
#6635=CARTESIAN_POINT('Ctrl Pts',(4.74343391393133,-1.96375640927986,-4.03894507509495));
#6636=CARTESIAN_POINT('Ctrl Pts',(4.73425002332634,-1.96209555135703,-4.0395343463408));
#6637=CARTESIAN_POINT('Ctrl Pts',(4.66973361276343,-1.94995989640804,-4.04365658295084));
#6638=CARTESIAN_POINT('Ctrl Pts',(4.61484932978633,-1.93720944384359,-4.0470736057074));
#6639=CARTESIAN_POINT('Ctrl Pts',(4.40425669863946,-1.87878568108783,-4.06008933401293));
#6640=CARTESIAN_POINT('Ctrl Pts',(4.25381105548481,-1.81651348921816,-4.06923032570495));
#6641=CARTESIAN_POINT('Ctrl Pts',(4.05395446586769,-1.70359140747278,-4.08289707375988));
#6642=CARTESIAN_POINT('Ctrl Pts',(3.99706650806883,-1.66753517257291,-4.08697697801182));
#6643=CARTESIAN_POINT('Ctrl Pts',(3.92938752943551,-1.61967615849919,-4.09213331696542));
#6644=CARTESIAN_POINT('Ctrl Pts',(3.91676766747666,-1.61052831120532,-4.09310832881417));
#6645=CARTESIAN_POINT('Ctrl Pts',(3.89693642513926,-1.59579550723166,-4.09466278238691));
#6646=CARTESIAN_POINT('Ctrl Pts',(3.88965375041438,-1.59030724306958,-4.09523848243564));
#6647=CARTESIAN_POINT('Ctrl Pts',(3.87602227143736,-1.57988716475571,-4.09632537556468));
#6648=CARTESIAN_POINT('Ctrl Pts',(3.86966513234895,-1.57496651614995,-4.09683612410842));
#6649=CARTESIAN_POINT('Ctrl Pts',(3.85542426677458,-1.5638052768759,-4.09798911518404));
#6650=CARTESIAN_POINT('Ctrl Pts',(3.84755767758726,-1.55754327102538,-4.09863219886563));
#6651=CARTESIAN_POINT('Ctrl Pts',(3.82754888121719,-1.54136712448305,-4.10028397909205));
#6652=CARTESIAN_POINT('Ctrl Pts',(3.81547576639889,-1.53136898987631,-4.10129602423558));
#6653=CARTESIAN_POINT('Ctrl Pts',(3.73532588951009,-1.4633859701508,-4.10812018908574));
#6654=CARTESIAN_POINT('Ctrl Pts',(3.67110615960361,-1.4010300534179,-4.11411216139587));
#6655=CARTESIAN_POINT('Ctrl Pts',(3.52400899548458,-1.23762591005276,-4.12917603371625));
#6656=CARTESIAN_POINT('Ctrl Pts',(3.44645445508747,-1.13234580086618,-4.13837704949277));
#6657=CARTESIAN_POINT('Ctrl Pts',(3.34745233602156,-0.96601574092247,-4.15170837516356));
#6658=CARTESIAN_POINT('Ctrl Pts',(3.31775838737324,-0.910270751724883,-4.15599226510809));
#6659=CARTESIAN_POINT('Ctrl Pts',(3.28643662159656,-0.844078775114153,-4.1607966931851));
#6660=CARTESIAN_POINT('Ctrl Pts',(3.28218694873499,-0.834918733842127,-4.16145545305156));
#6661=CARTESIAN_POINT('Ctrl Pts',(3.27577877584355,-0.820826793237541,-4.16245913091229));
#6662=CARTESIAN_POINT('Ctrl Pts',(3.27357045047088,-0.815917927681905,-4.16280695353903));
#6663=CARTESIAN_POINT('Ctrl Pts',(3.26955379137893,-0.806891861208777,-4.16344311837032));
#6664=CARTESIAN_POINT('Ctrl Pts',(3.26773951123744,-0.80277749034145,-4.16373180931219));
#6665=CARTESIAN_POINT('Ctrl Pts',(3.26368424215999,-0.793496185649858,-4.16438015754031));
#6666=CARTESIAN_POINT('Ctrl Pts',(3.26145121594805,-0.788325883062689,-4.16473933246207));
#6667=CARTESIAN_POINT('Ctrl Pts',(3.25494093675585,-0.773074994649688,-4.16579311955614));
#6668=CARTESIAN_POINT('Ctrl Pts',(3.25072467741744,-0.762968374747399,-4.16648418196291));
#6669=CARTESIAN_POINT('Ctrl Pts',(3.21018688627579,-0.663499552197041,-4.17321933987693));
#6670=CARTESIAN_POINT('Ctrl Pts',(3.18030430087733,-0.571635951841423,-4.17892031083755));
#6671=CARTESIAN_POINT('Ctrl Pts',(3.12644801056572,-0.353415784629972,-4.19203644737749));
#6672=CARTESIAN_POINT('Ctrl Pts',(3.10779738484874,-0.226203569255492,-4.19938133297649));
#6673=CARTESIAN_POINT('Ctrl Pts',(3.09850310754975,-0.0374104867927232,
-4.21068151259365));
#6674=CARTESIAN_POINT('Ctrl Pts',(3.09828944129431,0.0233613286147556,-4.21437541613127));
#6675=CARTESIAN_POINT('Ctrl Pts',(3.10148552692239,0.0991515865623322,-4.21909717287567));
#6676=CARTESIAN_POINT('Ctrl Pts',(3.10229435119605,0.114250915461581,-4.22004349623843));
#6677=CARTESIAN_POINT('Ctrl Pts',(3.10385933329893,0.138336244660656,-4.2215626038634));
#6678=CARTESIAN_POINT('Ctrl Pts',(3.10450490849791,0.14732903061136,-4.22213193519071));
#6679=CARTESIAN_POINT('Ctrl Pts',(3.10584248378942,0.164345241550075,-4.22321341087904));
#6680=CARTESIAN_POINT('Ctrl Pts',(3.10652215277935,0.172369476507214,-4.22372515968712));
#6681=CARTESIAN_POINT('Ctrl Pts',(3.10817402036281,0.190561032868495,-4.22488943462558));
#6682=CARTESIAN_POINT('Ctrl Pts',(3.10917575155063,0.200725381397563,-4.22554287201069));
#6683=CARTESIAN_POINT('Ctrl Pts',(3.11196856105278,0.226994824268064,-4.22723939005901));
#6684=CARTESIAN_POINT('Ctrl Pts',(3.11387787646451,0.243086333343761,-4.22828613567068));
#6685=CARTESIAN_POINT('Ctrl Pts',(3.13290023444264,0.388264453519185,-4.23780011921221));
#6686=CARTESIAN_POINT('Ctrl Pts',(3.16241581569613,0.515385773439488,-4.24666487721178));
#6687=CARTESIAN_POINT('Ctrl Pts',(3.23394076493474,0.727006276628773,-4.2621831004046));
#6688=CARTESIAN_POINT('Ctrl Pts',(3.26993821661244,0.813108287092982,-4.26872232569067));
#6689=CARTESIAN_POINT('Ctrl Pts',(3.33826630146429,0.948944690767107,-4.27917225756356));
#6690=CARTESIAN_POINT('Ctrl Pts',(3.36702388002236,1.00032084947295,-4.28315640945874));
#6691=CARTESIAN_POINT('Ctrl Pts',(3.40324799144324,1.05880520180743,-4.28766857034937));
#6692=CARTESIAN_POINT('Ctrl Pts',(3.40854518979459,1.06721650623256,-4.28831691433583));
#6693=CARTESIAN_POINT('Ctrl Pts',(3.41678921282733,1.08009254673717,-4.28930804957806));
#6694=CARTESIAN_POINT('Ctrl Pts',(3.4196914003144,1.08458547173938,-4.28965363760164));
#6695=CARTESIAN_POINT('Ctrl Pts',(3.42506764562894,1.09283553042148,-4.29028766654735));
#6696=CARTESIAN_POINT('Ctrl Pts',(3.42753633296724,1.09659595741381,-4.29057643997769));
#6697=CARTESIAN_POINT('Ctrl Pts',(3.4331465399791,1.10507901357269,-4.29122740153915));
#6698=CARTESIAN_POINT('Ctrl Pts',(3.43629549019093,1.1097966090267,-4.29158908898623));
#6699=CARTESIAN_POINT('Ctrl Pts',(3.44448421312517,1.12195193196274,-4.29252034520933));
#6700=CARTESIAN_POINT('Ctrl Pts',(3.44955425250108,1.12936925173042,-4.29308796102699));
#6701=CARTESIAN_POINT('Ctrl Pts',(3.4825895103442,1.17700481783655,-4.29673087141259));
#6702=CARTESIAN_POINT('Ctrl Pts',(3.5119805100421,1.21621920137834,-4.29971861923559));
#6703=CARTESIAN_POINT('Ctrl Pts',(3.64916115070864,1.38585166332398,-4.31278605982088));
#6704=CARTESIAN_POINT('Ctrl Pts',(3.77183710688056,1.5033278697646,-4.32228755490991));
#6705=CARTESIAN_POINT('Ctrl Pts',(3.96282247149054,1.64454420090413,-4.33642005677532));
#6706=CARTESIAN_POINT('Ctrl Pts',(4.01981463453745,1.68231770048992,-4.34055964339273));
#6707=CARTESIAN_POINT('Ctrl Pts',(4.09210227260022,1.72505647156196,-4.3457830575649));
#6708=CARTESIAN_POINT('Ctrl Pts',(4.10566921889857,1.73286365347448,-4.3467621500912));
#6709=CARTESIAN_POINT('Ctrl Pts',(4.12729559522146,1.74497212682861,-4.34832160300116));
#6710=CARTESIAN_POINT('Ctrl Pts',(4.13529528864739,1.7493792145158,-4.34889817917964));
#6711=CARTESIAN_POINT('Ctrl Pts',(4.15039056410396,1.75756068176564,-4.34998579424775));
#6712=CARTESIAN_POINT('Ctrl Pts',(4.15747926133873,1.76134743026092,-4.35049638164129));
#6713=CARTESIAN_POINT('Ctrl Pts',(4.1734678037457,1.76976463765027,-4.35164776450256));
#6714=CARTESIAN_POINT('Ctrl Pts',(4.18238003623957,1.77437097354945,-4.3522893915366));
#6715=CARTESIAN_POINT('Ctrl Pts',(4.20524093135888,1.78596907286016,-4.35393499202639));
#6716=CARTESIAN_POINT('Ctrl Pts',(4.21923736567524,1.79286465847605,-4.35494227196329));
#6717=CARTESIAN_POINT('Ctrl Pts',(4.31162263322291,1.8370406140559,-4.36159082484642));
#6718=CARTESIAN_POINT('Ctrl Pts',(4.39228216209262,1.86932959433386,-4.3674010995762));
#6719=CARTESIAN_POINT('Ctrl Pts',(4.60097563057918,1.9374591449058,-4.38242403563893));
#6720=CARTESIAN_POINT('Ctrl Pts',(4.73095965921986,1.965953754757,-4.3917883529302));
#6721=CARTESIAN_POINT('Ctrl Pts',(4.92590347328156,1.98868418719369,-4.40530812282914));
#6722=CARTESIAN_POINT('Ctrl Pts',(4.98932484977301,1.99302386922152,-4.4096206742469));
#6723=CARTESIAN_POINT('Ctrl Pts',(5.06296160025615,1.99453682379001,-4.4144530046761));
#6724=CARTESIAN_POINT('Ctrl Pts',(5.07307359673255,1.9946676725813,-4.41511275463619));
#6725=CARTESIAN_POINT('Ctrl Pts',(5.088572611292,1.9947503513828,-4.41611765195087));
#6726=CARTESIAN_POINT('Ctrl Pts',(5.09395899178952,1.99475726815225,-4.41646571376282));
#6727=CARTESIAN_POINT('Ctrl Pts',(5.10384442531742,1.99472992109081,-4.41710226978938));
#6728=CARTESIAN_POINT('Ctrl Pts',(5.10834332566282,1.99470225481539,-4.41739111313872));
#6729=CARTESIAN_POINT('Ctrl Pts',(5.11847566830532,1.99460566321285,-4.41803973591781));
#6730=CARTESIAN_POINT('Ctrl Pts',(5.12410892732,1.99452809382701,-4.41839903324672));
#6731=CARTESIAN_POINT('Ctrl Pts',(5.14068631937358,1.9942295758479,-4.41945268718569));
#6732=CARTESIAN_POINT('Ctrl Pts',(5.15162925705423,1.99394240443241,-4.42014350154778));
#6733=CARTESIAN_POINT('Ctrl Pts',(5.25327424289737,1.99043746697274,-4.42652099039321));
#6734=CARTESIAN_POINT('Ctrl Pts',(5.34367229657635,1.9811225154274,-4.43190471483805));
#6735=CARTESIAN_POINT('Ctrl Pts',(5.54777118497731,1.94589212340713,-4.44401492948166));
#6736=CARTESIAN_POINT('Ctrl Pts',(5.66045713842258,1.91611367525903,-4.4506785048057));
#6737=CARTESIAN_POINT('Ctrl Pts',(5.84171755960184,1.85081434792718,-4.46209033508492));
#6738=CARTESIAN_POINT('Ctrl Pts',(5.91197809981789,1.82084619297313,-4.4666960616515));
#6739=CARTESIAN_POINT('Ctrl Pts',(5.99479658747012,1.77975895382683,-4.4724429589768));
#6740=CARTESIAN_POINT('Ctrl Pts',(6.00916133940246,1.77241393554925,-4.47345165386652));
#6741=CARTESIAN_POINT('Ctrl Pts',(6.031610821903,1.76058931737076,-4.47504763724565));
#6742=CARTESIAN_POINT('Ctrl Pts',(6.03975641510934,1.75622628969103,-4.47563083371797));
#6743=CARTESIAN_POINT('Ctrl Pts',(6.05492279210039,1.74796659327411,-4.47672454149934));
#6744=CARTESIAN_POINT('Ctrl Pts',(6.06195095616856,1.74408381031365,-4.47723455267584));
#6745=CARTESIAN_POINT('Ctrl Pts',(6.07758496186762,1.73532302304659,-4.47837628555783));
#6746=CARTESIAN_POINT('Ctrl Pts',(6.08617829904213,1.73042324822964,-4.47900877606706));
#6747=CARTESIAN_POINT('Ctrl Pts',(6.10782798142887,1.71786466512814,-4.48061494645639));
#6748=CARTESIAN_POINT('Ctrl Pts',(6.12083406796983,1.7101208915003,-4.48159166463867));
#6749=CARTESIAN_POINT('Ctrl Pts',(6.19852213728233,1.66265983516997,-4.48749845659424));
#6750=CARTESIAN_POINT('Ctrl Pts',(6.26097462679387,1.61942985221343,-4.49255628981042));
#6751=CARTESIAN_POINT('Ctrl Pts',(6.43330008936526,1.48499045910724,-4.50742883549091));
#6752=CARTESIAN_POINT('Ctrl Pts',(6.53604904064144,1.38541491083227,-4.51750004466973));
#6753=CARTESIAN_POINT('Ctrl Pts',(6.66910944272399,1.22547536809944,-4.53184440186276));
#6754=CARTESIAN_POINT('Ctrl Pts',(6.70844069098723,1.17317054895337,-4.53628844546908));
#6755=CARTESIAN_POINT('Ctrl Pts',(6.75084211033075,1.1106000704371,-4.54124810129733));
#6756=CARTESIAN_POINT('Ctrl Pts',(6.75648530422564,1.10213382487608,-4.5419119406784));
#6757=CARTESIAN_POINT('Ctrl Pts',(6.76502372598777,1.08910914804173,-4.54292173403489));
#6758=CARTESIAN_POINT('Ctrl Pts',(6.76796553514449,1.08458167097817,-4.54327064582244));
#6759=CARTESIAN_POINT('Ctrl Pts',(6.77332205535212,1.07626420417809,-4.54390771528552));
#6760=CARTESIAN_POINT('Ctrl Pts',(6.77574234410805,1.07247799745834,-4.54419623095214));
#6761=CARTESIAN_POINT('Ctrl Pts',(6.78115401660499,1.06394880909253,-4.54484285365857));
#6762=CARTESIAN_POINT('Ctrl Pts',(6.78413820345533,1.05920138197598,-4.54520048849706));
#6763=CARTESIAN_POINT('Ctrl Pts',(6.79174440372774,1.046986961271,-4.5461149607564));
#6764=CARTESIAN_POINT('Ctrl Pts',(6.79633725607806,1.03950182442264,-4.54666995626584));
#6765=CARTESIAN_POINT('Ctrl Pts',(6.8242986707766,0.993249637249924,-4.55006783406308));
#6766=CARTESIAN_POINT('Ctrl Pts',(6.84639343582795,0.953723565624938,-4.55283600584275));
#6767=CARTESIAN_POINT('Ctrl Pts',(6.91835306494699,0.814030984313544,-4.56227756185806));
#6768=CARTESIAN_POINT('Ctrl Pts',(6.96112787857238,0.710445508161588,-4.56869742606057));
#6769=CARTESIAN_POINT('Ctrl Pts',(6.99966731673572,0.589100303223355,-4.57610185468638));
#6770=CARTESIAN_POINT('Ctrl Pts',(7.00416936418842,0.574333115412954,-4.57700085377444));
#6771=CARTESIAN_POINT('Ctrl Pts',(7.03938958154149,0.453808827565126,-4.58432928193687));
#6772=CARTESIAN_POINT('Ctrl Pts',(7.06146908121588,0.345740020740353,-4.59085955017007));
#6773=CARTESIAN_POINT('Ctrl Pts',(7.07643856747226,0.220322586196322,-4.59869211625329));
#6774=CARTESIAN_POINT('Ctrl Pts',(7.07816260134698,0.204212798742335,-4.59970262358146));
#6775=CARTESIAN_POINT('Ctrl Pts',(7.08065269348092,0.177921473039154,-4.60135978374042));
#6776=CARTESIAN_POINT('Ctrl Pts',(7.08153717675632,0.167751703794786,-4.60200273626659));
#6777=CARTESIAN_POINT('Ctrl Pts',(7.08297916169725,0.149554672700093,-4.60315685237495));
#6778=CARTESIAN_POINT('Ctrl Pts',(7.083566228947,0.141529927553974,-4.60366708052049));
#6779=CARTESIAN_POINT('Ctrl Pts',(7.08470744144815,0.124516470237078,-4.60475161859928));
#6780=CARTESIAN_POINT('Ctrl Pts',(7.08524929550807,0.11552714074415,-4.60532630077847));
#6781=CARTESIAN_POINT('Ctrl Pts',(7.08653653892849,0.0914592334197121,-4.60686950727209));
#6782=CARTESIAN_POINT('Ctrl Pts',(7.08717163842198,0.0763755841462476,-4.60784144410451));
#6783=CARTESIAN_POINT('Ctrl Pts',(7.08826331049372,0.040860677808651,-4.6101416498511));
#6784=CARTESIAN_POINT('Ctrl Pts',(7.08857715560486,0.0204294355058518,-4.61147408152769));
#6785=CARTESIAN_POINT('Ctrl Pts',(7.08857715545311,-1.48167178722712E-8,
-4.61281584510352));
#6786=CARTESIAN_POINT('Ctrl Pts',(7.09088663849909,-0.00131116008061021,
-4.77268148053433));
#6787=CARTESIAN_POINT('Ctrl Pts',(7.08670907753058,0.587748466385314,-4.73495468745384));
#6788=CARTESIAN_POINT('Ctrl Pts',(6.49966055308458,1.84456991813218,-4.65495213653729));
#6789=CARTESIAN_POINT('Ctrl Pts',(4.36544687253163,2.24101253756461,-4.53267382778465));
#6790=CARTESIAN_POINT('Ctrl Pts',(2.81680518329998,0.606947674192248,-4.40584655427643));
#6791=CARTESIAN_POINT('Ctrl Pts',(3.34667777853599,-1.58138652746787,-4.27901928076822));
#6792=CARTESIAN_POINT('Ctrl Pts',(5.47143637460349,-2.32605244650467,-4.15219200726));
#6793=CARTESIAN_POINT('Ctrl Pts',(6.90460273165936,-1.21611912267368,-4.05008002852675));
#6794=CARTESIAN_POINT('Ctrl Pts',(7.08680593434348,-0.276931585723664,-3.99024380762958));
#6795=CARTESIAN_POINT('Ctrl Pts',(7.08570592294226,-0.000894131601634556,
-3.97268334456847));
#6796=CARTESIAN_POINT('Origin',(5.09382715545311,0.,-6.77268258743872));
#6797=CARTESIAN_POINT('',(7.08881171545261,-0.000532106017552724,-3.01459230695388));
#6798=CARTESIAN_POINT('',(7.08857715545311,1.10874632379271E-10,-3.17330009074087));
#6799=CARTESIAN_POINT('',(7.08857715545311,8.3550772080578E-14,-6.77268258743872));
#6800=CARTESIAN_POINT('Ctrl Pts',(7.08797499842339,0.00179838134685419,
-3.81459200118186));
#6801=CARTESIAN_POINT('Ctrl Pts',(7.08951448073131,0.176350806397102,-3.80345567575527));
#6802=CARTESIAN_POINT('Ctrl Pts',(6.98867393212712,1.01178905137383,-3.7500435924926));
#6803=CARTESIAN_POINT('Ctrl Pts',(5.81786592990346,2.24253293940595,-3.65435575139387));
#6804=CARTESIAN_POINT('Ctrl Pts',(3.6051149786703,1.82672505437059,-3.52752847788566));
#6805=CARTESIAN_POINT('Ctrl Pts',(2.75131773613265,-0.256588620430347,-3.40070120437744));
#6806=CARTESIAN_POINT('Ctrl Pts',(4.03585363174242,-2.10567795733919,-3.27387393086923));
#6807=CARTESIAN_POINT('Ctrl Pts',(6.28614853368186,-2.03262335577032,-3.147046657361));
#6808=CARTESIAN_POINT('Ctrl Pts',(7.07793075003761,-0.718427647632865,-3.06061946381432));
#6809=CARTESIAN_POINT('Ctrl Pts',(7.09175582045521,-0.0297929789795935,
-3.01646802810371));
#6810=CARTESIAN_POINT('Ctrl Pts',(7.09165120934631,-0.000533538361054326,
-3.01459235022917));
#6811=CARTESIAN_POINT('Ctrl Pts',(7.08857700164759,-0.000783330765841211,
-3.97433649156488));
#6812=CARTESIAN_POINT('Ctrl Pts',(7.08858993222558,0.0321443539113238,-3.97232913016949));
#6813=CARTESIAN_POINT('Ctrl Pts',(7.08778754968188,0.0650660683111326,-3.97029974614309));
#6814=CARTESIAN_POINT('Ctrl Pts',(7.08567929427801,0.107948074877877,-3.96762078150855));
#6815=CARTESIAN_POINT('Ctrl Pts',(7.08511261760091,0.117940376035509,-3.96699401838726));
#6816=CARTESIAN_POINT('Ctrl Pts',(7.0839699121099,0.135721644367752,-3.96587402092352));
#6817=CARTESIAN_POINT('Ctrl Pts',(7.08342328576995,0.143512341162737,-3.96538170510721));
#6818=CARTESIAN_POINT('Ctrl Pts',(7.08223840163136,0.159088984934294,-3.96439408001313));
#6819=CARTESIAN_POINT('Ctrl Pts',(7.08160012798591,0.166874791084507,-3.96389877871134));
#6820=CARTESIAN_POINT('Ctrl Pts',(7.08013644389767,0.183527303688283,-3.96283579569347));
#6821=CARTESIAN_POINT('Ctrl Pts',(7.07929736189154,0.192392608178248,-3.96226769674993));
#6822=CARTESIAN_POINT('Ctrl Pts',(7.07692440530385,0.21579265154685,-3.96076224303042));
#6823=CARTESIAN_POINT('Ctrl Pts',(7.07529012163093,0.230316446873925,-3.95982176948879));
#6824=CARTESIAN_POINT('Ctrl Pts',(7.06753280767526,0.293043653296804,-3.95573280238148));
#6825=CARTESIAN_POINT('Ctrl Pts',(7.05980966597646,0.341028854858834,-3.95253480437207));
#6826=CARTESIAN_POINT('Ctrl Pts',(7.01669226902968,0.558070234406168,-3.93774025471924));
#6827=CARTESIAN_POINT('Ctrl Pts',(6.96118721536257,0.722358738604517,-3.92553481354265));
#6828=CARTESIAN_POINT('Ctrl Pts',(6.85589416538907,0.937336689641738,-3.90902048885455));
#6829=CARTESIAN_POINT('Ctrl Pts',(6.82355122215285,0.995759412735924,-3.90448253037066));
#6830=CARTESIAN_POINT('Ctrl Pts',(6.78294760842785,1.06113335282907,-3.89943235118866));
#6831=CARTESIAN_POINT('Ctrl Pts',(6.77749163267361,1.06976905726683,-3.89876584521586));
#6832=CARTESIAN_POINT('Ctrl Pts',(6.76904652537039,1.08291128827571,-3.8977529126801));
#6833=CARTESIAN_POINT('Ctrl Pts',(6.76610510200148,1.08744805245059,-3.89740349895455));
#6834=CARTESIAN_POINT('Ctrl Pts',(6.76068422698521,1.09573503916655,-3.89676580078874));
#6835=CARTESIAN_POINT('Ctrl Pts',(6.75821054574705,1.09948883755708,-3.89647715618809));
#6836=CARTESIAN_POINT('Ctrl Pts',(6.7526248719228,1.10790301921835,-3.89583062489912));
#6837=CARTESIAN_POINT('Ctrl Pts',(6.74950592453,1.1125586634533,-3.89547320775268));
#6838=CARTESIAN_POINT('Ctrl Pts',(6.74030906444032,1.12616246319816,-3.89442956453444));
#6839=CARTESIAN_POINT('Ctrl Pts',(6.73417782383085,1.13507456459261,-3.89374678562785));
#6840=CARTESIAN_POINT('Ctrl Pts',(6.68342809355681,1.20757204789041,-3.88819632975819));
#6841=CARTESIAN_POINT('Ctrl Pts',(6.63519727213266,1.26855921146998,-3.8835498753102));
#6842=CARTESIAN_POINT('Ctrl Pts',(6.50868069598603,1.4106321278625,-3.8723659197789));
#6843=CARTESIAN_POINT('Ctrl Pts',(6.42685633738313,1.48819609835596,-3.86592679131834));
#6844=CARTESIAN_POINT('Ctrl Pts',(6.29106677821567,1.59668325024419,-3.85571217889294));
#6845=CARTESIAN_POINT('Ctrl Pts',(6.24147473212306,1.63269234490218,-3.8520682700016));
#6846=CARTESIAN_POINT('Ctrl Pts',(6.16881606508225,1.68050238198347,-3.84678210194602));
#6847=CARTESIAN_POINT('Ctrl Pts',(6.14705408841845,1.6942261807163,-3.84520538515987));
#6848=CARTESIAN_POINT('Ctrl Pts',(6.11299083244211,1.71479762096456,-3.84274349201212));
#6849=CARTESIAN_POINT('Ctrl Pts',(6.10087182240738,1.72194265426581,-3.84186877344927));
#6850=CARTESIAN_POINT('Ctrl Pts',(6.08054652717708,1.73363792853391,-3.84040312009163));
#6851=CARTESIAN_POINT('Ctrl Pts',(6.07238177413091,1.73825960066172,-3.83981472652832));
#6852=CARTESIAN_POINT('Ctrl Pts',(6.05641994815166,1.74714672025037,-3.83866497242767));
#6853=CARTESIAN_POINT('Ctrl Pts',(6.04862636374287,1.75141800103964,-3.8381038351006));
#6854=CARTESIAN_POINT('Ctrl Pts',(6.03378182708759,1.75942503285489,-3.83703536869395));
#6855=CARTESIAN_POINT('Ctrl Pts',(6.02673647636054,1.76317084450366,-3.83652840841744));
#6856=CARTESIAN_POINT('Ctrl Pts',(6.01076301772389,1.77154093381101,-3.83537923785553));
#6857=CARTESIAN_POINT('Ctrl Pts',(6.00182209278322,1.77614015307733,-3.83473616391758));
#6858=CARTESIAN_POINT('Ctrl Pts',(5.97885424654842,1.78773608606241,-3.83308442439851));
#6859=CARTESIAN_POINT('Ctrl Pts',(5.96477913785966,1.79463530739242,-3.83207241051087));
#6860=CARTESIAN_POINT('Ctrl Pts',(5.8701125143009,1.83966226605252,-3.82526572676097));
#6861=CARTESIAN_POINT('Ctrl Pts',(5.78713515336401,1.87251069987953,-3.81929234428525));
#6862=CARTESIAN_POINT('Ctrl Pts',(5.57781533754034,1.93955021582627,-3.80423490474391));
#6863=CARTESIAN_POINT('Ctrl Pts',(5.44977648105083,1.9670781670994,-3.79501963952288));
#6864=CARTESIAN_POINT('Ctrl Pts',(5.25722455434304,1.9890493242337,-3.78167185230354));
#6865=CARTESIAN_POINT('Ctrl Pts',(5.19416661123743,1.99322593016015,-3.77738547630428));
#6866=CARTESIAN_POINT('Ctrl Pts',(5.1209133435733,1.99459166082764,-3.77257858850057));
#6867=CARTESIAN_POINT('Ctrl Pts',(5.11081442342066,1.99470323557337,-3.77191971614666));
#6868=CARTESIAN_POINT('Ctrl Pts',(5.09533164637251,1.99475669647646,-3.77091588711614));
#6869=CARTESIAN_POINT('Ctrl Pts',(5.08994832165143,1.99475349302295,-3.77056802498463));
#6870=CARTESIAN_POINT('Ctrl Pts',(5.0800678169924,1.9947076147131,-3.7699317845504));
#6871=CARTESIAN_POINT('Ctrl Pts',(5.07557077484762,1.99467152507711,-3.76964305752163));
#6872=CARTESIAN_POINT('Ctrl Pts',(5.06544153262143,1.99455597687536,-3.76899462320745));
#6873=CARTESIAN_POINT('Ctrl Pts',(5.05980953229785,1.99446787180285,-3.76863539837715));
#6874=CARTESIAN_POINT('Ctrl Pts',(5.04322853715343,1.99413822946573,-3.76758148609537));
#6875=CARTESIAN_POINT('Ctrl Pts',(5.03228086341701,1.99383037519932,-3.76689034846135));
#6876=CARTESIAN_POINT('Ctrl Pts',(4.9310190255478,1.99014798867427,-3.7605366252053));
#6877=CARTESIAN_POINT('Ctrl Pts',(4.8410171710236,1.98072888231259,-3.75517460587202));
#6878=CARTESIAN_POINT('Ctrl Pts',(4.6369834338069,1.94523512794317,-3.74306500086495));
#6879=CARTESIAN_POINT('Ctrl Pts',(4.52399194383545,1.91518499455189,-3.73638239312475));
#6880=CARTESIAN_POINT('Ctrl Pts',(4.3423563464161,1.84937033842983,-3.72494097189099));
#6881=CARTESIAN_POINT('Ctrl Pts',(4.27200314493709,1.81919826501401,-3.72032580552199));
#6882=CARTESIAN_POINT('Ctrl Pts',(4.18911924232615,1.77786152321856,-3.7145684968291));
#6883=CARTESIAN_POINT('Ctrl Pts',(4.17476576028368,1.77048415179864,-3.71355952484302));
#6884=CARTESIAN_POINT('Ctrl Pts',(4.15233845347735,1.75861079955517,-3.71196336486479));
#6885=CARTESIAN_POINT('Ctrl Pts',(4.14420345675096,1.75423138339808,-3.71138027530926));
#6886=CARTESIAN_POINT('Ctrl Pts',(4.12905933882607,1.74594244769987,-3.71028692940035));
#6887=CARTESIAN_POINT('Ctrl Pts',(4.12204279563869,1.74204682073354,-3.70977717420887));
#6888=CARTESIAN_POINT('Ctrl Pts',(4.10643778929325,1.73325921124141,-3.70863622758977));
#6889=CARTESIAN_POINT('Ctrl Pts',(4.09786183922552,1.72834554902696,-3.70800426927988));
#6890=CARTESIAN_POINT('Ctrl Pts',(4.0762618443915,1.71575550345355,-3.70639986211648));
#6891=CARTESIAN_POINT('Ctrl Pts',(4.06328807751761,1.70799452515282,-3.7054243830952));
#6892=CARTESIAN_POINT('Ctrl Pts',(3.98599928660353,1.66055877116631,-3.69954067266061));
#6893=CARTESIAN_POINT('Ctrl Pts',(3.92390049598485,1.61740755442843,-3.69450579958175));
#6894=CARTESIAN_POINT('Ctrl Pts',(3.75183242852889,1.48273822803268,-3.67963995908714));
#6895=CARTESIAN_POINT('Ctrl Pts',(3.64906119601404,1.38278985345386,-3.66954923257848));
#6896=CARTESIAN_POINT('Ctrl Pts',(3.51610418073227,1.2223346134719,-3.65518154404755));
#6897=CARTESIAN_POINT('Ctrl Pts',(3.47684344556298,1.16990479189016,-3.65073340549605));
#6898=CARTESIAN_POINT('Ctrl Pts',(3.43453785635198,1.10719921993365,-3.64576988721702));
#6899=CARTESIAN_POINT('Ctrl Pts',(3.4289116705794,1.09872086056335,-3.64510599940647));
#6900=CARTESIAN_POINT('Ctrl Pts',(3.42039982936918,1.08567844869955,-3.64409618095095));
#6901=CARTESIAN_POINT('Ctrl Pts',(3.41746751816599,1.08114526211422,-3.6437472913967));
#6902=CARTESIAN_POINT('Ctrl Pts',(3.4121269961297,1.07281515246834,-3.64311009027123));
#6903=CARTESIAN_POINT('Ctrl Pts',(3.40971321918714,1.0690219959047,-3.6428214223522));
#6904=CARTESIAN_POINT('Ctrl Pts',(3.40431464611503,1.06047468253158,-3.64217426401934));
#6905=CARTESIAN_POINT('Ctrl Pts',(3.40133708472929,1.0557160763432,-3.64181624745534));
#6906=CARTESIAN_POINT('Ctrl Pts',(3.39265676719619,1.04171246573089,-3.64076915795914));
#6907=CARTESIAN_POINT('Ctrl Pts',(3.38700928376603,1.03243320194305,-3.64008356684079));
#6908=CARTESIAN_POINT('Ctrl Pts',(3.34002025264241,0.95378703963689,-3.63433798850469));
#6909=CARTESIAN_POINT('Ctrl Pts',(3.30284502838723,0.882006015624495,-3.62951731511248));
#6910=CARTESIAN_POINT('Ctrl Pts',(3.23241131827574,0.72306432332293,-3.61931185922023));
#6911=CARTESIAN_POINT('Ctrl Pts',(3.20070344996527,0.635432275023037,-3.61396285837639));
#6912=CARTESIAN_POINT('Ctrl Pts',(3.14844689698162,0.451775373412142,-3.6028055912222));
#6913=CARTESIAN_POINT('Ctrl Pts',(3.12863016439159,0.355812882930063,-3.5970011822122));
#6914=CARTESIAN_POINT('Ctrl Pts',(3.11288180620557,0.235450959331615,-3.5895202925018));
#6915=CARTESIAN_POINT('Ctrl Pts',(3.11024146469447,0.212059816794458,-3.58805770654022));
#6916=CARTESIAN_POINT('Ctrl Pts',(3.1070019000896,0.177954813195792,-3.58591016361791));
#6917=CARTESIAN_POINT('Ctrl Pts',(3.10607414336318,0.167273628059104,-3.58523544886738));
#6918=CARTESIAN_POINT('Ctrl Pts',(3.10459519640669,0.148491408908575,-3.5840450347101));
#6919=CARTESIAN_POINT('Ctrl Pts',(3.1040072740782,0.140393454010487,-3.58353049339193));
#6920=CARTESIAN_POINT('Ctrl Pts',(3.10295869636622,0.124617430199431,-3.58252547907882));
#6921=CARTESIAN_POINT('Ctrl Pts',(3.10249298002836,0.116939832233686,-3.58203517351227));
#6922=CARTESIAN_POINT('Ctrl Pts',(3.10136167173533,0.0963166106193942,-3.5807148126886));
#6923=CARTESIAN_POINT('Ctrl Pts',(3.1007778546204,0.0833670476668602,-3.57988222601684));
#6924=CARTESIAN_POINT('Ctrl Pts',(3.09907616894667,0.0351895253706318,-3.57677108310428));
#6925=CARTESIAN_POINT('Ctrl Pts',(3.09876586897419,-5.87062418391966E-5,
-3.57446771398511));
#6926=CARTESIAN_POINT('Ctrl Pts',(3.10295193581801,-0.236604242933865,-3.55881876194408));
#6927=CARTESIAN_POINT('Ctrl Pts',(3.13697600794851,-0.43619781027102,-3.54451610489363));
#6928=CARTESIAN_POINT('Ctrl Pts',(3.2177511839886,-0.680043507221302,-3.52689355388902));
#6929=CARTESIAN_POINT('Ctrl Pts',(3.23744019343108,-0.732085305721768,-3.52313511793488));
#6930=CARTESIAN_POINT('Ctrl Pts',(3.26313234579382,-0.792262777690295,-3.51884452549687));
#6931=CARTESIAN_POINT('Ctrl Pts',(3.26705077693763,-0.801256430455693,-3.51820479417909));
#6932=CARTESIAN_POINT('Ctrl Pts',(3.27319687370313,-0.815083588195336,-3.51722398695612));
#6933=CARTESIAN_POINT('Ctrl Pts',(3.27537773495614,-0.819937549609063,-3.51688020308298));
#6934=CARTESIAN_POINT('Ctrl Pts',(3.27943911162035,-0.82888108224929,-3.51624782126948));
#6935=CARTESIAN_POINT('Ctrl Pts',(3.28131403656732,-0.832972998766319,-3.5159589042967));
#6936=CARTESIAN_POINT('Ctrl Pts',(3.28559812583545,-0.842239823727202,-3.51530551953203));
#6937=CARTESIAN_POINT('Ctrl Pts',(3.28801565938601,-0.847410754495733,-3.51494156855519));
#6938=CARTESIAN_POINT('Ctrl Pts',(3.29434598363828,-0.860800752295372,-3.5140006106066));
#6939=CARTESIAN_POINT('Ctrl Pts',(3.29829294727148,-0.869003646418099,-3.51342562449494));
#6940=CARTESIAN_POINT('Ctrl Pts',(3.32490777979735,-0.923361170637173,-3.50962324021939));
#6941=CARTESIAN_POINT('Ctrl Pts',(3.34929895941641,-0.968655753052552,-3.50649239296052));
#6942=CARTESIAN_POINT('Ctrl Pts',(3.40397974408077,-1.06141756119578,-3.500055317874));
#6943=CARTESIAN_POINT('Ctrl Pts',(3.43458199702876,-1.10864675254,-3.49676288490253));
#6944=CARTESIAN_POINT('Ctrl Pts',(3.52662621919236,-1.23833433182978,-3.4875057813317));
#6945=CARTESIAN_POINT('Ctrl Pts',(3.59249788133462,-1.31742185275793,-3.4815900870162));
#6946=CARTESIAN_POINT('Ctrl Pts',(3.71638749223596,-1.44474717709875,-3.47105964525621));
#6947=CARTESIAN_POINT('Ctrl Pts',(3.77158094330595,-1.49542552453557,-3.4665383579411));
#6948=CARTESIAN_POINT('Ctrl Pts',(3.8419008013251,-1.55305039122955,-3.46088637790085));
#6949=CARTESIAN_POINT('Ctrl Pts',(3.85443576402625,-1.56307199743044,-3.45988293176198));
#6950=CARTESIAN_POINT('Ctrl Pts',(3.87435995341661,-1.5786108782361,-3.45829355531653));
#6951=CARTESIAN_POINT('Ctrl Pts',(3.88166902426058,-1.58423016702624,-3.45771166445687));
#6952=CARTESIAN_POINT('Ctrl Pts',(3.89541439575823,-1.59464693829044,-3.45661938833823));
#6953=CARTESIAN_POINT('Ctrl Pts',(3.90184123274415,-1.59945664442279,-3.45610949514641));
#6954=CARTESIAN_POINT('Ctrl Pts',(3.91626688393793,-1.61011725711222,-3.45496670753169));
#6955=CARTESIAN_POINT('Ctrl Pts',(3.92428057879507,-1.6159475777058,-3.45433303477855));
#6956=CARTESIAN_POINT('Ctrl Pts',(3.94469748097262,-1.63057035891761,-3.45272135238427));
#6957=CARTESIAN_POINT('Ctrl Pts',(3.95715820293689,-1.63928105442005,-3.45174026462255));
#6958=CARTESIAN_POINT('Ctrl Pts',(4.0337835790358,-1.69155247116689,-3.44572142003717));
#6959=CARTESIAN_POINT('Ctrl Pts',(4.10033637937241,-1.73147786638581,-3.44054998856304));
#6960=CARTESIAN_POINT('Ctrl Pts',(4.28024725452151,-1.82561471497388,-3.42672055652551));
#6961=CARTESIAN_POINT('Ctrl Pts',(4.39669640324256,-1.87317527946742,-3.41789999336075));
#6962=CARTESIAN_POINT('Ctrl Pts',(4.58677199626836,-1.93061169153583,-3.40413318805183));
#6963=CARTESIAN_POINT('Ctrl Pts',(4.65783200214184,-1.94789035456335,-3.39912375310112));
#6964=CARTESIAN_POINT('Ctrl Pts',(4.74459457097091,-1.96399951096233,-3.39328596934377));
#6965=CARTESIAN_POINT('Ctrl Pts',(4.75953434046229,-1.96659752470657,-3.39229065478195));
#6966=CARTESIAN_POINT('Ctrl Pts',(4.78076214081627,-1.97004011856314,-3.39089180103772));
#6967=CARTESIAN_POINT('Ctrl Pts',(4.78702637909183,-1.97102538248803,-3.39048089814288));
#6968=CARTESIAN_POINT('Ctrl Pts',(4.79782285215946,-1.97267077579039,-3.38977608496365));
#6969=CARTESIAN_POINT('Ctrl Pts',(4.80235282673824,-1.97334519399073,-3.38948138540015));
#6970=CARTESIAN_POINT('Ctrl Pts',(4.81118727152128,-1.9746293721628,-3.38890869566478));
#6971=CARTESIAN_POINT('Ctrl Pts',(4.81549142723941,-1.97524066500056,-3.3886306152164));
#6972=CARTESIAN_POINT('Ctrl Pts',(4.82728644585311,-1.97687651972526,-3.38787104436784));
#6973=CARTESIAN_POINT('Ctrl Pts',(4.83478128256406,-1.97787258543727,-3.38739112648365));
#6974=CARTESIAN_POINT('Ctrl Pts',(4.8639432205056,-1.98157960745624,-3.38553377648084));
#6975=CARTESIAN_POINT('Ctrl Pts',(4.88564949996013,-1.98397744943346,-3.38417267571356));
#6976=CARTESIAN_POINT('Ctrl Pts',(5.10213901983201,-2.00430017052009,-3.37077131297073));
#6977=CARTESIAN_POINT('Ctrl Pts',(5.29853933438375,-1.99384145272988,-3.35991850942686));
#6978=CARTESIAN_POINT('Ctrl Pts',(5.56187027551054,-1.94043723539433,-3.34397517767664));
#6979=CARTESIAN_POINT('Ctrl Pts',(5.63258554169497,-1.92200381385197,-3.33956146615471));
#6980=CARTESIAN_POINT('Ctrl Pts',(5.71730838863226,-1.89487541859839,-3.33403022736528));
#6981=CARTESIAN_POINT('Ctrl Pts',(5.73243157381938,-1.8898322872339,-3.33303334955274));
#6982=CARTESIAN_POINT('Ctrl Pts',(5.75618079220295,-1.88159501294759,-3.33145204822371));
#6983=CARTESIAN_POINT('Ctrl Pts',(5.76484816868126,-1.87852147395482,-3.3308715946752));
#6984=CARTESIAN_POINT('Ctrl Pts',(5.78104285137447,-1.87265229603755,-3.32978060695943));
#6985=CARTESIAN_POINT('Ctrl Pts',(5.78857515614601,-1.86987091721108,-3.3292705540238));
#6986=CARTESIAN_POINT('Ctrl Pts',(5.80539565481545,-1.86354411588399,-3.32812556449234));
#6987=CARTESIAN_POINT('Ctrl Pts',(5.81467449740856,-1.85997459790029,-3.3274898357398));
#6988=CARTESIAN_POINT('Ctrl Pts',(5.838170608212,-1.85073355144428,-3.32586938631766));
#6989=CARTESIAN_POINT('Ctrl Pts',(5.85234978798798,-1.84496754671929,-3.32488152905417));
#6990=CARTESIAN_POINT('Ctrl Pts',(5.94016131241538,-1.80807537455423,-3.31870021287182));
#6991=CARTESIAN_POINT('Ctrl Pts',(6.01192438444461,-1.77271336706427,-3.31336436481765));
#6992=CARTESIAN_POINT('Ctrl Pts',(6.20215390356457,-1.66432149526925,-3.29843363152046));
#6993=CARTESIAN_POINT('Ctrl Pts',(6.31541326412989,-1.58305925286827,-3.28862212492309));
#6994=CARTESIAN_POINT('Ctrl Pts',(6.46761856069933,-1.44772468949067,-3.27458440940185));
#6995=CARTESIAN_POINT('Ctrl Pts',(6.51383330665341,-1.40242430308452,-3.2701914895724));
#6996=CARTESIAN_POINT('Ctrl Pts',(6.56466366995959,-1.3475052952286,-3.26528138061859));
#6997=CARTESIAN_POINT('Ctrl Pts',(6.57150098647643,-1.34000396737603,-3.26461917911686));
#6998=CARTESIAN_POINT('Ctrl Pts',(6.58188365994687,-1.32843686026594,-3.26361137940618));
#6999=CARTESIAN_POINT('Ctrl Pts',(6.58547015733078,-1.32440847508855,-3.26326284020086));
#7000=CARTESIAN_POINT('Ctrl Pts',(6.59201658581576,-1.31699514461143,-3.26262597076471));
#7001=CARTESIAN_POINT('Ctrl Pts',(6.59498140824904,-1.3136147419634,-3.26233728676683));
#7002=CARTESIAN_POINT('Ctrl Pts',(6.60162607270662,-1.30598681780852,-3.26168970998422));
#7003=CARTESIAN_POINT('Ctrl Pts',(6.60529940526895,-1.30173376043301,-3.26133129391622));
#7004=CARTESIAN_POINT('Ctrl Pts',(6.61603915299017,-1.2891923152664,-3.26028195439781));
#7005=CARTESIAN_POINT('Ctrl Pts',(6.62305584883763,-1.28086135356562,-3.25959453508755));
#7006=CARTESIAN_POINT('Ctrl Pts',(6.69339043930943,-1.19595081401608,-3.25268013641715));
#7007=CARTESIAN_POINT('Ctrl Pts',(6.75097959073715,-1.1147880100955,-3.24681781204656));
#7008=CARTESIAN_POINT('Ctrl Pts',(6.86735574098765,-0.921691598572518,-3.23367211857729));
#7009=CARTESIAN_POINT('Ctrl Pts',(6.92204263515108,-0.807803146408631,-3.2264463077888));
#7010=CARTESIAN_POINT('Ctrl Pts',(6.9864311224792,-0.633011784159669,-3.21530642648322));
#7011=CARTESIAN_POINT('Ctrl Pts',(7.00467515583797,-0.575597567339887,-3.21164363434802));
#7012=CARTESIAN_POINT('Ctrl Pts',(7.02420599853337,-0.502884233737741,-3.20695688826785));
#7013=CARTESIAN_POINT('Ctrl Pts',(7.02795296092032,-0.48827490141617,-3.20601294937423));
#7014=CARTESIAN_POINT('Ctrl Pts',(7.03367268999514,-0.464874189902465,-3.20449672401071));
#7015=CARTESIAN_POINT('Ctrl Pts',(7.0357522305277,-0.456109316747675,-3.20392786594849));
#7016=CARTESIAN_POINT('Ctrl Pts',(7.03957883273296,-0.439480224269286,-3.20284668200946));
#7017=CARTESIAN_POINT('Ctrl Pts',(7.04133776628294,-0.431618899907222,-3.20233474734071));
#7018=CARTESIAN_POINT('Ctrl Pts',(7.04522223009477,-0.413750507549254,-3.20116921049005));
#7019=CARTESIAN_POINT('Ctrl Pts',(7.04731847817624,-0.403737371883485,-3.20051469029228));
#7020=CARTESIAN_POINT('Ctrl Pts',(7.05254626487011,-0.377771496048739,-3.19881365291587));
#7021=CARTESIAN_POINT('Ctrl Pts',(7.05555991950373,-0.361796060520636,-3.19776343951684));
#7022=CARTESIAN_POINT('Ctrl Pts',(7.07847589111606,-0.231601099446928,-3.18917300757686));
#7023=CARTESIAN_POINT('Ctrl Pts',(7.08857715545955,-0.11590233033206,-3.18132259334605));
#7024=CARTESIAN_POINT('Ctrl Pts',(7.08857715545311,1.10873879521911E-10,
-3.17330009074087));
#7025=CARTESIAN_POINT('Origin',(5.09382715545311,0.,-6.77268258743872));
#7026=CARTESIAN_POINT('',(7.08857665886015,-0.00140753592614233,-2.21459235027784));
#7027=CARTESIAN_POINT('',(7.08857712371927,-0.000258951665618427,-2.37086691085377));
#7028=CARTESIAN_POINT('',(7.08857715545311,8.3550772080578E-14,-6.77268258743872));
#7029=CARTESIAN_POINT('Ctrl Pts',(7.08857708451418,-0.000531987661214402,
-3.01459230337799));
#7030=CARTESIAN_POINT('Ctrl Pts',(7.08859546216608,0.0683771666358918,-3.01016806646156));
#7031=CARTESIAN_POINT('Ctrl Pts',(7.08503884163906,0.137429399923423,-3.00574382954513));
#7032=CARTESIAN_POINT('Ctrl Pts',(7.07788887578466,0.206219912750995,-3.00131959262871));
#7033=CARTESIAN_POINT('Ctrl Pts',(7.07062135308658,0.276141451338347,-2.9968226142002));
#7034=CARTESIAN_POINT('Ctrl Pts',(7.05964116392455,0.345792070396834,-2.9923256357717));
#7035=CARTESIAN_POINT('Ctrl Pts',(7.04498431714381,0.414744852750578,-2.98782865734319));
#7036=CARTESIAN_POINT('Ctrl Pts',(7.03060188308933,0.482406667048755,-2.98341587356644));
#7037=CARTESIAN_POINT('Ctrl Pts',(7.01267938170586,0.549396040749643,-2.97900308978969));
#7038=CARTESIAN_POINT('Ctrl Pts',(6.9913029820738,0.615315406836321,-2.97459030601294));
#7039=CARTESIAN_POINT('Ctrl Pts',(6.9699387309686,0.681197309963696,-2.97018003008705));
#7040=CARTESIAN_POINT('Ctrl Pts',(6.94512462731208,0.746009939868335,-2.96576975416116));
#7041=CARTESIAN_POINT('Ctrl Pts',(6.91699706735104,0.809369529232541,-2.96135947823527));
#7042=CARTESIAN_POINT('Ctrl Pts',(6.88887561533916,0.872715359950376,-2.95695016000856));
#7043=CARTESIAN_POINT('Ctrl Pts',(6.85744233713536,0.934608322762615,-2.95254084178185));
#7044=CARTESIAN_POINT('Ctrl Pts',(6.82288156633736,0.994685079159087,-2.94813152355514));
#7045=CARTESIAN_POINT('Ctrl Pts',(6.78712705327514,1.05683690973798,-2.9435699057876));
#7046=CARTESIAN_POINT('Ctrl Pts',(6.74802527877163,1.1170442563506,-2.93900828802005));
#7047=CARTESIAN_POINT('Ctrl Pts',(6.70583059911535,1.1749350876202,-2.9344466702525));
#7048=CARTESIAN_POINT('Ctrl Pts',(6.66499381394337,1.23096289632124,-2.93003185287914));
#7049=CARTESIAN_POINT('Ctrl Pts',(6.62126055726187,1.28482067694877,-2.92561703550578));
#7050=CARTESIAN_POINT('Ctrl Pts',(6.57490247950192,1.33620486714939,-2.92120221813241));
#7051=CARTESIAN_POINT('Ctrl Pts',(6.52623217107194,1.3901519785555,-2.91656720016777));
#7052=CARTESIAN_POINT('Ctrl Pts',(6.4746687918193,1.44137184772516,-2.91193218220313));
#7053=CARTESIAN_POINT('Ctrl Pts',(6.42056820986394,1.48955890687171,-2.90729716423849));
#7054=CARTESIAN_POINT('Ctrl Pts',(6.36646762790858,1.53774596601826,-2.90266214627385));
#7055=CARTESIAN_POINT('Ctrl Pts',(6.30983038151407,1.5828998882487,-2.89802712830921));
#7056=CARTESIAN_POINT('Ctrl Pts',(6.25104729766899,1.62476740026068,-2.89339211034457));
#7057=CARTESIAN_POINT('Ctrl Pts',(6.19454093398137,1.66501334698032,-2.88893661067226));
#7058=CARTESIAN_POINT('Ctrl Pts',(6.13582155018381,1.70238706390389,-2.88448111099996));
#7059=CARTESIAN_POINT('Ctrl Pts',(6.07521305597278,1.73663734750846,-2.88002561132766));
#7060=CARTESIAN_POINT('Ctrl Pts',(6.01469518919593,1.77083641691666,-2.87557677393114));
#7061=CARTESIAN_POINT('Ctrl Pts',(5.95229424110062,1.80192108422637,-2.87112793653462));
#7062=CARTESIAN_POINT('Ctrl Pts',(5.88836409443915,1.82968265420173,-2.86667909913811));
#7063=CARTESIAN_POINT('Ctrl Pts',(5.82450877432407,1.85741173086194,-2.86223546884896));
#7064=CARTESIAN_POINT('Ctrl Pts',(5.75912825713365,1.8818252414749,-2.85779183855981));
#7065=CARTESIAN_POINT('Ctrl Pts',(5.69260050297275,1.90276063675916,-2.85334820827066));
#7066=CARTESIAN_POINT('Ctrl Pts',(5.62611434793073,1.92368294135656,-2.84890735653773));
#7067=CARTESIAN_POINT('Ctrl Pts',(5.55848284459192,1.94113129864609,-2.8444665048048));
#7068=CARTESIAN_POINT('Ctrl Pts',(5.49010195824456,1.9549920314857,-2.84002565307186));
#7069=CARTESIAN_POINT('Ctrl Pts',(5.42174063850237,1.96884879819529,-2.83558607205063));
#7070=CARTESIAN_POINT('Ctrl Pts',(5.35263084063515,1.97911988133681,-2.8311464910294));
#7071=CARTESIAN_POINT('Ctrl Pts',(5.28317991413158,1.98574245441871,-2.82670691000816));
#7072=CARTESIAN_POINT('Ctrl Pts',(5.21372530700011,1.99236537847113,-2.82226709370647));
#7073=CARTESIAN_POINT('Ctrl Pts',(5.14393002252826,1.99533936456506,-2.81782727740478));
#7074=CARTESIAN_POINT('Ctrl Pts',(5.07420596529435,1.99465349657447,-2.81338746110309));
#7075=CARTESIAN_POINT('Ctrl Pts',(5.00440830903407,1.99396690459823,-2.80894295823883));
#7076=CARTESIAN_POINT('Ctrl Pts',(4.93468252017194,1.98961275280332,-2.80449845537456));
#7077=CARTESIAN_POINT('Ctrl Pts',(4.86543896293322,1.98163225549482,-2.8000539525103));
#7078=CARTESIAN_POINT('Ctrl Pts',(4.79615478586587,1.97364707664705,-2.79560684240066));
#7079=CARTESIAN_POINT('Ctrl Pts',(4.72735388594296,1.96203139957156,-2.79115973229101));
#7080=CARTESIAN_POINT('Ctrl Pts',(4.65943721402408,1.94687774174068,-2.78671262218137));
#7081=CARTESIAN_POINT('Ctrl Pts',(4.59140328371494,1.93169792106239,-2.78225783411935));
#7082=CARTESIAN_POINT('Ctrl Pts',(4.52425709972242,1.91296805832542,-2.77780304605733));
#7083=CARTESIAN_POINT('Ctrl Pts',(4.45838443394178,1.8908305344949,-2.7733482579953));
#7084=CARTESIAN_POINT('Ctrl Pts',(4.42494909585679,1.87959407419887,-2.77108711760899));
#7085=CARTESIAN_POINT('Ctrl Pts',(4.39184153906994,1.86748046069015,-2.76882597722268));
#7086=CARTESIAN_POINT('Ctrl Pts',(4.35910994638159,1.85451292397604,-2.76656483683636));
#7087=CARTESIAN_POINT('Ctrl Pts',(4.29461346453262,1.82896083721171,-2.76210933718279));
#7088=CARTESIAN_POINT('Ctrl Pts',(4.23132485355215,1.79998994807284,-2.75765383752922));
#7089=CARTESIAN_POINT('Ctrl Pts',(4.16963103391141,1.76773558300649,-2.75319833787564));
#7090=CARTESIAN_POINT('Ctrl Pts',(4.10802946459828,1.73552944766171,-2.74874950049886));
#7091=CARTESIAN_POINT('Ctrl Pts',(4.04801838350661,1.70004980615064,-2.74430066312208));
#7092=CARTESIAN_POINT('Ctrl Pts',(3.98996532425878,1.66148024969673,-2.7398518257453));
#7093=CARTESIAN_POINT('Ctrl Pts',(3.931980212784,1.62295583669438,-2.73540819547726));
#7094=CARTESIAN_POINT('Ctrl Pts',(3.87594897684726,1.58134896129237,-2.73096456520922));
#7095=CARTESIAN_POINT('Ctrl Pts',(3.82221350513018,1.53688850825699,-2.72652093494118));
#7096=CARTESIAN_POINT('Ctrl Pts',(3.76851163366005,1.49245585589319,-2.72208008323021));
#7097=CARTESIAN_POINT('Ctrl Pts',(3.71710305459827,1.44517347682411,-2.71763923151923));
#7098=CARTESIAN_POINT('Ctrl Pts',(3.66829842272948,1.39531193454344,-2.71319837980825));
#7099=CARTESIAN_POINT('Ctrl Pts',(3.6195077558972,1.34546465972534,-2.70875879880979));
#7100=CARTESIAN_POINT('Ctrl Pts',(3.57331989904164,1.29304003624274,-2.70431921781132));
#7101=CARTESIAN_POINT('Ctrl Pts',(3.53000901333487,1.23834582442945,-2.69987963681286));
#7102=CARTESIAN_POINT('Ctrl Pts',(3.486695832328,1.18364871404625,-2.69543982053472));
#7103=CARTESIAN_POINT('Ctrl Pts',(3.44626022694456,1.12668216153398,-2.69100000425659));
#7104=CARTESIAN_POINT('Ctrl Pts',(3.40893526309196,1.06778596804588,-2.68656018797846));
#7105=CARTESIAN_POINT('Ctrl Pts',(3.37157089991985,1.00882760517551,-2.68211568513879));
#7106=CARTESIAN_POINT('Ctrl Pts',(3.33732399411704,0.947935949964705,-2.67767118229911));
#7107=CARTESIAN_POINT('Ctrl Pts',(3.30638301824751,0.885477847757544,-2.67322667945944));
#7108=CARTESIAN_POINT('Ctrl Pts',(3.27542389170962,0.822983106230917,-2.66877956937501));
#7109=CARTESIAN_POINT('Ctrl Pts',(3.24777474903842,0.758920537938394,-2.66433245929058));
#7110=CARTESIAN_POINT('Ctrl Pts',(3.22357588420632,0.693676974462737,-2.65988534920616));
#7111=CARTESIAN_POINT('Ctrl Pts',(3.19933523994645,0.628320767738441,-2.65543056117006));
#7112=CARTESIAN_POINT('Ctrl Pts',(3.17855690974961,0.561779962659622,-2.65097577313396));
#7113=CARTESIAN_POINT('Ctrl Pts',(3.16133108332908,0.494455755073375,-2.64652098509787));
#7114=CARTESIAN_POINT('Ctrl Pts',(3.1525876784805,0.460283646945397,-2.64425984450796));
#7115=CARTESIAN_POINT('Ctrl Pts',(3.1447586939971,0.425909860714845,-2.64199870391805));
#7116=CARTESIAN_POINT('Ctrl Pts',(3.13785082285429,0.391387466346655,-2.63973756332814));
#7117=CARTESIAN_POINT('Ctrl Pts',(3.12423910047957,0.323362276221473,-2.63528206360562));
#7118=CARTESIAN_POINT('Ctrl Pts',(3.11415354892744,0.254492525885905,-2.6308265638831));
#7119=CARTESIAN_POINT('Ctrl Pts',(3.10769090350001,0.185176540570627,-2.62637106416058));
#7120=CARTESIAN_POINT('Ctrl Pts',(3.10123792161815,0.115964202931781,-2.62192222671359));
#7121=CARTESIAN_POINT('Ctrl Pts',(3.09839713858282,0.046307437830558,-2.61747338926661));
#7122=CARTESIAN_POINT('Ctrl Pts',(3.09921424000532,-0.0233854661888446,
-2.61302455181963));
#7123=CARTESIAN_POINT('Ctrl Pts',(3.1000303850578,-0.0929967986895868,-2.60858092147991));
#7124=CARTESIAN_POINT('Ctrl Pts',(3.10449590537496,-0.162643699280447,-2.6041372911402));
#7125=CARTESIAN_POINT('Ctrl Pts',(3.11260452902494,-0.231914783981276,-2.59969366080048));
#7126=CARTESIAN_POINT('Ctrl Pts',(3.12070808243626,-0.301142554187889,-2.59525280901695));
#7127=CARTESIAN_POINT('Ctrl Pts',(3.13245016324974,-0.36999448994615,-2.59081195723341));
#7128=CARTESIAN_POINT('Ctrl Pts',(3.14777253806218,-0.43806276791281,-2.58637110544988));
#7129=CARTESIAN_POINT('Ctrl Pts',(3.16309052850817,-0.506111568724173,-2.58193152437808));
#7130=CARTESIAN_POINT('Ctrl Pts',(3.18198667173287,-0.573376679921284,-2.57749194330629));
#7131=CARTESIAN_POINT('Ctrl Pts',(3.20435167568506,-0.639460689843633,-2.57305236223449));
#7132=CARTESIAN_POINT('Ctrl Pts',(3.2267178648945,-0.705548201958608,-2.56861254588236));
#7133=CARTESIAN_POINT('Ctrl Pts',(3.25255312069787,-0.770454025956134,-2.56417272953023));
#7134=CARTESIAN_POINT('Ctrl Pts',(3.28169891876835,-0.833797826999921,-2.5597329131781));
#7135=CARTESIAN_POINT('Ctrl Pts',(3.31087548243368,-0.897208492217892,-2.55528841026392));
#7136=CARTESIAN_POINT('Ctrl Pts',(3.34336935812326,-0.959053398371881,-2.55084390734974));
#7137=CARTESIAN_POINT('Ctrl Pts',(3.3789750817013,-1.01897493965707,-2.54639940443556));
#7138=CARTESIAN_POINT('Ctrl Pts',(3.41460169239576,-1.07893163226298,-2.54195229427624));
#7139=CARTESIAN_POINT('Ctrl Pts',(3.45334351273831,-1.13696230731877,-2.53750518411691));
#7140=CARTESIAN_POINT('Ctrl Pts',(3.49495211405337,-1.19273893392016,-2.53305807395759));
#7141=CARTESIAN_POINT('Ctrl Pts',(3.53663255276655,-1.24861185906569,-2.52860328584677));
#7142=CARTESIAN_POINT('Ctrl Pts',(3.58118933945791,-1.3022225916835,-2.52414849773595));
#7143=CARTESIAN_POINT('Ctrl Pts',(3.6283347529994,-1.35327734808887,-2.51969370962512));
#7144=CARTESIAN_POINT('Ctrl Pts',(3.65226459537614,-1.3791914759242,-2.51743256969006));
#7145=CARTESIAN_POINT('Ctrl Pts',(3.67686077852925,-1.4044477074082,-2.51517142975499));
#7146=CARTESIAN_POINT('Ctrl Pts',(3.70208239602594,-1.42901157696745,-2.51291028981993));
#7147=CARTESIAN_POINT('Ctrl Pts',(3.75178073939385,-1.47741385029353,-2.50845479013159));
#7148=CARTESIAN_POINT('Ctrl Pts',(3.80410472858639,-1.5233154944615,-2.50399929044326));
#7149=CARTESIAN_POINT('Ctrl Pts',(3.8587726100201,-1.56641879211955,-2.49954379075493));
#7150=CARTESIAN_POINT('Ctrl Pts',(3.91335874697203,-1.60945763773304,-2.49509495334257));
#7151=CARTESIAN_POINT('Ctrl Pts',(3.97028143874275,-1.64970614153343,-2.49064611593021));
#7152=CARTESIAN_POINT('Ctrl Pts',(4.02922281934548,-1.68690401921414,-2.48619727851785));
#7153=CARTESIAN_POINT('Ctrl Pts',(4.08809521245999,-1.72405835892337,-2.48175364821323));
#7154=CARTESIAN_POINT('Ctrl Pts',(4.14898118984444,-1.75816890447243,-2.4773100179086));
#7155=CARTESIAN_POINT('Ctrl Pts',(4.21153204421828,-1.78901729985797,-2.47286638760397));
#7156=CARTESIAN_POINT('Ctrl Pts',(4.27404378618446,-1.8198464060583,-2.4684255358558));
#7157=CARTESIAN_POINT('Ctrl Pts',(4.33821790217517,-1.84741719284653,-2.46398468410762));
#7158=CARTESIAN_POINT('Ctrl Pts',(4.40368042830157,-1.87155685393258,-2.45954383235944));
#7159=CARTESIAN_POINT('Ctrl Pts',(4.4691242228829,-1.89568960765993,-2.45510425132322));
#7160=CARTESIAN_POINT('Ctrl Pts',(4.53585523696321,-1.91639301563523,-2.450664670287));
#7161=CARTESIAN_POINT('Ctrl Pts',(4.60348049127541,-1.93354278758703,-2.44622508925078));
#7162=CARTESIAN_POINT('Ctrl Pts',(4.67110932945783,-1.9506934684087,-2.44178527293437));
#7163=CARTESIAN_POINT('Ctrl Pts',(4.73963202720664,-1.96429002141534,-2.43734545661797));
#7164=CARTESIAN_POINT('Ctrl Pts',(4.80864317708997,-1.97425876241818,-2.43290564030157));
#7165=CARTESIAN_POINT('Ctrl Pts',(4.87772717346325,-1.98423802618137,-2.42846113742313));
#7166=CARTESIAN_POINT('Ctrl Pts',(4.94730016595045,-1.99058176482097,-2.4240166345447));
#7167=CARTESIAN_POINT('Ctrl Pts',(5.01695030931486,-1.99326804846409,-2.41957213166627));
#7168=CARTESIAN_POINT('Ctrl Pts',(5.08664131101592,-1.99595590794145,-2.41512502154273));
#7169=CARTESIAN_POINT('Ctrl Pts',(5.15640906443546,-1.99498204875988,-2.4106779114192));
#7170=CARTESIAN_POINT('Ctrl Pts',(5.22584319353913,-1.99037667997494,-2.40623080129567));
#7171=CARTESIAN_POINT('Ctrl Pts',(5.29539720091904,-1.98576336000406,-2.40177601322035));
#7172=CARTESIAN_POINT('Ctrl Pts',(5.36461594863852,-1.97750607333603,-2.39732122514503));
#7173=CARTESIAN_POINT('Ctrl Pts',(5.43309644768473,-1.96568662554555,-2.39286643706971));
#7174=CARTESIAN_POINT('Ctrl Pts',(5.46785545536319,-1.95968736616184,-2.39060529681704));
#7175=CARTESIAN_POINT('Ctrl Pts',(5.50242446312932,-1.95277118902458,-2.38834415656438));
#7176=CARTESIAN_POINT('Ctrl Pts',(5.53675230609656,-1.94495369441729,-2.38608301631171));
#7177=CARTESIAN_POINT('Ctrl Pts',(5.60439414895831,-1.92954958812657,-2.38162751662287));
#7178=CARTESIAN_POINT('Ctrl Pts',(5.67136432185437,-1.91058233412087,-2.37717201693402));
#7179=CARTESIAN_POINT('Ctrl Pts',(5.73725977785801,-1.88812659081036,-2.37271651724518));
#7180=CARTESIAN_POINT('Ctrl Pts',(5.80305670086891,-1.86570442540835,-2.36826767983239));
#7181=CARTESIAN_POINT('Ctrl Pts',(5.86778163730379,-1.83980428061653,-2.3638188424196));
#7182=CARTESIAN_POINT('Ctrl Pts',(5.93104332991556,-1.81055147392126,-2.3593700050068));
#7183=CARTESIAN_POINT('Ctrl Pts',(5.99423097836069,-1.78133290595096,-2.3549263747019));
#7184=CARTESIAN_POINT('Ctrl Pts',(6.05595834269379,-1.74876967434823,-2.350482744397));
#7185=CARTESIAN_POINT('Ctrl Pts',(6.11585259374666,-1.71303577486895,-2.3460391140921));
#7186=CARTESIAN_POINT('Ctrl Pts',(6.17570939353755,-1.67732421943117,-2.34159826234373));
#7187=CARTESIAN_POINT('Ctrl Pts',(6.23373493485255,-1.63844617932036,-2.33715741059537));
#7188=CARTESIAN_POINT('Ctrl Pts',(6.28958089198515,-1.59662160954613,-2.332716558847));
#7189=CARTESIAN_POINT('Ctrl Pts',(6.3454108692708,-1.55480900751777,-2.32827697781069));
#7190=CARTESIAN_POINT('Ctrl Pts',(6.39906210918047,-1.51005184274183,-2.32383739677439));
#7191=CARTESIAN_POINT('Ctrl Pts',(6.45021667187041,-1.46261240328846,-2.31939781573808));
#7192=CARTESIAN_POINT('Ctrl Pts',(6.50137394554798,-1.41517044973417,-2.3149579994217));
#7193=CARTESIAN_POINT('Ctrl Pts',(6.5500339222949,-1.36504627368842,-2.31051818310532));
#7194=CARTESIAN_POINT('Ctrl Pts',(6.59591438312211,-1.31254010337729,-2.30607836678895));
#7195=CARTESIAN_POINT('Ctrl Pts',(6.64184327424584,-1.25997850883215,-2.30163386391064));
#7196=CARTESIAN_POINT('Ctrl Pts',(6.6849864710863,-1.2050302707258,-2.29718936103235));
#7197=CARTESIAN_POINT('Ctrl Pts',(6.72510169553051,-1.14802915354762,-2.29274485815405));
#7198=CARTESIAN_POINT('Ctrl Pts',(6.76524045246458,-1.0909945982364,-2.28829774803073));
#7199=CARTESIAN_POINT('Ctrl Pts',(6.80234744129299,-1.03190518124544,-2.28385063790742));
#7200=CARTESIAN_POINT('Ctrl Pts',(6.83622494570269,-0.971121775594272,-2.2794035277841));
#7201=CARTESIAN_POINT('Ctrl Pts',(6.87016093974603,-0.910233427173865,-2.27494873970911));
#7202=CARTESIAN_POINT('Ctrl Pts',(6.90085610448131,-0.847645691295311,-2.27049395163411));
#7203=CARTESIAN_POINT('Ctrl Pts',(6.92816004693264,-0.78374128750267,-2.26603916355912));
#7204=CARTESIAN_POINT('Ctrl Pts',(6.94201885284491,-0.751304992609359,-2.26377802330725));
#7205=CARTESIAN_POINT('Ctrl Pts',(6.95500475721979,-0.718529756660505,-2.26151688305537));
#7206=CARTESIAN_POINT('Ctrl Pts',(6.96710304201812,-0.685467005270186,-2.2592557428035));
#7207=CARTESIAN_POINT('Ctrl Pts',(6.99459284271437,-0.610341608460643,-2.25411796534938));
#7208=CARTESIAN_POINT('Ctrl Pts',(7.01758619456045,-0.533487851592203,-2.24898018789526));
#7209=CARTESIAN_POINT('Ctrl Pts',(7.03589429966574,-0.455414942519256,-2.24384241044115));
#7210=CARTESIAN_POINT('Ctrl Pts',(7.05404569288441,-0.378010314123302,-2.23874861082052));
#7211=CARTESIAN_POINT('Ctrl Pts',(7.06759161076418,-0.299407491567439,-2.2336548111999));
#7212=CARTESIAN_POINT('Ctrl Pts',(7.07639445970045,-0.220123707558807,-2.22856101157927));
#7213=CARTESIAN_POINT('Ctrl Pts',(7.08444110624045,-0.147650739899122,-2.22390479114546));
#7214=CARTESIAN_POINT('Ctrl Pts',(7.08852500633563,-0.074609111606327,-2.21924857071165));
#7215=CARTESIAN_POINT('Ctrl Pts',(7.08857665886015,-0.00140753592614233,
-2.21459235027785));
#7216=CARTESIAN_POINT('Ctrl Pts',(7.08857715545311,1.10874632379271E-10,
-3.17330009074087));
#7217=CARTESIAN_POINT('Ctrl Pts',(7.08857715545308,0.000599462197711708,
-3.17325859730295));
#7218=CARTESIAN_POINT('Ctrl Pts',(7.08857688524422,0.0011989297675538,-3.17321709980395));
#7219=CARTESIAN_POINT('Ctrl Pts',(7.08855819985703,0.0219243629936726,-3.17178227682757));
#7220=CARTESIAN_POINT('Ctrl Pts',(7.08823546589232,0.0420486590280136,-3.17038492010015));
#7221=CARTESIAN_POINT('Ctrl Pts',(7.08334010096522,0.199056332811374,-3.15945848135308));
#7222=CARTESIAN_POINT('Ctrl Pts',(7.06498484703654,0.335153782962829,-3.14981256578896));
#7223=CARTESIAN_POINT('Ctrl Pts',(7.02925382032359,0.483097077674355,-3.13973835663072));
#7224=CARTESIAN_POINT('Ctrl Pts',(7.02551172499111,0.497849293242752,-3.1387388094495));
#7225=CARTESIAN_POINT('Ctrl Pts',(7.02008490974601,0.51826001278871,-3.13736418295022));
#7226=CARTESIAN_POINT('Ctrl Pts',(7.01854347430543,0.523955600119139,-3.13698149880969));
#7227=CARTESIAN_POINT('Ctrl Pts',(7.01584851381334,0.533741057508895,-3.13632567385635));
#7228=CARTESIAN_POINT('Ctrl Pts',(7.01470716129347,0.53783419605856,-3.13605185003928));
#7229=CARTESIAN_POINT('Ctrl Pts',(7.01228917827564,0.546399726230936,-3.13547992441716));
#7230=CARTESIAN_POINT('Ctrl Pts',(7.01100997372563,0.550871342282968,-3.13518198267385));
#7231=CARTESIAN_POINT('Ctrl Pts',(7.00784178879654,0.561801410411964,-3.13445517294403));
#7232=CARTESIAN_POINT('Ctrl Pts',(7.00593572353959,0.568254932546007,-3.13402728285012));
#7233=CARTESIAN_POINT('Ctrl Pts',(6.99892426319377,0.591559453513844,-3.13248621205023));
#7234=CARTESIAN_POINT('Ctrl Pts',(6.99362829990496,0.608352889783915,-3.13138346980831));
#7235=CARTESIAN_POINT('Ctrl Pts',(6.97984408802542,0.650125823019246,-3.12865480406176));
#7236=CARTESIAN_POINT('Ctrl Pts',(6.97108119055639,0.675011761329208,-3.12704216521398));
#7237=CARTESIAN_POINT('Ctrl Pts',(6.93081149283235,0.782517659410478,-3.1201027036711));
#7238=CARTESIAN_POINT('Ctrl Pts',(6.89432279725226,0.863170427002166,-3.11496381255671));
#7239=CARTESIAN_POINT('Ctrl Pts',(6.78401015454395,1.06931903808697,-3.10138862513449));
#7240=CARTESIAN_POINT('Ctrl Pts',(6.7016233009776,1.18959966672738,-3.0929708270439));
#7241=CARTESIAN_POINT('Ctrl Pts',(6.59069505190685,1.31872392252539,-3.08249444309442));
#7242=CARTESIAN_POINT('Ctrl Pts',(6.57413522328348,1.33728614082925,-3.08095037489573));
#7243=CARTESIAN_POINT('Ctrl Pts',(6.5505292194155,1.36277070092467,-3.07877380360066));
#7244=CARTESIAN_POINT('Ctrl Pts',(6.54377175695719,1.36995822324756,-3.07815344641891));
#7245=CARTESIAN_POINT('Ctrl Pts',(6.53129710752092,1.383031097873,-3.07701297483722));
#7246=CARTESIAN_POINT('Ctrl Pts',(6.5255963636265,1.38893189611541,-3.07649357206908));
#7247=CARTESIAN_POINT('Ctrl Pts',(6.51396563835607,1.40082307913303,-3.07543735871395));
#7248=CARTESIAN_POINT('Ctrl Pts',(6.50803377187297,1.40681137760315,-3.07490047142813));
#7249=CARTESIAN_POINT('Ctrl Pts',(6.49327891846793,1.42151897432977,-3.07356932572655));
#7250=CARTESIAN_POINT('Ctrl Pts',(6.48441230790119,1.4301938168302,-3.07277314627218));
#7251=CARTESIAN_POINT('Ctrl Pts',(6.45081512391981,1.46245655996554,-3.06976973918098));
#7252=CARTESIAN_POINT('Ctrl Pts',(6.42556181110556,1.48548918045345,-3.06753906195773));
#7253=CARTESIAN_POINT('Ctrl Pts',(6.36051183122157,1.54182660836251,-3.06185559227363));
#7254=CARTESIAN_POINT('Ctrl Pts',(6.31998585893191,1.57424694483761,-3.05837030204562));
#7255=CARTESIAN_POINT('Ctrl Pts',(6.18634616739285,1.6728640373679,-3.04705977449551));
#7256=CARTESIAN_POINT('Ctrl Pts',(6.08879785467727,1.73265736179203,-3.03905845787811));
#7257=CARTESIAN_POINT('Ctrl Pts',(5.90555242892172,1.82437944775786,-3.02480992475655));
#7258=CARTESIAN_POINT('Ctrl Pts',(5.82173868182922,1.859410380186,-3.01856146136709));
#7259=CARTESIAN_POINT('Ctrl Pts',(5.72545309783015,1.89214063303886,-3.01187724978873));
#7260=CARTESIAN_POINT('Ctrl Pts',(5.71505479225973,1.89558005436162,-3.01116172138711));
#7261=CARTESIAN_POINT('Ctrl Pts',(5.69926637141212,1.90065847653283,-3.0100854003819));
#7262=CARTESIAN_POINT('Ctrl Pts',(5.69389697192569,1.90236050891383,-3.00972112165501));
#7263=CARTESIAN_POINT('Ctrl Pts',(5.68422790960847,1.90538046974482,-3.00906839323145));
#7264=CARTESIAN_POINT('Ctrl Pts',(5.67993095539784,1.90670661662102,-3.00877947755593));
#7265=CARTESIAN_POINT('Ctrl Pts',(5.67048094406062,1.90958816028564,-3.00814662882166));
#7266=CARTESIAN_POINT('Ctrl Pts',(5.66532606828273,1.91113723423796,-3.00780306265572));
#7267=CARTESIAN_POINT('Ctrl Pts',(5.65048309252642,1.91553222010498,-3.00681835513865));
#7268=CARTESIAN_POINT('Ctrl Pts',(5.64077940472971,1.91832551086783,-3.00618016772019));
#7269=CARTESIAN_POINT('Ctrl Pts',(5.57026564435231,1.93804495109615,-3.00158015395771));
#7270=CARTESIAN_POINT('Ctrl Pts',(5.50869716520569,1.95215175051466,-2.9977649488736));
#7271=CARTESIAN_POINT('Ctrl Pts',(5.31807572058205,1.98639886348312,-2.98627866568773));
#7272=CARTESIAN_POINT('Ctrl Pts',(5.18763569593124,1.99681510417929,-2.97884991967218));
#7273=CARTESIAN_POINT('Ctrl Pts',(4.96779674576504,1.99276773575839,-2.96591712762864));
#7274=CARTESIAN_POINT('Ctrl Pts',(4.87870633027246,1.98512645102287,-2.96056572148074));
#7275=CARTESIAN_POINT('Ctrl Pts',(4.77494547054984,1.96915911626876,-2.95405053549089));
#7276=CARTESIAN_POINT('Ctrl Pts',(4.75948541340779,1.96659317904938,-2.95307251956547));
#7277=CARTESIAN_POINT('Ctrl Pts',(4.7341602256607,1.96208265015669,-2.9514577364435));
#7278=CARTESIAN_POINT('Ctrl Pts',(4.72427653730745,1.96024512781647,-2.95082434648351));
#7279=CARTESIAN_POINT('Ctrl Pts',(4.70651566754514,1.95680402430243,-2.94968022908205));
#7280=CARTESIAN_POINT('Ctrl Pts',(4.69863344113995,1.95522737892046,-2.94917036554373));
#7281=CARTESIAN_POINT('Ctrl Pts',(4.68183011782371,1.95176052843171,-2.9480788396038));
#7282=CARTESIAN_POINT('Ctrl Pts',(4.67291204795625,1.94985670937686,-2.94749675445292));
#7283=CARTESIAN_POINT('Ctrl Pts',(4.64878571595056,1.94453301924304,-2.94591433253504));
#7284=CARTESIAN_POINT('Ctrl Pts',(4.6336042300655,1.94099597679873,-2.94491028469131));
#7285=CARTESIAN_POINT('Ctrl Pts',(4.55305830992402,1.92123199614168,-2.93953776417323));
#7286=CARTESIAN_POINT('Ctrl Pts',(4.48851241563625,1.90188213171461,-2.93507014459762));
#7287=CARTESIAN_POINT('Ctrl Pts',(4.27204102409429,1.82485063381894,-2.9195228906552));
#7288=CARTESIAN_POINT('Ctrl Pts',(4.12623744836733,1.75190534748897,-2.9080144945353));
#7289=CARTESIAN_POINT('Ctrl Pts',(3.94415105596452,1.63108013443148,-2.89301170889262));
#7290=CARTESIAN_POINT('Ctrl Pts',(3.89871125274439,1.59808534164191,-2.88921488632742));
#7291=CARTESIAN_POINT('Ctrl Pts',(3.84741261208193,1.55742264339405,-2.88491815662332));
#7292=CARTESIAN_POINT('Ctrl Pts',(3.84014606263841,1.55157926952471,-2.88430927925407));
#7293=CARTESIAN_POINT('Ctrl Pts',(3.82844597196557,1.54203481452343,-2.88332888610201));
#7294=CARTESIAN_POINT('Ctrl Pts',(3.82398715849579,1.53836513639445,-2.88295526090424));
#7295=CARTESIAN_POINT('Ctrl Pts',(3.81607763090086,1.53179764267695,-2.88229257161583));
#7296=CARTESIAN_POINT('Ctrl Pts',(3.8126207405265,1.52890744956191,-2.88200297619616));
#7297=CARTESIAN_POINT('Ctrl Pts',(3.80514065358463,1.52261040757635,-2.8813764347959));
#7298=CARTESIAN_POINT('Ctrl Pts',(3.80112116155103,1.51919931813778,-2.8810398025404));
#7299=CARTESIAN_POINT('Ctrl Pts',(3.78983648953625,1.50954551365542,-2.88009468474169));
#7300=CARTESIAN_POINT('Ctrl Pts',(3.78260256871981,1.50326624601553,-2.87948879500414));
#7301=CARTESIAN_POINT('Ctrl Pts',(3.73748717842351,1.46353123690688,-2.87570779775224));
#7302=CARTESIAN_POINT('Ctrl Pts',(3.70083994449417,1.42869499687468,-2.87262618803146));
#7303=CARTESIAN_POINT('Ctrl Pts',(3.59548929689736,1.32063787629418,-2.86359261399795));
#7304=CARTESIAN_POINT('Ctrl Pts',(3.53094533123544,1.24358499474055,-2.85781284671031));
#7305=CARTESIAN_POINT('Ctrl Pts',(3.39557524041277,1.05470074869476,-2.8443091295812));
#7306=CARTESIAN_POINT('Ctrl Pts',(3.32952882804349,0.940052181009512,-2.83656388734938));
#7307=CARTESIAN_POINT('Ctrl Pts',(3.26863874945042,0.804970158107974,-2.82737491614366));
#7308=CARTESIAN_POINT('Ctrl Pts',(3.26216573805277,0.790130432826794,-2.8263650863912));
#7309=CARTESIAN_POINT('Ctrl Pts',(3.25190633900863,0.765806445899519,-2.82470847652323));
#7310=CARTESIAN_POINT('Ctrl Pts',(3.24801080184816,0.756368818228067,-2.82406538305793));
#7311=CARTESIAN_POINT('Ctrl Pts',(3.2411724132598,0.739434127479379,-2.82291064384033));
#7312=CARTESIAN_POINT('Ctrl Pts',(3.23820216995446,0.73194831289552,-2.82239993067219));
#7313=CARTESIAN_POINT('Ctrl Pts',(3.23200145828401,0.716040501512925,-2.82131396231731));
#7314=CARTESIAN_POINT('Ctrl Pts',(3.22878263051223,0.707614190108583,-2.82073833197637));
#7315=CARTESIAN_POINT('Ctrl Pts',(3.2203156685789,0.684990064607807,-2.81919159130164));
#7316=CARTESIAN_POINT('Ctrl Pts',(3.21517188729456,0.670754085046129,-2.81821705028842));
#7317=CARTESIAN_POINT('Ctrl Pts',(3.19013611969438,0.598916969227695,-2.81329195112207));
#7318=CARTESIAN_POINT('Ctrl Pts',(3.17273091629326,0.540489618055237,-2.80926097638077));
#7319=CARTESIAN_POINT('Ctrl Pts',(3.12687276047993,0.356070950706149,-2.79645435599716));
#7320=CARTESIAN_POINT('Ctrl Pts',(3.10795783213181,0.22806195218001,-2.78742380415097));
#7321=CARTESIAN_POINT('Ctrl Pts',(3.09680022457168,0.00384556538273569,
-2.77180067554752));
#7322=CARTESIAN_POINT('Ctrl Pts',(3.09890096906112,-0.0916795623901858,
-2.76521469552477));
#7323=CARTESIAN_POINT('Ctrl Pts',(3.10885811464207,-0.197599032530022,-2.75822224834573));
#7324=CARTESIAN_POINT('Ctrl Pts',(3.10997277672483,-0.208492895744148,-2.75750682781076));
#7325=CARTESIAN_POINT('Ctrl Pts',(3.11179654074277,-0.224975391926986,-2.75643063690742));
#7326=CARTESIAN_POINT('Ctrl Pts',(3.11243967545514,-0.23057090147684,-2.75606638162384));
#7327=CARTESIAN_POINT('Ctrl Pts',(3.11363891316854,-0.240628988111074,-2.75541367810742));
#7328=CARTESIAN_POINT('Ctrl Pts',(3.11418641163659,-0.245092454812895,-2.75512476405867));
#7329=CARTESIAN_POINT('Ctrl Pts',(3.11542243430872,-0.254894676855335,-2.7544918986872));
#7330=CARTESIAN_POINT('Ctrl Pts',(3.11611747457295,-0.260232505130362,-2.75414831439715));
#7331=CARTESIAN_POINT('Ctrl Pts',(3.11817859553243,-0.275576330403442,-2.75316350253923));
#7332=CARTESIAN_POINT('Ctrl Pts',(3.11959908821063,-0.285575024830621,-2.75252522987678));
#7333=CARTESIAN_POINT('Ctrl Pts',(3.13045409874494,-0.358026723464336,-2.74792264118044));
#7334=CARTESIAN_POINT('Ctrl Pts',(3.14277524680914,-0.420017931764002,-2.74410513326315));
#7335=CARTESIAN_POINT('Ctrl Pts',(3.18957166695359,-0.608224869583766,-2.73260349136378));
#7336=CARTESIAN_POINT('Ctrl Pts',(3.23352617170598,-0.731716781852988,-2.72516246728735));
#7337=CARTESIAN_POINT('Ctrl Pts',(3.32721120771476,-0.930607595809442,-2.71222973258471));
#7338=CARTESIAN_POINT('Ctrl Pts',(3.37052061051785,-1.00855047430586,-2.70689262587135));
#7339=CARTESIAN_POINT('Ctrl Pts',(3.42739549837876,-1.09648457176304,-2.70039337637139));
#7340=CARTESIAN_POINT('Ctrl Pts',(3.43605621509267,-1.10953520509804,-2.69941589002208));
#7341=CARTESIAN_POINT('Ctrl Pts',(3.45052509481402,-1.13079039226603,-2.69780180355726));
#7342=CARTESIAN_POINT('Ctrl Pts',(3.45624328259062,-1.13905558563002,-2.69716857562696));
#7343=CARTESIAN_POINT('Ctrl Pts',(3.46664674010609,-1.15385270745091,-2.69602463369584));
#7344=CARTESIAN_POINT('Ctrl Pts',(3.47130952444587,-1.16040023637221,-2.69551478244949));
#7345=CARTESIAN_POINT('Ctrl Pts',(3.48134732194818,-1.17431662592668,-2.69442315499969));
#7346=CARTESIAN_POINT('Ctrl Pts',(3.48673354148419,-1.18167713982591,-2.69384095521477));
#7347=CARTESIAN_POINT('Ctrl Pts',(3.50146616940529,-1.20152290279843,-2.69225789936058));
#7348=CARTESIAN_POINT('Ctrl Pts',(3.51090867614908,-1.21393569058628,-2.6912533271544));
#7349=CARTESIAN_POINT('Ctrl Pts',(3.5619713908644,-1.27945209224144,-2.68587234365543));
#7350=CARTESIAN_POINT('Ctrl Pts',(3.60611588380436,-1.3305236385502,-2.68139641038207));
#7351=CARTESIAN_POINT('Ctrl Pts',(3.76562628947781,-1.49718260190214,-2.66578553157318));
#7352=CARTESIAN_POINT('Ctrl Pts',(3.89254069301763,-1.6008041593079,-2.65421694403471));
#7353=CARTESIAN_POINT('Ctrl Pts',(4.07738317138215,-1.71724266913717,-2.63922608057721));
#7354=CARTESIAN_POINT('Ctrl Pts',(4.12534429680093,-1.74474150023,-2.63548991167286));
#7355=CARTESIAN_POINT('Ctrl Pts',(4.18263260946149,-1.77449664234036,-2.63125291024725));
#7356=CARTESIAN_POINT('Ctrl Pts',(4.1909053520917,-1.77872034318595,-2.63064641760298));
#7357=CARTESIAN_POINT('Ctrl Pts',(4.20435913868881,-1.78547120712331,-2.6296690978502));
#7358=CARTESIAN_POINT('Ctrl Pts',(4.20952205228512,-1.78803391210372,-2.62929618221603));
#7359=CARTESIAN_POINT('Ctrl Pts',(4.2187399988187,-1.79255971342181,-2.62863426021949));
#7360=CARTESIAN_POINT('Ctrl Pts',(4.22279064027287,-1.79453148439082,-2.62834472746863));
#7361=CARTESIAN_POINT('Ctrl Pts',(4.23160281608187,-1.79878420722699,-2.62771775740988));
#7362=CARTESIAN_POINT('Ctrl Pts',(4.23636673380252,-1.80105998301711,-2.62738063762035));
#7363=CARTESIAN_POINT('Ctrl Pts',(4.24983185105195,-1.80742688221737,-2.62643275574421));
#7364=CARTESIAN_POINT('Ctrl Pts',(4.25855381394333,-1.81147411301936,-2.62582461376662));
#7365=CARTESIAN_POINT('Ctrl Pts',(4.3139814206665,-1.83670859642773,-2.62199467609262));
#7366=CARTESIAN_POINT('Ctrl Pts',(4.36146461431275,-1.85615299318411,-2.61886920120932));
#7367=CARTESIAN_POINT('Ctrl Pts',(4.55391893185157,-1.92642559753121,-2.60661253281853));
#7368=CARTESIAN_POINT('Ctrl Pts',(4.70379578034513,-1.96226856984545,-2.5979392534222));
#7369=CARTESIAN_POINT('Ctrl Pts',(4.93545402025679,-1.99005012829157,-2.58415291208009));
#7370=CARTESIAN_POINT('Ctrl Pts',(5.0150882535075,-1.99478809674902,-2.57935517585511));
#7371=CARTESIAN_POINT('Ctrl Pts',(5.11008303245937,-1.99474241310027,-2.57345672839195));
#7372=CARTESIAN_POINT('Ctrl Pts',(5.1253786860223,-1.99455910636388,-2.57250172253999));
#7373=CARTESIAN_POINT('Ctrl Pts',(5.15060636511678,-1.99396651472431,-2.57091723461746));
#7374=CARTESIAN_POINT('Ctrl Pts',(5.1605403054555,-1.99365887011127,-2.57029091349595));
#7375=CARTESIAN_POINT('Ctrl Pts',(5.17849470039393,-1.9929684990042,-2.56915440867983));
#7376=CARTESIAN_POINT('Ctrl Pts',(5.18651597785913,-1.99261155530148,-2.56864503884174));
#7377=CARTESIAN_POINT('Ctrl Pts',(5.20372150112516,-1.99174180220805,-2.56754886083598));
#7378=CARTESIAN_POINT('Ctrl Pts',(5.21290476363112,-1.99121387410926,-2.56696159251266));
#7379=CARTESIAN_POINT('Ctrl Pts',(5.23800282211048,-1.98959679408237,-2.56535041177679));
#7380=CARTESIAN_POINT('Ctrl Pts',(5.25390845052865,-1.98838024039937,-2.56432255550063));
#7381=CARTESIAN_POINT('Ctrl Pts',(5.34271759863926,-1.98051512736598,-2.55854423134054));
#7382=CARTESIAN_POINT('Ctrl Pts',(5.41521838799733,-1.97004874809723,-2.55367573803175));
#7383=CARTESIAN_POINT('Ctrl Pts',(5.58306179456705,-1.93630658823773,-2.54205108104042));
#7384=CARTESIAN_POINT('Ctrl Pts',(5.67758910638322,-1.90993530281414,-2.5352260734693));
#7385=CARTESIAN_POINT('Ctrl Pts',(5.86815384222339,-1.84129762540535,-2.52110583258603));
#7386=CARTESIAN_POINT('Ctrl Pts',(5.96359245790004,-1.79818558055694,-2.51383148247287));
#7387=CARTESIAN_POINT('Ctrl Pts',(6.06945908717783,-1.73995231235122,-2.5058220191991));
#7388=CARTESIAN_POINT('Ctrl Pts',(6.08360394316704,-1.73194505292132,-2.50475338193356));
#7389=CARTESIAN_POINT('Ctrl Pts',(6.10346738184406,-1.72037771904275,-2.50325652823694));
#7390=CARTESIAN_POINT('Ctrl Pts',(6.10926780035158,-1.71696044880687,-2.50281989183592));
#7391=CARTESIAN_POINT('Ctrl Pts',(6.11890370945152,-1.71121761841299,-2.50209545576842));
#7392=CARTESIAN_POINT('Ctrl Pts',(6.12274881544539,-1.70890839368137,-2.50180662423489));
#7393=CARTESIAN_POINT('Ctrl Pts',(6.13059990769312,-1.7041572206578,-2.5012174338885));
#7394=CARTESIAN_POINT('Ctrl Pts',(6.13460512208584,-1.70171407638988,-2.50091715561444));
#7395=CARTESIAN_POINT('Ctrl Pts',(6.14468431829071,-1.6955169624728,-2.50016214899386));
#7396=CARTESIAN_POINT('Ctrl Pts',(6.15074689275019,-1.69174443085517,-2.49970861472096));
#7397=CARTESIAN_POINT('Ctrl Pts',(6.16390253631906,-1.68345980287491,-2.49872546297339));
#7398=CARTESIAN_POINT('Ctrl Pts',(6.17098763765437,-1.67893523693992,-2.49819662000978));
#7399=CARTESIAN_POINT('Ctrl Pts',(6.19139450518203,-1.66572099835597,-2.49667464060269));
#7400=CARTESIAN_POINT('Ctrl Pts',(6.20464152324734,-1.65691641483263,-2.49568817162834));
#7401=CARTESIAN_POINT('Ctrl Pts',(6.25053053157035,-1.62561870653975,-2.49227101656605));
#7402=CARTESIAN_POINT('Ctrl Pts',(6.28260783228616,-1.60231075923823,-2.48988241958157));
#7403=CARTESIAN_POINT('Ctrl Pts',(6.38771542861098,-1.52104242085849,-2.48197949488714));
#7404=CARTESIAN_POINT('Ctrl Pts',(6.45737577984375,-1.45892211827249,-2.47660883735775));
#7405=CARTESIAN_POINT('Ctrl Pts',(6.61331371178524,-1.2989006158401,-2.46362201147581));
#7406=CARTESIAN_POINT('Ctrl Pts',(6.69482689403146,-1.1969860626194,-2.45597534774945));
#7407=CARTESIAN_POINT('Ctrl Pts',(6.77466215837702,-1.07428292892219,-2.44689708306991));
#7408=CARTESIAN_POINT('Ctrl Pts',(6.7833329776571,-1.06059425376905,-2.44588640953958));
#7409=CARTESIAN_POINT('Ctrl Pts',(6.79719604010469,-1.03810709182073,-2.44422869124023));
#7410=CARTESIAN_POINT('Ctrl Pts',(6.80248926118714,-1.02937150412238,-2.4435853414909));
#7411=CARTESIAN_POINT('Ctrl Pts',(6.81183584765462,-1.01367576831297,-2.44243031917921));
#7412=CARTESIAN_POINT('Ctrl Pts',(6.81591461598052,-1.0067309496303,-2.44191958101522));
#7413=CARTESIAN_POINT('Ctrl Pts',(6.82447082349166,-0.991958354125411,-2.44083374727074));
#7414=CARTESIAN_POINT('Ctrl Pts',(6.82893745106589,-0.984124554978757,-2.4402582777393));
#7415=CARTESIAN_POINT('Ctrl Pts',(6.84075334876596,-0.963070721916951,-2.43871242491866));
#7416=CARTESIAN_POINT('Ctrl Pts',(6.84800551274211,-0.949797141649947,-2.43773861781169));
#7417=CARTESIAN_POINT('Ctrl Pts',(6.88364374943014,-0.882768086197412,-2.43282397972328));
#7418=CARTESIAN_POINT('Ctrl Pts',(6.90971035575264,-0.827822346857297,-2.42880314442229));
#7419=CARTESIAN_POINT('Ctrl Pts',(7.00196426767203,-0.607950867054155,-2.41273593145567));
#7420=CARTESIAN_POINT('Ctrl Pts',(7.04849773362159,-0.435706415553922,-2.40010830636737));
#7421=CARTESIAN_POINT('Ctrl Pts',(7.07540191313661,-0.230730475128536,-2.38597561417028));
#7422=CARTESIAN_POINT('Ctrl Pts',(7.07855837344646,-0.201785105911168,-2.38400261190848));
#7423=CARTESIAN_POINT('Ctrl Pts',(7.08314538899354,-0.14902681609023,-2.380459073846));
#7424=CARTESIAN_POINT('Ctrl Pts',(7.08478463972377,-0.125237544368088,-2.37888063083536));
#7425=CARTESIAN_POINT('Ctrl Pts',(7.08639479754835,-0.0936106371364966,
-2.37681274808185));
#7426=CARTESIAN_POINT('Ctrl Pts',(7.08674659769538,-0.0857954621362452,
-2.37630424185497));
#7427=CARTESIAN_POINT('Ctrl Pts',(7.08724338861386,-0.0730968440859805,
-2.3754822302458));
#7428=CARTESIAN_POINT('Ctrl Pts',(7.08741642779279,-0.0682146736635013,
-2.37516721412269));
#7429=CARTESIAN_POINT('Ctrl Pts',(7.08770735024483,-0.0590561701382827,
-2.37457824453436));
#7430=CARTESIAN_POINT('Ctrl Pts',(7.08782941437726,-0.0547800525580501,
-2.37430406518427));
#7431=CARTESIAN_POINT('Ctrl Pts',(7.08805314365561,-0.0459461989416382,
-2.37373927019286));
#7432=CARTESIAN_POINT('Ctrl Pts',(7.08815294255975,-0.0413884172803767,
-2.37344875705754));
#7433=CARTESIAN_POINT('Ctrl Pts',(7.08834967083952,-0.0307353121714973,
-2.37277172434694));
#7434=CARTESIAN_POINT('Ctrl Pts',(7.08843428665534,-0.0246397686534487,
-2.37238586387929));
#7435=CARTESIAN_POINT('Ctrl Pts',(7.08854690723388,-0.0125257633651796,
-2.37162188786747));
#7436=CARTESIAN_POINT('Ctrl Pts',(7.08857562044022,-0.00650738880385826,
-2.37124374122592));
#7437=CARTESIAN_POINT('Ctrl Pts',(7.08857709553938,-0.000488902672746962,
-2.37086691085377));
#7438=CARTESIAN_POINT('Origin',(5.09382715545311,0.,-6.77268258743872));
#7439=CARTESIAN_POINT('',(7.08857715545311,-2.35333930719797E-11,-1.41355420449641));
#7440=CARTESIAN_POINT('',(7.08857715545311,2.4467182997506E-11,-1.57370881642439));
#7441=CARTESIAN_POINT('',(7.08857715545311,8.3550772080578E-14,-6.77268258743872));
#7442=CARTESIAN_POINT('Ctrl Pts',(7.08857715545311,-2.35333930719797E-11,
-1.41355420449641));
#7443=CARTESIAN_POINT('Ctrl Pts',(7.08857715545221,-0.0760979527884141,
-1.4180590646126));
#7444=CARTESIAN_POINT('Ctrl Pts',(7.08422265901158,-0.152126174664224,-1.42264720274503));
#7445=CARTESIAN_POINT('Ctrl Pts',(7.07380624441203,-0.242776045741805,-1.42831398992487));
#7446=CARTESIAN_POINT('Ctrl Pts',(7.07190396716427,-0.257816811514585,-1.42926063316788));
#7447=CARTESIAN_POINT('Ctrl Pts',(7.06847680026894,-0.282638095745051,-1.43083410243593));
#7448=CARTESIAN_POINT('Ctrl Pts',(7.06705020328532,-0.292431719854238,-1.43145784456551));
#7449=CARTESIAN_POINT('Ctrl Pts',(7.06433477461791,-0.310147880213191,-1.43259160122804));
#7450=CARTESIAN_POINT('Ctrl Pts',(7.06307088536315,-0.318074069881306,-1.43310082018308));
#7451=CARTESIAN_POINT('Ctrl Pts',(7.06025093570649,-0.335097382806626,-1.43419883612959));
#7452=CARTESIAN_POINT('Ctrl Pts',(7.05867951192604,-0.344191737359292,-1.43478810757055));
#7453=CARTESIAN_POINT('Ctrl Pts',(7.05419493901455,-0.369113400100443,-1.43641043444629));
#7454=CARTESIAN_POINT('Ctrl Pts',(7.05115332601244,-0.384916596047755,-1.43744752561958));
#7455=CARTESIAN_POINT('Ctrl Pts',(7.03271966714409,-0.474816311443012,-1.44339632336613));
#7456=CARTESIAN_POINT('Ctrl Pts',(7.01331380419635,-0.548017567586935,-1.44843453417937));
#7457=CARTESIAN_POINT('Ctrl Pts',(6.95485760376048,-0.726797243136719,-1.46122412816399));
#7458=CARTESIAN_POINT('Ctrl Pts',(6.91094536633002,-0.830509608792088,-1.46909053202858));
#7459=CARTESIAN_POINT('Ctrl Pts',(6.81398900352541,-1.0144956315532,-1.48356403772491));
#7460=CARTESIAN_POINT('Ctrl Pts',(6.76341905098709,-1.0957305166476,-1.49016014346713));
#7461=CARTESIAN_POINT('Ctrl Pts',(6.70077471425887,-1.18189128702913,-1.49716182494519));
#7462=CARTESIAN_POINT('Ctrl Pts',(6.69426228757446,-1.19069512131317,-1.4978772469108));
#7463=CARTESIAN_POINT('Ctrl Pts',(6.68429084513701,-1.20394540427319,-1.49895343953243));
#7464=CARTESIAN_POINT('Ctrl Pts',(6.68088507605155,-1.20843139781207,-1.49931769511946));
#7465=CARTESIAN_POINT('Ctrl Pts',(6.67472596013743,-1.21647307990937,-1.49997039890692));
#7466=CARTESIAN_POINT('Ctrl Pts',(6.67197956235814,-1.22003392024961,-1.5002593129258));
#7467=CARTESIAN_POINT('Ctrl Pts',(6.66591924104566,-1.22783672012552,-1.50089217789054));
#7468=CARTESIAN_POINT('Ctrl Pts',(6.6626001843452,-1.23207456037774,-1.50123576180621));
#7469=CARTESIAN_POINT('Ctrl Pts',(6.65300504670706,-1.24422419569824,-1.50222057185984));
#7470=CARTESIAN_POINT('Ctrl Pts',(6.64668587778284,-1.25210197041621,-1.50285884310738));
#7471=CARTESIAN_POINT('Ctrl Pts',(6.60041327654971,-1.3088984223833,-1.50746139371859));
#7472=CARTESIAN_POINT('Ctrl Pts',(6.55821191719384,-1.35594830603633,-1.51127886768112));
#7473=CARTESIAN_POINT('Ctrl Pts',(6.42201158970083,-1.49400525578319,-1.52278028367437));
#7474=CARTESIAN_POINT('Ctrl Pts',(6.32124652972505,-1.5778371325406,-1.53022112715308));
#7475=CARTESIAN_POINT('Ctrl Pts',(6.13925881703669,-1.70118655634368,-1.54315386280845));
#7476=CARTESIAN_POINT('Ctrl Pts',(6.06226281206282,-1.74616509531594,-1.54849118000131));
#7477=CARTESIAN_POINT('Ctrl Pts',(5.96850269381051,-1.79282335723927,-1.55499066383679));
#7478=CARTESIAN_POINT('Ctrl Pts',(5.95439878359246,-1.79963589060291,-1.55596815772121));
#7479=CARTESIAN_POINT('Ctrl Pts',(5.93111553709109,-1.81054597854394,-1.55758225395842));
#7480=CARTESIAN_POINT('Ctrl Pts',(5.92198269523603,-1.81474157125658,-1.55821548405231));
#7481=CARTESIAN_POINT('Ctrl Pts',(5.90548925022832,-1.82216816416182,-1.55935942812834));
#7482=CARTESIAN_POINT('Ctrl Pts',(5.89814003881371,-1.8254240485874,-1.5598692793393));
#7483=CARTESIAN_POINT('Ctrl Pts',(5.88241021177907,-1.83227932207668,-1.56096090478734));
#7484=CARTESIAN_POINT('Ctrl Pts',(5.87402421041016,-1.83586581800781,-1.56154310259313));
#7485=CARTESIAN_POINT('Ctrl Pts',(5.85123284343791,-1.8454287891068,-1.56312614820089));
#7486=CARTESIAN_POINT('Ctrl Pts',(5.8367817441206,-1.85129393889771,-1.56413071206119));
#7487=CARTESIAN_POINT('Ctrl Pts',(5.75945520057769,-1.88162663463422,-1.56951156482025));
#7488=CARTESIAN_POINT('Ctrl Pts',(5.69544406989846,-1.90305933057875,-1.57398736994295));
#7489=CARTESIAN_POINT('Ctrl Pts',(5.47327113697508,-1.9651186959548,-1.58959726260307));
#7490=CARTESIAN_POINT('Ctrl Pts',(5.31127463664889,-1.98956670050335,-1.60116491633589));
#7491=CARTESIAN_POINT('Ctrl Pts',(5.09289479782387,-1.99551531734772,-1.61615596848631));
#7492=CARTESIAN_POINT('Ctrl Pts',(5.03760171519455,-1.99472357592404,-1.6198930803525));
#7493=CARTESIAN_POINT('Ctrl Pts',(4.97313366120662,-1.99111700440142,-1.6241310108593));
#7494=CARTESIAN_POINT('Ctrl Pts',(4.96386286024713,-1.99053337944126,-1.62473754077677));
#7495=CARTESIAN_POINT('Ctrl Pts',(4.94884631802394,-1.98948268226163,-1.62571490848222));
#7496=CARTESIAN_POINT('Ctrl Pts',(4.94309805552074,-1.98905543579943,-1.62608783512299));
#7497=CARTESIAN_POINT('Ctrl Pts',(4.93286046947233,-1.98824987966763,-1.62674976891576));
#7498=CARTESIAN_POINT('Ctrl Pts',(4.92837050167491,-1.9878812728814,-1.62703930253347));
#7499=CARTESIAN_POINT('Ctrl Pts',(4.91862150306144,-1.98704766264577,-1.62766626559148));
#7500=CARTESIAN_POINT('Ctrl Pts',(4.91336306038342,-1.98657699226482,-1.62800337757333));
#7501=CARTESIAN_POINT('Ctrl Pts',(4.89853393341771,-1.98519030693725,-1.62895121534531));
#7502=CARTESIAN_POINT('Ctrl Pts',(4.88896776112337,-1.98422595352618,-1.62955932141436));
#7503=CARTESIAN_POINT('Ctrl Pts',(4.82843158041389,-1.97768091359596,-1.63338847261488));
#7504=CARTESIAN_POINT('Ctrl Pts',(4.77768100065934,-1.97020537075589,-1.63651324264127));
#7505=CARTESIAN_POINT('Ctrl Pts',(4.5763949731471,-1.93257611911304,-1.64876347564443));
#7506=CARTESIAN_POINT('Ctrl Pts',(4.42927300728366,-1.88705067219852,-1.65743153142407));
#7507=CARTESIAN_POINT('Ctrl Pts',(4.2157942573648,-1.79289041213985,-1.67121740888998));
#7508=CARTESIAN_POINT('Ctrl Pts',(4.14477520687709,-1.75633026346884,-1.67602103355296));
#7509=CARTESIAN_POINT('Ctrl Pts',(4.06298206147126,-1.70781148698273,-1.68192603608728));
#7510=CARTESIAN_POINT('Ctrl Pts',(4.04991273995426,-1.69985421600065,-1.68288131228921));
#7511=CARTESIAN_POINT('Ctrl Pts',(4.02850636709828,-1.68648094716839,-1.68446615631666));
#7512=CARTESIAN_POINT('Ctrl Pts',(4.02011581218113,-1.68115148420791,-1.68509256068817));
#7513=CARTESIAN_POINT('Ctrl Pts',(4.00502023517102,-1.6714040573979,-1.68622915443043));
#7514=CARTESIAN_POINT('Ctrl Pts',(3.99830135145635,-1.66700787114163,-1.68673852935459));
#7515=CARTESIAN_POINT('Ctrl Pts',(3.98394342631604,-1.65748914436901,-1.68783464915381));
#7516=CARTESIAN_POINT('Ctrl Pts',(3.97631292981377,-1.65235411057693,-1.68842185372859));
#7517=CARTESIAN_POINT('Ctrl Pts',(3.95554972286836,-1.6381716544067,-1.69003268024754));
#7518=CARTESIAN_POINT('Ctrl Pts',(3.94248979186402,-1.62901937791495,-1.69106024315119));
#7519=CARTESIAN_POINT('Ctrl Pts',(3.87016143092115,-1.57702809668791,-1.69683328265526));
#7520=CARTESIAN_POINT('Ctrl Pts',(3.81318067113999,-1.53111651544855,-1.70169652706301));
#7521=CARTESIAN_POINT('Ctrl Pts',(3.61255882237539,-1.35042064660988,-1.720028856873));
#7522=CARTESIAN_POINT('Ctrl Pts',(3.48659610216878,-1.19774315429533,-1.73415325122234));
#7523=CARTESIAN_POINT('Ctrl Pts',(3.374306119416,-1.01129003143331,-1.74866593791251));
#7524=CARTESIAN_POINT('Ctrl Pts',(3.36385503599482,-0.993305929066541,-1.75003925240561));
#7525=CARTESIAN_POINT('Ctrl Pts',(3.35006116952603,-0.968691255488288,-1.75187995194017));
#7526=CARTESIAN_POINT('Ctrl Pts',(3.34647170970935,-0.962201388766289,-1.75236164985777));
#7527=CARTESIAN_POINT('Ctrl Pts',(3.34084932748408,-0.951900703247766,-1.75312030978925));
#7528=CARTESIAN_POINT('Ctrl Pts',(3.33879248700933,-0.94810312077189,-1.75339874893728));
#7529=CARTESIAN_POINT('Ctrl Pts',(3.33457180739576,-0.940249602439723,-1.75397192985947));
#7530=CARTESIAN_POINT('Ctrl Pts',(3.33240964403256,-0.936192846267882,-1.75426655451327));
#7531=CARTESIAN_POINT('Ctrl Pts',(3.32725188957452,-0.926434494890934,-1.7549718548187));
#7532=CARTESIAN_POINT('Ctrl Pts',(3.32426981851092,-0.920725734059634,-1.75538168749883));
#7533=CARTESIAN_POINT('Ctrl Pts',(3.31408414040363,-0.900994385267099,-1.75678899992654));
#7534=CARTESIAN_POINT('Ctrl Pts',(3.30701892827018,-0.886900489123544,-1.75777827632187));
#7535=CARTESIAN_POINT('Ctrl Pts',(3.26550157265754,-0.80157002832534,-1.76368119422108));
#7536=CARTESIAN_POINT('Ctrl Pts',(3.23514233688776,-0.728410939277028,-1.7683832248744));
#7537=CARTESIAN_POINT('Ctrl Pts',(3.19116541366846,-0.601612518618675,-1.77624342920264));
#7538=CARTESIAN_POINT('Ctrl Pts',(3.17528441653814,-0.548865452274119,-1.77943226326048));
#7539=CARTESIAN_POINT('Ctrl Pts',(3.12985329458514,-0.371715135196965,-1.7900517899023));
#7540=CARTESIAN_POINT('Ctrl Pts',(3.11007804444024,-0.245152309848009,-1.79751608522849));
#7541=CARTESIAN_POINT('Ctrl Pts',(3.10108422514295,-0.0928309925308564,
-1.80690246507649));
#7542=CARTESIAN_POINT('Ctrl Pts',(3.10008459530949,-0.0680624661680096,
-1.80844039725096));
#7543=CARTESIAN_POINT('Ctrl Pts',(3.09932720458535,-0.0331650522634131,
-1.81062633069008));
#7544=CARTESIAN_POINT('Ctrl Pts',(3.09918462038584,-0.0230461708683548,
-1.8112624170591));
#7545=CARTESIAN_POINT('Ctrl Pts',(3.09907030950185,-0.00540707666466319,
-1.81237534388369));
#7546=CARTESIAN_POINT('Ctrl Pts',(3.09906410068734,0.00211276621998525,
-1.81285110494454));
#7547=CARTESIAN_POINT('Ctrl Pts',(3.09914016723497,0.0178650461105865,-1.81385051894081));
#7548=CARTESIAN_POINT('Ctrl Pts',(3.09923088819271,0.0260972823136664,-1.81437442548822));
#7549=CARTESIAN_POINT('Ctrl Pts',(3.09956878121841,0.045728490073413,-1.8156277120367));
#7550=CARTESIAN_POINT('Ctrl Pts',(3.09986272779776,0.0571262667256657,-1.81635853335772));
#7551=CARTESIAN_POINT('Ctrl Pts',(3.10119839893522,0.0959868948211802,-1.8188614166134));
#7552=CARTESIAN_POINT('Ctrl Pts',(3.10270990775319,0.123429440423981,-1.82064796080307));
#7553=CARTESIAN_POINT('Ctrl Pts',(3.10771576720183,0.189442774388229,-1.82499354244146));
#7554=CARTESIAN_POINT('Ctrl Pts',(3.11176726212538,0.227958904195587,-1.82756878706819));
#7555=CARTESIAN_POINT('Ctrl Pts',(3.13215891140683,0.379319795090397,-1.83784551027739));
#7556=CARTESIAN_POINT('Ctrl Pts',(3.15703834481352,0.490784732535586,-1.84577482906485));
#7557=CARTESIAN_POINT('Ctrl Pts',(3.22285594812107,0.699658234463698,-1.86104201299441));
#7558=CARTESIAN_POINT('Ctrl Pts',(3.26227883319992,0.797176251632727,-1.8683496531302));
#7559=CARTESIAN_POINT('Ctrl Pts',(3.31647981299466,0.905720394206073,-1.87639215639055));
#7560=CARTESIAN_POINT('Ctrl Pts',(3.32393699594441,0.920207515825462,-1.87746338280441));
#7561=CARTESIAN_POINT('Ctrl Pts',(3.33471702848311,0.940534000899643,-1.87896160187262));
#7562=CARTESIAN_POINT('Ctrl Pts',(3.33789291743876,0.94644999897255,-1.87939707654038));
#7563=CARTESIAN_POINT('Ctrl Pts',(3.34329574346284,0.956393494073345,-1.88012789017254));
#7564=CARTESIAN_POINT('Ctrl Pts',(3.34550683753067,0.960429491069186,-1.88042420799356));
#7565=CARTESIAN_POINT('Ctrl Pts',(3.35006398123735,0.968679936332645,-1.88102924594712));
#7566=CARTESIAN_POINT('Ctrl Pts',(3.35241137756574,0.972893579240374,-1.88133787818584));
#7567=CARTESIAN_POINT('Ctrl Pts',(3.3584687166546,0.983674510629271,-1.88212669297813));
#7568=CARTESIAN_POINT('Ctrl Pts',(3.36220070656579,0.990229417773981,-1.882605492478));
#7569=CARTESIAN_POINT('Ctrl Pts',(3.37784597404471,1.01734999331573,-1.88458380860641));
#7570=CARTESIAN_POINT('Ctrl Pts',(3.3900896917811,1.03772404623634,-1.88606354420312));
#7571=CARTESIAN_POINT('Ctrl Pts',(3.42384956451334,1.09169296900248,-1.88997924537867));
#7572=CARTESIAN_POINT('Ctrl Pts',(3.44601483621355,1.12487050229805,-1.89238227155398));
#7573=CARTESIAN_POINT('Ctrl Pts',(3.52308446842537,1.23305816293596,-1.90028144822588));
#7574=CARTESIAN_POINT('Ctrl Pts',(3.58223414171343,1.30489587443794,-1.90563612008514));
#7575=CARTESIAN_POINT('Ctrl Pts',(3.73568729464565,1.46676859989317,-1.91860062568755));
#7576=CARTESIAN_POINT('Ctrl Pts',(3.83420393443117,1.55219101579464,-1.92624130773067));
#7577=CARTESIAN_POINT('Ctrl Pts',(3.95354995120486,1.63678286629157,-1.93531306357665));
#7578=CARTESIAN_POINT('Ctrl Pts',(3.96688642258813,1.64599356452771,-1.93632399352648));
#7579=CARTESIAN_POINT('Ctrl Pts',(3.98880905762478,1.66074288210554,-1.93798204858651));
#7580=CARTESIAN_POINT('Ctrl Pts',(3.99732831022964,1.66637996663326,-1.93862547613114));
#7581=CARTESIAN_POINT('Ctrl Pts',(4.01264115702831,1.67634401859768,-1.93978058429788));
#7582=CARTESIAN_POINT('Ctrl Pts',(4.01941841414815,1.6806957741929,-1.94029132997025));
#7583=CARTESIAN_POINT('Ctrl Pts',(4.0338385931314,1.68983227459826,-1.94137712264019));
#7584=CARTESIAN_POINT('Ctrl Pts',(4.04148795619025,1.69460646577168,-1.94195254322311));
#7585=CARTESIAN_POINT('Ctrl Pts',(4.06205175543019,1.70724800805633,-1.94349812617435));
#7586=CARTESIAN_POINT('Ctrl Pts',(4.07502352197986,1.71502051670292,-1.94447171027733));
#7587=CARTESIAN_POINT('Ctrl Pts',(4.14054028501352,1.7532716793363,-1.94938317749088));
#7588=CARTESIAN_POINT('Ctrl Pts',(4.1943648702007,1.78148357840924,-1.95340094019957));
#7589=CARTESIAN_POINT('Ctrl Pts',(4.36560427091852,1.86149781037265,-1.96613695666556));
#7590=CARTESIAN_POINT('Ctrl Pts',(4.48677739467328,1.90445962130019,-1.97510646505271));
#7591=CARTESIAN_POINT('Ctrl Pts',(4.70481567651747,1.95882689511632,-1.99074759218179));
#7592=CARTESIAN_POINT('Ctrl Pts',(4.79999444564586,1.97534793080907,-1.99740927664585));
#7593=CARTESIAN_POINT('Ctrl Pts',(4.90690167216118,1.98600260511815,-2.0044707704093));
#7594=CARTESIAN_POINT('Ctrl Pts',(4.91780760347756,1.98699889635208,-2.00518623091826));
#7595=CARTESIAN_POINT('Ctrl Pts',(4.93433451862203,1.98837154095326,-2.00626246984286));
#7596=CARTESIAN_POINT('Ctrl Pts',(4.93994959347915,1.98881396411933,-2.00662673362541));
#7597=CARTESIAN_POINT('Ctrl Pts',(4.95005103741942,1.9895668404777,-2.00727944599431));
#7598=CARTESIAN_POINT('Ctrl Pts',(4.9545366285985,1.98988591008562,-2.00756836045675));
#7599=CARTESIAN_POINT('Ctrl Pts',(4.96439377948814,1.99055357549616,-2.00820121920363));
#7600=CARTESIAN_POINT('Ctrl Pts',(4.96976567951689,1.99089559936241,-2.00854479650785));
#7601=CARTESIAN_POINT('Ctrl Pts',(4.98521925860994,1.99181672359592,-2.00952956851799));
#7602=CARTESIAN_POINT('Ctrl Pts',(4.99530421028151,1.99234102879653,-2.01016780868806));
#7603=CARTESIAN_POINT('Ctrl Pts',(5.06847692451208,1.99558822214792,-2.01476942041657));
#7604=CARTESIAN_POINT('Ctrl Pts',(5.13166528471118,1.99539093417366,-2.01858605471588));
#7605=CARTESIAN_POINT('Ctrl Pts',(5.32719508098362,1.98548615311052,-2.03019711301372));
#7606=CARTESIAN_POINT('Ctrl Pts',(5.45864981989365,1.96558466732515,-2.03773976363913));
#7607=CARTESIAN_POINT('Ctrl Pts',(5.67173539166069,1.91119555815945,-2.05068642434002));
#7608=CARTESIAN_POINT('Ctrl Pts',(5.75479205074167,1.88408307746055,-2.05592046699359));
#7609=CARTESIAN_POINT('Ctrl Pts',(5.85031598601377,1.84580517650454,-2.06230721219072));
#7610=CARTESIAN_POINT('Ctrl Pts',(5.8647624153107,1.8398181714033,-2.06328316210525));
#7611=CARTESIAN_POINT('Ctrl Pts',(5.88836844798812,1.82970832515533,-2.06489522657505));
#7612=CARTESIAN_POINT('Ctrl Pts',(5.89757011977773,1.82568498434705,-2.06552798357116));
#7613=CARTESIAN_POINT('Ctrl Pts',(5.91408067683418,1.81831689333237,-2.06667141482714));
#7614=CARTESIAN_POINT('Ctrl Pts',(5.92140051558812,1.81499710590205,-2.06718122966382));
#7615=CARTESIAN_POINT('Ctrl Pts',(5.92884851008935,1.81156477293497,-2.06770296546701));
#7616=CARTESIAN_POINT('Ctrl Pts',(5.92899700691455,1.81149631753623,-2.06771336896331));
#7617=CARTESIAN_POINT('Ctrl Pts',(5.9292823162582,1.81136475053615,-2.06773335970989));
#7618=CARTESIAN_POINT('Ctrl Pts',(5.92941913005179,1.81130164168948,-2.06774294686551));
#7619=CARTESIAN_POINT('Ctrl Pts',(5.92968201915897,1.81118034126934,-2.06776137067221));
#7620=CARTESIAN_POINT('Ctrl Pts',(5.92980809555902,1.81112215202644,-2.06777020724352));
#7621=CARTESIAN_POINT('Ctrl Pts',(5.93005037719339,1.81101029878513,-2.06778719021585));
#7622=CARTESIAN_POINT('Ctrl Pts',(5.93016658334015,1.81095663676551,-2.06779533654865));
#7623=CARTESIAN_POINT('Ctrl Pts',(5.93038991960546,1.81085347780007,-2.0678109943993));
#7624=CARTESIAN_POINT('Ctrl Pts',(5.93049705050445,1.81080398252864,-2.06781850585978));
#7625=CARTESIAN_POINT('Ctrl Pts',(5.93070296526726,1.81070882620346,-2.06783294475181));
#7626=CARTESIAN_POINT('Ctrl Pts',(5.93080174978758,1.81066316657235,-2.0678398721343));
#7627=CARTESIAN_POINT('Ctrl Pts',(5.93099164016013,1.81057537764115,-2.0678531894628));
#7628=CARTESIAN_POINT('Ctrl Pts',(5.9310827465768,1.8105332495448,-2.06785957936768));
#7629=CARTESIAN_POINT('Ctrl Pts',(5.93125789365983,1.81045224454577,-2.06787186449336));
#7630=CARTESIAN_POINT('Ctrl Pts',(5.9313419348035,1.81041336866582,-2.06787775967909));
#7631=CARTESIAN_POINT('Ctrl Pts',(5.93150351354332,1.81033861166806,-2.06788909460288));
#7632=CARTESIAN_POINT('Ctrl Pts',(5.93158105153806,1.81030273142202,-2.06789453431068));
#7633=CARTESIAN_POINT('Ctrl Pts',(5.93173013976533,1.81023373010148,-2.06790499429368));
#7634=CARTESIAN_POINT('Ctrl Pts',(5.93180169034993,1.8102006097615,-2.06791001454411));
#7635=CARTESIAN_POINT('Ctrl Pts',(5.93193927715159,1.81013691174393,-2.06791966868298));
#7636=CARTESIAN_POINT('Ctrl Pts',(5.93200531366934,1.81010633469004,-2.06792430255046));
#7637=CARTESIAN_POINT('Ctrl Pts',(5.93213230695122,1.81004752423371,-2.06793321429796));
#7638=CARTESIAN_POINT('Ctrl Pts',(5.93219326396951,1.81001929136236,-2.06793749216006));
#7639=CARTESIAN_POINT('Ctrl Pts',(5.93231049747237,1.80996498626438,-2.06794571980887));
#7640=CARTESIAN_POINT('Ctrl Pts',(5.93236677414189,1.80993891450404,-2.06794966957813));
#7641=CARTESIAN_POINT('Ctrl Pts',(5.93250958038024,1.80987274738125,-2.06795969285791));
#7642=CARTESIAN_POINT('Ctrl Pts',(5.93259610830154,1.8098326484326,-2.0679657664927));
#7643=CARTESIAN_POINT('Ctrl Pts',(5.93276767924201,1.80975312372476,-2.06797781035748));
#7644=CARTESIAN_POINT('Ctrl Pts',(5.93285272235516,1.80971369817753,-2.06798378057997));
#7645=CARTESIAN_POINT('Ctrl Pts',(5.93302135799563,1.80963550512518,-2.06799561998734));
#7646=CARTESIAN_POINT('Ctrl Pts',(5.93310495061014,1.80959673782502,-2.0680014891648));
#7647=CARTESIAN_POINT('Ctrl Pts',(5.94188927979675,1.8055221368139,-2.06861829244457));
#7648=CARTESIAN_POINT('Ctrl Pts',(5.9505606704281,1.80142366818618,-2.06923137467807));
#7649=CARTESIAN_POINT('Ctrl Pts',(5.97545962206154,1.78943492256857,-2.0710041264902));
#7650=CARTESIAN_POINT('Ctrl Pts',(5.99160977767954,1.78138695295338,-2.0721692189174));
#7651=CARTESIAN_POINT('Ctrl Pts',(6.02793282923505,1.76266698883203,-2.07482506153702));
#7652=CARTESIAN_POINT('Ctrl Pts',(6.04803594204269,1.75186581803919,-2.07632017285381));
#7653=CARTESIAN_POINT('Ctrl Pts',(6.11276257030876,1.71564430585971,-2.08121778490656));
#7654=CARTESIAN_POINT('Ctrl Pts',(6.15658793285239,1.68884681548474,-2.08466625592449));
#7655=CARTESIAN_POINT('Ctrl Pts',(6.297264134024,1.59518351362657,-2.09617054623165));
#7656=CARTESIAN_POINT('Ctrl Pts',(6.38923361596424,1.52144310940326,-2.10441913208435));
#7657=CARTESIAN_POINT('Ctrl Pts',(6.53780282432056,1.37903358794513,-2.11872097298468));
#7658=CARTESIAN_POINT('Ctrl Pts',(6.59733894861155,1.31387034900419,-2.12478531565143));
#7659=CARTESIAN_POINT('Ctrl Pts',(6.65920296503921,1.23642463521693,-2.13130014555501));
#7660=CARTESIAN_POINT('Ctrl Pts',(6.66596226204759,1.22781860359573,-2.13201506090664));
#7661=CARTESIAN_POINT('Ctrl Pts',(6.67609190665993,1.21470058999055,-2.13309064489747));
#7662=CARTESIAN_POINT('Ctrl Pts',(6.67951440385955,1.21022940732468,-2.13345479273994));
#7663=CARTESIAN_POINT('Ctrl Pts',(6.68563613265604,1.20216137196907,-2.13410738372912));
#7664=CARTESIAN_POINT('Ctrl Pts',(6.68834216205974,1.19856984737877,-2.13439629193668));
#7665=CARTESIAN_POINT('Ctrl Pts',(6.69426153818052,1.19065794349972,-2.13502923874101));
#7666=CARTESIAN_POINT('Ctrl Pts',(6.69746954355457,1.18633369865247,-2.13537290965031));
#7667=CARTESIAN_POINT('Ctrl Pts',(6.70664794654209,1.17385636869069,-2.13635822037577));
#7668=CARTESIAN_POINT('Ctrl Pts',(6.7125740533571,1.16567069497755,-2.13699690063305));
#7669=CARTESIAN_POINT('Ctrl Pts',(6.7551975335594,1.10584335771317,-2.14161184268976));
#7670=CARTESIAN_POINT('Ctrl Pts',(6.78948242457366,1.05251888617775,-2.14544039818007));
#7671=CARTESIAN_POINT('Ctrl Pts',(6.88917915974975,0.879901948210566,-2.1572608929734));
#7672=CARTESIAN_POINT('Ctrl Pts',(6.94496855236489,0.755509551438774,-2.16498676156849));
#7673=CARTESIAN_POINT('Ctrl Pts',(7.00455075623325,0.575371358662103,-2.17617400497363));
#7674=CARTESIAN_POINT('Ctrl Pts',(7.01935974533257,0.523679781749934,-2.17938068596302));
#7675=CARTESIAN_POINT('Ctrl Pts',(7.04095495856879,0.434898167312737,-2.1849344434968));
#7676=CARTESIAN_POINT('Ctrl Pts',(7.04881068916503,0.398098228737879,-2.18724945218381));
#7677=CARTESIAN_POINT('Ctrl Pts',(7.05802773711904,0.348023591918383,-2.1904271058849));
#7678=CARTESIAN_POINT('Ctrl Pts',(7.06030379602823,0.334923803400872,-2.19126090328228));
#7679=CARTESIAN_POINT('Ctrl Pts',(7.0638389147781,0.313297771354655,-2.19264193188578));
#7680=CARTESIAN_POINT('Ctrl Pts',(7.06517400074274,0.304784246989489,-2.19318675581137));
#7681=CARTESIAN_POINT('Ctrl Pts',(7.06759305274723,0.288677289587745,-2.19421981341622));
#7682=CARTESIAN_POINT('Ctrl Pts',(7.06868847042942,0.281085714271129,-2.19470767627308));
#7683=CARTESIAN_POINT('Ctrl Pts',(7.0708314196408,0.265603208538821,-2.195704668048));
#7684=CARTESIAN_POINT('Ctrl Pts',(7.07187555478401,0.257711955254293,-2.19621389442358));
#7685=CARTESIAN_POINT('Ctrl Pts',(7.07418209936535,0.239439391289865,-2.1973955915975));
#7686=CARTESIAN_POINT('Ctrl Pts',(7.07541014876699,0.229054054103397,-2.19806912603359));
#7687=CARTESIAN_POINT('Ctrl Pts',(7.07947027967402,0.192238214384171,-2.20046378649389));
#7688=CARTESIAN_POINT('Ctrl Pts',(7.0818555550484,0.16576223376657,-2.20219869070669));
#7689=CARTESIAN_POINT('Ctrl Pts',(7.08698906676703,0.0924029900823677,-2.20704281944523));
#7690=CARTESIAN_POINT('Ctrl Pts',(7.08861168295073,0.0454612257313511,-2.21018466912641));
#7691=CARTESIAN_POINT('Ctrl Pts',(7.0885765985467,-0.00149056292464214,
-2.21336761392587));
#7692=CARTESIAN_POINT('Ctrl Pts',(7.0885770951979,-0.000490293958327712,
-2.37086699796518));
#7693=CARTESIAN_POINT('Ctrl Pts',(7.08858062860284,0.0138852845779169,-2.36996691156082));
#7694=CARTESIAN_POINT('Ctrl Pts',(7.08842876113032,0.0282610016564163,-2.36907436554716));
#7695=CARTESIAN_POINT('Ctrl Pts',(7.08465333163941,0.204863214486289,-2.35818874130353));
#7696=CARTESIAN_POINT('Ctrl Pts',(7.06140305434961,0.366083502392327,-2.34903163477475));
#7697=CARTESIAN_POINT('Ctrl Pts',(6.9941308187758,0.613829127704159,-2.33401184281283));
#7698=CARTESIAN_POINT('Ctrl Pts',(6.9629579969907,0.703055498021072,-2.3284018228086));
#7699=CARTESIAN_POINT('Ctrl Pts',(6.91643565497422,0.810962553252018,-2.32115677411448));
#7700=CARTESIAN_POINT('Ctrl Pts',(6.90691504659619,0.832030189079554,-2.31971987530524));
#7701=CARTESIAN_POINT('Ctrl Pts',(6.89247926954782,0.862549385337824,-2.31760318736121));
#7702=CARTESIAN_POINT('Ctrl Pts',(6.88785091826512,0.872135081926787,-2.31693322188843));
#7703=CARTESIAN_POINT('Ctrl Pts',(6.87956229407106,0.888956309554531,-2.31574824533235));
#7704=CARTESIAN_POINT('Ctrl Pts',(6.87593418125697,0.896207482125178,-2.31523435814891));
#7705=CARTESIAN_POINT('Ctrl Pts',(6.86827843090544,0.911278001215554,-2.3141597874125));
#7706=CARTESIAN_POINT('Ctrl Pts',(6.86424308955388,0.919093216528032,-2.31359884286087));
#7707=CARTESIAN_POINT('Ctrl Pts',(6.85359831041912,0.939378641736502,-2.31213303788419));
#7708=CARTESIAN_POINT('Ctrl Pts',(6.84690807096786,0.951805671942332,-2.31122534924936));
#7709=CARTESIAN_POINT('Ctrl Pts',(6.8187733172895,1.00276252617067,-2.30746234454801));
#7710=CARTESIAN_POINT('Ctrl Pts',(6.79618737235399,1.04064457502452,-2.30456678225045));
#7711=CARTESIAN_POINT('Ctrl Pts',(6.68013903614349,1.22138463343181,-2.29025558967698));
#7712=CARTESIAN_POINT('Ctrl Pts',(6.5698633972145,1.35257722953066,-2.27822523191417));
#7713=CARTESIAN_POINT('Ctrl Pts',(6.40722685475483,1.50217907212634,-2.26293643992146));
#7714=CARTESIAN_POINT('Ctrl Pts',(6.36890536313873,1.53484102589633,-2.25948574374275));
#7715=CARTESIAN_POINT('Ctrl Pts',(6.31474041008112,1.57757613034927,-2.25485170157798));
#7716=CARTESIAN_POINT('Ctrl Pts',(6.29993186502775,1.58892640042156,-2.2536084669937));
#7717=CARTESIAN_POINT('Ctrl Pts',(6.27742159942448,1.60568371985401,-2.25175652205332));
#7718=CARTESIAN_POINT('Ctrl Pts',(6.26983770636503,1.61124647650269,-2.25113891960059));
#7719=CARTESIAN_POINT('Ctrl Pts',(6.25746046607455,1.62019118824391,-2.25014156837339));
#7720=CARTESIAN_POINT('Ctrl Pts',(6.25269114439442,1.62360593286225,-2.24975978584511));
#7721=CARTESIAN_POINT('Ctrl Pts',(6.24352136900703,1.63011032935057,-2.24903068456829));
#7722=CARTESIAN_POINT('Ctrl Pts',(6.23912335728919,1.63320331931891,-2.2486831496498));
#7723=CARTESIAN_POINT('Ctrl Pts',(6.23469423101349,1.63629150181637,-2.24833536008383));
#7724=CARTESIAN_POINT('Ctrl Pts',(6.23467563032359,1.63630447056771,-2.24833389953539));
#7725=CARTESIAN_POINT('Ctrl Pts',(6.23463797992693,1.63633072017934,-2.24833094325997));
#7726=CARTESIAN_POINT('Ctrl Pts',(6.23461893009051,1.63634400110702,-2.24832944752471));
#7727=CARTESIAN_POINT('Ctrl Pts',(6.23458036492786,1.63637088648601,-2.24832641958799));
#7728=CARTESIAN_POINT('Ctrl Pts',(6.2345608496664,1.63638449086773,-2.24832488739365));
#7729=CARTESIAN_POINT('Ctrl Pts',(6.23452133644111,1.63641203507991,-2.24832178519349));
#7730=CARTESIAN_POINT('Ctrl Pts',(6.23450133839714,1.63642597494027,-2.24832021518353));
#7731=CARTESIAN_POINT('Ctrl Pts',(6.23446084144457,1.63645420269126,-2.24831703593276));
#7732=CARTESIAN_POINT('Ctrl Pts',(6.23444034257257,1.63646849052878,-2.24831542669711));
#7733=CARTESIAN_POINT('Ctrl Pts',(6.23083342070655,1.63898243614546,-2.24803227859395));
#7734=CARTESIAN_POINT('Ctrl Pts',(6.2272388254637,1.64147027397583,-2.24775155250582));
#7735=CARTESIAN_POINT('Ctrl Pts',(6.21908958129172,1.64707087514468,-2.24711839296449));
#7736=CARTESIAN_POINT('Ctrl Pts',(6.21453018859606,1.6501765687392,-2.2467664348131));
#7737=CARTESIAN_POINT('Ctrl Pts',(6.20150531677765,1.65896975944463,-2.24576730595274));
#7738=CARTESIAN_POINT('Ctrl Pts',(6.1930088798427,1.66461140178497,-2.24512310395784));
#7739=CARTESIAN_POINT('Ctrl Pts',(6.13628659719297,1.70165137727086,-2.24086967605587));
#7740=CARTESIAN_POINT('Ctrl Pts',(6.08675989570854,1.73101848673347,-2.23738097778244));
#7741=CARTESIAN_POINT('Ctrl Pts',(5.89402619583833,1.83430211435706,-2.2243701029479));
#7742=CARTESIAN_POINT('Ctrl Pts',(5.74332723460475,1.892917669139,-2.21528738380476));
#7743=CARTESIAN_POINT('Ctrl Pts',(5.52215376724536,1.94937741091136,-2.2016958874161));
#7744=CARTESIAN_POINT('Ctrl Pts',(5.45630435265326,1.96268816747233,-2.19762598486409));
#7745=CARTESIAN_POINT('Ctrl Pts',(5.37451182492044,1.97496487196394,-2.1924809207216));
#7746=CARTESIAN_POINT('Ctrl Pts',(5.35908360926192,1.97709613355135,-2.19150664607561));
#7747=CARTESIAN_POINT('Ctrl Pts',(5.334588001054,1.98018809241791,-2.18995312469982));
#7748=CARTESIAN_POINT('Ctrl Pts',(5.32553605181541,1.98126768737313,-2.18937761257643));
#7749=CARTESIAN_POINT('Ctrl Pts',(5.30848859560037,1.98318245518445,-2.18829092403521));
#7750=CARTESIAN_POINT('Ctrl Pts',(5.30049479754256,1.9840314178617,-2.18778019100062));
#7751=CARTESIAN_POINT('Ctrl Pts',(5.28248873054808,1.98583371031093,-2.18662703448826));
#7752=CARTESIAN_POINT('Ctrl Pts',(5.27247400231071,1.98675967669244,-2.18598376837826));
#7753=CARTESIAN_POINT('Ctrl Pts',(5.24682315798228,1.98893585397185,-2.18433112647639));
#7754=CARTESIAN_POINT('Ctrl Pts',(5.23117875265129,1.99007741646309,-2.18331839556056));
#7755=CARTESIAN_POINT('Ctrl Pts',(5.12594088808117,1.9965097502446,-2.17647232762051));
#7756=CARTESIAN_POINT('Ctrl Pts',(5.03610420952479,1.99593250143225,-2.17045775765614));
#7757=CARTESIAN_POINT('Ctrl Pts',(4.81681462188701,1.97970548733625,-2.15538958529781));
#7758=CARTESIAN_POINT('Ctrl Pts',(4.68826878170434,1.95741898932754,-2.14620967108578));
#7759=CARTESIAN_POINT('Ctrl Pts',(4.50202491027066,1.90598397309354,-2.1329026529644));
#7760=CARTESIAN_POINT('Ctrl Pts',(4.44205874730041,1.88632034143467,-2.12862243982622));
#7761=CARTESIAN_POINT('Ctrl Pts',(4.37368662223361,1.8602492015479,-2.12382159946081));
#7762=CARTESIAN_POINT('Ctrl Pts',(4.36428093490859,1.85658067472828,-2.12316297327043));
#7763=CARTESIAN_POINT('Ctrl Pts',(4.34990406940519,1.85084709564284,-2.12215946213798));
#7764=CARTESIAN_POINT('Ctrl Pts',(4.34491288554786,1.84883313129778,-2.1218116738586));
#7765=CARTESIAN_POINT('Ctrl Pts',(4.3357663996273,1.84509936747695,-2.12117552298269));
#7766=CARTESIAN_POINT('Ctrl Pts',(4.33160876815354,1.84338572096059,-2.12088681207999));
#7767=CARTESIAN_POINT('Ctrl Pts',(4.32225609175746,1.83949378568759,-2.12023836325715));
#7768=CARTESIAN_POINT('Ctrl Pts',(4.31706446492211,1.83730754594363,-2.11987910814428));
#7769=CARTESIAN_POINT('Ctrl Pts',(4.30180470084323,1.83080528358261,-2.11882500286456));
#7770=CARTESIAN_POINT('Ctrl Pts',(4.29176258266189,1.82642820521991,-2.11813370462089));
#7771=CARTESIAN_POINT('Ctrl Pts',(4.19929161178927,1.78521292794018,-2.11178556685109));
#7772=CARTESIAN_POINT('Ctrl Pts',(4.11940562575843,1.74289586546341,-2.10642867273829));
#7773=CARTESIAN_POINT('Ctrl Pts',(3.94510813087981,1.63482274301659,-2.09443648937829));
#7774=CARTESIAN_POINT('Ctrl Pts',(3.85296696157566,1.56603533502187,-2.08786212961973));
#7775=CARTESIAN_POINT('Ctrl Pts',(3.72856822254267,1.45525897450899,-2.07800688076357));
#7776=CARTESIAN_POINT('Ctrl Pts',(3.69124327960925,1.41931974226747,-2.07490444260612));
#7777=CARTESIAN_POINT('Ctrl Pts',(3.63171180254486,1.35735459229981,-2.06966244340371));
#7778=CARTESIAN_POINT('Ctrl Pts',(3.60869953293345,1.33213682710641,-2.06755628576632));
#7779=CARTESIAN_POINT('Ctrl Pts',(3.5782266737681,1.29697204080412,-2.06464814789894));
#7780=CARTESIAN_POINT('Ctrl Pts',(3.57019445927486,1.28752657868965,-2.06386974606849));
#7781=CARTESIAN_POINT('Ctrl Pts',(3.55685139506303,1.27153611915698,-2.06255619943343));
#7782=CARTESIAN_POINT('Ctrl Pts',(3.55149295796404,1.26503114984298,-2.06202299949656));
#7783=CARTESIAN_POINT('Ctrl Pts',(3.54099900883453,1.25212604883943,-2.06096735234555));
#7784=CARTESIAN_POINT('Ctrl Pts',(3.53586144539942,1.24572779455031,-2.06044500215379));
#7785=CARTESIAN_POINT('Ctrl Pts',(3.52463231606024,1.23156506551814,-2.05929092797132));
#7786=CARTESIAN_POINT('Ctrl Pts',(3.51855862899044,1.22378675362338,-2.05865851256569));
#7787=CARTESIAN_POINT('Ctrl Pts',(3.49736679797947,1.19622811540705,-2.05642257773849));
#7788=CARTESIAN_POINT('Ctrl Pts',(3.48256200104205,1.17621081724702,-2.05480694112109));
#7789=CARTESIAN_POINT('Ctrl Pts',(3.38419683273877,1.03786990551446,-2.04369318222381));
#7790=CARTESIAN_POINT('Ctrl Pts',(3.31338063896541,0.911046378908459,-2.03371244814949));
#7791=CARTESIAN_POINT('Ctrl Pts',(3.22229970809843,0.695916960728751,-2.01742803487771));
#7792=CARTESIAN_POINT('Ctrl Pts',(3.19317253352785,0.611906067753148,-2.01122440863533));
#7793=CARTESIAN_POINT('Ctrl Pts',(3.16276392903024,0.500721223268661,-2.00340107121701));
#7794=CARTESIAN_POINT('Ctrl Pts',(3.15629501476564,0.475075015445877,-2.00162285903775));
#7795=CARTESIAN_POINT('Ctrl Pts',(3.14636441778663,0.432119908282408,-1.99869625141013));
#7796=CARTESIAN_POINT('Ctrl Pts',(3.1426191046834,0.414880613727094,-1.99753545711134));
#7797=CARTESIAN_POINT('Ctrl Pts',(3.13776063432445,0.390994465850365,-1.99594813206982));
#7798=CARTESIAN_POINT('Ctrl Pts',(3.13645184116614,0.384388852052085,-1.99551137597878));
#7799=CARTESIAN_POINT('Ctrl Pts',(3.13429550657772,0.373208948657815,-1.99477605431741));
#7800=CARTESIAN_POINT('Ctrl Pts',(3.13343047766951,0.36863812826439,-1.99447651838746));
#7801=CARTESIAN_POINT('Ctrl Pts',(3.13180608524489,0.359887384887357,-1.99390520826274));
#7802=CARTESIAN_POINT('Ctrl Pts',(3.13104407657434,0.355708020473965,-1.99363328045654));
#7803=CARTESIAN_POINT('Ctrl Pts',(3.12925631544612,0.345722063083701,-1.99298570212458));
#7804=CARTESIAN_POINT('Ctrl Pts',(3.12824293888099,0.33991325359577,-1.99261074220388));
#7805=CARTESIAN_POINT('Ctrl Pts',(3.12471061916884,0.31912139028839,-1.99127454758547));
#7806=CARTESIAN_POINT('Ctrl Pts',(3.12233704012091,0.304113717187655,-1.99032106405391));
#7807=CARTESIAN_POINT('Ctrl Pts',(3.10023650338972,0.153222356487361,-1.98083133082115));
#7808=CARTESIAN_POINT('Ctrl Pts',(3.09441555649905,0.0156528983931978,-1.9729491464414));
#7809=CARTESIAN_POINT('Ctrl Pts',(3.11095558111533,-0.255527934421143,-1.95716955983568));
#7810=CARTESIAN_POINT('Ctrl Pts',(3.13265636811305,-0.388428686682874,-1.94930737402893));
#7811=CARTESIAN_POINT('Ctrl Pts',(3.17255310717885,-0.536754580247637,-1.93979670208566));
#7812=CARTESIAN_POINT('Ctrl Pts',(3.17783181584777,-0.555302859861251,-1.93859444779035));
#7813=CARTESIAN_POINT('Ctrl Pts',(3.18622671508031,-0.583254810269179,-1.93676173944622));
#7814=CARTESIAN_POINT('Ctrl Pts',(3.18914549201619,-0.592716938434015,-1.93613768237315));
#7815=CARTESIAN_POINT('Ctrl Pts',(3.19455757989457,-0.609809043564306,-1.93500359091428));
#7816=CARTESIAN_POINT('Ctrl Pts',(3.19702673977691,-0.617446491834715,-1.93449435433881));
#7817=CARTESIAN_POINT('Ctrl Pts',(3.20243272360087,-0.633829450706263,-1.93339656683139));
#7818=CARTESIAN_POINT('Ctrl Pts',(3.20538424765164,-0.642569878455398,-1.93280754321444));
#7819=CARTESIAN_POINT('Ctrl Pts',(3.2135099592179,-0.666093165803048,-1.9312130865811));
#7820=CARTESIAN_POINT('Ctrl Pts',(3.21879771252874,-0.680835831182161,-1.93020393475504));
#7821=CARTESIAN_POINT('Ctrl Pts',(3.24582499662956,-0.753486187097219,-1.92518081472669));
#7822=CARTESIAN_POINT('Ctrl Pts',(3.27007412107615,-0.810417744100414,-1.92108431788049));
#7823=CARTESIAN_POINT('Ctrl Pts',(3.37136604221896,-1.02056207300495,-1.9053431799186));
#7824=CARTESIAN_POINT('Ctrl Pts',(3.46540448874965,-1.16475156889398,-1.89317489703163));
#7825=CARTESIAN_POINT('Ctrl Pts',(3.61126322066226,-1.33561495660148,-1.87778408998894));
#7826=CARTESIAN_POINT('Ctrl Pts',(3.64744783066827,-1.37471854462379,-1.8741902155852));
#7827=CARTESIAN_POINT('Ctrl Pts',(3.69202977952111,-1.4191849397538,-1.87006213735716));
#7828=CARTESIAN_POINT('Ctrl Pts',(3.69895223745265,-1.42598939289992,-1.86942924761186));
#7829=CARTESIAN_POINT('Ctrl Pts',(3.70973042233325,-1.4364302548682,-1.86845666905404));
#7830=CARTESIAN_POINT('Ctrl Pts',(3.71355132129755,-1.44010217240138,-1.86811434165934));
#7831=CARTESIAN_POINT('Ctrl Pts',(3.72064609800737,-1.44686613883657,-1.86748329739197));
#7832=CARTESIAN_POINT('Ctrl Pts',(3.72391579635187,-1.44996231299428,-1.86719427223295));
#7833=CARTESIAN_POINT('Ctrl Pts',(3.73137520600397,-1.45697809280154,-1.86653894244609));
#7834=CARTESIAN_POINT('Ctrl Pts',(3.7355713568665,-1.46089070947657,-1.86617316777992));
#7835=CARTESIAN_POINT('Ctrl Pts',(3.74653973121813,-1.47102983953291,-1.86522431852028));
#7836=CARTESIAN_POINT('Ctrl Pts',(3.7533383393475,-1.47722778669541,-1.86464332121148));
#7837=CARTESIAN_POINT('Ctrl Pts',(3.7997186436483,-1.51892649567303,-1.86072582179016));
#7838=CARTESIAN_POINT('Ctrl Pts',(3.84066690019801,-1.55288280046686,-1.85749257820214));
#7839=CARTESIAN_POINT('Ctrl Pts',(4.01416773722097,-1.68541928329054,-1.84445891415586));
#7840=CARTESIAN_POINT('Ctrl Pts',(4.15735337543459,-1.76899002275367,-1.83516551565781));
#7841=CARTESIAN_POINT('Ctrl Pts',(4.37150485881377,-1.86060985445224,-1.82130162960991));
#7842=CARTESIAN_POINT('Ctrl Pts',(4.4351114643409,-1.88406759936948,-1.81719589091012));
#7843=CARTESIAN_POINT('Ctrl Pts',(4.514689932897,-1.90889273189382,-1.81201054531643));
#7844=CARTESIAN_POINT('Ctrl Pts',(4.52964998710048,-1.91336757717838,-1.81103379246082));
#7845=CARTESIAN_POINT('Ctrl Pts',(4.55343300755407,-1.92017837492005,-1.80947722474925));
#7846=CARTESIAN_POINT('Ctrl Pts',(4.5622223209512,-1.9226302614049,-1.80890117000283));
#7847=CARTESIAN_POINT('Ctrl Pts',(4.5787846958186,-1.92712828600353,-1.80781401756826));
#7848=CARTESIAN_POINT('Ctrl Pts',(4.58655392695947,-1.92918792099368,-1.80730336745326));
#7849=CARTESIAN_POINT('Ctrl Pts',(4.60405957132796,-1.93371563660825,-1.80615114758416));
#7850=CARTESIAN_POINT('Ctrl Pts',(4.61380254885207,-1.93615723036723,-1.8055087409522));
#7851=CARTESIAN_POINT('Ctrl Pts',(4.63876496371416,-1.94221282325051,-1.80385977858443));
#7852=CARTESIAN_POINT('Ctrl Pts',(4.65400900234703,-1.94572151612302,-1.80284989303897));
#7853=CARTESIAN_POINT('Ctrl Pts',(4.75575495810615,-1.96788343394683,-1.79608881186536));
#7854=CARTESIAN_POINT('Ctrl Pts',(4.84336276102063,-1.98093962023899,-1.79016164913342));
#7855=CARTESIAN_POINT('Ctrl Pts',(5.07636325173751,-1.99995919140142,-1.77415134467348));
#7856=CARTESIAN_POINT('Ctrl Pts',(5.22203550746561,-1.99592101731892,-1.76386577138007));
#7857=CARTESIAN_POINT('Ctrl Pts',(5.41571564699917,-1.96924776649251,-1.75049664133769));
#7858=CARTESIAN_POINT('Ctrl Pts',(5.46518814609382,-1.96052057389863,-1.74711380444139));
#7859=CARTESIAN_POINT('Ctrl Pts',(5.52363060481675,-1.94791889019578,-1.74319537663327));
#7860=CARTESIAN_POINT('Ctrl Pts',(5.53296407946433,-1.94583601019851,-1.7425719883546));
#7861=CARTESIAN_POINT('Ctrl Pts',(5.54741582043407,-1.94250164477213,-1.74161085337273));
#7862=CARTESIAN_POINT('Ctrl Pts',(5.55254456570101,-1.94129690053478,-1.74127056308892));
#7863=CARTESIAN_POINT('Ctrl Pts',(5.56205137523225,-1.93902396831564,-1.74064136100771));
#7864=CARTESIAN_POINT('Ctrl Pts',(5.56643056560525,-1.93796127077238,-1.74035215603611));
#7865=CARTESIAN_POINT('Ctrl Pts',(5.57641805286127,-1.93550174124016,-1.73969397788211));
#7866=CARTESIAN_POINT('Ctrl Pts',(5.58202390221554,-1.9340953707264,-1.7393255537349));
#7867=CARTESIAN_POINT('Ctrl Pts',(5.59667332082039,-1.93035243916039,-1.73836521013965));
#7868=CARTESIAN_POINT('Ctrl Pts',(5.60570685154834,-1.92797665703044,-1.73777545140949));
#7869=CARTESIAN_POINT('Ctrl Pts',(5.66928811630474,-1.91077665271845,-1.73363955515462));
#7870=CARTESIAN_POINT('Ctrl Pts',(5.723206173322,-1.89370168054198,-1.73021025284902));
#7871=CARTESIAN_POINT('Ctrl Pts',(5.92859742999109,-1.81891321859054,-1.71719443510743));
#7872=CARTESIAN_POINT('Ctrl Pts',(6.07354317976386,-1.74512131857496,-1.70806266097327));
#7873=CARTESIAN_POINT('Ctrl Pts',(6.26378675584202,-1.61701888855633,-1.69440764811976));
#7874=CARTESIAN_POINT('Ctrl Pts',(6.31765998583622,-1.5766379838887,-1.69032921642944));
#7875=CARTESIAN_POINT('Ctrl Pts',(6.38136792341492,-1.52364995974087,-1.68517456440074));
#7876=CARTESIAN_POINT('Ctrl Pts',(6.3932319680045,-1.5135446939177,-1.68419969724806));
#7877=CARTESIAN_POINT('Ctrl Pts',(6.41184789078608,-1.49730826676337,-1.682645447522));
#7878=CARTESIAN_POINT('Ctrl Pts',(6.41867837945663,-1.49126789487776,-1.6820698056457));
#7879=CARTESIAN_POINT('Ctrl Pts',(6.43145214793448,-1.47981470443325,-1.68098300636625));
#7880=CARTESIAN_POINT('Ctrl Pts',(6.43740460633235,-1.47441236103352,-1.68047229334903));
#7881=CARTESIAN_POINT('Ctrl Pts',(6.45072836084524,-1.46217227783025,-1.6793193617295));
#7882=CARTESIAN_POINT('Ctrl Pts',(6.45808089670971,-1.4553145277299,-1.67867630187591));
#7883=CARTESIAN_POINT('Ctrl Pts',(6.47676319871346,-1.43762344920925,-1.67702454319768));
#7884=CARTESIAN_POINT('Ctrl Pts',(6.48801751123237,-1.42671178243116,-1.67601249533346));
#7885=CARTESIAN_POINT('Ctrl Pts',(6.56262196859957,-1.35265298315237,-1.66918683263692));
#7886=CARTESIAN_POINT('Ctrl Pts',(6.62178284007282,-1.28544769403604,-1.66319325655863));
#7887=CARTESIAN_POINT('Ctrl Pts',(6.75564430867713,-1.11103749073305,-1.64812929812363));
#7888=CARTESIAN_POINT('Ctrl Pts',(6.82471357757324,-1.00003481566623,-1.63893001010521));
#7889=CARTESIAN_POINT('Ctrl Pts',(6.91039308217543,-0.826498102702352,-1.62560066827608));
#7890=CARTESIAN_POINT('Ctrl Pts',(6.93563541288106,-0.768605823072363,-1.62131707211403));
#7891=CARTESIAN_POINT('Ctrl Pts',(6.96168395391258,-0.700171759922608,-1.61651294717067));
#7892=CARTESIAN_POINT('Ctrl Pts',(6.96520424847747,-0.690707824548839,-1.61585421118863));
#7893=CARTESIAN_POINT('Ctrl Pts',(6.97049074793894,-0.676158482769902,-1.6148505683007));
#7894=CARTESIAN_POINT('Ctrl Pts',(6.9723084227119,-0.671092142249585,-1.61450275690487));
#7895=CARTESIAN_POINT('Ctrl Pts',(6.97560706736833,-0.661779531517981,-1.61386658392977));
#7896=CARTESIAN_POINT('Ctrl Pts',(6.97709418323862,-0.657535617341168,-1.61357787387638));
#7897=CARTESIAN_POINT('Ctrl Pts',(6.98041169243418,-0.647964562360384,-1.61292945202371));
#7898=CARTESIAN_POINT('Ctrl Pts',(6.98223387915297,-0.642634683939797,-1.61257022284331));
#7899=CARTESIAN_POINT('Ctrl Pts',(6.98753257154999,-0.626918902005126,-1.61151626510544));
#7900=CARTESIAN_POINT('Ctrl Pts',(6.99094621294328,-0.616511806128984,-1.61082508698636));
#7901=CARTESIAN_POINT('Ctrl Pts',(7.0219567838781,-0.519273405415327,-1.60442530062435));
#7902=CARTESIAN_POINT('Ctrl Pts',(7.04366363410773,-0.430663230940203,-1.59902224504291));
#7903=CARTESIAN_POINT('Ctrl Pts',(7.07867992308661,-0.228763448657466,-1.58704350817181));
#7904=CARTESIAN_POINT('Ctrl Pts',(7.08849541672183,-0.1152024391642,-1.58052419577023));
#7905=CARTESIAN_POINT('Ctrl Pts',(7.08857698602155,-0.000949408941870256,
-1.57376499307923));
#7906=CARTESIAN_POINT('Ctrl Pts',(7.08857715545312,-0.000474703094148514,
-1.5737369062833));
#7907=CARTESIAN_POINT('Ctrl Pts',(7.08857715545311,2.4467182997506E-11,
-1.57370881642439));
#7908=CARTESIAN_POINT('Origin',(5.09382715545311,0.,-6.77268258743872));
#7909=CARTESIAN_POINT('',(7.0885771212009,0.000270376244464336,-0.616403823242141));
#7910=CARTESIAN_POINT('',(7.08857666516212,0.0013985762946109,-0.772682587389958));
#7911=CARTESIAN_POINT('',(7.08857715545311,8.3550772080578E-14,-6.77268258743872));
#7912=CARTESIAN_POINT('Ctrl Pts',(7.08857709145056,0.000505309959526276,
-0.616403784479595));
#7913=CARTESIAN_POINT('Ctrl Pts',(7.08858289021834,-0.0223857719132102,
-0.617835630335221));
#7914=CARTESIAN_POINT('Ctrl Pts',(7.08819465309331,-0.0452765254613356,
-0.619248452783894));
#7915=CARTESIAN_POINT('Ctrl Pts',(7.08480907112761,-0.144304803472926,-0.625297633396242));
#7916=CARTESIAN_POINT('Ctrl Pts',(7.07784471547868,-0.220247985752777,-0.629777142771891));
#7917=CARTESIAN_POINT('Ctrl Pts',(7.05553837196678,-0.369106108127607,-0.638549028210189));
#7918=CARTESIAN_POINT('Ctrl Pts',(7.04042698139936,-0.441926830394387,-0.642836821697343));
#7919=CARTESIAN_POINT('Ctrl Pts',(6.99648402095372,-0.60679474210903,-0.652812289300294));
#7920=CARTESIAN_POINT('Ctrl Pts',(6.96497628648473,-0.697926019428036,-0.658529303843982));
#7921=CARTESIAN_POINT('Ctrl Pts',(6.91780763715039,-0.807878715294661,-0.665904141088645));
#7922=CARTESIAN_POINT('Ctrl Pts',(6.90822598185459,-0.829174073519144,-0.667355249116568));
#7923=CARTESIAN_POINT('Ctrl Pts',(6.89371739824139,-0.859963309400044,-0.669489014208158));
#7924=CARTESIAN_POINT('Ctrl Pts',(6.88908423477748,-0.869594038404518,-0.670161617281624));
#7925=CARTESIAN_POINT('Ctrl Pts',(6.88079755904406,-0.886470632540912,-0.671349614697471));
#7926=CARTESIAN_POINT('Ctrl Pts',(6.87717677573109,-0.893732361705636,-0.671863866204003));
#7927=CARTESIAN_POINT('Ctrl Pts',(6.86954763597928,-0.908802161267996,-0.672937577918472));
#7928=CARTESIAN_POINT('Ctrl Pts',(6.86553185883164,-0.916606258581189,-0.673497289044717));
#7929=CARTESIAN_POINT('Ctrl Pts',(6.85496437049203,-0.936813769660552,-0.674956291037723));
#7930=CARTESIAN_POINT('Ctrl Pts',(6.84833318420155,-0.94917485622856,-0.675858361531553));
#7931=CARTESIAN_POINT('Ctrl Pts',(6.82066760771554,-0.999465185523764,-0.679568527353132));
#7932=CARTESIAN_POINT('Ctrl Pts',(6.79853059049359,-1.03677110385418,-0.682415467955409));
#7933=CARTESIAN_POINT('Ctrl Pts',(6.68291248507604,-1.21788772898224,-0.696724198763139));
#7934=CARTESIAN_POINT('Ctrl Pts',(6.57237720829435,-1.34993124987602,-0.708811086967108));
#7935=CARTESIAN_POINT('Ctrl Pts',(6.40931332786564,-1.50035434560631,-0.724160611262132));
#7936=CARTESIAN_POINT('Ctrl Pts',(6.370989149762,-1.53310956880177,-0.727615733405562));
#7937=CARTESIAN_POINT('Ctrl Pts',(6.31681996805741,-1.57596471094612,-0.732255104929704));
#7938=CARTESIAN_POINT('Ctrl Pts',(6.30201430555295,-1.58734371020412,-0.733499377030884));
#7939=CARTESIAN_POINT('Ctrl Pts',(6.27950939233213,-1.60414268403876,-0.7353527061248));
#7940=CARTESIAN_POINT('Ctrl Pts',(6.27192838417006,-1.60971849104384,-0.73597066999277));
#7941=CARTESIAN_POINT('Ctrl Pts',(6.25955657932952,-1.61868369494767,-0.736968526545846));
#7942=CARTESIAN_POINT('Ctrl Pts',(6.25478988437308,-1.62210589607492,-0.737350455694226));
#7943=CARTESIAN_POINT('Ctrl Pts',(6.24562545066598,-1.62862431961302,-0.738079805786516));
#7944=CARTESIAN_POINT('Ctrl Pts',(6.24123016227255,-1.63172388254662,-0.738427443253408));
#7945=CARTESIAN_POINT('Ctrl Pts',(6.23679918682208,-1.63482185537315,-0.738775693026422));
#7946=CARTESIAN_POINT('Ctrl Pts',(6.23677604366833,-1.63483803547171,-0.738777511887826));
#7947=CARTESIAN_POINT('Ctrl Pts',(6.23673437116238,-1.63486716869928,-0.738780786894967));
#7948=CARTESIAN_POINT('Ctrl Pts',(6.23671584186986,-1.63488012204924,-0.738782243057715));
#7949=CARTESIAN_POINT('Ctrl Pts',(6.23667831977713,-1.63490635182576,-0.738785191730456));
#7950=CARTESIAN_POINT('Ctrl Pts',(6.23665932700194,-1.63491962821111,-0.738786684236524));
#7951=CARTESIAN_POINT('Ctrl Pts',(6.23662086078775,-1.63494651597904,-0.738789706938133));
#7952=CARTESIAN_POINT('Ctrl Pts',(6.23660138737839,-1.63496012731567,-0.73879123712926));
#7953=CARTESIAN_POINT('Ctrl Pts',(6.23656194194624,-1.63498769745592,-0.738794336605116));
#7954=CARTESIAN_POINT('Ctrl Pts',(6.23654196988223,-1.63500165626153,-0.738795905890866));
#7955=CARTESIAN_POINT('Ctrl Pts',(6.23650150820266,-1.63502993449456,-0.73879908503728));
#7956=CARTESIAN_POINT('Ctrl Pts',(6.23648101859543,-1.63504425388758,-0.738800694894928));
#7957=CARTESIAN_POINT('Ctrl Pts',(6.2364395019224,-1.63507326712108,-0.738803956742057));
#7958=CARTESIAN_POINT('Ctrl Pts',(6.23641847481323,-1.63508796096141,-0.738805608732427));
#7959=CARTESIAN_POINT('Ctrl Pts',(6.23637586214765,-1.63511773766419,-0.738808956486331));
#7960=CARTESIAN_POINT('Ctrl Pts',(6.23635427657312,-1.63513282050684,-0.738810652248604));
#7961=CARTESIAN_POINT('Ctrl Pts',(6.23631052481319,-1.63516339060256,-0.738814089279339));
#7962=CARTESIAN_POINT('Ctrl Pts',(6.23628835865227,-1.63517887780387,-0.738815830543013));
#7963=CARTESIAN_POINT('Ctrl Pts',(6.23624342236974,-1.63521027282604,-0.738819360402095));
#7964=CARTESIAN_POINT('Ctrl Pts',(6.23622065225917,-1.63522618060217,-0.738821148993577));
#7965=CARTESIAN_POINT('Ctrl Pts',(6.23617448348139,-1.63525843384503,-0.73882477543099));
#7966=CARTESIAN_POINT('Ctrl Pts',(6.23615108475217,-1.63527477931552,-0.73882661327852));
#7967=CARTESIAN_POINT('Ctrl Pts',(6.23610363268735,-1.63530792602438,-0.738830340264159));
#7968=CARTESIAN_POINT('Ctrl Pts',(6.23607957932842,-1.63532472723671,-0.738832229400598));
#7969=CARTESIAN_POINT('Ctrl Pts',(6.23603079044056,-1.63535880455384,-0.73883606111824));
#7970=CARTESIAN_POINT('Ctrl Pts',(6.23600605488848,-1.63537608062944,-0.738838003697509));
#7971=CARTESIAN_POINT('Ctrl Pts',(6.235955872445,-1.63541112790815,-0.738841944580185));
#7972=CARTESIAN_POINT('Ctrl Pts',(6.23593042553645,-1.63542889907459,-0.738843942880916));
#7973=CARTESIAN_POINT('Ctrl Pts',(6.23587878947609,-1.63546495796937,-0.738847997621108));
#7974=CARTESIAN_POINT('Ctrl Pts',(6.2358526003056,-1.63548324565853,-0.738850054057717));
#7975=CARTESIAN_POINT('Ctrl Pts',(6.23224338193742,-1.63800340513623,-0.739133447888702));
#7976=CARTESIAN_POINT('Ctrl Pts',(6.22865219236113,-1.64049346119307,-0.73941396923231));
#7977=CARTESIAN_POINT('Ctrl Pts',(6.22039429054586,-1.64617922520578,-0.740055714979887));
#7978=CARTESIAN_POINT('Ctrl Pts',(6.21572215522225,-1.64936689755544,-0.740416398428976));
#7979=CARTESIAN_POINT('Ctrl Pts',(6.20207763187366,-1.65859138668314,-0.741462964024277));
#7980=CARTESIAN_POINT('Ctrl Pts',(6.19306946809851,-1.66457527820847,-0.742145428951207));
#7981=CARTESIAN_POINT('Ctrl Pts',(6.10291374198274,-1.72341234507652,-0.748896450113127));
#7982=CARTESIAN_POINT('Ctrl Pts',(6.0180563434217,-1.77037040443351,-0.7546188859221));
#7983=CARTESIAN_POINT('Ctrl Pts',(5.81388476642289,-1.86465390604705,-0.767741134133508));
#7984=CARTESIAN_POINT('Ctrl Pts',(5.69276565915337,-1.90701040605596,-0.77507228147667));
#7985=CARTESIAN_POINT('Ctrl Pts',(5.50948168052885,-1.95190716769005,-0.786353968874066));
#7986=CARTESIAN_POINT('Ctrl Pts',(5.44991580250582,-1.96364713573061,-0.790044347807438));
#7987=CARTESIAN_POINT('Ctrl Pts',(5.37496133098747,-1.97489738447856,-0.794762200590383));
#7988=CARTESIAN_POINT('Ctrl Pts',(5.35998651766781,-1.97697123854038,-0.795708329606422));
#7989=CARTESIAN_POINT('Ctrl Pts',(5.33604562990981,-1.98000986405481,-0.797227248428666));
#7990=CARTESIAN_POINT('Ctrl Pts',(5.32709389129463,-1.98108441939477,-0.797796588101359));
#7991=CARTESIAN_POINT('Ctrl Pts',(5.31013205160602,-1.98300394012794,-0.798878159441434));
#7992=CARTESIAN_POINT('Ctrl Pts',(5.30212349622851,-1.98386115088095,-0.799389996078179));
#7993=CARTESIAN_POINT('Ctrl Pts',(5.28394466167901,-1.98569566753748,-0.800554581853837));
#7994=CARTESIAN_POINT('Ctrl Pts',(5.27377168756263,-1.98664337746271,-0.801208243244641));
#7995=CARTESIAN_POINT('Ctrl Pts',(5.2474376854137,-1.98889271569778,-0.802905570964789));
#7996=CARTESIAN_POINT('Ctrl Pts',(5.23126752185967,-1.99007551351617,-0.803952906813853));
#7997=CARTESIAN_POINT('Ctrl Pts',(5.08527100454034,-1.99896687370866,-0.8134571266548));
#7998=CARTESIAN_POINT('Ctrl Pts',(4.95501901233134,-1.99415713900583,-0.822310405395853));
#7999=CARTESIAN_POINT('Ctrl Pts',(4.73420610133288,-1.96425946123062,-0.837789554167223));
#8000=CARTESIAN_POINT('Ctrl Pts',(4.64320939007224,-1.9454013923649,-0.844300937635326));
#8001=CARTESIAN_POINT('Ctrl Pts',(4.51534860304006,-1.90944760851642,-0.853431311364357));
#8002=CARTESIAN_POINT('Ctrl Pts',(4.47717342355976,-1.89746308983248,-0.856153783391403));
#8003=CARTESIAN_POINT('Ctrl Pts',(4.41688694311996,-1.87652513749285,-0.860421870190493));
#8004=CARTESIAN_POINT('Ctrl Pts',(4.39453208902037,-1.86830971026244,-0.861997464657784));
#8005=CARTESIAN_POINT('Ctrl Pts',(4.36529154864434,-1.85696537537849,-0.864044174040803));
#8006=CARTESIAN_POINT('Ctrl Pts',(4.35826994395572,-1.85419527794546,-0.864534563995572));
#8007=CARTESIAN_POINT('Ctrl Pts',(4.34678634033727,-1.84958937573845,-0.865334589709168));
#8008=CARTESIAN_POINT('Ctrl Pts',(4.34231505483757,-1.8477771516406,-0.865645592455148));
#8009=CARTESIAN_POINT('Ctrl Pts',(4.33359241145023,-1.84420494172435,-0.866251265583746));
#8010=CARTESIAN_POINT('Ctrl Pts',(4.3293405130243,-1.8424464462249,-0.866546017023707));
#8011=CARTESIAN_POINT('Ctrl Pts',(4.31890270636355,-1.83808723648958,-0.867268477769702));
#8012=CARTESIAN_POINT('Ctrl Pts',(4.31272369152793,-1.83546995956914,-0.86769520027713));
#8013=CARTESIAN_POINT('Ctrl Pts',(4.29161078623088,-1.82640113248664,-0.869150342559267));
#8014=CARTESIAN_POINT('Ctrl Pts',(4.27674221285872,-1.81979791078204,-0.87017010189741));
#8015=CARTESIAN_POINT('Ctrl Pts',(4.17093278136729,-1.77124897625112,-0.877402555868397));
#8016=CARTESIAN_POINT('Ctrl Pts',(4.08317247633702,-1.72268368726434,-0.883275021406064));
#8017=CARTESIAN_POINT('Ctrl Pts',(3.93013555056186,-1.62225692499831,-0.893925138837197));
#8018=CARTESIAN_POINT('Ctrl Pts',(3.86374935412762,-1.572515177416,-0.898706348328159));
#8019=CARTESIAN_POINT('Ctrl Pts',(3.73728472955712,-1.4648366582771,-0.908472411864932));
#8020=CARTESIAN_POINT('Ctrl Pts',(3.67736367815897,-1.40697643654294,-0.913448834056087));
#8021=CARTESIAN_POINT('Ctrl Pts',(3.60660699495583,-1.32953902324299,-0.919926233545728));
#8022=CARTESIAN_POINT('Ctrl Pts',(3.59224170212754,-1.31329314680827,-0.921275559929294));
#8023=CARTESIAN_POINT('Ctrl Pts',(3.57139900333033,-1.28893279253484,-0.923286700333308));
#8024=CARTESIAN_POINT('Ctrl Pts',(3.56471518925752,-1.28099641309917,-0.923940052399901));
#8025=CARTESIAN_POINT('Ctrl Pts',(3.55294200233535,-1.26679346083781,-0.925106207113582));
#8026=CARTESIAN_POINT('Ctrl Pts',(3.54782814494878,-1.26054741438958,-0.925618004417759));
#8027=CARTESIAN_POINT('Ctrl Pts',(3.53713937934953,-1.24732931390649,-0.926698997964977));
#8028=CARTESIAN_POINT('Ctrl Pts',(3.53157309122741,-1.24035054889988,-0.927268523058301));
#8029=CARTESIAN_POINT('Ctrl Pts',(3.5169581783219,-1.2217725679385,-0.928781604221853));
#8030=CARTESIAN_POINT('Ctrl Pts',(3.50799084127706,-1.2101103851649,-0.929728334851506));
#8031=CARTESIAN_POINT('Ctrl Pts',(3.46940301769535,-1.15876063929167,-0.933884330608955));
#8032=CARTESIAN_POINT('Ctrl Pts',(3.44113950433593,-1.11807996807281,-0.937145132506772));
#8033=CARTESIAN_POINT('Ctrl Pts',(3.33526818861873,-0.952897711911929,-0.950271567276726));
#8034=CARTESIAN_POINT('Ctrl Pts',(3.2699876569743,-0.82106153185355,-0.960545422710943));
#8035=CARTESIAN_POINT('Ctrl Pts',(3.19143779420518,-0.605620590632464,-0.976488158561092));
#8036=CARTESIAN_POINT('Ctrl Pts',(3.16797287025663,-0.526260065823266,-0.982184617951813));
#8037=CARTESIAN_POINT('Ctrl Pts',(3.14590220465467,-0.429971147437003,-0.988728424216045));
#8038=CARTESIAN_POINT('Ctrl Pts',(3.14249496353832,-0.41423365126618,-0.989786334341946));
#8039=CARTESIAN_POINT('Ctrl Pts',(3.13798112874736,-0.392091912257889,-0.991256882777223));
#8040=CARTESIAN_POINT('Ctrl Pts',(3.13671480103206,-0.385721379823161,-0.991677916204127));
#8041=CARTESIAN_POINT('Ctrl Pts',(3.13460354167175,-0.374822110741027,-0.992394596106027));
#8042=CARTESIAN_POINT('Ctrl Pts',(3.13374314671583,-0.370296454061504,-0.992691102399556));
#8043=CARTESIAN_POINT('Ctrl Pts',(3.1319987438127,-0.360944482072323,-0.99330153966421));
#8044=CARTESIAN_POINT('Ctrl Pts',(3.13111685651705,-0.356117845053312,-0.993615351665187));
#8045=CARTESIAN_POINT('Ctrl Pts',(3.12885819148717,-0.343492712574617,-0.994433072608047));
#8046=CARTESIAN_POINT('Ctrl Pts',(3.12751001162107,-0.335689093970517,-0.994935397011909));
#8047=CARTESIAN_POINT('Ctrl Pts',(3.12216709753426,-0.303625843306616,-0.996987343730424));
#8048=CARTESIAN_POINT('Ctrl Pts',(3.11857437746895,-0.279300247551327,-0.998515989308374));
#8049=CARTESIAN_POINT('Ctrl Pts',(3.09813378656615,-0.120659712985837,-1.00833899078208));
#8050=CARTESIAN_POINT('Ctrl Pts',(3.09454380485881,0.0150220097502235,-1.01607927461657));
#8051=CARTESIAN_POINT('Ctrl Pts',(3.11113602919546,0.23499569193905,-1.02890952578856));
#8052=CARTESIAN_POINT('Ctrl Pts',(3.12298101761858,0.319454110522624,-1.03390087217809));
#8053=CARTESIAN_POINT('Ctrl Pts',(3.14989194620357,0.449946448848493,-1.04193752356205));
#8054=CARTESIAN_POINT('Ctrl Pts',(3.1612921083441,0.496632290651053,-1.04487856168617));
#8055=CARTESIAN_POINT('Ctrl Pts',(3.17818194593755,0.556352078378552,-1.04874765643286));
#8056=CARTESIAN_POINT('Ctrl Pts',(3.18214028745376,0.569804797047334,-1.04962630489286));
#8057=CARTESIAN_POINT('Ctrl Pts',(3.18880586394903,0.59160667258499,-1.05106230161777));
#8058=CARTESIAN_POINT('Ctrl Pts',(3.19142698840851,0.599981813544971,-1.05161684362798));
#8059=CARTESIAN_POINT('Ctrl Pts',(3.19657800280133,0.616067418186978,-1.05268764560082));
#8060=CARTESIAN_POINT('Ctrl Pts',(3.19909985085554,0.6237802890608,-1.0532036334809));
#8061=CARTESIAN_POINT('Ctrl Pts',(3.20499532383959,0.641445478869986,-1.05439139206596));
#8062=CARTESIAN_POINT('Ctrl Pts',(3.20840065038579,0.651386887727188,-1.05506419305756));
#8063=CARTESIAN_POINT('Ctrl Pts',(3.21922973981671,0.682204525022113,-1.05716369235184));
#8064=CARTESIAN_POINT('Ctrl Pts',(3.22692268027671,0.702983712366555,-1.05859921375342));
#8065=CARTESIAN_POINT('Ctrl Pts',(3.29808975885858,0.885798401157605,-1.07141079859375));
#8066=CARTESIAN_POINT('Ctrl Pts',(3.382158903225,1.0389797366191,-1.08351978686854));
#8067=CARTESIAN_POINT('Ctrl Pts',(3.54302532713859,1.25844160301574,-1.10246767441928));
#8068=CARTESIAN_POINT('Ctrl Pts',(3.60682335832631,1.33322380363297,-1.1092557686333));
#8069=CARTESIAN_POINT('Ctrl Pts',(3.68421842089496,1.41144304985929,-1.11649788076805));
#8070=CARTESIAN_POINT('Ctrl Pts',(3.69263681147172,1.41980065636516,-1.1172735795204));
#8071=CARTESIAN_POINT('Ctrl Pts',(3.70524041403133,1.43209196500548,-1.11841652141854));
#8072=CARTESIAN_POINT('Ctrl Pts',(3.70936868594647,1.4360833133506,-1.11878800935537));
#8073=CARTESIAN_POINT('Ctrl Pts',(3.71676530255033,1.4431730652731,-1.11944839223463));
#8074=CARTESIAN_POINT('Ctrl Pts',(3.72002695427016,1.44627827599345,-1.11973780361887));
#8075=CARTESIAN_POINT('Ctrl Pts',(3.72714683685021,1.45301084339284,-1.12036565824509));
#8076=CARTESIAN_POINT('Ctrl Pts',(3.73100900188762,1.4566338888509,-1.12070377622699));
#8077=CARTESIAN_POINT('Ctrl Pts',(3.74178494652321,1.46666228368675,-1.12164051083259));
#8078=CARTESIAN_POINT('Ctrl Pts',(3.74872986912068,1.47303417736222,-1.12223666195639));
#8079=CARTESIAN_POINT('Ctrl Pts',(3.7868373953119,1.5075031848339,-1.12546857903114));
#8080=CARTESIAN_POINT('Ctrl Pts',(3.81883782178845,1.5346631071771,-1.12804092809379));
#8081=CARTESIAN_POINT('Ctrl Pts',(3.96703687127094,1.65260679335656,-1.13945616323681));
#8082=CARTESIAN_POINT('Ctrl Pts',(4.09223098340434,1.73135142873996,-1.14780307873569));
#8083=CARTESIAN_POINT('Ctrl Pts',(4.3031814276704,1.83342746495134,-1.1615581968844));
#8084=CARTESIAN_POINT('Ctrl Pts',(4.38377390548446,1.86611863538257,-1.16674303265909));
#8085=CARTESIAN_POINT('Ctrl Pts',(4.48727625842137,1.90042494222461,-1.17347280024468));
#8086=CARTESIAN_POINT('Ctrl Pts',(4.50843194597942,1.90704780738036,-1.17485159767248));
#8087=CARTESIAN_POINT('Ctrl Pts',(4.53973309882718,1.91627683446841,-1.17689831621412));
#8088=CARTESIAN_POINT('Ctrl Pts',(4.54979621094097,1.91915800668901,-1.17755732819381));
#8089=CARTESIAN_POINT('Ctrl Pts',(4.56767039414373,1.92412369045163,-1.17872985240924));
#8090=CARTESIAN_POINT('Ctrl Pts',(4.57547239340425,1.92624018522141,-1.17924231903356));
#8091=CARTESIAN_POINT('Ctrl Pts',(4.59187067673215,1.93058180380697,-1.18032091488799));
#8092=CARTESIAN_POINT('Ctrl Pts',(4.60046936607575,1.9327970651867,-1.18088734894532));
#8093=CARTESIAN_POINT('Ctrl Pts',(4.6231437700986,1.93847745487856,-1.18238340339468));
#8094=CARTESIAN_POINT('Ctrl Pts',(4.6372427574233,1.94184663695781,-1.18331607183031));
#8095=CARTESIAN_POINT('Ctrl Pts',(4.69764551290223,1.95558667036054,-1.1873229024814));
#8096=CARTESIAN_POINT('Ctrl Pts',(4.74427137312759,1.96445647619298,-1.19044412396938));
#8097=CARTESIAN_POINT('Ctrl Pts',(4.97599827618466,2.00002797374892,-1.20610505563317));
#8098=CARTESIAN_POINT('Ctrl Pts',(5.16389226027774,2.00226509918841,-1.21938695356209));
#8099=CARTESIAN_POINT('Ctrl Pts',(5.40345895116653,1.9713291085138,-1.23594900869008));
#8100=CARTESIAN_POINT('Ctrl Pts',(5.45731914213056,1.96211239430875,-1.23963791043293));
#8101=CARTESIAN_POINT('Ctrl Pts',(5.52028924153241,1.94865416293136,-1.24385993806747));
#8102=CARTESIAN_POINT('Ctrl Pts',(5.52982568748204,1.94654263938508,-1.2444968396957));
#8103=CARTESIAN_POINT('Ctrl Pts',(5.5445244597398,1.94317465032612,-1.24547424635385));
#8104=CARTESIAN_POINT('Ctrl Pts',(5.54969776346179,1.94196750026914,-1.24581743052318));
#8105=CARTESIAN_POINT('Ctrl Pts',(5.55924623704794,1.93969917973655,-1.24644926025576));
#8106=CARTESIAN_POINT('Ctrl Pts',(5.56362261719699,1.93864386987071,-1.24673822043001));
#8107=CARTESIAN_POINT('Ctrl Pts',(5.5735515309157,1.93621403878744,-1.24739240019901));
#8108=CARTESIAN_POINT('Ctrl Pts',(5.57910174357462,1.93483044644351,-1.24775709759942));
#8109=CARTESIAN_POINT('Ctrl Pts',(5.59350727074235,1.93117345858889,-1.24870128532219));
#8110=CARTESIAN_POINT('Ctrl Pts',(5.60235315908241,1.9288629956175,-1.24927873176008));
#8111=CARTESIAN_POINT('Ctrl Pts',(5.6615964053081,1.9129533284828,-1.25313222067828));
#8112=CARTESIAN_POINT('Ctrl Pts',(5.71146379575825,1.8974399502471,-1.2563087420089));
#8113=CARTESIAN_POINT('Ctrl Pts',(5.91719399177631,1.82446623421212,-1.26934999890745));
#8114=CARTESIAN_POINT('Ctrl Pts',(6.06617646748187,1.74961519986767,-1.27869161062462));
#8115=CARTESIAN_POINT('Ctrl Pts',(6.26056699817922,1.61936870403373,-1.29261768816255));
#8116=CARTESIAN_POINT('Ctrl Pts',(6.31499747994002,1.57872684182096,-1.2967313369423));
#8117=CARTESIAN_POINT('Ctrl Pts',(6.37927243981559,1.52541865754462,-1.30192557262718));
#8118=CARTESIAN_POINT('Ctrl Pts',(6.39118032738342,1.51530405707303,-1.30290286841909));
#8119=CARTESIAN_POINT('Ctrl Pts',(6.4098541705187,1.4990609585207,-1.30446010345531));
#8120=CARTESIAN_POINT('Ctrl Pts',(6.41669914279628,1.49302396577715,-1.30503627699238));
#8121=CARTESIAN_POINT('Ctrl Pts',(6.42949363124932,1.48158267652179,-1.30612353115639));
#8122=CARTESIAN_POINT('Ctrl Pts',(6.43545239999776,1.47618896556273,-1.30663416329348));
#8123=CARTESIAN_POINT('Ctrl Pts',(6.44878200613385,1.46397600546527,-1.30778617909207));
#8124=CARTESIAN_POINT('Ctrl Pts',(6.4561342330428,1.45713685432712,-1.3084283983776));
#8125=CARTESIAN_POINT('Ctrl Pts',(6.4748000680814,1.43950886356093,-1.3100765591874));
#8126=CARTESIAN_POINT('Ctrl Pts',(6.48603888442882,1.42864216386905,-1.31108582501924));
#8127=CARTESIAN_POINT('Ctrl Pts',(6.55983887813781,1.3555878169169,-1.31782808293402));
#8128=CARTESIAN_POINT('Ctrl Pts',(6.61833513760812,1.28944961857603,-1.32373588577135));
#8129=CARTESIAN_POINT('Ctrl Pts',(6.75268873949323,1.11557598102997,-1.33878255090068));
#8130=CARTESIAN_POINT('Ctrl Pts',(6.82262059997119,1.00379351305069,-1.34806102897913));
#8131=CARTESIAN_POINT('Ctrl Pts',(6.9091576394201,0.829223127540357,-1.36148163602892));
#8132=CARTESIAN_POINT('Ctrl Pts',(6.93456294866335,0.771186879097831,-1.36577905863849));
#8133=CARTESIAN_POINT('Ctrl Pts',(6.96077324543181,0.702596574505435,-1.37059660451248));
#8134=CARTESIAN_POINT('Ctrl Pts',(6.96430817313933,0.693130883840755,-1.37125578751839));
#8135=CARTESIAN_POINT('Ctrl Pts',(6.9696162664558,0.678580694983217,-1.37225996678204));
#8136=CARTESIAN_POINT('Ctrl Pts',(6.9714409626117,0.673515360906222,-1.37260787222532));
#8137=CARTESIAN_POINT('Ctrl Pts',(6.97475206747224,0.664205736124418,-1.37324413507345));
#8138=CARTESIAN_POINT('Ctrl Pts',(6.97624463054939,0.659963813251686,-1.37353284163636));
#8139=CARTESIAN_POINT('Ctrl Pts',(6.97957390216103,0.65039870659977,-1.37418115366984));
#8140=CARTESIAN_POINT('Ctrl Pts',(6.98140242061994,0.645072779197203,-1.37454027728808));
#8141=CARTESIAN_POINT('Ctrl Pts',(6.98671835366424,0.629372903894551,-1.37559363474468));
#8142=CARTESIAN_POINT('Ctrl Pts',(6.99014304056991,0.618977719301734,-1.37628432418162));
#8143=CARTESIAN_POINT('Ctrl Pts',(7.02046018163391,0.52434018555716,-1.38251562447046));
#8144=CARTESIAN_POINT('Ctrl Pts',(7.04181204608914,0.438413472640924,-1.3877686451868));
#8145=CARTESIAN_POINT('Ctrl Pts',(7.07805807749167,0.235844000376361,-1.39981019930376));
#8146=CARTESIAN_POINT('Ctrl Pts',(7.08849340272321,0.118748857292228,-1.4065260971332));
#8147=CARTESIAN_POINT('Ctrl Pts',(7.08857698811124,0.000943538781985227,
-1.41349835193204));
#8148=CARTESIAN_POINT('Ctrl Pts',(7.08857715545312,0.000471768043527199,
-1.41352627668663));
#8149=CARTESIAN_POINT('Ctrl Pts',(7.08857715545311,-2.35333930719797E-11,
-1.41355420449641));
#8150=CARTESIAN_POINT('Ctrl Pts',(7.08857715545311,2.4467182997506E-11,
-1.57370881642439));
#8151=CARTESIAN_POINT('Ctrl Pts',(7.08857715545217,0.0768861269152348,-1.56915919293977));
#8152=CARTESIAN_POINT('Ctrl Pts',(7.08413199193511,0.153700428581474,-1.56452529786783));
#8153=CARTESIAN_POINT('Ctrl Pts',(7.07351340899662,0.245154597534047,-1.55880772583754));
#8154=CARTESIAN_POINT('Ctrl Pts',(7.07158860242346,0.260226974266608,-1.55785898216073));
#8155=CARTESIAN_POINT('Ctrl Pts',(7.06812460139678,0.285088259280509,-1.55628274489061));
#8156=CARTESIAN_POINT('Ctrl Pts',(7.06668430205023,0.294890478106148,-1.5556583544683));
#8157=CARTESIAN_POINT('Ctrl Pts',(7.06394499566413,0.312614285930607,-1.55452390847148));
#8158=CARTESIAN_POINT('Ctrl Pts',(7.06267107243397,0.32053958193332,-1.55401465307066));
#8159=CARTESIAN_POINT('Ctrl Pts',(7.05983097275455,0.3375523453662,-1.55291710636448));
#8160=CARTESIAN_POINT('Ctrl Pts',(7.05824955151252,0.346637044575541,-1.55232834423656));
#8161=CARTESIAN_POINT('Ctrl Pts',(7.05374185745093,0.371510100853789,-1.55070885343642));
#8162=CARTESIAN_POINT('Ctrl Pts',(7.05068789766292,0.387274327601949,-1.54967411249181));
#8163=CARTESIAN_POINT('Ctrl Pts',(7.03228431834651,0.476489164352646,-1.54376946965414));
#8164=CARTESIAN_POINT('Ctrl Pts',(7.01299189755982,0.549055913182397,-1.53877529113696));
#8165=CARTESIAN_POINT('Ctrl Pts',(6.95814151957859,0.716680755396122,-1.52678713662946));
#8166=CARTESIAN_POINT('Ctrl Pts',(6.91932913515949,0.810455970617528,-1.51971877267814));
#8167=CARTESIAN_POINT('Ctrl Pts',(6.84845330252681,0.950476840054279,-1.50878147734263));
#8168=CARTESIAN_POINT('Ctrl Pts',(6.82127819641459,0.9990157641976,-1.50491521831595));
#8169=CARTESIAN_POINT('Ctrl Pts',(6.76423143520207,1.09160508115647,-1.49746161270735));
#8170=CARTESIAN_POINT('Ctrl Pts',(6.7345531732624,1.13572502132681,-1.49387246181544));
#8171=CARTESIAN_POINT('Ctrl Pts',(6.69771028153764,1.18603165721879,-1.48978059415843));
#8172=CARTESIAN_POINT('Ctrl Pts',(6.6922239255966,1.19341524498623,-1.48918005244011));
#8173=CARTESIAN_POINT('Ctrl Pts',(6.68323320448872,1.20534181265451,-1.48821040722493));
#8174=CARTESIAN_POINT('Ctrl Pts',(6.67976004357428,1.20990799253566,-1.48783926693516));
#8175=CARTESIAN_POINT('Ctrl Pts',(6.67352562192623,1.21803144237959,-1.48717925767719));
#8176=CARTESIAN_POINT('Ctrl Pts',(6.67077197394222,1.22159440092352,-1.48688987469165));
#8177=CARTESIAN_POINT('Ctrl Pts',(6.66475137993622,1.22933019446755,-1.48626179953753));
#8178=CARTESIAN_POINT('Ctrl Pts',(6.66147986550272,1.23349934265803,-1.48592343453841));
#8179=CARTESIAN_POINT('Ctrl Pts',(6.65216869559997,1.24526842120195,-1.48496847939245));
#8180=CARTESIAN_POINT('Ctrl Pts',(6.6460900253029,1.25283749484317,-1.48435457202789));
#8181=CARTESIAN_POINT('Ctrl Pts',(6.60629620498284,1.30165392837125,-1.48039463096743));
#8182=CARTESIAN_POINT('Ctrl Pts',(6.57099223478799,1.34158488252399,-1.47715263298696));
#8183=CARTESIAN_POINT('Ctrl Pts',(6.41537130766339,1.50399910773336,-1.46371744861686));
#8184=CARTESIAN_POINT('Ctrl Pts',(6.28111142856201,1.61209653390755,-1.45407869495032));
#8185=CARTESIAN_POINT('Ctrl Pts',(6.08209068898047,1.7338282404175,-1.44014883016587));
#8186=CARTESIAN_POINT('Ctrl Pts',(6.028062743396,1.76352712750665,-1.43640620186798));
#8187=CARTESIAN_POINT('Ctrl Pts',(5.958705569321,1.79756993727488,-1.43160165100466));
#8188=CARTESIAN_POINT('Ctrl Pts',(5.94458022224486,1.8042980761701,-1.43062324213204));
#8189=CARTESIAN_POINT('Ctrl Pts',(5.92200602842218,1.81472652333584,-1.429059074028));
#8190=CARTESIAN_POINT('Ctrl Pts',(5.91360795602271,1.81853568415618,-1.42847705489128));
#8191=CARTESIAN_POINT('Ctrl Pts',(5.89785086193264,1.82555138934413,-1.42738467039266));
#8192=CARTESIAN_POINT('Ctrl Pts',(5.89049828665048,1.82877202006165,-1.42687479811112));
#8193=CARTESIAN_POINT('Ctrl Pts',(5.87402799139166,1.83586828763527,-1.4257322298307));
#8194=CARTESIAN_POINT('Ctrl Pts',(5.86490048308439,1.83972053082239,-1.42509875680098));
#8195=CARTESIAN_POINT('Ctrl Pts',(5.83789964634047,1.85087993562018,-1.42322378419378));
#8196=CARTESIAN_POINT('Ctrl Pts',(5.81994889368163,1.85799558280552,-1.42197590918335));
#8197=CARTESIAN_POINT('Ctrl Pts',(5.6755575287839,1.91282003467045,-1.41192453448759));
#8198=CARTESIAN_POINT('Ctrl Pts',(5.54469266456362,1.94781890112191,-1.40269455013442));
#8199=CARTESIAN_POINT('Ctrl Pts',(5.27666430574581,1.99103028085902,-1.38380865480221));
#8200=CARTESIAN_POINT('Ctrl Pts',(5.14012811850766,1.99887286780517,-1.37420434704263));
#8201=CARTESIAN_POINT('Ctrl Pts',(4.98861217754417,1.99203165282899,-1.36416446514001));
#8202=CARTESIAN_POINT('Ctrl Pts',(4.97337988877494,1.99116869879459,-1.36316243091137));
#8203=CARTESIAN_POINT('Ctrl Pts',(4.9522659971156,1.98972934929157,-1.36178497725543));
#8204=CARTESIAN_POINT('Ctrl Pts',(4.94637525652777,1.9893014815796,-1.36140191287495));
#8205=CARTESIAN_POINT('Ctrl Pts',(4.93624824512703,1.98852068592968,-1.36074560910017));
#8206=CARTESIAN_POINT('Ctrl Pts',(4.93201108312698,1.98818037182525,-1.36047168450437));
#8207=CARTESIAN_POINT('Ctrl Pts',(4.92314158343221,1.98743946229763,-1.35989974558767));
#8208=CARTESIAN_POINT('Ctrl Pts',(4.91850951541889,1.98703621166551,-1.35960189032805));
#8209=CARTESIAN_POINT('Ctrl Pts',(4.90718444039631,1.98601038325817,-1.35887561680763));
#8210=CARTESIAN_POINT('Ctrl Pts',(4.90049301049568,1.98537015616635,-1.35844817305147));
#8211=CARTESIAN_POINT('Ctrl Pts',(4.87633352190744,1.98293530627907,-1.35691052482799));
#8212=CARTESIAN_POINT('Ctrl Pts',(4.85888552049683,1.98094381225378,-1.35581069808715));
#8213=CARTESIAN_POINT('Ctrl Pts',(4.81539197746638,1.97539674381059,-1.35309068693876));
#8214=CARTESIAN_POINT('Ctrl Pts',(4.78938555395295,1.9715562097802,-1.35148367924389));
#8215=CARTESIAN_POINT('Ctrl Pts',(4.67682236457926,1.95265270658149,-1.34458323424197));
#8216=CARTESIAN_POINT('Ctrl Pts',(4.5912322449369,1.93239393326732,-1.33947557748124));
#8217=CARTESIAN_POINT('Ctrl Pts',(4.36756250820291,1.86357913676258,-1.32588764687039));
#8218=CARTESIAN_POINT('Ctrl Pts',(4.23303702886595,1.80538691636256,-1.31742819370428));
#8219=CARTESIAN_POINT('Ctrl Pts',(4.08477931931321,1.72088673071914,-1.3069257333719));
#8220=CARTESIAN_POINT('Ctrl Pts',(4.06370496791276,1.7083550195488,-1.3054039281175));
#8221=CARTESIAN_POINT('Ctrl Pts',(4.03439120010911,1.69018415471465,-1.30324344087637));
#8222=CARTESIAN_POINT('Ctrl Pts',(4.02595441758008,1.68486641318354,-1.30261643818217));
#8223=CARTESIAN_POINT('Ctrl Pts',(4.01125659756604,1.67544757116724,-1.30151481735425));
#8224=CARTESIAN_POINT('Ctrl Pts',(4.00497805609663,1.67137404936516,-1.30104122217721));
#8225=CARTESIAN_POINT('Ctrl Pts',(3.99181301925058,1.66272690078038,-1.30004173497001));
#8226=CARTESIAN_POINT('Ctrl Pts',(3.98493174881525,1.65814561385241,-1.2995155636511));
#8227=CARTESIAN_POINT('Ctrl Pts',(3.96847528340446,1.64704127421749,-1.29824808889974));
#8228=CARTESIAN_POINT('Ctrl Pts',(3.95892814195743,1.64047737403499,-1.29750525856094));
#8229=CARTESIAN_POINT('Ctrl Pts',(3.92599092804313,1.61740707724775,-1.29491594113832));
#8230=CARTESIAN_POINT('Ctrl Pts',(3.90290031391413,1.60048124798541,-1.29305358628486));
#8231=CARTESIAN_POINT('Ctrl Pts',(3.76267341018936,1.49297740583364,-1.28144261947988));
#8232=CARTESIAN_POINT('Ctrl Pts',(3.65557942579559,1.3901008799441,-1.27119789647535));
#8233=CARTESIAN_POINT('Ctrl Pts',(3.49166330538878,1.19322961525116,-1.25333764453476));
#8234=CARTESIAN_POINT('Ctrl Pts',(3.42932548616171,1.10461062277575,-1.24580123940056));
#8235=CARTESIAN_POINT('Ctrl Pts',(3.36620987721488,0.997312367766644,-1.23754907466764));
#8236=CARTESIAN_POINT('Ctrl Pts',(3.35811526454825,0.98315700247315,-1.23647700619968));
#8237=CARTESIAN_POINT('Ctrl Pts',(3.34693245486155,0.963032490996198,-1.23497782209772));
#8238=CARTESIAN_POINT('Ctrl Pts',(3.3436996943103,0.957144997665118,-1.23454221011597));
#8239=CARTESIAN_POINT('Ctrl Pts',(3.33830197154852,0.947195899620492,-1.23381123320434));
#8240=CARTESIAN_POINT('Ctrl Pts',(3.33612123579191,0.943142961100182,-1.23351488844479));
#8241=CARTESIAN_POINT('Ctrl Pts',(3.33168408795248,0.934827594069914,-1.23290986155207));
#8242=CARTESIAN_POINT('Ctrl Pts',(3.32942907838012,0.930564478041992,-1.23260126692047));
#8243=CARTESIAN_POINT('Ctrl Pts',(3.32368825782938,0.919615515074339,-1.23181266332265));
#8244=CARTESIAN_POINT('Ctrl Pts',(3.3202248149079,0.912917934096015,-1.23133403597237));
#8245=CARTESIAN_POINT('Ctrl Pts',(3.30601302874139,0.885049121368304,-1.22935737611577));
#8246=CARTESIAN_POINT('Ctrl Pts',(3.29560463352925,0.863705492415834,-1.22787908323097));
#8247=CARTESIAN_POINT('Ctrl Pts',(3.26876210355763,0.806071796077251,-1.22396819964988));
#8248=CARTESIAN_POINT('Ctrl Pts',(3.25302918088304,0.769465654246573,-1.22156844859414));
#8249=CARTESIAN_POINT('Ctrl Pts',(3.20425498421416,0.645905397347893,-1.21366842706614));
#8250=CARTESIAN_POINT('Ctrl Pts',(3.17619772852972,0.557113830700254,-1.20831013083785));
#8251=CARTESIAN_POINT('Ctrl Pts',(3.12399340216493,0.340169798654947,-1.19534054034536));
#8252=CARTESIAN_POINT('Ctrl Pts',(3.10600567911421,0.210997357617773,-1.18769847724863));
#8253=CARTESIAN_POINT('Ctrl Pts',(3.10006439052321,0.0648093677771114,-1.17862522918925));
#8254=CARTESIAN_POINT('Ctrl Pts',(3.09960365997113,0.0486090833919524,-1.17761436914685));
#8255=CARTESIAN_POINT('Ctrl Pts',(3.09917444345262,0.0221916315012395,-1.17595640585021));
#8256=CARTESIAN_POINT('Ctrl Pts',(3.09908695771417,0.0119769489165365,-1.17531299946694));
#8257=CARTESIAN_POINT('Ctrl Pts',(3.0990708186893,-0.00629191974975199,
-1.17415791459135));
#8258=CARTESIAN_POINT('Ctrl Pts',(3.09911248332419,-0.0143459057394821,
-1.1736471708984));
#8259=CARTESIAN_POINT('Ctrl Pts',(3.09930417725768,-0.0314159464480813,
-1.17256136685666));
#8260=CARTESIAN_POINT('Ctrl Pts',(3.09946656891587,-0.0404316549372829,
-1.17198593282258));
#8261=CARTESIAN_POINT('Ctrl Pts',(3.10006494771478,-0.0645641103545041,
-1.17044027594198));
#8262=CARTESIAN_POINT('Ctrl Pts',(3.10061171914711,-0.0796772803540742,
-1.16946663079102));
#8263=CARTESIAN_POINT('Ctrl Pts',(3.10421717908372,-0.155470518225676,-1.1645542969945));
#8264=CARTESIAN_POINT('Ctrl Pts',(3.10987494328644,-0.215989034429837,-1.1605356946821));
#8265=CARTESIAN_POINT('Ctrl Pts',(3.13605033054297,-0.403244387221179,-1.1477952072643));
#8266=CARTESIAN_POINT('Ctrl Pts',(3.16603794446212,-0.528316267293695,-1.13882183741282));
#8267=CARTESIAN_POINT('Ctrl Pts',(3.23921550968878,-0.740766878977301,-1.12318184647927));
#8268=CARTESIAN_POINT('Ctrl Pts',(3.27717816630783,-0.829524407888211,-1.11652495514493));
#8269=CARTESIAN_POINT('Ctrl Pts',(3.32643997921539,-0.924927052015169,-1.10946783366581));
#8270=CARTESIAN_POINT('Ctrl Pts',(3.33154440861088,-0.934615972152766,-1.10875237788209));
#8271=CARTESIAN_POINT('Ctrl Pts',(3.33939471564807,-0.949223946216446,-1.10767614459492));
#8272=CARTESIAN_POINT('Ctrl Pts',(3.34208196589076,-0.954174029532902,-1.10731188177832));
#8273=CARTESIAN_POINT('Ctrl Pts',(3.34695239162603,-0.963055732733448,-1.10665917037015));
#8274=CARTESIAN_POINT('Ctrl Pts',(3.34912791731066,-0.966991393165042,-1.1063702559096));
#8275=CARTESIAN_POINT('Ctrl Pts',(3.35393676363011,-0.975621832643846,-1.10573739625538));
#8276=CARTESIAN_POINT('Ctrl Pts',(3.35657578132915,-0.980313317583523,-1.1053938180484));
#8277=CARTESIAN_POINT('Ctrl Pts',(3.36422023774594,-0.993775350464348,-1.10440904102709));
#8278=CARTESIAN_POINT('Ctrl Pts',(3.36927341407417,-1.00251879791121,-1.10377079679464));
#8279=CARTESIAN_POINT('Ctrl Pts',(3.40640526148438,-1.0656559356145,-1.09916906478161));
#8280=CARTESIAN_POINT('Ctrl Pts',(3.44098790230944,-1.11854340209923,-1.09535232297778));
#8281=CARTESIAN_POINT('Ctrl Pts',(3.55465984221424,-1.27556690800239,-1.08385579033966));
#8282=CARTESIAN_POINT('Ctrl Pts',(3.64151378687392,-1.37364317600236,-1.07641885075015));
#8283=CARTESIAN_POINT('Ctrl Pts',(3.80271151906069,-1.52315383809513,-1.06348609632469));
#8284=CARTESIAN_POINT('Ctrl Pts',(3.87206679725908,-1.57932768116212,-1.05814423095602));
#8285=CARTESIAN_POINT('Ctrl Pts',(3.95774707164088,-1.63969357409771,-1.05163967840722));
#8286=CARTESIAN_POINT('Ctrl Pts',(3.97065896306921,-1.64856488001505,-1.05066201580661));
#8287=CARTESIAN_POINT('Ctrl Pts',(3.99202457489852,-1.66287692411542,-1.04904769749925));
#8288=CARTESIAN_POINT('Ctrl Pts',(4.00041746196959,-1.66840757236939,-1.04841441565892));
#8289=CARTESIAN_POINT('Ctrl Pts',(4.01559687510943,-1.67824659639889,-1.04727041537831));
#8290=CARTESIAN_POINT('Ctrl Pts',(4.02236836621946,-1.68257785426699,-1.04676056007491));
#8291=CARTESIAN_POINT('Ctrl Pts',(4.03687831104672,-1.69173575980882,-1.04566896651476));
#8292=CARTESIAN_POINT('Ctrl Pts',(4.04462403627758,-1.69655048580351,-1.04508680495376));
#8293=CARTESIAN_POINT('Ctrl Pts',(4.06570181892477,-1.70945283786425,-1.04350396039319));
#8294=CARTESIAN_POINT('Ctrl Pts',(4.07909591372472,-1.71743739237585,-1.04249956294312));
#8295=CARTESIAN_POINT('Ctrl Pts',(4.15090163236803,-1.75910935462844,-1.03712140143012));
#8296=CARTESIAN_POINT('Ctrl Pts',(4.21089355240965,-1.78997227911487,-1.03264824053934));
#8297=CARTESIAN_POINT('Ctrl Pts',(4.42083251040441,-1.88485118200897,-1.01705864893429));
#8298=CARTESIAN_POINT('Ctrl Pts',(4.57699929103611,-1.93351094892902,-1.00551021381818));
#8299=CARTESIAN_POINT('Ctrl Pts',(4.79196343746431,-1.97255956546963,-0.990515375249305));
#8300=CARTESIAN_POINT('Ctrl Pts',(4.84701171775522,-1.98020107366046,-0.986758935272432));
#8301=CARTESIAN_POINT('Ctrl Pts',(4.91156957355505,-1.98642800863067,-0.98250196070733));
#8302=CARTESIAN_POINT('Ctrl Pts',(4.92083333916232,-1.98725620067313,-0.981894664825687));
#8303=CARTESIAN_POINT('Ctrl Pts',(4.93585077927576,-1.9884929697595,-0.980916309747214));
#8304=CARTESIAN_POINT('Ctrl Pts',(4.94160090304123,-1.98894142606119,-0.980543154998738));
#8305=CARTESIAN_POINT('Ctrl Pts',(4.95184614098072,-1.98969576870291,-0.979880974602804));
#8306=CARTESIAN_POINT('Ctrl Pts',(4.95634042094851,-1.99001137174198,-0.979591420901822));
#8307=CARTESIAN_POINT('Ctrl Pts',(4.96610099312964,-1.99066356655519,-0.978964596075611));
#8308=CARTESIAN_POINT('Ctrl Pts',(4.97136756076725,-1.99099448943703,-0.978627641186583));
#8309=CARTESIAN_POINT('Ctrl Pts',(4.98622151248584,-1.99186867009812,-0.977680694641381));
#8310=CARTESIAN_POINT('Ctrl Pts',(4.99581174823293,-1.99236361189293,-0.977073314857825));
#8311=CARTESIAN_POINT('Ctrl Pts',(5.05638700014822,-1.99505138702975,-0.973260051893567));
#8312=CARTESIAN_POINT('Ctrl Pts',(5.10744151684906,-1.99535646581558,-0.970149522679433));
#8313=CARTESIAN_POINT('Ctrl Pts',(5.30991937716985,-1.98879284262045,-0.958027869018999));
#8314=CARTESIAN_POINT('Ctrl Pts',(5.46033616239323,-1.96663921428979,-0.94946407076443));
#8315=CARTESIAN_POINT('Ctrl Pts',(5.68574676728199,-1.90665479757553,-0.935696227872132));
#8316=CARTESIAN_POINT('Ctrl Pts',(5.7633188714487,-1.88081893085974,-0.930784537706651));
#8317=CARTESIAN_POINT('Ctrl Pts',(5.85343180877563,-1.84452368324058,-0.924753862395435));
#8318=CARTESIAN_POINT('Ctrl Pts',(5.86771245360311,-1.83857781225466,-0.923788279759531));
#8319=CARTESIAN_POINT('Ctrl Pts',(5.8911007013813,-1.82851915019943,-0.922189862035545));
#8320=CARTESIAN_POINT('Ctrl Pts',(5.90024928284875,-1.82450287374515,-0.92156028653491));
#8321=CARTESIAN_POINT('Ctrl Pts',(5.91669834298389,-1.81713376065756,-0.920420291048438));
#8322=CARTESIAN_POINT('Ctrl Pts',(5.92400951614949,-1.81380521013281,-0.919910707966358));
#8323=CARTESIAN_POINT('Ctrl Pts',(5.93144163465702,-1.81036724754357,-0.91938970034031));
#8324=CARTESIAN_POINT('Ctrl Pts',(5.93158296354498,-1.81030185128305,-0.919379791771803));
#8325=CARTESIAN_POINT('Ctrl Pts',(5.93185451897547,-1.81017615747267,-0.919360750892484));
#8326=CARTESIAN_POINT('Ctrl Pts',(5.93198474668212,-1.81011586241321,-0.919351618666983));
#8327=CARTESIAN_POINT('Ctrl Pts',(5.93223499665919,-1.80999996458596,-0.919334068064972));
#8328=CARTESIAN_POINT('Ctrl Pts',(5.93235501992212,-1.8099443639256,-0.91932564976036));
#8329=CARTESIAN_POINT('Ctrl Pts',(5.93258568350518,-1.80983748137534,-0.919309469724261));
#8330=CARTESIAN_POINT('Ctrl Pts',(5.93269632465075,-1.80978620127925,-0.919301708054864));
#8331=CARTESIAN_POINT('Ctrl Pts',(5.93290897811127,-1.80968761669767,-0.919286788737124));
#8332=CARTESIAN_POINT('Ctrl Pts',(5.93301099113292,-1.80964031373031,-0.919279631140989));
#8333=CARTESIAN_POINT('Ctrl Pts',(5.93320707983826,-1.80954936815609,-0.919265871749315));
#8334=CARTESIAN_POINT('Ctrl Pts',(5.93330115611567,-1.80950572683993,-0.919259269998498));
#8335=CARTESIAN_POINT('Ctrl Pts',(5.93348200544767,-1.80942181498176,-0.919246578050966));
#8336=CARTESIAN_POINT('Ctrl Pts',(5.93356877901262,-1.80938154553232,-0.919240487891772));
#8337=CARTESIAN_POINT('Ctrl Pts',(5.93373560456005,-1.80930411136666,-0.919228778519481));
#8338=CARTESIAN_POINT('Ctrl Pts',(5.93381565697793,-1.80926694757728,-0.919223159338115));
#8339=CARTESIAN_POINT('Ctrl Pts',(5.93396957384581,-1.80919548030332,-0.919212354646954));
#8340=CARTESIAN_POINT('Ctrl Pts',(5.93404343867405,-1.80916117760223,-0.919207169163538));
#8341=CARTESIAN_POINT('Ctrl Pts',(5.9341854701528,-1.80909520784966,-0.919197197638442));
#8342=CARTESIAN_POINT('Ctrl Pts',(5.93425363709459,-1.80906354147808,-0.919192411621305));
#8343=CARTESIAN_POINT('Ctrl Pts',(5.93438472234664,-1.80900263793383,-0.919183207597438));
#8344=CARTESIAN_POINT('Ctrl Pts',(5.93444764093444,-1.80897340132536,-0.919178789609484));
#8345=CARTESIAN_POINT('Ctrl Pts',(5.93456864237285,-1.80891716747187,-0.919170292763325));
#8346=CARTESIAN_POINT('Ctrl Pts',(5.93462672545113,-1.80889017071065,-0.919166213921685));
#8347=CARTESIAN_POINT('Ctrl Pts',(5.93473843517084,-1.80883824197768,-0.919158368827159));
#8348=CARTESIAN_POINT('Ctrl Pts',(5.93479206200654,-1.80881331041736,-0.919154602588332));
#8349=CARTESIAN_POINT('Ctrl Pts',(5.93493162711471,-1.80874841789375,-0.919144800445906));
#8350=CARTESIAN_POINT('Ctrl Pts',(5.93501756365072,-1.80870845318935,-0.919138764413097));
#8351=CARTESIAN_POINT('Ctrl Pts',(5.93518796475567,-1.80862919354634,-0.919126794920098));
#8352=CARTESIAN_POINT('Ctrl Pts',(5.93527242941148,-1.80858989881938,-0.919120861467726));
#8353=CARTESIAN_POINT('Ctrl Pts',(5.94402968012073,-1.80451509611075,-0.918505643051591));
#8354=CARTESIAN_POINT('Ctrl Pts',(5.95267320169202,-1.80041732069438,-0.917894221385039));
#8355=CARTESIAN_POINT('Ctrl Pts',(5.97742726585404,-1.78846293752613,-0.916130905918012));
#8356=CARTESIAN_POINT('Ctrl Pts',(5.99346149258386,-1.78045130761798,-0.914973677976082));
#8357=CARTESIAN_POINT('Ctrl Pts',(6.02949121042656,-1.76183781424405,-0.912338332072786));
#8358=CARTESIAN_POINT('Ctrl Pts',(6.04941833475516,-1.75110968723624,-0.910855947989299));
#8359=CARTESIAN_POINT('Ctrl Pts',(6.11341436099436,-1.71523860952733,-0.906013006214644));
#8360=CARTESIAN_POINT('Ctrl Pts',(6.15670492268725,-1.68875448350377,-0.90260761709076));
#8361=CARTESIAN_POINT('Ctrl Pts',(6.29692086832602,-1.59544534311504,-0.891148584970972));
#8362=CARTESIAN_POINT('Ctrl Pts',(6.38893642939663,-1.52169912646323,-0.882899299916485));
#8363=CARTESIAN_POINT('Ctrl Pts',(6.53825559993723,-1.37862135605198,-0.868524620877928));
#8364=CARTESIAN_POINT('Ctrl Pts',(6.59840852010042,-1.31271055972378,-0.862391087466903));
#8365=CARTESIAN_POINT('Ctrl Pts',(6.66077822635619,-1.23442770256218,-0.855812460215527));
#8366=CARTESIAN_POINT('Ctrl Pts',(6.66752956696062,-1.22580917944168,-0.855097218842239));
#8367=CARTESIAN_POINT('Ctrl Pts',(6.67764605651602,-1.21267347903028,-0.854021243135279));
#8368=CARTESIAN_POINT('Ctrl Pts',(6.68106346401881,-1.20819707860783,-0.853657025913144));
#8369=CARTESIAN_POINT('Ctrl Pts',(6.68717551216369,-1.20012032677696,-0.853004362245831));
#8370=CARTESIAN_POINT('Ctrl Pts',(6.68987696438829,-1.19652529983947,-0.852715450252279));
#8371=CARTESIAN_POINT('Ctrl Pts',(6.6957856890142,-1.18860649458396,-0.852082556000752));
#8372=CARTESIAN_POINT('Ctrl Pts',(6.6989876211743,-1.18427886206775,-0.851738941007445));
#8373=CARTESIAN_POINT('Ctrl Pts',(6.70814701355804,-1.17179391908996,-0.850753952284036));
#8374=CARTESIAN_POINT('Ctrl Pts',(6.71406018725152,-1.16360411045334,-0.850115535109336));
#8375=CARTESIAN_POINT('Ctrl Pts',(6.75653348249325,-1.10382657714879,-0.845508573168104));
#8376=CARTESIAN_POINT('Ctrl Pts',(6.79068861253648,-1.05056573398017,-0.841687154181984));
#8377=CARTESIAN_POINT('Ctrl Pts',(6.89065319632637,-0.877049248422192,-0.829811551901653));
#8378=CARTESIAN_POINT('Ctrl Pts',(6.94663611327104,-0.751599042259346,-0.822029168856653));
#8379=CARTESIAN_POINT('Ctrl Pts',(7.00605985538138,-0.570334324611354,-0.810777203479737));
#8380=CARTESIAN_POINT('Ctrl Pts',(7.02072836573836,-0.518619563541358,-0.807569791955741));
#8381=CARTESIAN_POINT('Ctrl Pts',(7.04192617252939,-0.430467145676259,-0.802055639977398));
#8382=CARTESIAN_POINT('Ctrl Pts',(7.04956212402777,-0.394325005806245,-0.799782079915123));
#8383=CARTESIAN_POINT('Ctrl Pts',(7.05855933362424,-0.34500624662049,-0.79665284697295));
#8384=CARTESIAN_POINT('Ctrl Pts',(7.06079954751239,-0.331996141197615,-0.795824881290785));
#8385=CARTESIAN_POINT('Ctrl Pts',(7.06414771905988,-0.311326699292858,-0.794505148165942));
#8386=CARTESIAN_POINT('Ctrl Pts',(7.06534055155126,-0.303681351655337,-0.794016061946849));
#8387=CARTESIAN_POINT('Ctrl Pts',(7.06764215613092,-0.288344063952135,-0.793032950706052));
#8388=CARTESIAN_POINT('Ctrl Pts',(7.06875051989567,-0.280652200958789,-0.792538922112808));
#8389=CARTESIAN_POINT('Ctrl Pts',(7.07088754748584,-0.265181697031638,-0.791543236316246));
#8390=CARTESIAN_POINT('Ctrl Pts',(7.07191531843868,-0.257403074466527,-0.791041560441624));
#8391=CARTESIAN_POINT('Ctrl Pts',(7.07416351688411,-0.239578518695906,-0.789889517242021));
#8392=CARTESIAN_POINT('Ctrl Pts',(7.07535343413771,-0.229529021409757,-0.789238205857419));
#8393=CARTESIAN_POINT('Ctrl Pts',(7.07938889522422,-0.193073803378723,-0.786868827789353));
#8394=CARTESIAN_POINT('Ctrl Pts',(7.08178337595365,-0.16662193566441,-0.785136834312907));
#8395=CARTESIAN_POINT('Ctrl Pts',(7.08696839595962,-0.0929961565994294,
-0.780278748685038));
#8396=CARTESIAN_POINT('Ctrl Pts',(7.08861171172832,-0.0457620549677525,
-0.777119293896236));
#8397=CARTESIAN_POINT('Ctrl Pts',(7.08857660471327,0.00148228751319614,
-0.773917982071593));
#8398=CARTESIAN_POINT('Origin',(5.09382715545311,0.,-6.77268258743872));
#8399=CARTESIAN_POINT('',(7.08857715545311,-1.12589837781526E-10,0.186011338956535));
#8400=CARTESIAN_POINT('',(7.08880671729685,0.00054701437290982,0.0273173682685466));
#8401=CARTESIAN_POINT('',(7.08857715545311,8.3550772080578E-14,-6.77268258743872));
#8402=CARTESIAN_POINT('Ctrl Pts',(7.08857715545311,-1.12589837781526E-10,
0.186011338956534));
#8403=CARTESIAN_POINT('Ctrl Pts',(7.08857715545308,-0.000600192261292308,
0.185969784536992));
#8404=CARTESIAN_POINT('Ctrl Pts',(7.0885768845847,-0.00120038994982216,
0.185928226101576));
#8405=CARTESIAN_POINT('Ctrl Pts',(7.08846930102655,-0.120384617245889,0.177675041757695));
#8406=CARTESIAN_POINT('Ctrl Pts',(7.0777883325812,-0.238722073627921,0.169320437128287));
#8407=CARTESIAN_POINT('Ctrl Pts',(7.04839332461821,-0.401062440880801,0.158061675733446));
#8408=CARTESIAN_POINT('Ctrl Pts',(7.03853620070026,-0.446416258112179,0.154941279742027));
#8409=CARTESIAN_POINT('Ctrl Pts',(7.02492514575313,-0.499966444455275,0.15131812106603));
#8410=CARTESIAN_POINT('Ctrl Pts',(7.02268779462601,-0.50852977814502,0.15074062684239));
#8411=CARTESIAN_POINT('Ctrl Pts',(7.01893366416992,-0.52251718346597,0.149800763933142));
#8412=CARTESIAN_POINT('Ctrl Pts',(7.01745080661349,-0.527950118378297,0.149436553642766));
#8413=CARTESIAN_POINT('Ctrl Pts',(7.01474251373248,-0.537709931890585,0.148783897283026));
#8414=CARTESIAN_POINT('Ctrl Pts',(7.01352544364508,-0.542038991238084,0.14849498571365));
#8415=CARTESIAN_POINT('Ctrl Pts',(7.01081919459467,-0.551541535177392,0.147862086371448));
#8416=CARTESIAN_POINT('Ctrl Pts',(7.00932371039755,-0.556713115340731,0.147518465904997));
#8417=CARTESIAN_POINT('Ctrl Pts',(7.00496192756431,-0.571571066731513,0.146533445501946));
#8418=CARTESIAN_POINT('Ctrl Pts',(7.00204291482573,-0.581241969653556,0.145895002416735));
#8419=CARTESIAN_POINT('Ctrl Pts',(6.98031707328297,-0.651293153351429,0.141287253539343));
#8420=CARTESIAN_POINT('Ctrl Pts',(6.958719665787,-0.710777483463359,0.137465130731298));
#8421=CARTESIAN_POINT('Ctrl Pts',(6.88373666759687,-0.890206795267031,0.12593270731537));
#8422=CARTESIAN_POINT('Ctrl Pts',(6.82132079467698,-1.00598840618957,0.1184670754301));
#8423=CARTESIAN_POINT('Ctrl Pts',(6.69848112489066,-1.18825888437743,0.105534450798882));
#8424=CARTESIAN_POINT('Ctrl Pts',(6.64414608460326,-1.2583250367509,0.100226027108668));
#8425=CARTESIAN_POINT('Ctrl Pts',(6.57495118299308,-1.33624247705346,0.0937587316688997));
#8426=CARTESIAN_POINT('Ctrl Pts',(6.56442533891264,-1.3478179786439,0.0927823067676446));
#8427=CARTESIAN_POINT('Ctrl Pts',(6.54691963810087,-1.36662017578259,0.0911696172275229));
#8428=CARTESIAN_POINT('Ctrl Pts',(6.5400192941925,-1.37392021599271,0.090536714667003));
#8429=CARTESIAN_POINT('Ctrl Pts',(6.5274988892059,-1.38696702449002,0.0893931256753902));
#8430=CARTESIAN_POINT('Ctrl Pts',(6.52189863819049,-1.39273256740069,0.0888832996976042));
#8431=CARTESIAN_POINT('Ctrl Pts',(6.50986696334501,-1.40497049004328,0.0877914700335683));
#8432=CARTESIAN_POINT('Ctrl Pts',(6.50342568827995,-1.41143288438844,0.0872090410970939));
#8433=CARTESIAN_POINT('Ctrl Pts',(6.48584351007915,-1.42883230850661,0.0856247152244667));
#8434=CARTESIAN_POINT('Ctrl Pts',(6.47461836137105,-1.43968292347054,0.084619091990734));
#8435=CARTESIAN_POINT('Ctrl Pts',(6.41403111114575,-1.49688823714525,0.0792210716612793));
#8436=CARTESIAN_POINT('Ctrl Pts',(6.36246518406953,-1.54083375273024,0.0747283949014611));
#8437=CARTESIAN_POINT('Ctrl Pts',(6.17799610270443,-1.68249594039927,0.0589868787249901));
#8438=CARTESIAN_POINT('Ctrl Pts',(6.03529593146887,-1.76630720326369,0.0472957275249053));
#8439=CARTESIAN_POINT('Ctrl Pts',(5.83481567995111,-1.85278816885954,0.0323285036762399));
#8440=CARTESIAN_POINT('Ctrl Pts',(5.78486989871763,-1.87199065581956,0.0287159183836105));
#8441=CARTESIAN_POINT('Ctrl Pts',(5.72548284609896,-1.89212143641683,0.0246008843656744));
#8442=CARTESIAN_POINT('Ctrl Pts',(5.71673693296706,-1.89501869608009,0.0239993795893232));
#8443=CARTESIAN_POINT('Ctrl Pts',(5.70250871307328,-1.89962293248718,0.0230284919898422));
#8444=CARTESIAN_POINT('Ctrl Pts',(5.69703867436649,-1.9013669792164,0.0226570640384776));
#8445=CARTESIAN_POINT('Ctrl Pts',(5.68726471019914,-1.90443684879979,0.0219967456655443));
#8446=CARTESIAN_POINT('Ctrl Pts',(5.68296375886098,-1.90577173509957,0.021707339220391));
#8447=CARTESIAN_POINT('Ctrl Pts',(5.67359479394345,-1.9086448325516,0.0210794467096769));
#8448=CARTESIAN_POINT('Ctrl Pts',(5.66852516676361,-1.9101774286243,0.0207412862329052));
#8449=CARTESIAN_POINT('Ctrl Pts',(5.65416079596607,-1.91445755050441,0.0197874939278794));
#8450=CARTESIAN_POINT('Ctrl Pts',(5.64485189624997,-1.91715759534056,0.019174534532152));
#8451=CARTESIAN_POINT('Ctrl Pts',(5.58457425549715,-1.93416579929945,0.0152364533001346));
#8452=CARTESIAN_POINT('Ctrl Pts',(5.53306792423637,-1.94650935721105,0.0120140479844558));
#8453=CARTESIAN_POINT('Ctrl Pts',(5.31603016415036,-1.98946678000028,-0.00120430811957895));
#8454=CARTESIAN_POINT('Ctrl Pts',(5.14745808018485,-2.00112036177713,-0.0106641100520869));
#8455=CARTESIAN_POINT('Ctrl Pts',(4.91461712540124,-1.98774345746366,-0.0245610189936562));
#8456=CARTESIAN_POINT('Ctrl Pts',(4.85004457780563,-1.98086068640027,-0.0284964312311433));
#8457=CARTESIAN_POINT('Ctrl Pts',(4.77024309358754,-1.96839348115497,-0.0335175945513442));
#8458=CARTESIAN_POINT('Ctrl Pts',(4.75458965566949,-1.965756199963,-0.034510044728272));
#8459=CARTESIAN_POINT('Ctrl Pts',(4.72984386099876,-1.96128267382114,-0.0360916198212695));
#8460=CARTESIAN_POINT('Ctrl Pts',(4.72072975818503,-1.95956931307585,-0.0366768596795332));
#8461=CARTESIAN_POINT('Ctrl Pts',(4.70375395364451,-1.95625530648223,-0.0377721625827098));
#8462=CARTESIAN_POINT('Ctrl Pts',(4.69588929178882,-1.95467065780994,-0.0382817083412731));
#8463=CARTESIAN_POINT('Ctrl Pts',(4.67840161737721,-1.95103715573355,-0.0394195147352495));
#8464=CARTESIAN_POINT('Ctrl Pts',(4.66878382354482,-1.9489644740296,-0.0400485224361274));
#8465=CARTESIAN_POINT('Ctrl Pts',(4.64066423237808,-1.94268652217119,-0.0418972659175536));
#8466=CARTESIAN_POINT('Ctrl Pts',(4.62220704824959,-1.93828841807665,-0.0431231107221309));
#8467=CARTESIAN_POINT('Ctrl Pts',(4.48263948960501,-1.90291983745407,-0.0524894446724259));
#8468=CARTESIAN_POINT('Ctrl Pts',(4.36463966305213,-1.86089488315989,-0.0609911000013024));
#8469=CARTESIAN_POINT('Ctrl Pts',(4.12747487632397,-1.75039191044516,-0.079152725547265));
#8470=CARTESIAN_POINT('Ctrl Pts',(4.00984097859791,-1.68008511467575,-0.0887996469414836));
#8471=CARTESIAN_POINT('Ctrl Pts',(3.88182034174079,-1.58448727905861,-0.0994816523230889));
#8472=CARTESIAN_POINT('Ctrl Pts',(3.86356404598011,-1.57035449673139,-0.101008952652158));
#8473=CARTESIAN_POINT('Ctrl Pts',(3.83952866578315,-1.55107142936336,-0.103020665602361));
#8474=CARTESIAN_POINT('Ctrl Pts',(3.83352906705225,-1.5462005087499,-0.103522898672078));
#8475=CARTESIAN_POINT('Ctrl Pts',(3.82417310226454,-1.53851400270541,-0.104306018192094));
#8476=CARTESIAN_POINT('Ctrl Pts',(3.82079752426466,-1.53572208107877,-0.104588546945842));
#8477=CARTESIAN_POINT('Ctrl Pts',(3.81392477006144,-1.52999943300144,-0.10516370018827));
#8478=CARTESIAN_POINT('Ctrl Pts',(3.81042844376182,-1.52706782046322,-0.105456241705951));
#8479=CARTESIAN_POINT('Ctrl Pts',(3.80217776756194,-1.52010141229719,-0.106146527497702));
#8480=CARTESIAN_POINT('Ctrl Pts',(3.79743217725701,-1.51605623507771,-0.106543522255797));
#8481=CARTESIAN_POINT('Ctrl Pts',(3.78168205223525,-1.50250267717501,-0.107861274034392));
#8482=CARTESIAN_POINT('Ctrl Pts',(3.77076224015238,-1.49289595271181,-0.108775166391714));
#8483=CARTESIAN_POINT('Ctrl Pts',(3.71001425204032,-1.43826266685922,-0.11386729567284));
#8484=CARTESIAN_POINT('Ctrl Pts',(3.66237473750464,-1.39085710770181,-0.117892114403733));
#8485=CARTESIAN_POINT('Ctrl Pts',(3.50442823448687,-1.21695500812358,-0.13173793511042));
#8486=CARTESIAN_POINT('Ctrl Pts',(3.40776079220736,-1.07905057996273,-0.141215259364283));
#8487=CARTESIAN_POINT('Ctrl Pts',(3.3076738741116,-0.889309216331047,-0.154158667736021));
#8488=CARTESIAN_POINT('Ctrl Pts',(3.28731837813025,-0.847195339820908,-0.15702113546422));
#8489=CARTESIAN_POINT('Ctrl Pts',(3.26264628460628,-0.791209327991986,-0.160833108224414));
#8490=CARTESIAN_POINT('Ctrl Pts',(3.25697351173675,-0.777948749480136,-0.161736423544074));
#8491=CARTESIAN_POINT('Ctrl Pts',(3.24804760690145,-0.756441657777049,-0.163202714999555));
#8492=CARTESIAN_POINT('Ctrl Pts',(3.24470470826121,-0.748232781071678,-0.163762655686476));
#8493=CARTESIAN_POINT('Ctrl Pts',(3.23841614017006,-0.732490919022245,-0.164837098741973));
#8494=CARTESIAN_POINT('Ctrl Pts',(3.23546135586276,-0.724961746472034,-0.165351282759005));
#8495=CARTESIAN_POINT('Ctrl Pts',(3.22877622929245,-0.70761772870826,-0.166536507299769));
#8496=CARTESIAN_POINT('Ctrl Pts',(3.22507745338121,-0.697791051256904,-0.167208583873025));
#8497=CARTESIAN_POINT('Ctrl Pts',(3.21375240750098,-0.666967412995959,-0.169318703382814));
#8498=CARTESIAN_POINT('Ctrl Pts',(3.20640137475594,-0.645871847374074,-0.170765763156876));
#8499=CARTESIAN_POINT('Ctrl Pts',(3.17178107201273,-0.540877717004986,-0.17798482425887));
#8500=CARTESIAN_POINT('Ctrl Pts',(3.14974749998642,-0.455368485299618,-0.183923610536241));
#8501=CARTESIAN_POINT('Ctrl Pts',(3.11346522651393,-0.262450980989509,-0.197411632423579));
#8502=CARTESIAN_POINT('Ctrl Pts',(3.10215444585066,-0.15476398699513,-0.205004033418503));
#8503=CARTESIAN_POINT('Ctrl Pts',(3.09781469267797,0.0305591832669149,-0.217847915183087));
#8504=CARTESIAN_POINT('Ctrl Pts',(3.1004964726237,0.107866218868336,-0.223135399237172));
#8505=CARTESIAN_POINT('Ctrl Pts',(3.10866033654096,0.195594300054974,-0.228924947609783));
#8506=CARTESIAN_POINT('Ctrl Pts',(3.10974953183513,0.206350248483781,-0.229631102878834));
#8507=CARTESIAN_POINT('Ctrl Pts',(3.11153585827572,0.222666028907593,-0.230696156430305));
#8508=CARTESIAN_POINT('Ctrl Pts',(3.11216903756611,0.228232453777321,-0.231058435535144));
#8509=CARTESIAN_POINT('Ctrl Pts',(3.11335259633733,0.238260980750037,-0.231709078251876));
#8510=CARTESIAN_POINT('Ctrl Pts',(3.11389461380411,0.242723929417162,-0.231997893765927));
#8511=CARTESIAN_POINT('Ctrl Pts',(3.11512197098991,0.252552192257652,-0.232632296430501));
#8512=CARTESIAN_POINT('Ctrl Pts',(3.11581404464018,0.257916560050992,-0.232977504315233));
#8513=CARTESIAN_POINT('Ctrl Pts',(3.11787704316272,0.273410309871004,-0.233971678132952));
#8514=CARTESIAN_POINT('Ctrl Pts',(3.11930404141261,0.283532231647796,-0.234617601285223));
#8515=CARTESIAN_POINT('Ctrl Pts',(3.13066109229315,0.359841459175427,-0.239463345375374));
#8516=CARTESIAN_POINT('Ctrl Pts',(3.14383990919655,0.425509820343862,-0.24349815008954));
#8517=CARTESIAN_POINT('Ctrl Pts',(3.19691375458047,0.634768200016442,-0.256270576132744));
#8518=CARTESIAN_POINT('Ctrl Pts',(3.24958366131185,0.774583600701349,-0.264706931228053));
#8519=CARTESIAN_POINT('Ctrl Pts',(3.34862979051256,0.968529986462011,-0.277652424679086));
#8520=CARTESIAN_POINT('Ctrl Pts',(3.38307949114601,1.02815616797849,-0.28181718267952));
#8521=CARTESIAN_POINT('Ctrl Pts',(3.4293263517402,1.09942040651705,-0.287096665412004));
#8522=CARTESIAN_POINT('Ctrl Pts',(3.43827788540632,1.11285432394628,-0.288105668525936));
#8523=CARTESIAN_POINT('Ctrl Pts',(3.45266161187775,1.13388287109671,-0.289707757397677));
#8524=CARTESIAN_POINT('Ctrl Pts',(3.45798589262008,1.14155072810215,-0.290296784141614));
#8525=CARTESIAN_POINT('Ctrl Pts',(3.46798341343878,1.15573525997183,-0.291395593532152));
#8526=CARTESIAN_POINT('Ctrl Pts',(3.47264252424855,1.16226169732652,-0.291904830710072));
#8527=CARTESIAN_POINT('Ctrl Pts',(3.48306080503986,1.17667099585416,-0.293037399693551));
#8528=CARTESIAN_POINT('Ctrl Pts',(3.48883871927485,1.1845399876176,-0.293661445191679));
#8529=CARTESIAN_POINT('Ctrl Pts',(3.50579451151298,1.20728040810507,-0.295481250446377));
#8530=CARTESIAN_POINT('Ctrl Pts',(3.51712271804736,1.22203794553453,-0.296682831735835));
#8531=CARTESIAN_POINT('Ctrl Pts',(3.6204989940738,1.35287824933403,-0.307525801938078));
#8532=CARTESIAN_POINT('Ctrl Pts',(3.724988658736,1.45850619327345,-0.3176892073628));
#8533=CARTESIAN_POINT('Ctrl Pts',(3.93639982503237,1.6293225136517,-0.33662610749281));
#8534=CARTESIAN_POINT('Ctrl Pts',(4.039650773892,1.69795386080959,-0.34529703567476));
#8535=CARTESIAN_POINT('Ctrl Pts',(4.16259178078155,1.76410901412941,-0.354546599378821));
#8536=CARTESIAN_POINT('Ctrl Pts',(4.17667124427512,1.77146973137946,-0.355590703907002));
#8537=CARTESIAN_POINT('Ctrl Pts',(4.19618130207751,1.78137458119246,-0.357015238490354));
#8538=CARTESIAN_POINT('Ctrl Pts',(4.20153722570376,1.78406338454955,-0.357404014117713));
#8539=CARTESIAN_POINT('Ctrl Pts',(4.2107332661,1.78862824796189,-0.358067519356253));
#8540=CARTESIAN_POINT('Ctrl Pts',(4.21456740515156,1.79051615998201,-0.358342967401517));
#8541=CARTESIAN_POINT('Ctrl Pts',(4.22256765028322,1.79442354842247,-0.358915191732509));
#8542=CARTESIAN_POINT('Ctrl Pts',(4.22673475147267,1.79644085901353,-0.359211823722823));
#8543=CARTESIAN_POINT('Ctrl Pts',(4.23687644678574,1.80130698550387,-0.359930384937204));
#8544=CARTESIAN_POINT('Ctrl Pts',(4.24285833945941,1.80414064038547,-0.360351388247232));
#8545=CARTESIAN_POINT('Ctrl Pts',(4.26415070771659,1.81409748879608,-0.361840309495893));
#8546=CARTESIAN_POINT('Ctrl Pts',(4.27953789704593,1.8210562195592,-0.362898694307669));
#8547=CARTESIAN_POINT('Ctrl Pts',(4.31787080086471,1.83780891640602,-0.365496494217798));
#8548=CARTESIAN_POINT('Ctrl Pts',(4.34091587791336,1.84736964397415,-0.3670242046751));
#8549=CARTESIAN_POINT('Ctrl Pts',(4.43877987365078,1.88583488331559,-0.373393810163138));
#8550=CARTESIAN_POINT('Ctrl Pts',(4.51513196957062,1.91064753556587,-0.378078054703925));
#8551=CARTESIAN_POINT('Ctrl Pts',(4.74474081461945,1.9702321680669,-0.391866676259247));
#8552=CARTESIAN_POINT('Ctrl Pts',(4.90081118493827,1.99158602882379,-0.400906347312344));
#8553=CARTESIAN_POINT('Ctrl Pts',(5.08197402114595,1.99486173466594,-0.412065013907606));
#8554=CARTESIAN_POINT('Ctrl Pts',(5.10618827807214,1.99485863187619,-0.413568766245585));
#8555=CARTESIAN_POINT('Ctrl Pts',(5.1411195981775,1.99421814958416,-0.415758332265714));
#8556=CARTESIAN_POINT('Ctrl Pts',(5.15184156994278,1.99393503500094,-0.416433157918545));
#8557=CARTESIAN_POINT('Ctrl Pts',(5.17070500818579,1.9932846683157,-0.417625457157231));
#8558=CARTESIAN_POINT('Ctrl Pts',(5.17884754672173,1.99295396410719,-0.418141782162685));
#8559=CARTESIAN_POINT('Ctrl Pts',(5.19566232732439,1.99216780752531,-0.419211550951107));
#8560=CARTESIAN_POINT('Ctrl Pts',(5.20433406563859,1.99170559934392,-0.419765194565772));
#8561=CARTESIAN_POINT('Ctrl Pts',(5.22658096692162,1.9903740919839,-0.421190652674178));
#8562=CARTESIAN_POINT('Ctrl Pts',(5.24015058068346,1.9894225394784,-0.422065011721406));
#8563=CARTESIAN_POINT('Ctrl Pts',(5.29756005070113,1.9848062389891,-0.425785593836174));
#8564=CARTESIAN_POINT('Ctrl Pts',(5.34127920689039,1.97983077014022,-0.428672223842259));
#8565=CARTESIAN_POINT('Ctrl Pts',(5.54159408987943,1.95029552357698,-0.44215361767715));
#8566=CARTESIAN_POINT('Ctrl Pts',(5.69506043980011,1.90857317245293,-0.45326750700625));
#8567=CARTESIAN_POINT('Ctrl Pts',(5.92177897452171,1.81684907451172,-0.470255489441496));
#8568=CARTESIAN_POINT('Ctrl Pts',(5.9994501193327,1.77940868906003,-0.476173968018696));
#8569=CARTESIAN_POINT('Ctrl Pts',(6.08396940890362,1.73169425757625,-0.482552846946853));
#8570=CARTESIAN_POINT('Ctrl Pts',(6.09342978908017,1.72625063981266,-0.483265881719269));
#8571=CARTESIAN_POINT('Ctrl Pts',(6.10769714252797,1.71788441028284,-0.484339206088336));
#8572=CARTESIAN_POINT('Ctrl Pts',(6.1125370389865,1.71501876749111,-0.48470295366314));
#8573=CARTESIAN_POINT('Ctrl Pts',(6.12115311422296,1.70986795307525,-0.485349779423056));
#8574=CARTESIAN_POINT('Ctrl Pts',(6.12493387149097,1.70759069562882,-0.485633351656116));
#8575=CARTESIAN_POINT('Ctrl Pts',(6.13318026817938,1.70258628182991,-0.4862512995475));
#8576=CARTESIAN_POINT('Ctrl Pts',(6.1376427408819,1.69985410113087,-0.48658534388251));
#8577=CARTESIAN_POINT('Ctrl Pts',(6.14692190644068,1.69412254670215,-0.487279322380664));
#8578=CARTESIAN_POINT('Ctrl Pts',(6.15173666423004,1.69112011130864,-0.487639058884533));
#8579=CARTESIAN_POINT('Ctrl Pts',(6.16410249493643,1.68333542300669,-0.488562240127163));
#8580=CARTESIAN_POINT('Ctrl Pts',(6.1716344459629,1.67852283269386,-0.48912383253046));
#8581=CARTESIAN_POINT('Ctrl Pts',(6.19369522189635,1.66421723021552,-0.490767401613386));
#8582=CARTESIAN_POINT('Ctrl Pts',(6.20813316916562,1.65458481313967,-0.491841368111471));
#8583=CARTESIAN_POINT('Ctrl Pts',(6.25964969823477,1.61923482003678,-0.495674339848237));
#8584=CARTESIAN_POINT('Ctrl Pts',(6.29598087199812,1.59244798352437,-0.498379345324519));
#8585=CARTESIAN_POINT('Ctrl Pts',(6.44726128406627,1.47277868799808,-0.50979376172227));
#8586=CARTESIAN_POINT('Ctrl Pts',(6.55260429089217,1.36851489123446,-0.518165350263008));
#8587=CARTESIAN_POINT('Ctrl Pts',(6.68957658443352,1.1989735512608,-0.531111383008197));
#8588=CARTESIAN_POINT('Ctrl Pts',(6.73076826020462,1.1420928403117,-0.53535578063878));
#8589=CARTESIAN_POINT('Ctrl Pts',(6.77769092777207,1.06952979588961,-0.540725176889794));
#8590=CARTESIAN_POINT('Ctrl Pts',(6.78634048741768,1.05578870271875,-0.54173994028905));
#8591=CARTESIAN_POINT('Ctrl Pts',(6.79970839947311,1.03396532154878,-0.543349165718451));
#8592=CARTESIAN_POINT('Ctrl Pts',(6.80453939015688,1.02595260616638,-0.54393950741807));
#8593=CARTESIAN_POINT('Ctrl Pts',(6.81336600280249,1.01107703689446,-0.545034690982643));
#8594=CARTESIAN_POINT('Ctrl Pts',(6.81737737476225,1.00422371044698,-0.545538949189676));
#8595=CARTESIAN_POINT('Ctrl Pts',(6.82619894064773,0.988943731945201,-0.546662649974919));
#8596=CARTESIAN_POINT('Ctrl Pts',(6.83098876288862,0.980505610014253,-0.547282808412147));
#8597=CARTESIAN_POINT('Ctrl Pts',(6.84464223173192,0.956038502928189,-0.54908009376178));
#8598=CARTESIAN_POINT('Ctrl Pts',(6.85334672117221,0.93992229001771,-0.550262823121048));
#8599=CARTESIAN_POINT('Ctrl Pts',(6.92753536883622,0.797920395550181,-0.560677162917791));
#8600=CARTESIAN_POINT('Ctrl Pts',(6.9796230408858,0.665523982844454,-0.570384737091377));
#8601=CARTESIAN_POINT('Ctrl Pts',(7.04888150915202,0.413587693016349,-0.58857494240901));
#8602=CARTESIAN_POINT('Ctrl Pts',(7.07013529736856,0.295807504302604,-0.596960125366271));
#8603=CARTESIAN_POINT('Ctrl Pts',(7.08287314345197,0.152680432198282,-0.606579315606909));
#8604=CARTESIAN_POINT('Ctrl Pts',(7.08458189315883,0.128494970074411,-0.608184763692582));
#8605=CARTESIAN_POINT('Ctrl Pts',(7.08626098919135,0.0964207779197302,-0.610282291731446));
#8606=CARTESIAN_POINT('Ctrl Pts',(7.08662604221146,0.0885559153652952,-0.610794110692069));
#8607=CARTESIAN_POINT('Ctrl Pts',(7.08714258508254,0.0757966629662215,-0.611620144125036));
#8608=CARTESIAN_POINT('Ctrl Pts',(7.08732263219669,0.070903607618745,-0.611935896173381));
#8609=CARTESIAN_POINT('Ctrl Pts',(7.08762640562701,0.0617289170494633,-0.612525962807788));
#8610=CARTESIAN_POINT('Ctrl Pts',(7.08775435910392,0.0574475070171664,-0.612800505435861));
#8611=CARTESIAN_POINT('Ctrl Pts',(7.08798983537845,0.0486156934111297,-0.613365214198298));
#8612=CARTESIAN_POINT('Ctrl Pts',(7.08809557641243,0.0440652447741042,-0.613655282533092));
#8613=CARTESIAN_POINT('Ctrl Pts',(7.08831313837811,0.0330845301316651,-0.614353189587575));
#8614=CARTESIAN_POINT('Ctrl Pts',(7.08840944037348,0.0266539590409399,-0.61476019777572));
#8615=CARTESIAN_POINT('Ctrl Pts',(7.08854128019806,0.013650208383668,-0.615579999299495));
#8616=CARTESIAN_POINT('Ctrl Pts',(7.08857543143116,0.00707710677119785,
-0.615992716324821));
#8617=CARTESIAN_POINT('Ctrl Pts',(7.08857709181507,0.000503868992114988,
-0.616403874612628));
#8618=CARTESIAN_POINT('Ctrl Pts',(7.08857666516212,0.0013985762946109,-0.772682587389958));
#8619=CARTESIAN_POINT('Ctrl Pts',(7.08852067831295,0.0812510236518176,-0.767603483263897));
#8620=CARTESIAN_POINT('Ctrl Pts',(7.08366576807236,0.160913471443935,-0.762524379137835));
#8621=CARTESIAN_POINT('Ctrl Pts',(7.07410411760675,0.239855614200625,-0.757445275011775));
#8622=CARTESIAN_POINT('Ctrl Pts',(7.06445696132819,0.319503703291223,-0.752320750596727));
#8623=CARTESIAN_POINT('Ctrl Pts',(7.05001861828069,0.398418352407743,-0.747196226181679));
#8624=CARTESIAN_POINT('Ctrl Pts',(7.0309335007,0.476074122069483,-0.742071701766631));
#8625=CARTESIAN_POINT('Ctrl Pts',(7.01328532357908,0.547883099491694,-0.737333008690473));
#8626=CARTESIAN_POINT('Ctrl Pts',(6.99166436661312,0.618615733605399,-0.732594315614317));
#8627=CARTESIAN_POINT('Ctrl Pts',(6.96622088098845,0.687873025402144,-0.72785562253816));
#8628=CARTESIAN_POINT('Ctrl Pts',(6.94229794684064,0.752991368672771,-0.723400122844453));
#8629=CARTESIAN_POINT('Ctrl Pts',(6.91492693121006,0.816988152165582,-0.718944623150746));
#8630=CARTESIAN_POINT('Ctrl Pts',(6.88423339278693,0.879473176291434,-0.71448912345704));
#8631=CARTESIAN_POINT('Ctrl Pts',(6.85358575018637,0.941864767019658,-0.7100402860393));
#8632=CARTESIAN_POINT('Ctrl Pts',(6.81962565955996,1.00274864955535,-0.705591448621559));
#8633=CARTESIAN_POINT('Ctrl Pts',(6.78252741640302,1.06175279192838,-0.701142611203819));
#8634=CARTESIAN_POINT('Ctrl Pts',(6.74547259460109,1.12068787335419,-0.696698980893814));
#8635=CARTESIAN_POINT('Ctrl Pts',(6.70528717467093,1.17774717229729,-0.692255350583809));
#8636=CARTESIAN_POINT('Ctrl Pts',(6.66219137591145,1.23258315520135,-0.687811720273803));
#8637=CARTESIAN_POINT('Ctrl Pts',(6.61912252451289,1.28738484972775,-0.683370868520251));
#8638=CARTESIAN_POINT('Ctrl Pts',(6.57314720612321,1.33996560245424,-0.6789300167667));
#8639=CARTESIAN_POINT('Ctrl Pts',(6.52452809064639,1.39000805628495,-0.674489165013148));
#8640=CARTESIAN_POINT('Ctrl Pts',(6.47592288711615,1.44003619089291,-0.670049583971574));
#8641=CARTESIAN_POINT('Ctrl Pts',(6.42467572905522,1.48752711785398,-0.665610002930001));
#8642=CARTESIAN_POINT('Ctrl Pts',(6.37108738870107,1.53219902723614,-0.661170421888427));
#8643=CARTESIAN_POINT('Ctrl Pts',(6.31749620837785,1.57687330405195,-0.656730605566701));
#8644=CARTESIAN_POINT('Ctrl Pts',(6.26156397672323,1.61872795532988,-0.652290789244975));
#8645=CARTESIAN_POINT('Ctrl Pts',(6.20362452957619,1.65752144809336,-0.64785097292325));
#8646=CARTESIAN_POINT('Ctrl Pts',(6.14562392296001,1.69635589032289,-0.643406470039558));
#8647=CARTESIAN_POINT('Ctrl Pts',(6.08561227932795,1.73212245212697,-0.638961967155866));
#8648=CARTESIAN_POINT('Ctrl Pts',(6.02395159099266,1.76462350004533,-0.634517464272174));
#8649=CARTESIAN_POINT('Ctrl Pts',(5.96225473111489,1.79714361380722,-0.630070354143426));
#8650=CARTESIAN_POINT('Ctrl Pts',(5.89890734530683,1.82639419570988,-0.625623244014679));
#8651=CARTESIAN_POINT('Ctrl Pts',(5.8342926167455,1.85222527332208,-0.621176133885931));
#8652=CARTESIAN_POINT('Ctrl Pts',(5.76956633062213,1.87810094838299,-0.616721345805497));
#8653=CARTESIAN_POINT('Ctrl Pts',(5.70356879718913,1.90054517729538,-0.612266557725061));
#8654=CARTESIAN_POINT('Ctrl Pts',(5.63669881869021,1.91945771502114,-0.607811769644627));
#8655=CARTESIAN_POINT('Ctrl Pts',(5.60275727216669,1.9290572512182,-0.605550629439731));
#8656=CARTESIAN_POINT('Ctrl Pts',(5.56859112792846,1.93774772530178,-0.603289489234835));
#8657=CARTESIAN_POINT('Ctrl Pts',(5.5342532709229,1.94552111253314,-0.601028349029939));
#8658=CARTESIAN_POINT('Ctrl Pts',(5.46659169423707,1.96083830708545,-0.596572849336225));
#8659=CARTESIAN_POINT('Ctrl Pts',(5.39799719595367,1.97265167236967,-0.592117349642511));
#8660=CARTESIAN_POINT('Ctrl Pts',(5.32886554407487,1.98085449197413,-0.587661849948798));
#8661=CARTESIAN_POINT('Ctrl Pts',(5.25983726424732,1.98904504596269,-0.583213012531049));
#8662=CARTESIAN_POINT('Ctrl Pts',(5.19027390689186,1.99363571273677,-0.5787641751133));
#8663=CARTESIAN_POINT('Ctrl Pts',(5.12058248328074,1.99457055902589,-0.574315337695551));
#8664=CARTESIAN_POINT('Ctrl Pts',(5.0509726294635,1.99550431113131,-0.56987170738554));
#8665=CARTESIAN_POINT('Ctrl Pts',(4.98123549391188,1.99279073491001,-0.565428077075528));
#8666=CARTESIAN_POINT('Ctrl Pts',(4.91178248827855,1.98642576041827,-0.560984446765517));
#8667=CARTESIAN_POINT('Ctrl Pts',(4.84237291089729,1.9800647658798,-0.556543595011961));
#8668=CARTESIAN_POINT('Ctrl Pts',(4.77324759700005,1.9700569470899,-0.552102743258405));
#8669=CARTESIAN_POINT('Ctrl Pts',(4.70481570474851,1.95645026865512,-0.54766189150485));
#8670=CARTESIAN_POINT('Ctrl Pts',(4.63640339370116,1.9428474836557,-0.54322231046327));
#8671=CARTESIAN_POINT('Ctrl Pts',(4.56868458993034,1.92564797875571,-0.538782729421691));
#8672=CARTESIAN_POINT('Ctrl Pts',(4.50205932653326,1.90495102277079,-0.534343148380112));
#8673=CARTESIAN_POINT('Ctrl Pts',(4.43543053226201,1.88425296992947,-0.529903332058381));
#8674=CARTESIAN_POINT('Ctrl Pts',(4.36989585984738,1.86005724545217,-0.52546351573665));
#8675=CARTESIAN_POINT('Ctrl Pts',(4.30583950838136,1.83251276409261,-0.521023699414919));
#8676=CARTESIAN_POINT('Ctrl Pts',(4.24171554059099,1.80493920744944,-0.516579196531222));
#8677=CARTESIAN_POINT('Ctrl Pts',(4.17907345852527,1.77401003240079,-0.512134693647524));
#8678=CARTESIAN_POINT('Ctrl Pts',(4.11827591922954,1.7399216499609,-0.507690190763827));
#8679=CARTESIAN_POINT('Ctrl Pts',(4.0574427147339,1.70581327051146,-0.503243080635074));
#8680=CARTESIAN_POINT('Ctrl Pts',(3.99845662035562,1.66854225629977,-0.49879597050632));
#8681=CARTESIAN_POINT('Ctrl Pts',(3.94165180747088,1.62834871265402,-0.494348860377566));
#8682=CARTESIAN_POINT('Ctrl Pts',(3.88474892087168,1.58808577471012,-0.489894072297126));
#8683=CARTESIAN_POINT('Ctrl Pts',(3.83003521680561,1.54489053865226,-0.485439284216686));
#8684=CARTESIAN_POINT('Ctrl Pts',(3.77781161784099,1.49904325063137,-0.480984496136245));
#8685=CARTESIAN_POINT('Ctrl Pts',(3.75130421117469,1.4757723016311,-0.478723355931404));
#8686=CARTESIAN_POINT('Ctrl Pts',(3.72543774509184,1.45181868636682,-0.476462215726563));
#8687=CARTESIAN_POINT('Ctrl Pts',(3.70024770244909,1.42722243209145,-0.474201075521722));
#8688=CARTESIAN_POINT('Ctrl Pts',(3.65061158212398,1.37875635150263,-0.469745575828008));
#8689=CARTESIAN_POINT('Ctrl Pts',(3.60340930693106,1.32760260275726,-0.465290076134292));
#8690=CARTESIAN_POINT('Ctrl Pts',(3.5589455818756,1.27403536748092,-0.460834576440577));
#8691=CARTESIAN_POINT('Ctrl Pts',(3.51454834310164,1.22054823089803,-0.456385739022829));
#8692=CARTESIAN_POINT('Ctrl Pts',(3.4728818367189,1.16465514408179,-0.451936901605084));
#8693=CARTESIAN_POINT('Ctrl Pts',(3.43421425417683,1.10666733050964,-0.447488064187336));
#8694=CARTESIAN_POINT('Ctrl Pts',(3.39559192981105,1.04874738833044,-0.443044433877322));
#8695=CARTESIAN_POINT('Ctrl Pts',(3.35996182778489,0.988737994062009,-0.438600803567306));
#8696=CARTESIAN_POINT('Ctrl Pts',(3.32755099966797,0.926982256574998,-0.434157173257293));
#8697=CARTESIAN_POINT('Ctrl Pts',(3.29516043770945,0.86526513431723,-0.429716321503735));
#8698=CARTESIAN_POINT('Ctrl Pts',(3.26598538302946,0.801804267298664,-0.425275469750176));
#8699=CARTESIAN_POINT('Ctrl Pts',(3.24020798668413,0.736969157883973,-0.420834617996618));
#8700=CARTESIAN_POINT('Ctrl Pts',(3.21443796632163,0.672152600484658,-0.416395036955037));
#8701=CARTESIAN_POINT('Ctrl Pts',(3.19206385483186,0.605963035687771,-0.411955455913459));
#8702=CARTESIAN_POINT('Ctrl Pts',(3.17321978051959,0.538790194649985,-0.407515874871877));
#8703=CARTESIAN_POINT('Ctrl Pts',(3.15437470754627,0.471613793718569,-0.403076058550144));
#8704=CARTESIAN_POINT('Ctrl Pts',(3.13906017295436,0.403454484730628,-0.398636242228407));
#8705=CARTESIAN_POINT('Ctrl Pts',(3.12736002732783,0.334715695034933,-0.394196425906673));
#8706=CARTESIAN_POINT('Ctrl Pts',(3.11564753131257,0.26590434634716,-0.389751923022975));
#8707=CARTESIAN_POINT('Ctrl Pts',(3.10755712127305,0.196512779279445,-0.385307420139277));
#8708=CARTESIAN_POINT('Ctrl Pts',(3.10312107163794,0.126952157765381,-0.380862917255578));
#8709=CARTESIAN_POINT('Ctrl Pts',(3.09868241971665,0.0573507304308743,-0.376415807126822));
#8710=CARTESIAN_POINT('Ctrl Pts',(3.09790240054779,-0.0124194594819549,
-0.371968696998067));
#8711=CARTESIAN_POINT('Ctrl Pts',(3.10076112917571,-0.0819474062969565,
-0.36752158686931));
#8712=CARTESIAN_POINT('Ctrl Pts',(3.10362479340891,-0.151595393363038,-0.363066798788869));
#8713=CARTESIAN_POINT('Ctrl Pts',(3.1101396997005,-0.220999815604975,-0.358612010708428));
#8714=CARTESIAN_POINT('Ctrl Pts',(3.12023419720762,-0.289755755186719,-0.354157222627986));
#8715=CARTESIAN_POINT('Ctrl Pts',(3.12535791437412,-0.32465456889044,-0.35189608242316));
#8716=CARTESIAN_POINT('Ctrl Pts',(3.13140303511768,-0.35938648889242,-0.349634942218332));
#8717=CARTESIAN_POINT('Ctrl Pts',(3.13835525008304,-0.393899974369568,-0.347373802013506));
#8718=CARTESIAN_POINT('Ctrl Pts',(3.15205435267856,-0.461907620973757,-0.342918302319794));
#8719=CARTESIAN_POINT('Ctrl Pts',(3.16933235935426,-0.529333367387134,-0.338462802626082));
#8720=CARTESIAN_POINT('Ctrl Pts',(3.19012476562827,-0.595772417517969,-0.33400730293237));
#8721=CARTESIAN_POINT('Ctrl Pts',(3.21088608116992,-0.66211212182518,-0.329558465514623));
#8722=CARTESIAN_POINT('Ctrl Pts',(3.23515122109042,-0.727467595143257,-0.325109628096875));
#8723=CARTESIAN_POINT('Ctrl Pts',(3.26280474150934,-0.791444554050085,-0.320660790679127));
#8724=CARTESIAN_POINT('Ctrl Pts',(3.29042589507674,-0.855346631614569,-0.316217160369116));
#8725=CARTESIAN_POINT('Ctrl Pts',(3.32142735900801,-0.917872952512026,-0.311773530059105));
#8726=CARTESIAN_POINT('Ctrl Pts',(3.35564456335289,-0.978646432078394,-0.307329899749094));
#8727=CARTESIAN_POINT('Ctrl Pts',(3.38984037203086,-1.03938191061133,-0.302889047995538));
#8728=CARTESIAN_POINT('Ctrl Pts',(3.4272476926212,-1.09836629688919,-0.298448196241982));
#8729=CARTESIAN_POINT('Ctrl Pts',(3.46765539455952,-1.15524584681022,-0.294007344488427));
#8730=CARTESIAN_POINT('Ctrl Pts',(3.50805153417745,-1.21210912113159,-0.289567763446847));
#8731=CARTESIAN_POINT('Ctrl Pts',(3.55144606756506,-1.2668683561977,-0.285128182405269));
#8732=CARTESIAN_POINT('Ctrl Pts',(3.5975847807408,-1.31919912015406,-0.280688601363689));
#8733=CARTESIAN_POINT('Ctrl Pts',(3.64372593908497,-1.37153265743295,-0.276248785041958));
#8734=CARTESIAN_POINT('Ctrl Pts',(3.69261124062395,-1.42143710277521,-0.271808968720226));
#8735=CARTESIAN_POINT('Ctrl Pts',(3.74394764538402,-1.46862278029303,-0.267369152398495));
#8736=CARTESIAN_POINT('Ctrl Pts',(3.79533823960252,-1.5158582658627,-0.262924649514798));
#8737=CARTESIAN_POINT('Ctrl Pts',(3.84918474015865,-1.56036892405346,-0.258480146631104));
#8738=CARTESIAN_POINT('Ctrl Pts',(3.90515957752016,-1.60190416432164,-0.254035643747407));
#8739=CARTESIAN_POINT('Ctrl Pts',(3.96116725097647,-1.64346377009316,-0.249588533618655));
#8740=CARTESIAN_POINT('Ctrl Pts',(4.01930533862264,-1.68204421326344,-0.245141423489901));
#8741=CARTESIAN_POINT('Ctrl Pts',(4.07921805092624,-1.71743876965416,-0.240694313361148));
#8742=CARTESIAN_POINT('Ctrl Pts',(4.13923420274386,-1.75289443487422,-0.236239525280709));
#8743=CARTESIAN_POINT('Ctrl Pts',(4.20103066145826,-1.785153007705,-0.23178473720027));
#8744=CARTESIAN_POINT('Ctrl Pts',(4.26422860847048,-1.81405452325566,-0.227329949119831));
#8745=CARTESIAN_POINT('Ctrl Pts',(4.29630632266763,-1.82872421743922,-0.225068808914983));
#8746=CARTESIAN_POINT('Ctrl Pts',(4.32874481068465,-1.84252980496825,-0.222807668710136));
#8747=CARTESIAN_POINT('Ctrl Pts',(4.36149303308618,-1.85545527990223,-0.220546528505288));
#8748=CARTESIAN_POINT('Ctrl Pts',(4.42602228897526,-1.88092448764353,-0.216091028811574));
#8749=CARTESIAN_POINT('Ctrl Pts',(4.4920085461044,-1.90307340780185,-0.21163552911786));
#8750=CARTESIAN_POINT('Ctrl Pts',(4.55907697268545,-1.92173614331675,-0.207180029424146));
#8751=CARTESIAN_POINT('Ctrl Pts',(4.62604511234083,-1.94037097258032,-0.2027311920064));
#8752=CARTESIAN_POINT('Ctrl Pts',(4.69409174222398,-1.95552983366991,-0.198282354588654));
#8753=CARTESIAN_POINT('Ctrl Pts',(4.76282316475469,-1.96709530034559,-0.193833517170908));
#8754=CARTESIAN_POINT('Ctrl Pts',(4.8314741411175,-1.97864723030925,-0.189389886860896));
#8755=CARTESIAN_POINT('Ctrl Pts',(4.90080783809015,-1.98661403863874,-0.184946256550884));
#8756=CARTESIAN_POINT('Ctrl Pts',(4.97041829000542,-1.99092888231321,-0.180502626240873));
#8757=CARTESIAN_POINT('Ctrl Pts',(5.0399852152191,-1.99524102796018,-0.176061774487317));
#8758=CARTESIAN_POINT('Ctrl Pts',(5.10982806494276,-1.99590570893784,-0.171620922733762));
#8759=CARTESIAN_POINT('Ctrl Pts',(5.17953515512022,-1.99290785067776,-0.167180070980206));
#8760=CARTESIAN_POINT('Ctrl Pts',(5.24922229920643,-1.98991085022934,-0.162740489938626));
#8761=CARTESIAN_POINT('Ctrl Pts',(5.31877327238994,-1.9832534121198,-0.158300908897045));
#8762=CARTESIAN_POINT('Ctrl Pts',(5.38777757473776,-1.9729725577165,-0.153861327855465));
#8763=CARTESIAN_POINT('Ctrl Pts',(5.45678553403936,-1.96269115846878,-0.149421511533734));
#8764=CARTESIAN_POINT('Ctrl Pts',(5.5252462815185,-1.94878603617264,-0.144981695212005));
#8765=CARTESIAN_POINT('Ctrl Pts',(5.592757384843,-1.93134569373299,-0.140541878890275));
#8766=CARTESIAN_POINT('Ctrl Pts',(5.66033975124378,-1.91388694169265,-0.136097376006578));
#8767=CARTESIAN_POINT('Ctrl Pts',(5.72696999824245,-1.89288564412286,-0.131652873122878));
#8768=CARTESIAN_POINT('Ctrl Pts',(5.79225973045888,-1.8684805325908,-0.127208370239181));
#8769=CARTESIAN_POINT('Ctrl Pts',(5.85758776309628,-1.84406110447306,-0.122761260110429));
#8770=CARTESIAN_POINT('Ctrl Pts',(5.92157326705565,-1.81623408319097,-0.118314149981678));
#8771=CARTESIAN_POINT('Ctrl Pts',(5.98384932664628,-1.78518573187346,-0.113867039852925));
#8772=CARTESIAN_POINT('Ctrl Pts',(6.04623290607856,-1.75408377546535,-0.109412251772485));
#8773=CARTESIAN_POINT('Ctrl Pts',(6.10690072439177,-1.71974962844176,-0.104957463692044));
#8774=CARTESIAN_POINT('Ctrl Pts',(6.16551259547016,-1.682414300984,-0.100502675611604));
#8775=CARTESIAN_POINT('Ctrl Pts',(6.19526253099646,-1.66346381255416,-0.0982415354067602));
#8776=CARTESIAN_POINT('Ctrl Pts',(6.22448328231698,-1.6437407944253,-0.0959803952019159));
#8777=CARTESIAN_POINT('Ctrl Pts',(6.25313367068295,-1.62327938637982,-0.0937192549970725));
#8778=CARTESIAN_POINT('Ctrl Pts',(6.30919037597055,-1.58324505574795,-0.0892951589444203));
#8779=CARTESIAN_POINT('Ctrl Pts',(6.36328866553822,-1.54021934802962,-0.0848710628917686));
#8780=CARTESIAN_POINT('Ctrl Pts',(6.41508822762698,-1.49442187539462,-0.0804469668391166));
#8781=CARTESIAN_POINT('Ctrl Pts',(6.4676615397328,-1.44794030826531,-0.0759567863591415));
#8782=CARTESIAN_POINT('Ctrl Pts',(6.51786641192738,-1.39860370997102,-0.0714666058791641));
#8783=CARTESIAN_POINT('Ctrl Pts',(6.56537740272673,-1.34668757781787,-0.0669764253991891));
#8784=CARTESIAN_POINT('Ctrl Pts',(6.61206431068767,-1.29567193611596,-0.0625641275441112));
#8785=CARTESIAN_POINT('Ctrl Pts',(6.6561496902821,-1.24216591063384,-0.0581518296890356));
#8786=CARTESIAN_POINT('Ctrl Pts',(6.69735963513394,-1.18647003717272,-0.0537395318339575));
#8787=CARTESIAN_POINT('Ctrl Pts',(6.73854493269571,-1.13080747490272,-0.0493298729337603));
#8788=CARTESIAN_POINT('Ctrl Pts',(6.7768579111523,-1.0729580606177,-0.0449202140335616));
#8789=CARTESIAN_POINT('Ctrl Pts',(6.81206500521088,-1.01325527591017,-0.0405105551333644));
#8790=CARTESIAN_POINT('Ctrl Pts',(6.8472634151172,-0.953567217441383,-0.0361019839159287));
#8791=CARTESIAN_POINT('Ctrl Pts',(6.87935720924913,-0.892027123974326,-0.0316934126984937));
#8792=CARTESIAN_POINT('Ctrl Pts',(6.90815724295914,-0.828995715351019,-0.027284841481058));
#8793=CARTESIAN_POINT('Ctrl Pts',(6.93788239464903,-0.763939604604037,-0.0227346576342798));
#8794=CARTESIAN_POINT('Ctrl Pts',(6.96409828625227,-0.697295220640624,-0.0181844737875009));
#8795=CARTESIAN_POINT('Ctrl Pts',(6.98665028780398,-0.629482447839057,-0.0136342899407227));
#8796=CARTESIAN_POINT('Ctrl Pts',(7.0085260120177,-0.563703208130607,-0.0092205545689134));
#8797=CARTESIAN_POINT('Ctrl Pts',(7.02695442780144,-0.496825181044442,-0.00480681919710362));
#8798=CARTESIAN_POINT('Ctrl Pts',(7.04184558333137,-0.429245579064855,-0.000393083825294127));
#8799=CARTESIAN_POINT('Ctrl Pts',(7.05742726807003,-0.358532191464125,0.00422532425896908));
#8800=CARTESIAN_POINT('Ctrl Pts',(7.06913552823614,-0.287051180071464,0.00884373234323341));
#8801=CARTESIAN_POINT('Ctrl Pts',(7.07692790107709,-0.215264941887005,0.0134621404274968));
#8802=CARTESIAN_POINT('Ctrl Pts',(7.08472027391804,-0.143478703702551,0.0180805485117599));
#8803=CARTESIAN_POINT('Ctrl Pts',(7.08859680264803,-0.0713878568362601,
0.0226989565960213));
#8804=CARTESIAN_POINT('Ctrl Pts',(7.08857708048266,0.000546895438558494,
0.0273173646802842));
#8805=CARTESIAN_POINT('Origin',(5.09382715545311,0.,-6.77268258743872));
#8806=CARTESIAN_POINT('',(7.08574931755807,0.000877333601738076,0.985439685988923));
#8807=CARTESIAN_POINT('',(7.08799998082202,-0.00180011721095886,0.827317077323091));
#8808=CARTESIAN_POINT('',(7.08857715545311,8.3550772080578E-14,-6.77268258743872));
#8809=CARTESIAN_POINT('Ctrl Pts',(7.08857700753084,0.000768203024997985,
0.987067856572719));
#8810=CARTESIAN_POINT('Ctrl Pts',(7.08858933050406,-0.0312301726838211,
0.985115999279288));
#8811=CARTESIAN_POINT('Ctrl Pts',(7.08783171154698,-0.0632230386489601,
0.983143267450536));
#8812=CARTESIAN_POINT('Ctrl Pts',(7.08582640517304,-0.10520044196499,0.980521111364263));
#8813=CARTESIAN_POINT('Ctrl Pts',(7.08527231882626,-0.115214145691052,0.979893078406499));
#8814=CARTESIAN_POINT('Ctrl Pts',(7.0841520241521,-0.133024757699987,0.978771364884858));
#8815=CARTESIAN_POINT('Ctrl Pts',(7.08361544695922,-0.140823369208531,0.978278609708121));
#8816=CARTESIAN_POINT('Ctrl Pts',(7.08245151287011,-0.156402210144011,0.977290972367816));
#8817=CARTESIAN_POINT('Ctrl Pts',(7.08182430136326,-0.164182311125906,0.976796103198259));
#8818=CARTESIAN_POINT('Ctrl Pts',(7.08038496486011,-0.180816727992611,0.975734435668629));
#8819=CARTESIAN_POINT('Ctrl Pts',(7.07955927011479,-0.189669670309279,0.975167223349754));
#8820=CARTESIAN_POINT('Ctrl Pts',(7.07722641219046,-0.212994494590406,0.973666882126047));
#8821=CARTESIAN_POINT('Ctrl Pts',(7.07562006848579,-0.227455704845281,0.972730673515336));
#8822=CARTESIAN_POINT('Ctrl Pts',(7.06803439242719,-0.289547460062802,0.968684232211899));
#8823=CARTESIAN_POINT('Ctrl Pts',(7.06049540021652,-0.336967820483085,0.965525760615543));
#8824=CARTESIAN_POINT('Ctrl Pts',(7.03874955882005,-0.447797169767986,0.957977989053789));
#8825=CARTESIAN_POINT('Ctrl Pts',(7.02314118997258,-0.510873300347682,0.953551498920586));
#8826=CARTESIAN_POINT('Ctrl Pts',(6.95640893442295,-0.733363187520309,0.937521287450869));
#8827=CARTESIAN_POINT('Ctrl Pts',(6.8883532505423,-0.886967348123215,0.925610988045209));
#8828=CARTESIAN_POINT('Ctrl Pts',(6.79399179646186,-1.04340939160515,0.91352171192033));
#8829=CARTESIAN_POINT('Ctrl Pts',(6.7859157462078,-1.05645596236879,0.912514397992516));
#8830=CARTESIAN_POINT('Ctrl Pts',(6.7742740563903,-1.07478666093634,0.911101763884265));
#8831=CARTESIAN_POINT('Ctrl Pts',(6.77083263355208,-1.08014850021139,0.910688887000755));
#8832=CARTESIAN_POINT('Ctrl Pts',(6.76487056722645,-1.08934039639549,0.909981774099608));
#8833=CARTESIAN_POINT('Ctrl Pts',(6.76236231640633,-1.09317839423996,0.909686735073077));
#8834=CARTESIAN_POINT('Ctrl Pts',(6.75745491332863,-1.1006312130914,0.909114265270557));
#8835=CARTESIAN_POINT('Ctrl Pts',(6.75505719229214,-1.10424686985238,0.908836739015987));
#8836=CARTESIAN_POINT('Ctrl Pts',(6.7484736346999,-1.11410460679468,0.908080558286499));
#8837=CARTESIAN_POINT('Ctrl Pts',(6.74426423540385,-1.12033097591016,0.907603452194914));
#8838=CARTESIAN_POINT('Ctrl Pts',(6.72787207223092,-1.14428468496136,0.905769336658876));
#8839=CARTESIAN_POINT('Ctrl Pts',(6.71543757080607,-1.16183905044525,0.904428145343044));
#8840=CARTESIAN_POINT('Ctrl Pts',(6.62109818806065,-1.29055629895297,0.894588147964476));
#8841=CARTESIAN_POINT('Ctrl Pts',(6.52812236524608,-1.39316166472405,0.886693171431795));
#8842=CARTESIAN_POINT('Ctrl Pts',(6.3612172466165,-1.54277408394262,0.873659216233273));
#8843=CARTESIAN_POINT('Ctrl Pts',(6.29350915655238,-1.59599214914898,0.868621600466437));
#8844=CARTESIAN_POINT('Ctrl Pts',(6.19616101741754,-1.66280319583515,0.861501493332392));
#8845=CARTESIAN_POINT('Ctrl Pts',(6.16930838452484,-1.68029591886193,0.859549952475419));
#8846=CARTESIAN_POINT('Ctrl Pts',(6.12808169278104,-1.70575922916512,0.856564380963674));
#8847=CARTESIAN_POINT('Ctrl Pts',(6.11401068859891,-1.71421192687885,0.855547217671982));
#8848=CARTESIAN_POINT('Ctrl Pts',(6.08787919982655,-1.72947387034107,0.853660539173462));
#8849=CARTESIAN_POINT('Ctrl Pts',(6.07584896049266,-1.73633305972348,0.852792850501278));
#8850=CARTESIAN_POINT('Ctrl Pts',(6.05818042832948,-1.74616463451512,0.851519363036846));
#8851=CARTESIAN_POINT('Ctrl Pts',(6.05259758309059,-1.7492362422812,0.851117096240894));
#8852=CARTESIAN_POINT('Ctrl Pts',(6.04009706425186,-1.75603604041251,0.850216607511358));
#8853=CARTESIAN_POINT('Ctrl Pts',(6.03317191333847,-1.75975019206691,0.849717899072887));
#8854=CARTESIAN_POINT('Ctrl Pts',(6.01795902973239,-1.76779389953994,0.848622598668168));
#8855=CARTESIAN_POINT('Ctrl Pts',(6.0096624723894,-1.77210627775708,0.848025416819078));
#8856=CARTESIAN_POINT('Ctrl Pts',(5.98690064656054,-1.78373486509993,0.846387289583115));
#8857=CARTESIAN_POINT('Ctrl Pts',(5.97237628243857,-1.79093320236204,0.845342273931895));
#8858=CARTESIAN_POINT('Ctrl Pts',(5.89536697714466,-1.82793712914644,0.839801682783555));
#8859=CARTESIAN_POINT('Ctrl Pts',(5.83145620865386,-1.8546486793968,0.835201608660842));
#8860=CARTESIAN_POINT('Ctrl Pts',(5.62644295420648,-1.92805953393274,0.820440128352348));
#8861=CARTESIAN_POINT('Ctrl Pts',(5.48144298219736,-1.96235556190953,0.80995367117517));
#8862=CARTESIAN_POINT('Ctrl Pts',(5.26767490901941,-1.9882828992491,0.795097658815514));
#8863=CARTESIAN_POINT('Ctrl Pts',(5.20097514536843,-1.99299101370848,0.790553546167207));
#8864=CARTESIAN_POINT('Ctrl Pts',(5.1239422999561,-1.99454883392951,0.785497343036555));
#8865=CARTESIAN_POINT('Ctrl Pts',(5.11372455186526,-1.99467693551602,0.784830592702827));
#8866=CARTESIAN_POINT('Ctrl Pts',(5.09809808085482,-1.99475275864742,0.783817337421511));
#8867=CARTESIAN_POINT('Ctrl Pts',(5.09268998530334,-1.99475700711887,0.783467843307091));
#8868=CARTESIAN_POINT('Ctrl Pts',(5.08278608712546,-1.99472450968177,0.782830052056166));
#8869=CARTESIAN_POINT('Ctrl Pts',(5.07829042772335,-1.99469455948538,0.782541394241501));
#8870=CARTESIAN_POINT('Ctrl Pts',(5.06819200070896,-1.99459314032741,0.781894892319105));
#8871=CARTESIAN_POINT('Ctrl Pts',(5.06258941940835,-1.99451326450462,0.781537517341971));
#8872=CARTESIAN_POINT('Ctrl Pts',(5.04617466811118,-1.99421005738547,0.780494083514686));
#8873=CARTESIAN_POINT('Ctrl Pts',(5.03536368767618,-1.99392240263961,0.7798114699834));
#8874=CARTESIAN_POINT('Ctrl Pts',(4.94707989597268,-1.99085471342288,0.774270910373587));
#8875=CARTESIAN_POINT('Ctrl Pts',(4.86981751251485,-1.98364811129229,0.769633299231163));
#8876=CARTESIAN_POINT('Ctrl Pts',(4.76900055770527,-1.96827655985396,0.763637456767907));
#8877=CARTESIAN_POINT('Ctrl Pts',(4.74490795980959,-1.96414876383731,0.762208956312499));
#8878=CARTESIAN_POINT('Ctrl Pts',(4.62076477469177,-1.94052290456797,0.754845453550176));
#8879=CARTESIAN_POINT('Ctrl Pts',(4.52224323688292,-1.91382038714486,0.748983722388977));
#8880=CARTESIAN_POINT('Ctrl Pts',(4.3765906672322,-1.86208763549841,0.739844790245944));
#8881=CARTESIAN_POINT('Ctrl Pts',(4.32770641704029,-1.84251375999521,0.736693940895876));
#8882=CARTESIAN_POINT('Ctrl Pts',(4.24812590021483,-1.80693381427013,0.731377947360863));
#8883=CARTESIAN_POINT('Ctrl Pts',(4.21696894987898,-1.79202117429641,0.729247488087762));
#8884=CARTESIAN_POINT('Ctrl Pts',(4.17512609362116,-1.77064141506663,0.726311037434362));
#8885=CARTESIAN_POINT('Ctrl Pts',(4.16408952991408,-1.76487126959923,0.72552923771205));
#8886=CARTESIAN_POINT('Ctrl Pts',(4.14566614664093,-1.75501837121576,0.724211571744321));
#8887=CARTESIAN_POINT('Ctrl Pts',(4.13824980314967,-1.75099134839588,0.723677677806174));
#8888=CARTESIAN_POINT('Ctrl Pts',(4.12368086677061,-1.74296039242088,0.722621911625202));
#8889=CARTESIAN_POINT('Ctrl Pts',(4.11652695371705,-1.73895918968645,0.722100144261402));
#8890=CARTESIAN_POINT('Ctrl Pts',(4.10084471896527,-1.73006073780542,0.72094888675366));
#8891=CARTESIAN_POINT('Ctrl Pts',(4.09232758368497,-1.72514430634191,0.720318717642497));
#8892=CARTESIAN_POINT('Ctrl Pts',(4.06256597544102,-1.70767003927824,0.718099162861348));
#8893=CARTESIAN_POINT('Ctrl Pts',(4.04151921849765,-1.69478154935099,0.716497893791444));
#8894=CARTESIAN_POINT('Ctrl Pts',(3.89457901009348,-1.6010067511858,0.705087663659892));
#8895=CARTESIAN_POINT('Ctrl Pts',(3.77792111874581,-1.50658361087159,0.69475971840475));
#8896=CARTESIAN_POINT('Ctrl Pts',(3.61303446982983,-1.33924019962458,0.678381243629311));
#8897=CARTESIAN_POINT('Ctrl Pts',(3.55709443014078,-1.27466286401111,0.672427474676137));
#8898=CARTESIAN_POINT('Ctrl Pts',(3.48981916624115,-1.18610896681386,0.664884785239939));
#8899=CARTESIAN_POINT('Ctrl Pts',(3.47457874721772,-1.16521707575679,0.663147262203817));
#8900=CARTESIAN_POINT('Ctrl Pts',(3.44980002268579,-1.12982442012886,0.660280431883248));
#8901=CARTESIAN_POINT('Ctrl Pts',(3.44003726457693,-1.11548531111601,0.659139328091417));
#8902=CARTESIAN_POINT('Ctrl Pts',(3.42677010260964,-1.09544196281118,0.657574253910239));
#8903=CARTESIAN_POINT('Ctrl Pts',(3.42310581638526,-1.08984518240066,0.657140421393751));
#8904=CARTESIAN_POINT('Ctrl Pts',(3.41694593465387,-1.08033258437424,0.656408583271429));
#8905=CARTESIAN_POINT('Ctrl Pts',(3.41443574970077,-1.07642632326586,0.656109627980898));
#8906=CARTESIAN_POINT('Ctrl Pts',(3.40964993606804,-1.06892131818717,0.655538301422917));
#8907=CARTESIAN_POINT('Ctrl Pts',(3.40737216849611,-1.06532402045757,0.655265783233808));
#8908=CARTESIAN_POINT('Ctrl Pts',(3.40194818500458,-1.05669688600632,0.654615330133348));
#8909=CARTESIAN_POINT('Ctrl Pts',(3.3988128340925,-1.05166021701891,0.654238099889289));
#8910=CARTESIAN_POINT('Ctrl Pts',(3.38760148493088,-1.03346976879617,0.65288444572383));
#8911=CARTESIAN_POINT('Ctrl Pts',(3.37965550819028,-1.02023595291727,0.65191604332005));
#8912=CARTESIAN_POINT('Ctrl Pts',(3.304928558915,-0.892442028525047,0.642707489967446));
#8913=CARTESIAN_POINT('Ctrl Pts',(3.24956440567278,-0.771567186257269,0.635075328255049));
#8914=CARTESIAN_POINT('Ctrl Pts',(3.16174589489612,-0.515044827721414,0.619332800805632));
#8915=CARTESIAN_POINT('Ctrl Pts',(3.13066181454087,-0.379716056752711,0.611245451444885));
#8916=CARTESIAN_POINT('Ctrl Pts',(3.1114862375932,-0.222999696529675,0.601470774210416));
#8917=CARTESIAN_POINT('Ctrl Pts',(3.10941007728325,-0.203698792149985,0.600260704707658));
#8918=CARTESIAN_POINT('Ctrl Pts',(3.10669835558373,-0.174485701038683,0.598418478188881));
#8919=CARTESIAN_POINT('Ctrl Pts',(3.10585455797687,-0.164593660582055,0.597792820940868));
#8920=CARTESIAN_POINT('Ctrl Pts',(3.10446203099679,-0.146691582730595,0.596657025150946));
#8921=CARTESIAN_POINT('Ctrl Pts',(3.10388774767208,-0.138683701777267,0.596147695761916));
#8922=CARTESIAN_POINT('Ctrl Pts',(3.10275874292916,-0.121486189425074,0.595051052305967));
#8923=CARTESIAN_POINT('Ctrl Pts',(3.10221926949032,-0.11229577673031,0.594463274439087));
#8924=CARTESIAN_POINT('Ctrl Pts',(3.10093822586508,-0.0875441320799671,
0.592875463044831));
#8925=CARTESIAN_POINT('Ctrl Pts',(3.10031531586669,-0.0719776590437602,
0.591871762972886));
#8926=CARTESIAN_POINT('Ctrl Pts',(3.09815180318625,0.0045027353531572,0.58691424663997));
#8927=CARTESIAN_POINT('Ctrl Pts',(3.09922065736666,0.0654522681362345,0.582880450135189));
#8928=CARTESIAN_POINT('Ctrl Pts',(3.11398924657116,0.298323779092428,0.567145057156788));
#8929=CARTESIAN_POINT('Ctrl Pts',(3.14716716388484,0.468248884516733,0.554906658301742));
#8930=CARTESIAN_POINT('Ctrl Pts',(3.21865593293446,0.682353377977116,0.539441611548483));
#8931=CARTESIAN_POINT('Ctrl Pts',(3.23757538508093,0.732259319725125,0.535841133344036));
#8932=CARTESIAN_POINT('Ctrl Pts',(3.26227854851062,0.790285745881826,0.531706517414003));
#8933=CARTESIAN_POINT('Ctrl Pts',(3.26614754188102,0.799192779633129,0.5310733437841));
#8934=CARTESIAN_POINT('Ctrl Pts',(3.2722285820963,0.812917148938568,0.53010042354739));
#8935=CARTESIAN_POINT('Ctrl Pts',(3.2743949798016,0.817754372213337,0.529758035496906));
#8936=CARTESIAN_POINT('Ctrl Pts',(3.27843757834327,0.826685262209806,0.529126935881807));
#8937=CARTESIAN_POINT('Ctrl Pts',(3.28030835103319,0.830781190271786,0.528837915582169));
#8938=CARTESIAN_POINT('Ctrl Pts',(3.28459371740461,0.840080252108739,0.528182668327269));
#8939=CARTESIAN_POINT('Ctrl Pts',(3.28701689168331,0.845279324270073,0.527816970778189));
#8940=CARTESIAN_POINT('Ctrl Pts',(3.29338296313067,0.858785670227963,0.526868455338145));
#8941=CARTESIAN_POINT('Ctrl Pts',(3.29736098714569,0.867076369626628,0.526287712332161));
#8942=CARTESIAN_POINT('Ctrl Pts',(3.32468672233866,0.923031223800151,0.522376362590108));
#8943=CARTESIAN_POINT('Ctrl Pts',(3.34987358980212,0.969779122122044,0.51914864448852));
#8944=CARTESIAN_POINT('Ctrl Pts',(3.40403769129978,1.06135827035434,0.512796574315339));
#8945=CARTESIAN_POINT('Ctrl Pts',(3.43300767941705,1.10614148658201,0.509675215368583));
#8946=CARTESIAN_POINT('Ctrl Pts',(3.46646291681158,1.15357511447568,0.506295635134601));
#8947=CARTESIAN_POINT('Ctrl Pts',(3.46920131922337,1.15742853012372,0.506020542850604));
#8948=CARTESIAN_POINT('Ctrl Pts',(3.53984361356951,1.25609005430591,0.498962361133775));
#8949=CARTESIAN_POINT('Ctrl Pts',(3.61591376547616,1.34476668441478,0.492250380324655));
#8950=CARTESIAN_POINT('Ctrl Pts',(3.72732247486301,1.45369505229739,0.48292690179726));
#8951=CARTESIAN_POINT('Ctrl Pts',(3.75615302617345,1.48026754011568,0.480554907324072));
#8952=CARTESIAN_POINT('Ctrl Pts',(3.80668964077068,1.52416341503441,0.476447089226139));
#8953=CARTESIAN_POINT('Ctrl Pts',(3.82800916317559,1.54191497525253,0.474728503231998));
#8954=CARTESIAN_POINT('Ctrl Pts',(3.85863613430209,1.5663529805301,0.472275666010715));
#8955=CARTESIAN_POINT('Ctrl Pts',(3.86764223140399,1.57341318212586,0.47155629866383));
#8956=CARTESIAN_POINT('Ctrl Pts',(3.88323713766525,1.58542337437207,0.470313640984269));
#8957=CARTESIAN_POINT('Ctrl Pts',(3.88979685633321,1.59041079682835,0.469791836538894));
#8958=CARTESIAN_POINT('Ctrl Pts',(3.90239466325912,1.59986643197529,0.468791332550558));
#8959=CARTESIAN_POINT('Ctrl Pts',(3.9084274682486,1.6043414732104,0.468312910852757));
#8960=CARTESIAN_POINT('Ctrl Pts',(3.92415832427271,1.61587321154236,0.467067116136874));
#8961=CARTESIAN_POINT('Ctrl Pts',(3.93389488746113,1.62287662307256,0.466297710979303));
#8962=CARTESIAN_POINT('Ctrl Pts',(3.96208379917769,1.64276935341432,0.464074618630753));
#8963=CARTESIAN_POINT('Ctrl Pts',(3.98069143837439,1.65543437801828,0.462612548269991));
#8964=CARTESIAN_POINT('Ctrl Pts',(4.1185324620018,1.74587906234593,0.451817389919458));
#8965=CARTESIAN_POINT('Ctrl Pts',(4.24555351083098,1.81099736871511,0.442017271612711));
#8966=CARTESIAN_POINT('Ctrl Pts',(4.48674195265708,1.90366674384796,0.424009238702443));
#8967=CARTESIAN_POINT('Ctrl Pts',(4.59852427816608,1.93576318956978,0.415887783591245));
#8968=CARTESIAN_POINT('Ctrl Pts',(4.73094737885038,1.9615555416094,0.406918458820201));
#8969=CARTESIAN_POINT('Ctrl Pts',(4.74947420859436,1.96489261407854,0.40567841748981));
#8970=CARTESIAN_POINT('Ctrl Pts',(4.77486026315743,1.9690950679872,0.404001987608267));
#8971=CARTESIAN_POINT('Ctrl Pts',(4.78168017386383,1.97018768913885,0.403553850334167));
#8972=CARTESIAN_POINT('Ctrl Pts',(4.79313720605387,1.97196224149596,0.402804906332139));
#8973=CARTESIAN_POINT('Ctrl Pts',(4.79777125658616,1.97266328442418,0.402503048148923));
#8974=CARTESIAN_POINT('Ctrl Pts',(4.80657726369382,1.97396373463445,0.401931515785278));
#8975=CARTESIAN_POINT('Ctrl Pts',(4.81074870473869,1.97456626060287,0.401661662978566));
#8976=CARTESIAN_POINT('Ctrl Pts',(4.82172924761074,1.9761167861845,0.400953577408447));
#8977=CARTESIAN_POINT('Ctrl Pts',(4.82854146718782,1.97704282477957,0.400516564026644));
#8978=CARTESIAN_POINT('Ctrl Pts',(4.85246627418038,1.98016922577878,0.39898930705221));
#8979=CARTESIAN_POINT('Ctrl Pts',(4.86960305301516,1.98218284640876,0.397908912076251));
#8980=CARTESIAN_POINT('Ctrl Pts',(5.08690571252716,2.00486221309185,0.384355771215339));
#8981=CARTESIAN_POINT('Ctrl Pts',(5.28908317093018,1.99535015550772,0.373219953486289));
#8982=CARTESIAN_POINT('Ctrl Pts',(5.55844915347913,1.94127488704387,0.356921542620261));
#8983=CARTESIAN_POINT('Ctrl Pts',(5.6295973500766,1.92285472482053,0.352483673434621));
#8984=CARTESIAN_POINT('Ctrl Pts',(5.71477497335138,1.89570733033441,0.346925318252895));
#8985=CARTESIAN_POINT('Ctrl Pts',(5.72992789989978,1.89067667636234,0.345926946017115));
#8986=CARTESIAN_POINT('Ctrl Pts',(5.75371585769108,1.88246092413269,0.344343807939059));
#8987=CARTESIAN_POINT('Ctrl Pts',(5.7623922383161,1.87939696595334,0.343763027837884));
#8988=CARTESIAN_POINT('Ctrl Pts',(5.77859905554735,1.87354729620979,0.342671749511088));
#8989=CARTESIAN_POINT('Ctrl Pts',(5.78613449904791,1.87077592597892,0.342161734989936));
#8990=CARTESIAN_POINT('Ctrl Pts',(5.80295594601757,1.86447381717529,0.341017254691192));
#8991=CARTESIAN_POINT('Ctrl Pts',(5.81223266609789,1.86091906673445,0.340381999937955));
#8992=CARTESIAN_POINT('Ctrl Pts',(5.83571199729209,1.85172028338359,0.338763570870283));
#8993=CARTESIAN_POINT('Ctrl Pts',(5.84987680765042,1.84598213110689,0.337777273468373));
#8994=CARTESIAN_POINT('Ctrl Pts',(5.9372083701089,1.80943042988531,0.331633431469182));
#8995=CARTESIAN_POINT('Ctrl Pts',(6.00853832505779,1.77443822790524,0.326335532534088));
#8996=CARTESIAN_POINT('Ctrl Pts',(6.19895626974579,1.66648791979571,0.311412832064357));
#8997=CARTESIAN_POINT('Ctrl Pts',(6.31276890968104,1.58513981081485,0.301566077684162));
#8998=CARTESIAN_POINT('Ctrl Pts',(6.46561006475343,1.44963220491833,0.287487060666978));
#8999=CARTESIAN_POINT('Ctrl Pts',(6.51195452894013,1.40432846317499,0.283087468987644));
#9000=CARTESIAN_POINT('Ctrl Pts',(6.56292253644513,1.349403349098,0.278170898965221));
#9001=CARTESIAN_POINT('Ctrl Pts',(6.56977165177564,1.34190852564304,0.277508489135789));
#9002=CARTESIAN_POINT('Ctrl Pts',(6.5801717762404,1.33035195638334,0.276500438671891));
#9003=CARTESIAN_POINT('Ctrl Pts',(6.58376390907266,1.32632768630837,0.276151854861484));
#9004=CARTESIAN_POINT('Ctrl Pts',(6.59032031333211,1.31892229053519,0.275514941508939));
#9005=CARTESIAN_POINT('Ctrl Pts',(6.59328947449365,1.31554571742619,0.275226257883646));
#9006=CARTESIAN_POINT('Ctrl Pts',(6.59994345340446,1.30792692145483,0.274578728297315));
#9007=CARTESIAN_POINT('Ctrl Pts',(6.60362177345716,1.30367915842826,0.27422035870733));
#9008=CARTESIAN_POINT('Ctrl Pts',(6.61437490586963,1.29115477527212,0.273171285709451));
#9009=CARTESIAN_POINT('Ctrl Pts',(6.62140009252877,1.28283555043032,0.272484083755965));
#9010=CARTESIAN_POINT('Ctrl Pts',(6.69210067218446,1.19770754798058,0.265544488935228));
#9011=CARTESIAN_POINT('Ctrl Pts',(6.7500055793617,1.11627063992951,0.259659780319202));
#9012=CARTESIAN_POINT('Ctrl Pts',(6.86656164731685,0.92317534566154,0.246510170043034));
#9013=CARTESIAN_POINT('Ctrl Pts',(6.92121678538167,0.809620980763616,0.239301175932445));
#9014=CARTESIAN_POINT('Ctrl Pts',(6.98567245401892,0.635268419905961,0.228183968001383));
#9015=CARTESIAN_POINT('Ctrl Pts',(7.00396305018982,0.577948450553578,0.224525631253163));
#9016=CARTESIAN_POINT('Ctrl Pts',(7.02356493823274,0.505338447638272,0.219843908597162));
#9017=CARTESIAN_POINT('Ctrl Pts',(7.02732905994982,0.49073946514589,0.218900323853748));
#9018=CARTESIAN_POINT('Ctrl Pts',(7.033077004583,0.467352875729911,0.217384533140573));
#9019=CARTESIAN_POINT('Ctrl Pts',(7.03516745732663,0.458591883741971,0.216815752055405));
#9020=CARTESIAN_POINT('Ctrl Pts',(7.03901510331051,0.441968673891558,0.215734628264384));
#9021=CARTESIAN_POINT('Ctrl Pts',(7.04078414526777,0.434109361674526,0.215222676144252));
#9022=CARTESIAN_POINT('Ctrl Pts',(7.04469197690292,0.416243574058273,0.21405698053053));
#9023=CARTESIAN_POINT('Ctrl Pts',(7.0468014622848,0.406230987177652,0.213402318075054));
#9024=CARTESIAN_POINT('Ctrl Pts',(7.05206423375543,0.380262584027074,0.211700668782033));
#9025=CARTESIAN_POINT('Ctrl Pts',(7.05509952453204,0.364283894837235,0.210649981332873));
#9026=CARTESIAN_POINT('Ctrl Pts',(7.07832854179385,0.233281068275994,0.202004230086555));
#9027=CARTESIAN_POINT('Ctrl Pts',(7.0885771554597,0.116744612167536,0.19409417477583));
#9028=CARTESIAN_POINT('Ctrl Pts',(7.08857715545311,-1.12589937373286E-10,
0.186011338956534));
#9029=CARTESIAN_POINT('Ctrl Pts',(7.09164130412058,0.000548482472640843,
0.0273174125612813));
#9030=CARTESIAN_POINT('Ctrl Pts',(7.09175165964625,0.0306588665693442,0.0292476145445689));
#9031=CARTESIAN_POINT('Ctrl Pts',(7.07750675584133,0.720147590609536,0.0734535743639286));
#9032=CARTESIAN_POINT('Ctrl Pts',(6.28353627797873,2.03415344877187,0.159935292019361));
#9033=CARTESIAN_POINT('Ctrl Pts',(4.03314932025975,2.10431712897573,0.286762565527578));
#9034=CARTESIAN_POINT('Ctrl Pts',(2.75099003209035,0.253578908358813,0.413589839035793));
#9035=CARTESIAN_POINT('Ctrl Pts',(3.60746290235971,-1.82863592781539,0.540417112544011));
#9036=CARTESIAN_POINT('Ctrl Pts',(5.82074643570099,-2.24160130473173,0.667244386052225));
#9037=CARTESIAN_POINT('Ctrl Pts',(6.98930590305859,-1.01005560487751,0.762877707645254));
#9038=CARTESIAN_POINT('Ctrl Pts',(7.0895351504061,-0.175492384774626,0.816235271402208));
#9039=CARTESIAN_POINT('Ctrl Pts',(7.08799998082202,-0.00180011721095886,
0.827317077323091));
#9040=CARTESIAN_POINT('Origin',(5.09382715545311,0.,-6.77268258743872));
#9041=CARTESIAN_POINT('',(7.09089099632987,0.00118553966962425,1.78540654381999));
#9042=CARTESIAN_POINT('',(7.08857697543044,0.000847467636836062,1.62559580930988));
#9043=CARTESIAN_POINT('',(7.08857715545311,8.3550772080578E-14,-6.77268258743872));
#9044=CARTESIAN_POINT('Ctrl Pts',(7.08569498022126,0.000879430672124808,
0.98540839880601));
#9045=CARTESIAN_POINT('Ctrl Pts',(7.08678274233512,0.277777209942647,1.00302338867406));
#9046=CARTESIAN_POINT('Ctrl Pts',(6.90380563625223,1.21784867470375,1.06291413637816));
#9047=CARTESIAN_POINT('Ctrl Pts',(5.46844469401115,2.32655315630881,1.16508064191835));
#9048=CARTESIAN_POINT('Ctrl Pts',(3.34465355126974,1.57910721350831,1.29190791542657));
#9049=CARTESIAN_POINT('Ctrl Pts',(2.81757559157258,-0.609808746458473,1.41873518893479));
#9050=CARTESIAN_POINT('Ctrl Pts',(4.36834792145259,-2.24206774437344,1.545562462443));
#9051=CARTESIAN_POINT('Ctrl Pts',(6.50103911243751,-1.84272189433612,1.66778624740474));
#9052=CARTESIAN_POINT('Ctrl Pts',(7.08669410382909,-0.587071448118138,1.7477342745304));
#9053=CARTESIAN_POINT('Ctrl Pts',(7.09089099632987,0.00118553966962425,
1.78540654381999));
#9054=CARTESIAN_POINT('Ctrl Pts',(7.0885763647563,-0.00177608679726875,
0.826985646114236));
#9055=CARTESIAN_POINT('Ctrl Pts',(7.08868588521213,0.121227948264429,0.834139298127843));
#9056=CARTESIAN_POINT('Ctrl Pts',(7.07741849588526,0.243966340480971,0.841373813191014));
#9057=CARTESIAN_POINT('Ctrl Pts',(7.05234424202085,0.37873053609996,0.849854099289273));
#9058=CARTESIAN_POINT('Ctrl Pts',(7.04962091607336,0.392551586002556,0.850729931092804));
#9059=CARTESIAN_POINT('Ctrl Pts',(7.04483881375989,0.415534874801099,0.852197153040885));
#9060=CARTESIAN_POINT('Ctrl Pts',(7.04286128675278,0.424713636800601,0.85278599318071));
#9061=CARTESIAN_POINT('Ctrl Pts',(7.03885051903425,0.442711628765464,0.853946447802865));
#9062=CARTESIAN_POINT('Ctrl Pts',(7.03682191146503,0.451531665422038,0.854517903215624));
#9063=CARTESIAN_POINT('Ctrl Pts',(7.03287599886028,0.468168690931863,0.855601194125967));
#9064=CARTESIAN_POINT('Ctrl Pts',(7.03097126152878,0.475988497217635,0.85611261786743));
#9065=CARTESIAN_POINT('Ctrl Pts',(7.02655505248188,0.493653390368693,0.857273118556198));
#9066=CARTESIAN_POINT('Ctrl Pts',(7.0240155952107,0.503491186129817,0.857923082986224));
#9067=CARTESIAN_POINT('Ctrl Pts',(7.01727740638661,0.52879438030944,0.859604479214082));
#9068=CARTESIAN_POINT('Ctrl Pts',(7.01296733037436,0.544229114153417,0.860639466959637));
#9069=CARTESIAN_POINT('Ctrl Pts',(6.9802897750228,0.6560318371411,0.868206274058423));
#9070=CARTESIAN_POINT('Ctrl Pts',(6.94486879863639,0.750172200959767,0.874967460973669));
#9071=CARTESIAN_POINT('Ctrl Pts',(6.86897249869979,0.913352553146966,0.887357286841124));
#9072=CARTESIAN_POINT('Ctrl Pts',(6.83114694016992,0.983398676253002,0.892915225182642));
#9073=CARTESIAN_POINT('Ctrl Pts',(6.7457906570638,1.12109121095605,0.904198058605296));
#9074=CARTESIAN_POINT('Ctrl Pts',(6.69802961713367,1.18842991395529,0.909910786085606));
#9075=CARTESIAN_POINT('Ctrl Pts',(6.63098309168,1.27152229034517,0.917055776786366));
#9076=CARTESIAN_POINT('Ctrl Pts',(6.61538860095439,1.29014270609605,0.91866336862861));
#9077=CARTESIAN_POINT('Ctrl Pts',(6.59570283851815,1.31279463438316,0.92062229974999));
#9078=CARTESIAN_POINT('Ctrl Pts',(6.59192991242095,1.31709849704309,0.920994645150306));
#9079=CARTESIAN_POINT('Ctrl Pts',(6.58459339276969,1.32539512136817,0.921712608816385));
#9080=CARTESIAN_POINT('Ctrl Pts',(6.58103215601027,1.32938989390171,0.922058388856411));
#9081=CARTESIAN_POINT('Ctrl Pts',(6.57444765594131,1.33671640046393,0.922692635044146));
#9082=CARTESIAN_POINT('Ctrl Pts',(6.57142920746619,1.34005222971507,0.922981434857892));
#9083=CARTESIAN_POINT('Ctrl Pts',(6.56458099061302,1.3475692435902,0.923632294358708));
#9084=CARTESIAN_POINT('Ctrl Pts',(6.56074467006493,1.35174432387743,0.923993854523405));
#9085=CARTESIAN_POINT('Ctrl Pts',(6.55078880798085,1.36248702210499,0.924924504355055));
#9086=CARTESIAN_POINT('Ctrl Pts',(6.54464256510118,1.36902987423392,0.925491645721486));
#9087=CARTESIAN_POINT('Ctrl Pts',(6.50478428292887,1.41089026656067,0.92912402867857));
#9088=CARTESIAN_POINT('Ctrl Pts',(6.4698263874983,1.44500461267795,0.932102313942063));
#9089=CARTESIAN_POINT('Ctrl Pts',(6.42479674488353,1.48582982815332,0.935743528451845));
#9090=CARTESIAN_POINT('Ctrl Pts',(6.41587276406192,1.49377566706049,0.936456066889964));
#9091=CARTESIAN_POINT('Ctrl Pts',(6.39518527671644,1.51186502349082,0.938088563889319));
#9092=CARTESIAN_POINT('Ctrl Pts',(6.38337355393024,1.52195233509276,0.939006585551655));
#9093=CARTESIAN_POINT('Ctrl Pts',(6.27208436503667,1.61476843457911,0.947538457978001));
#9094=CARTESIAN_POINT('Ctrl Pts',(6.16489763445384,1.68777261484291,0.954910765022636));
#9095=CARTESIAN_POINT('Ctrl Pts',(6.00527918727699,1.77511863148812,0.965669602161265));
#9096=CARTESIAN_POINT('Ctrl Pts',(5.95818750901853,1.79851926391426,0.968816309368003));
#9097=CARTESIAN_POINT('Ctrl Pts',(5.88907081627617,1.82952256855478,0.973435991059897));
#9098=CARTESIAN_POINT('Ctrl Pts',(5.86774938100145,1.83864342170898,0.974861134518082));
#9099=CARTESIAN_POINT('Ctrl Pts',(5.82939159871417,1.8542666547606,0.977428271221079));
#9100=CARTESIAN_POINT('Ctrl Pts',(5.81241576623851,1.86091113472771,0.978565513292725));
#9101=CARTESIAN_POINT('Ctrl Pts',(5.78618747575369,1.87076470600111,0.980325383990736));
#9102=CARTESIAN_POINT('Ctrl Pts',(5.77699818656824,1.87413999880106,0.980942486878824));
#9103=CARTESIAN_POINT('Ctrl Pts',(5.76023605057662,1.88015719277037,0.982069248550743));
#9104=CARTESIAN_POINT('Ctrl Pts',(5.7526713649376,1.88282133767239,0.982578158905946));
#9105=CARTESIAN_POINT('Ctrl Pts',(5.73628839733822,1.88848030020195,0.983681288950033));
#9106=CARTESIAN_POINT('Ctrl Pts',(5.72746482732273,1.89145911600715,0.984276021662022));
#9107=CARTESIAN_POINT('Ctrl Pts',(5.7033830829423,1.89940163740608,0.985901009224233));
#9108=CARTESIAN_POINT('Ctrl Pts',(5.68808562198402,1.90424311972026,0.986935227127497));
#9109=CARTESIAN_POINT('Ctrl Pts',(5.6083402182553,1.92842720330545,0.99233804363489));
#9110=CARTESIAN_POINT('Ctrl Pts',(5.5430088348754,1.94468230016142,0.996805127362824));
#9111=CARTESIAN_POINT('Ctrl Pts',(5.32520107462839,1.98731358011449,1.01183187748595));
#9112=CARTESIAN_POINT('Ctrl Pts',(5.1704806266177,1.99926599218372,1.02276545288767));
#9113=CARTESIAN_POINT('Ctrl Pts',(4.95285332191976,1.99076433039015,1.03776580876369));
#9114=CARTESIAN_POINT('Ctrl Pts',(4.88989111252952,1.98530300523955,1.04205238743651));
#9115=CARTESIAN_POINT('Ctrl Pts',(4.81728024913999,1.97551293365793,1.04685940784675));
#9116=CARTESIAN_POINT('Ctrl Pts',(4.80728243225285,1.97408755487096,1.04751824048855));
#9117=CARTESIAN_POINT('Ctrl Pts',(4.79197268023666,1.9717860969947,1.04852199936756));
#9118=CARTESIAN_POINT('Ctrl Pts',(4.78665292169807,1.9709643650444,1.04886983110966));
#9119=CARTESIAN_POINT('Ctrl Pts',(4.7768950503948,1.96941662069338,1.04950602353467));
#9120=CARTESIAN_POINT('Ctrl Pts',(4.77245607308137,1.96869713599838,1.04979473283966));
#9121=CARTESIAN_POINT('Ctrl Pts',(4.7624627727306,1.9670426866259,1.05044313095317));
#9122=CARTESIAN_POINT('Ctrl Pts',(4.75690996183444,1.9660992069719,1.05080233730861));
#9123=CARTESIAN_POINT('Ctrl Pts',(4.74057325746439,1.96325218933645,1.05185616520005));
#9124=CARTESIAN_POINT('Ctrl Pts',(4.72980075185064,1.96128332109259,1.0525472376041));
#9125=CARTESIAN_POINT('Ctrl Pts',(4.62539700811044,1.94131181532914,1.05921248716136));
#9126=CARTESIAN_POINT('Ctrl Pts',(4.53314083208464,1.91670397416537,1.06485158582226));
#9127=CARTESIAN_POINT('Ctrl Pts',(4.32090679316549,1.84344820613787,1.07795806450416));
#9128=CARTESIAN_POINT('Ctrl Pts',(4.20321119964475,1.78955563110373,1.08534972944516));
#9129=CARTESIAN_POINT('Ctrl Pts',(4.0388540677999,1.69404080767417,1.09671272475468));
#9130=CARTESIAN_POINT('Ctrl Pts',(3.98759227486737,1.66101949795878,1.10041870225073));
#9131=CARTESIAN_POINT('Ctrl Pts',(3.92558875594306,1.61693405840853,1.10515413976605));
#9132=CARTESIAN_POINT('Ctrl Pts',(3.91335231108198,1.60802233482565,1.1061014975676));
#9133=CARTESIAN_POINT('Ctrl Pts',(3.89398807404771,1.59357933872107,1.10762192721523));
#9134=CARTESIAN_POINT('Ctrl Pts',(3.88679417305922,1.58813736974165,1.10819153670643));
#9135=CARTESIAN_POINT('Ctrl Pts',(3.8732477905546,1.57774473097067,1.10927332532144));
#9136=CARTESIAN_POINT('Ctrl Pts',(3.86688788106388,1.5728040043109,1.10978510727268));
#9137=CARTESIAN_POINT('Ctrl Pts',(3.85253358663092,1.56151275240015,1.11094916213402));
#9138=CARTESIAN_POINT('Ctrl Pts',(3.8445577380757,1.555139130859,1.11160234408242));
#9139=CARTESIAN_POINT('Ctrl Pts',(3.82406251242802,1.53850167011593,1.11329760302683));
#9140=CARTESIAN_POINT('Ctrl Pts',(3.81161872439032,1.52814631216959,1.11434333470068));
#9141=CARTESIAN_POINT('Ctrl Pts',(3.69886261633687,1.43196707372869,1.12397309232721));
#9142=CARTESIAN_POINT('Ctrl Pts',(3.60719428583301,1.33655026569795,1.13296646418753));
#9143=CARTESIAN_POINT('Ctrl Pts',(3.46360618589662,1.15389776730633,1.14911250125984));
#9144=CARTESIAN_POINT('Ctrl Pts',(3.40762141382675,1.07042586172218,1.15615824221394));
#9145=CARTESIAN_POINT('Ctrl Pts',(3.33324494159126,0.939112720499902,1.1664801153287));
#9146=CARTESIAN_POINT('Ctrl Pts',(3.31001220405886,0.894196627364318,1.16988600621986));
#9147=CARTESIAN_POINT('Ctrl Pts',(3.28443485263501,0.839773073438701,1.17382740609879));
#9148=CARTESIAN_POINT('Ctrl Pts',(3.28042293007745,0.83107427138136,1.17445187390053));
#9149=CARTESIAN_POINT('Ctrl Pts',(3.27430041537561,0.817543757974525,1.17541430968631));
#9150=CARTESIAN_POINT('Ctrl Pts',(3.27214611711516,0.812732151555461,1.17575483197036));
#9151=CARTESIAN_POINT('Ctrl Pts',(3.2681858941751,0.803792169150238,1.17638424198223));
#9152=CARTESIAN_POINT('Ctrl Pts',(3.26637489307639,0.799666240014152,1.17667342461088));
#9153=CARTESIAN_POINT('Ctrl Pts',(3.26227486617728,0.790238647117166,1.17733126997386));
#9154=CARTESIAN_POINT('Ctrl Pts',(3.2599948719872,0.784933160130323,1.17769938588998));
#9155=CARTESIAN_POINT('Ctrl Pts',(3.25409378739322,0.77103542923949,1.17865839010778));
#9156=CARTESIAN_POINT('Ctrl Pts',(3.25050979584178,0.762427451199525,1.17924712749256));
#9157=CARTESIAN_POINT('Ctrl Pts',(3.22578006475225,0.701838150012314,1.18335649095078));
#9158=CARTESIAN_POINT('Ctrl Pts',(3.20677370348674,0.649004804328121,1.1867619785163));
#9159=CARTESIAN_POINT('Ctrl Pts',(3.14153607493148,0.440418054127619,1.19977972615778));
#9160=CARTESIAN_POINT('Ctrl Pts',(3.11216579189744,0.280057282763585,1.2089310684923));
#9161=CARTESIAN_POINT('Ctrl Pts',(3.09858391442029,0.0506725858960808,1.22261140241009));
#9162=CARTESIAN_POINT('Ctrl Pts',(3.0980108666019,-0.0167097643938952,1.22669320503519));
#9163=CARTESIAN_POINT('Ctrl Pts',(3.10150236903982,-0.0995615022827879,
1.23185164631077));
#9164=CARTESIAN_POINT('Ctrl Pts',(3.10234120635525,-0.115127061154027,1.23282674717197));
#9165=CARTESIAN_POINT('Ctrl Pts',(3.10395977710108,-0.139780314017471,1.23438128418566));
#9166=CARTESIAN_POINT('Ctrl Pts',(3.10461957050992,-0.148875448515927,1.23495697723747));
#9167=CARTESIAN_POINT('Ctrl Pts',(3.10597826079827,-0.165978764400661,1.23604382022391));
#9168=CARTESIAN_POINT('Ctrl Pts',(3.10666324956169,-0.173987891092742,1.23655452537729));
#9169=CARTESIAN_POINT('Ctrl Pts',(3.1083138179867,-0.192003679451014,1.23770736845103));
#9170=CARTESIAN_POINT('Ctrl Pts',(3.10930666819829,-0.202007563601819,1.23835034707886));
#9171=CARTESIAN_POINT('Ctrl Pts',(3.11204063916505,-0.227585932798022,1.24000175797526));
#9172=CARTESIAN_POINT('Ctrl Pts',(3.11388973105284,-0.243147949275802,1.24101353688902));
#9173=CARTESIAN_POINT('Ctrl Pts',(3.12750631684129,-0.347259863561881,1.24783117968266));
#9174=CARTESIAN_POINT('Ctrl Pts',(3.1450255154403,-0.434942856405148,1.25381650631273));
#9175=CARTESIAN_POINT('Ctrl Pts',(3.20246250893086,-0.647153923318922,1.26887880832107));
#9176=CARTESIAN_POINT('Ctrl Pts',(3.24885120636143,-0.769499210961667,1.27808571170147));
#9177=CARTESIAN_POINT('Ctrl Pts',(3.33491077256789,-0.94298803141268,1.29142382870392));
#9178=CARTESIAN_POINT('Ctrl Pts',(3.36563801139996,-0.998186977223847,1.29570875444621));
#9179=CARTESIAN_POINT('Ctrl Pts',(3.40425965363882,-1.06042028597661,1.30051417019413));
#9180=CARTESIAN_POINT('Ctrl Pts',(3.4096494230972,-1.06895972898002,1.30117294928082));
#9181=CARTESIAN_POINT('Ctrl Pts',(3.4180113242286,-1.08198790865894,1.30217664389418));
#9182=CARTESIAN_POINT('Ctrl Pts',(3.42093707257289,-1.08650600868829,1.30252446436339));
#9183=CARTESIAN_POINT('Ctrl Pts',(3.42634069087662,-1.09477699812055,1.30316064601167));
#9184=CARTESIAN_POINT('Ctrl Pts',(3.42881295903287,-1.09853334572575,1.30344935573086));
#9185=CARTESIAN_POINT('Ctrl Pts',(3.43441045278032,-1.10697583275807,1.30409776699518));
#9186=CARTESIAN_POINT('Ctrl Pts',(3.43754283127734,-1.11165710845368,1.30445698599538));
#9187=CARTESIAN_POINT('Ctrl Pts',(3.44682380083002,-1.12540101558673,1.30551088581962));
#9188=CARTESIAN_POINT('Ctrl Pts',(3.45302736014259,-1.13442652493345,1.30620201678799));
#9189=CARTESIAN_POINT('Ctrl Pts',(3.51469158211374,-1.22257718702694,1.31294758963633));
#9190=CARTESIAN_POINT('Ctrl Pts',(3.57576585207085,-1.29763596365087,1.31865777531509));
#9191=CARTESIAN_POINT('Ctrl Pts',(3.72992466539398,-1.46123813505024,1.33177479200388));
#9192=CARTESIAN_POINT('Ctrl Pts',(3.82657750061869,-1.54580855188678,1.3391121715747));
#9193=CARTESIAN_POINT('Ctrl Pts',(3.97999522860306,-1.65592633917945,1.35040223775383));
#9194=CARTESIAN_POINT('Ctrl Pts',(4.03090428074749,-1.68905520510378,1.3540942315785));
#9195=CARTESIAN_POINT('Ctrl Pts',(4.09627689004247,-1.72746914139894,1.3588139050938));
#9196=CARTESIAN_POINT('Ctrl Pts',(4.10939894780213,-1.7349804756009,1.35976016172238));
#9197=CARTESIAN_POINT('Ctrl Pts',(4.13048041244361,-1.74673178023111,1.36127923750642));
#9198=CARTESIAN_POINT('Ctrl Pts',(4.13838554503755,-1.75106829795945,1.36184860526043));
#9199=CARTESIAN_POINT('Ctrl Pts',(4.1534073220118,-1.75917678766124,1.36293019928703));
#9200=CARTESIAN_POINT('Ctrl Pts',(4.16051796093685,-1.76295955078381,1.36344203030652));
#9201=CARTESIAN_POINT('Ctrl Pts',(4.17669951808578,-1.77144258485193,1.36460656106286));
#9202=CARTESIAN_POINT('Ctrl Pts',(4.18578397209565,-1.77611641099654,1.36526017271778));
#9203=CARTESIAN_POINT('Ctrl Pts',(4.20937507982432,-1.78802541175428,1.36695728561161));
#9204=CARTESIAN_POINT('Ctrl Pts',(4.22393451538618,-1.79515378624694,1.36800445482687));
#9205=CARTESIAN_POINT('Ctrl Pts',(4.3561196040296,-1.85788661773408,1.37751181064768));
#9206=CARTESIAN_POINT('Ctrl Pts',(4.47881396472044,-1.90202589465157,1.38636873105349));
#9207=CARTESIAN_POINT('Ctrl Pts',(4.69501908764519,-1.9566855956825,1.40186051902902));
#9208=CARTESIAN_POINT('Ctrl Pts',(4.78661181556632,-1.97314103692516,1.40838099060096));
#9209=CARTESIAN_POINT('Ctrl Pts',(4.93785018435352,-1.98952267502758,1.41883742924191));
#9210=CARTESIAN_POINT('Ctrl Pts',(4.99694223377235,-1.99327470206726,1.42284488258068));
#9211=CARTESIAN_POINT('Ctrl Pts',(5.06607120701462,-1.99458172255865,1.42737992105554));
#9212=CARTESIAN_POINT('Ctrl Pts',(5.07602474636018,-1.99469539646983,1.42802917776658));
#9213=CARTESIAN_POINT('Ctrl Pts',(5.09133097324201,-1.9947556181219,1.42902143887776));
#9214=CARTESIAN_POINT('Ctrl Pts',(5.09668312232891,-1.99475513585723,1.42936724897319));
#9215=CARTESIAN_POINT('Ctrl Pts',(5.10653401486099,-1.99471460043362,1.43000152344635));
#9216=CARTESIAN_POINT('Ctrl Pts',(5.11103261183845,-1.99468087033309,1.43029032170984));
#9217=CARTESIAN_POINT('Ctrl Pts',(5.1212001710391,-1.99457023479798,1.43094114414589));
#9218=CARTESIAN_POINT('Ctrl Pts',(5.12686893598415,-1.99448438102811,1.43130266905137));
#9219=CARTESIAN_POINT('Ctrl Pts',(5.14151042168657,-1.99420019434433,1.43223316704755));
#9220=CARTESIAN_POINT('Ctrl Pts',(5.15048242131318,-1.99396547034398,1.43280019289785));
#9221=CARTESIAN_POINT('Ctrl Pts',(5.20821349402025,-1.99206513865789,1.43643015098726));
#9222=CARTESIAN_POINT('Ctrl Pts',(5.25690345640201,-1.98867159853613,1.43940625996395));
#9223=CARTESIAN_POINT('Ctrl Pts',(5.31727077717616,-1.98223168462877,1.44304330572243));
#9224=CARTESIAN_POINT('Ctrl Pts',(5.32910608160495,-1.9808617667577,1.44375381807446));
#9225=CARTESIAN_POINT('Ctrl Pts',(5.38519704842794,-1.97385951536751,1.44711192356172));
#9226=CARTESIAN_POINT('Ctrl Pts',(5.42926927204036,-1.96684942625532,1.449723412437));
#9227=CARTESIAN_POINT('Ctrl Pts',(5.57133357311861,-1.93933825542637,1.45815151630666));
#9228=CARTESIAN_POINT('Ctrl Pts',(5.66802211307992,-1.91294141462753,1.46391060009365));
#9229=CARTESIAN_POINT('Ctrl Pts',(5.81198757905177,-1.86173363410699,1.47294461755129));
#9230=CARTESIAN_POINT('Ctrl Pts',(5.86093208789885,-1.84210638622161,1.47609981891295));
#9231=CARTESIAN_POINT('Ctrl Pts',(5.94059422850549,-1.8064352845173,1.48142245761996));
#9232=CARTESIAN_POINT('Ctrl Pts',(5.97177475682855,-1.79148840389108,1.48355509354209));
#9233=CARTESIAN_POINT('Ctrl Pts',(6.01364066590578,-1.77006380954949,1.48649407898795));
#9234=CARTESIAN_POINT('Ctrl Pts',(6.02467793756905,-1.76428444252867,1.48727618153017));
#9235=CARTESIAN_POINT('Ctrl Pts',(6.04310029392587,-1.75441708486186,1.4885942148425));
#9236=CARTESIAN_POINT('Ctrl Pts',(6.05051497491265,-1.75038487528702,1.48912817085473));
#9237=CARTESIAN_POINT('Ctrl Pts',(6.06507902621646,-1.74234455315991,1.49018394878059));
#9238=CARTESIAN_POINT('Ctrl Pts',(6.07222972927428,-1.73833918975679,1.49070566511893));
#9239=CARTESIAN_POINT('Ctrl Pts',(6.08790301718155,-1.72943268072501,1.49185667499705));
#9240=CARTESIAN_POINT('Ctrl Pts',(6.09641442112615,-1.72451239051302,1.49248664640925));
#9241=CARTESIAN_POINT('Ctrl Pts',(6.12614594634335,-1.70703062531568,1.49470476312118));
#9242=CARTESIAN_POINT('Ctrl Pts',(6.14716848577829,-1.69413918955307,1.49630477140708));
#9243=CARTESIAN_POINT('Ctrl Pts',(6.29419952297177,-1.6001821549085,1.50772621058428));
#9244=CARTESIAN_POINT('Ctrl Pts',(6.41093886649239,-1.50554892768608,1.51806815817619));
#9245=CARTESIAN_POINT('Ctrl Pts',(6.57572230825244,-1.3380120299621,1.53445124953916));
#9246=CARTESIAN_POINT('Ctrl Pts',(6.63152695485236,-1.27348747834946,1.54039579366242));
#9247=CARTESIAN_POINT('Ctrl Pts',(6.69864955264566,-1.18500634576088,1.54792809271975));
#9248=CARTESIAN_POINT('Ctrl Pts',(6.71386268603432,-1.16412197641763,1.54966408729761));
#9249=CARTESIAN_POINT('Ctrl Pts',(6.73859881770702,-1.12874010624515,1.55252866853464));
#9250=CARTESIAN_POINT('Ctrl Pts',(6.74834591273059,-1.11440377736808,1.55366902934093));
#9251=CARTESIAN_POINT('Ctrl Pts',(6.76159302367388,-1.09436250737981,1.55523326308586));
#9252=CARTESIAN_POINT('Ctrl Pts',(6.76525276526315,-1.08876476923418,1.55566698456514));
#9253=CARTESIAN_POINT('Ctrl Pts',(6.77140541001005,-1.07924988687978,1.55639869056438));
#9254=CARTESIAN_POINT('Ctrl Pts',(6.77391289650791,-1.07534228169564,1.55669762398468));
#9255=CARTESIAN_POINT('Ctrl Pts',(6.77869389049834,-1.06783415335291,1.55726895192234));
#9256=CARTESIAN_POINT('Ctrl Pts',(6.7809695338261,-1.06423507264721,1.55754149310483));
#9257=CARTESIAN_POINT('Ctrl Pts',(6.78638888899157,-1.05560293404586,1.55819205759979));
#9258=CARTESIAN_POINT('Ctrl Pts',(6.7895217228161,-1.0505630454944,1.55856937569974));
#9259=CARTESIAN_POINT('Ctrl Pts',(6.80072717755369,-1.03235576239227,1.55992373592898));
#9260=CARTESIAN_POINT('Ctrl Pts',(6.8086695410251,-1.01910830260573,1.56089274540703));
#9261=CARTESIAN_POINT('Ctrl Pts',(6.88317644899737,-0.891496690866052,1.57008446312052));
#9262=CARTESIAN_POINT('Ctrl Pts',(6.93836908015773,-0.770851691292086,1.57770181565766));
#9263=CARTESIAN_POINT('Ctrl Pts',(7.01224746100827,-0.554876411634715,1.5909546887953));
#9264=CARTESIAN_POINT('Ctrl Pts',(7.03670053823518,-0.462023181029013,1.59653848531472));
#9265=CARTESIAN_POINT('Ctrl Pts',(7.06068877438946,-0.334146345189335,1.60436519464526));
#9266=CARTESIAN_POINT('Ctrl Pts',(7.06613089193132,-0.300360091902404,1.60644484331557));
#9267=CARTESIAN_POINT('Ctrl Pts',(7.074040471966,-0.241676923280253,1.61008855110985));
#9268=CARTESIAN_POINT('Ctrl Pts',(7.0769136057831,-0.216842242814626,1.61164023631095));
#9269=CARTESIAN_POINT('Ctrl Pts',(7.08037599207359,-0.181030062406835,1.61389450174166));
#9270=CARTESIAN_POINT('Ctrl Pts',(7.08134250711003,-0.170090808104385,1.61458532230418));
#9271=CARTESIAN_POINT('Ctrl Pts',(7.08286965505979,-0.151010213238009,1.61579438933496));
#9272=CARTESIAN_POINT('Ctrl Pts',(7.08347075439294,-0.142872305672123,1.61631136111081));
#9273=CARTESIAN_POINT('Ctrl Pts',(7.08453639539062,-0.127131069107989,1.61731395542222));
#9274=CARTESIAN_POINT('Ctrl Pts',(7.08500735027745,-0.119528305453479,1.61779936839217));
#9275=CARTESIAN_POINT('Ctrl Pts',(7.08602425914138,-0.101432996149796,1.61895757754274));
#9276=CARTESIAN_POINT('Ctrl Pts',(7.08653087790814,-0.0909385517432676,
1.61963158787929));
#9277=CARTESIAN_POINT('Ctrl Pts',(7.08804761812425,-0.0533573980563534,
1.62205376793542));
#9278=CARTESIAN_POINT('Ctrl Pts',(7.08858849018638,-0.026255737248853,1.6238163996891));
#9279=CARTESIAN_POINT('Ctrl Pts',(7.08857697543068,0.000847466486712864,
1.62559580923438));
#9280=CARTESIAN_POINT('Origin',(5.09382715545311,0.,-6.77268258743872));
#9281=CARTESIAN_POINT('',(7.08857715545311,-4.46037469243765E-12,2.58513735103561));
#9282=CARTESIAN_POINT('',(7.08857715545311,3.31900585956301E-12,2.42843892255116));
#9283=CARTESIAN_POINT('',(7.08857715545311,8.3550772080578E-14,-6.77268258743872));
#9284=CARTESIAN_POINT('Ctrl Pts',(7.08857715545311,-4.46037469243765E-12,
2.58513735103561));
#9285=CARTESIAN_POINT('Ctrl Pts',(7.08857715545311,-0.000573719608935291,
2.58509735546341));
#9286=CARTESIAN_POINT('Ctrl Pts',(7.08857690794817,-0.00114744621619411,
2.5850573598134));
#9287=CARTESIAN_POINT('Ctrl Pts',(7.08848669686533,-0.105696979192502,2.5777690776299));
#9288=CARTESIAN_POINT('Ctrl Pts',(7.0802675235093,-0.209517219190061,2.57053655223239));
#9289=CARTESIAN_POINT('Ctrl Pts',(7.06143895699791,-0.328324287216113,2.56256261290403));
#9290=CARTESIAN_POINT('Ctrl Pts',(7.05869142175094,-0.344385677503512,2.56149132306044));
#9291=CARTESIAN_POINT('Ctrl Pts',(7.05453409991877,-0.367016247174239,2.55999303130221));
#9292=CARTESIAN_POINT('Ctrl Pts',(7.05328755290711,-0.373614241838874,2.55955754629472));
#9293=CARTESIAN_POINT('Ctrl Pts',(7.05113055116343,-0.384723481594506,2.55882672037121));
#9294=CARTESIAN_POINT('Ctrl Pts',(7.05023776523568,-0.38923806029832,2.55853040052529));
#9295=CARTESIAN_POINT('Ctrl Pts',(7.04837726867743,-0.398477955800474,2.55792536341682));
#9296=CARTESIAN_POINT('Ctrl Pts',(7.04740803185068,-0.40320291037588,2.55761673401851));
#9297=CARTESIAN_POINT('Ctrl Pts',(7.04487923356733,-0.415307403405743,2.55682793516335));
#9298=CARTESIAN_POINT('Ctrl Pts',(7.04329492154234,-0.422681776465845,2.55634914865173));
#9299=CARTESIAN_POINT('Ctrl Pts',(7.03654530011051,-0.45325329490668,2.55437095749661));
#9300=CARTESIAN_POINT('Ctrl Pts',(7.0310072414085,-0.476367264709833,2.5528913307589));
#9301=CARTESIAN_POINT('Ctrl Pts',(7.01507216005735,-0.537992550662144,2.54897599316184));
#9302=CARTESIAN_POINT('Ctrl Pts',(7.00393064837729,-0.576301476716016,2.54657321417147));
#9303=CARTESIAN_POINT('Ctrl Pts',(6.96302695915687,-0.702679160232502,2.53867397384158));
#9304=CARTESIAN_POINT('Ctrl Pts',(6.9282601985986,-0.78900125435267,2.5333190285089));
#9305=CARTESIAN_POINT('Ctrl Pts',(6.83068645720054,-0.989582874354239,2.52035413885513));
#9306=CARTESIAN_POINT('Ctrl Pts',(6.76247293712642,-1.10071311236439,2.51271335222203));
#9307=CARTESIAN_POINT('Ctrl Pts',(6.67414690560076,-1.21732482860213,2.50364148351342));
#9308=CARTESIAN_POINT('Ctrl Pts',(6.66420405110684,-1.23012464107434,2.50263055900577));
#9309=CARTESIAN_POINT('Ctrl Pts',(6.64774199701153,-1.25079198175833,2.500972511094));
#9310=CARTESIAN_POINT('Ctrl Pts',(6.64131625733275,-1.25873324806766,2.50032908520142));
#9311=CARTESIAN_POINT('Ctrl Pts',(6.62971568100584,-1.27284675782588,2.49917397885932));
#9312=CARTESIAN_POINT('Ctrl Pts',(6.62456388861122,-1.27903771738645,2.49866323334785));
#9313=CARTESIAN_POINT('Ctrl Pts',(6.61356524242223,-1.29209326901283,2.49757743981052));
#9314=CARTESIAN_POINT('Ctrl Pts',(6.6077090676292,-1.29894973744654,2.49700201819154));
#9315=CARTESIAN_POINT('Ctrl Pts',(6.59190776114077,-1.31719806337294,2.49545642952337));
#9316=CARTESIAN_POINT('Ctrl Pts',(6.58187939399751,-1.32851674955159,2.49448284069538));
#9317=CARTESIAN_POINT('Ctrl Pts',(6.53092557945538,-1.38472584832802,2.48957130630115));
#9318=CARTESIAN_POINT('Ctrl Pts',(6.48809716165513,-1.42784012020302,2.48555347849539));
#9319=CARTESIAN_POINT('Ctrl Pts',(6.34890602483313,-1.55571872228121,2.47281711541159));
#9320=CARTESIAN_POINT('Ctrl Pts',(6.24629634363261,-1.63318451950424,2.46384730766719));
#9321=CARTESIAN_POINT('Ctrl Pts',(6.05475870269731,-1.7506976620583,2.44820626857386));
#9322=CARTESIAN_POINT('Ctrl Pts',(5.9689803915567,-1.79511641088729,2.44154495567969));
#9323=CARTESIAN_POINT('Ctrl Pts',(5.87025165707929,-1.83747448335675,2.43448380087461));
#9324=CARTESIAN_POINT('Ctrl Pts',(5.86015226473081,-1.84170934828089,2.43376834075116));
#9325=CARTESIAN_POINT('Ctrl Pts',(5.84480627547875,-1.84799611670255,2.4326921022895));
#9326=CARTESIAN_POINT('Ctrl Pts',(5.8395852131858,-1.85010924198218,2.43232783858872));
#9327=CARTESIAN_POINT('Ctrl Pts',(5.83017962902903,-1.85386968784311,2.43167512630488));
#9328=CARTESIAN_POINT('Ctrl Pts',(5.8259984441861,-1.85552499039581,2.43138621184632));
#9329=CARTESIAN_POINT('Ctrl Pts',(5.81680014102241,-1.85913060269655,2.43075335303533));
#9330=CARTESIAN_POINT('Ctrl Pts',(5.81178071873145,-1.86107474819246,2.43040977566365));
#9331=CARTESIAN_POINT('Ctrl Pts',(5.79732221245928,-1.86660768254147,2.42942500326855));
#9332=CARTESIAN_POINT('Ctrl Pts',(5.78786350363949,-1.87014520646106,2.42878676278455));
#9333=CARTESIAN_POINT('Ctrl Pts',(5.71906671136189,-1.89528111443893,2.42418514161373));
#9334=CARTESIAN_POINT('Ctrl Pts',(5.65875314684194,-1.91412521714479,2.42036849887057));
#9335=CARTESIAN_POINT('Ctrl Pts',(5.47119934078904,-1.96308295014561,2.40887262654789));
#9336=CARTESIAN_POINT('Ctrl Pts',(5.34181735192287,-1.98358464360659,2.40143621479675));
#9337=CARTESIAN_POINT('Ctrl Pts',(5.12233882242346,-1.99653855467507,2.38850345739401));
#9338=CARTESIAN_POINT('Ctrl Pts',(5.03308044899175,-1.99581713805682,2.38316097668914));
#9339=CARTESIAN_POINT('Ctrl Pts',(4.92855467919921,-1.98795321724429,2.37665573846926));
#9340=CARTESIAN_POINT('Ctrl Pts',(4.91294759723048,-1.98659395675224,2.37567805316845));
#9341=CARTESIAN_POINT('Ctrl Pts',(4.88735593673216,-1.98406104476503,2.37406370505062));
#9342=CARTESIAN_POINT('Ctrl Pts',(4.87736116652256,-1.98299547735774,2.37343041631689));
#9343=CARTESIAN_POINT('Ctrl Pts',(4.85938873959165,-1.98094189846097,2.37228640864415));
#9344=CARTESIAN_POINT('Ctrl Pts',(4.85140814392135,-1.97998110992984,2.37177655289128));
#9345=CARTESIAN_POINT('Ctrl Pts',(4.83438567337417,-1.97782730709113,2.37068496388786));
#9346=CARTESIAN_POINT('Ctrl Pts',(4.82534576313014,-1.97662046856116,2.37010280736916));
#9347=CARTESIAN_POINT('Ctrl Pts',(4.80087328572113,-1.97318238686339,2.36851999043552));
#9348=CARTESIAN_POINT('Ctrl Pts',(4.78545834529982,-1.97083214803336,2.36751561578986));
#9349=CARTESIAN_POINT('Ctrl Pts',(4.70354291555591,-1.95735836392356,2.36213782085551));
#9350=CARTESIAN_POINT('Ctrl Pts',(4.63761780627047,-1.9430503921944,2.35766501998584));
#9351=CARTESIAN_POINT('Ctrl Pts',(4.41527893604923,-1.8828560118263,2.34207818634153));
#9352=CARTESIAN_POINT('Ctrl Pts',(4.26382249444988,-1.82116901288849,2.3305323609567));
#9353=CARTESIAN_POINT('Ctrl Pts',(4.07304642713492,-1.71467892953277,2.31553700698514));
#9354=CARTESIAN_POINT('Ctrl Pts',(4.02566046045887,-1.68556763416592,2.31177793981085));
#9355=CARTESIAN_POINT('Ctrl Pts',(3.97183298482576,-1.64931597028355,2.30751837738337));
#9356=CARTESIAN_POINT('Ctrl Pts',(3.96415390008503,-1.64406582374947,2.30691097775461));
#9357=CARTESIAN_POINT('Ctrl Pts',(3.95177306966717,-1.63547341670854,2.30593248898806));
#9358=CARTESIAN_POINT('Ctrl Pts',(3.94704870530792,-1.63216421352643,2.30555930339028));
#9359=CARTESIAN_POINT('Ctrl Pts',(3.93865978803633,-1.62623375135579,2.30489708968436));
#9360=CARTESIAN_POINT('Ctrl Pts',(3.93498970032776,-1.62362052671022,2.30460753330765));
#9361=CARTESIAN_POINT('Ctrl Pts',(3.92704052122951,-1.61791976140729,2.30398072729817));
#9362=CARTESIAN_POINT('Ctrl Pts',(3.92276481898809,-1.61482767186317,2.30364379373602));
#9363=CARTESIAN_POINT('Ctrl Pts',(3.91074390443229,-1.60606156922683,2.30269696796216));
#9364=CARTESIAN_POINT('Ctrl Pts',(3.9030271914508,-1.60034846125837,2.30208968656104));
#9365=CARTESIAN_POINT('Ctrl Pts',(3.85458379453603,-1.56393873265297,2.29827856599865));
#9366=CARTESIAN_POINT('Ctrl Pts',(3.81500190856164,-1.53174261143752,2.29516995696243));
#9367=CARTESIAN_POINT('Ctrl Pts',(3.66307971639062,-1.39816886611485,2.28306543251376));
#9368=CARTESIAN_POINT('Ctrl Pts',(3.56119267277551,-1.28567172073096,2.27451550732722));
#9369=CARTESIAN_POINT('Ctrl Pts',(3.42513065256275,-1.09600338927351,2.26073953776204));
#9370=CARTESIAN_POINT('Ctrl Pts',(3.38143397847467,-1.02639109805841,2.25580258936769));
#9371=CARTESIAN_POINT('Ctrl Pts',(3.33478690212518,-0.940766759608716,2.24974907106564));
#9372=CARTESIAN_POINT('Ctrl Pts',(3.32757675490616,-0.927159215387747,2.24878774231288));
#9373=CARTESIAN_POINT('Ctrl Pts',(3.31595931342593,-0.904606491047544,2.24719492621851));
#9374=CARTESIAN_POINT('Ctrl Pts',(3.31146017417314,-0.895709163519963,2.24656665863416));
#9375=CARTESIAN_POINT('Ctrl Pts',(3.30345749830837,-0.879584310686831,2.24542806908599));
#9376=CARTESIAN_POINT('Ctrl Pts',(3.29993053373128,-0.872368601185418,2.24491857476578));
#9377=CARTESIAN_POINT('Ctrl Pts',(3.29246765359788,-0.856863877629572,2.24382373283922));
#9378=CARTESIAN_POINT('Ctrl Pts',(3.28854517631425,-0.848568636518223,2.24323793562943));
#9379=CARTESIAN_POINT('Ctrl Pts',(3.27800430532759,-0.825872939481146,2.24163492871836));
#9380=CARTESIAN_POINT('Ctrl Pts',(3.27150018904831,-0.811420445118591,2.24061384193927));
#9381=CARTESIAN_POINT('Ctrl Pts',(3.23661781731842,-0.731374587668034,2.23495557412002));
#9382=CARTESIAN_POINT('Ctrl Pts',(3.21161145830348,-0.664377380568385,2.23020614307114));
#9383=CARTESIAN_POINT('Ctrl Pts',(3.13074538170396,-0.406180303545514,2.21185322607464));
#9384=CARTESIAN_POINT('Ctrl Pts',(3.10002531576418,-0.208360686616569,2.19756165325407));
#9385=CARTESIAN_POINT('Ctrl Pts',(3.09900330149986,0.0112260014355715,2.18292509024981));
#9386=CARTESIAN_POINT('Ctrl Pts',(3.0992241727132,0.031737221718923,2.18157112332532));
#9387=CARTESIAN_POINT('Ctrl Pts',(3.09995457959188,0.0596165245670277,2.17975195303466));
#9388=CARTESIAN_POINT('Ctrl Pts',(3.10018868346224,0.0669897446255821,2.17927285375449));
#9389=CARTESIAN_POINT('Ctrl Pts',(3.10062439742731,0.0786696425545959,2.17851728627743));
#9390=CARTESIAN_POINT('Ctrl Pts',(3.1007990729447,0.0829771682582987,2.17823936138324));
#9391=CARTESIAN_POINT('Ctrl Pts',(3.1011890859604,0.0918818019196473,2.17766637784101));
#9392=CARTESIAN_POINT('Ctrl Pts',(3.10140636869013,0.09647875615187,2.17737144083562));
#9393=CARTESIAN_POINT('Ctrl Pts',(3.10196736203407,0.107535936348531,2.17666401576725));
#9394=CARTESIAN_POINT('Ctrl Pts',(3.10232659874164,0.113995393095449,2.1762523839259));
#9395=CARTESIAN_POINT('Ctrl Pts',(3.10367987786609,0.136365324376934,2.17483216710323));
#9396=CARTESIAN_POINT('Ctrl Pts',(3.10483324373412,0.152266033455754,2.17383198872394));
#9397=CARTESIAN_POINT('Ctrl Pts',(3.11300310290739,0.248838426580558,2.16780490114641));
#9398=CARTESIAN_POINT('Ctrl Pts',(3.12473665448713,0.329044153011078,2.16299934898406));
#9399=CARTESIAN_POINT('Ctrl Pts',(3.14335931388687,0.418093792678475,2.15767544688168));
#9400=CARTESIAN_POINT('Ctrl Pts',(3.14547613124226,0.427849867520452,2.15709235779567));
#9401=CARTESIAN_POINT('Ctrl Pts',(3.18494951883587,0.603406034773257,2.14659730859552));
#9402=CARTESIAN_POINT('Ctrl Pts',(3.2432656605022,0.763760633117595,2.13689461735431));
#9403=CARTESIAN_POINT('Ctrl Pts',(3.33287164656392,0.937395842272723,2.12488322039284));
#9404=CARTESIAN_POINT('Ctrl Pts',(3.34497421363898,0.959785687809845,2.12330493213328));
#9405=CARTESIAN_POINT('Ctrl Pts',(3.36253858954976,0.990844171914539,2.12107095219737));
#9406=CARTESIAN_POINT('Ctrl Pts',(3.36764415169489,0.999712209973037,2.12042789487105));
#9407=CARTESIAN_POINT('Ctrl Pts',(3.37663378895675,1.0150524487599,2.11930625250237));
#9408=CARTESIAN_POINT('Ctrl Pts',(3.38048681988609,1.02154266854423,2.11882879059802));
#9409=CARTESIAN_POINT('Ctrl Pts',(3.38860722345512,1.03504586217697,2.11782922766435));
#9410=CARTESIAN_POINT('Ctrl Pts',(3.39288123180449,1.04205466018784,2.11730689195173));
#9411=CARTESIAN_POINT('Ctrl Pts',(3.40312522985354,1.05862248937828,2.11606368430328));
#9412=CARTESIAN_POINT('Ctrl Pts',(3.40913315713055,1.06815761929625,2.11534143147613));
#9413=CARTESIAN_POINT('Ctrl Pts',(3.42963834521986,1.10009786666879,2.11289885138197));
#9414=CARTESIAN_POINT('Ctrl Pts',(3.44450380888544,1.12226204464093,2.11116496894654));
#9415=CARTESIAN_POINT('Ctrl Pts',(3.48117831717035,1.17464011011243,2.10697109318897));
#9416=CARTESIAN_POINT('Ctrl Pts',(3.50339742555177,1.2045532964318,2.10449634357187));
#9417=CARTESIAN_POINT('Ctrl Pts',(3.63306096163795,1.36927108110008,2.09041226106833));
#9418=CARTESIAN_POINT('Ctrl Pts',(3.75678498732379,1.49031695341213,2.0781989271691));
#9419=CARTESIAN_POINT('Ctrl Pts',(3.90465801102348,1.60158241139967,2.06547736257107));
#9420=CARTESIAN_POINT('Ctrl Pts',(3.91489880817895,1.60913561800787,2.06460537013808));
#9421=CARTESIAN_POINT('Ctrl Pts',(3.96316921555431,1.6440297755906,2.06053945428449));
#9422=CARTESIAN_POINT('Ctrl Pts',(4.00208523368305,1.67012623195947,2.05738841463674));
#9423=CARTESIAN_POINT('Ctrl Pts',(4.04942704916241,1.69951014410303,2.05373447625333));
#9424=CARTESIAN_POINT('Ctrl Pts',(4.05699818960729,1.7041396698787,2.05315541968772));
#9425=CARTESIAN_POINT('Ctrl Pts',(4.06943032267463,1.71162802232842,2.05221353495416));
#9426=CARTESIAN_POINT('Ctrl Pts',(4.07427289377631,1.71451697781279,2.05184885220961));
#9427=CARTESIAN_POINT('Ctrl Pts',(4.08299960641099,1.71967306587462,2.05119570073469));
#9428=CARTESIAN_POINT('Ctrl Pts',(4.08687920534985,1.72194762242423,2.05090676318343));
#9429=CARTESIAN_POINT('Ctrl Pts',(4.09541458688559,1.72691309011338,2.05027422045819));
#9430=CARTESIAN_POINT('Ctrl Pts',(4.10007356496417,1.72959830044494,2.04993097971947));
#9431=CARTESIAN_POINT('Ctrl Pts',(4.11349072492165,1.7372591937295,2.04894814375579));
#9432=CARTESIAN_POINT('Ctrl Pts',(4.12227596127596,1.74218750722841,2.04831148504797));
#9433=CARTESIAN_POINT('Ctrl Pts',(4.1857627619635,1.77717253870128,2.0437571747549));
#9434=CARTESIAN_POINT('Ctrl Pts',(4.24181691384659,1.80471698307592,2.03998284885645));
#9435=CARTESIAN_POINT('Ctrl Pts',(4.38286813413549,1.86598787435336,2.03085801275357));
#9436=CARTESIAN_POINT('Ctrl Pts',(4.46906499874804,1.89658829808944,2.0255953723878));
#9437=CARTESIAN_POINT('Ctrl Pts',(4.68053928028881,1.95567337128066,2.01282934090382));
#9438=CARTESIAN_POINT('Ctrl Pts',(4.80704042443649,1.97818409794303,2.00529278787818));
#9439=CARTESIAN_POINT('Ctrl Pts',(4.95099119604566,1.98969563311818,1.99633749199456));
#9440=CARTESIAN_POINT('Ctrl Pts',(4.9671796843881,1.99079160579118,1.99532548432424));
#9441=CARTESIAN_POINT('Ctrl Pts',(4.99358439491918,1.99225586059443,1.99366601371448));
#9442=CARTESIAN_POINT('Ctrl Pts',(5.00379345406848,1.99274332303448,1.9930222590483));
#9443=CARTESIAN_POINT('Ctrl Pts',(5.02205392319621,1.99347461586095,1.99186678946396));
#9444=CARTESIAN_POINT('Ctrl Pts',(5.03010396839057,1.9937481769985,1.99135601181253));
#9445=CARTESIAN_POINT('Ctrl Pts',(5.04716569491351,1.994224541048,1.99027039036127));
#9446=CARTESIAN_POINT('Ctrl Pts',(5.0561775127827,1.99441503003834,1.98969517450829));
#9447=CARTESIAN_POINT('Ctrl Pts',(5.08029634194139,1.99476131965319,1.98815072127568));
#9448=CARTESIAN_POINT('Ctrl Pts',(5.09540411274227,1.99480658153842,1.98717807087926));
#9449=CARTESIAN_POINT('Ctrl Pts',(5.1710639023163,1.99417376521607,1.98227985532387));
#9450=CARTESIAN_POINT('Ctrl Pts',(5.23155677862222,1.99091029114466,1.9782749306638));
#9451=CARTESIAN_POINT('Ctrl Pts',(5.41865194796816,1.97224928255046,1.96560703263229));
#9452=CARTESIAN_POINT('Ctrl Pts',(5.54398486227364,1.94746750731485,1.95669629285439));
#9453=CARTESIAN_POINT('Ctrl Pts',(5.75953130068192,1.88291845464412,1.94103254837983));
#9454=CARTESIAN_POINT('Ctrl Pts',(5.85081543380803,1.84811177632074,1.93429255838266));
#9455=CARTESIAN_POINT('Ctrl Pts',(5.94907212931743,1.80213832006741,1.9271630749843));
#9456=CARTESIAN_POINT('Ctrl Pts',(5.95891196845178,1.79743560916145,1.92645062905898));
#9457=CARTESIAN_POINT('Ctrl Pts',(5.97376597049668,1.79018626352909,1.92537801233651));
#9458=CARTESIAN_POINT('Ctrl Pts',(5.9788085611389,1.7876988252523,1.9250143901954));
#9459=CARTESIAN_POINT('Ctrl Pts',(5.98786477122631,1.7831838163046,1.92436234884548));
#9460=CARTESIAN_POINT('Ctrl Pts',(5.99188209244253,1.78116397686074,1.92407346827394));
#9461=CARTESIAN_POINT('Ctrl Pts',(5.99591029478403,1.77912157331222,1.92378417215569));
#9462=CARTESIAN_POINT('Ctrl Pts',(5.99592790994126,1.77911264163964,1.92378290708299));
#9463=CARTESIAN_POINT('Ctrl Pts',(5.99596290533334,1.77909489675728,1.92378039382278));
#9464=CARTESIAN_POINT('Ctrl Pts',(5.99598028551632,1.77908608358249,1.92377914563881));
#9465=CARTESIAN_POINT('Ctrl Pts',(5.99601481435387,1.7790685740007,1.92377666591178));
#9466=CARTESIAN_POINT('Ctrl Pts',(5.99603196306253,1.77905987757471,1.92377543436464));
#9467=CARTESIAN_POINT('Ctrl Pts',(5.99606603252794,1.77904259970207,1.92377298765389));
#9468=CARTESIAN_POINT('Ctrl Pts',(5.99608295328133,1.77903401826534,1.92377177249034));
#9469=CARTESIAN_POINT('Ctrl Pts',(5.99611657020711,1.77901696868618,1.92376935830415));
#9470=CARTESIAN_POINT('Ctrl Pts',(5.99613326639525,1.77900850054376,1.92376815928021));
#9471=CARTESIAN_POINT('Ctrl Pts',(5.996166437788,1.77899167575248,1.92376577711439));
#9472=CARTESIAN_POINT('Ctrl Pts',(5.99618291289591,1.77898331916044,1.92376459397928));
#9473=CARTESIAN_POINT('Ctrl Pts',(5.99621564508729,1.77896671599219,1.92376224337815));
#9474=CARTESIAN_POINT('Ctrl Pts',(5.9962319022911,1.7789584693625,1.92376107590331));
#9475=CARTESIAN_POINT('Ctrl Pts',(5.99626420221967,1.77894208434307,1.92375875636761));
#9476=CARTESIAN_POINT('Ctrl Pts',(5.99628024485766,1.77893394600468,1.92375760431284));
#9477=CARTESIAN_POINT('Ctrl Pts',(5.99631211889415,1.77891777594637,1.92375531538416));
#9478=CARTESIAN_POINT('Ctrl Pts',(5.99632795023058,1.77890974426506,1.92375417851457));
#9479=CARTESIAN_POINT('Ctrl Pts',(5.99635940445583,1.7788937861258,1.92375191975534));
#9480=CARTESIAN_POINT('Ctrl Pts',(5.99637502748337,1.77888585960443,1.92375079785558));
#9481=CARTESIAN_POINT('Ctrl Pts',(5.9964060686142,1.77887011001812,1.92374856878256));
#9482=CARTESIAN_POINT('Ctrl Pts',(5.9964214865825,1.77886228702843,1.92374746161885));
#9483=CARTESIAN_POINT('Ctrl Pts',(5.9964521204165,1.77884674309396,1.92374526181487));
#9484=CARTESIAN_POINT('Ctrl Pts',(5.99646733632971,1.77883902213162,1.92374416917106));
#9485=CARTESIAN_POINT('Ctrl Pts',(5.99649756890053,1.77882368082681,1.92374199820201));
#9486=CARTESIAN_POINT('Ctrl Pts',(5.99651258566599,1.77881606043598,1.9237409198689));
#9487=CARTESIAN_POINT('Ctrl Pts',(5.99654242319735,1.77880091864089,1.92373877728707));
#9488=CARTESIAN_POINT('Ctrl Pts',(5.99655724387355,1.77879339728835,1.92373771304465));
#9489=CARTESIAN_POINT('Ctrl Pts',(5.99658669190428,1.77877845222938,1.9237355984515));
#9490=CARTESIAN_POINT('Ctrl Pts',(5.9966013193187,1.77877102849857,1.92373454809635));
#9491=CARTESIAN_POINT('Ctrl Pts',(5.99663038372448,1.77875627722994,1.92373246106921));
#9492=CARTESIAN_POINT('Ctrl Pts',(5.99664482072874,1.77874894969143,1.92373142439618));
#9493=CARTESIAN_POINT('Ctrl Pts',(5.99667350712362,1.77873438939899,1.92372936453119));
#9494=CARTESIAN_POINT('Ctrl Pts',(5.99668775650225,1.77872715665685,1.92372834133997));
#9495=CARTESIAN_POINT('Ctrl Pts',(5.99671607052577,1.77871278451236,1.92372630823145));
#9496=CARTESIAN_POINT('Ctrl Pts',(5.99673013509837,1.77870564515225,1.92372529831922));
#9497=CARTESIAN_POINT('Ctrl Pts',(5.99675808198086,1.77869145853409,1.9237232915909));
#9498=CARTESIAN_POINT('Ctrl Pts',(5.99677196436856,1.77868441124192,1.92372229476911));
#9499=CARTESIAN_POINT('Ctrl Pts',(5.99679954967086,1.77867040735962,1.92372031402101));
#9500=CARTESIAN_POINT('Ctrl Pts',(5.99681325256722,1.77866345078398,1.9237193300959));
#9501=CARTESIAN_POINT('Ctrl Pts',(5.99684048147304,1.77864962703747,1.92371737495515));
#9502=CARTESIAN_POINT('Ctrl Pts',(5.99685400747479,1.77864275987561,1.92371640373995));
#9503=CARTESIAN_POINT('Ctrl Pts',(5.9968808852602,1.77862911361693,1.92371447382707));
#9504=CARTESIAN_POINT('Ctrl Pts',(5.99689423699637,1.77862233454918,1.92371351513269));
#9505=CARTESIAN_POINT('Ctrl Pts',(5.99692076856352,1.77860886331922,1.92371161009505));
#9506=CARTESIAN_POINT('Ctrl Pts',(5.99693394848435,1.77860217111622,1.92371066374524));
#9507=CARTESIAN_POINT('Ctrl Pts',(5.99696013901644,1.77858887231224,1.92370878321007));
#9508=CARTESIAN_POINT('Ctrl Pts',(5.99697314962433,1.77858226571767,1.92370784902485));
#9509=CARTESIAN_POINT('Ctrl Pts',(5.99699900403606,1.77856913687232,1.92370599263868));
#9510=CARTESIAN_POINT('Ctrl Pts',(5.99701184779509,1.77856261464887,1.92370507044084));
#9511=CARTESIAN_POINT('Ctrl Pts',(5.99703737090359,1.77854965334346,1.92370323785721));
#9512=CARTESIAN_POINT('Ctrl Pts',(5.99705005022729,1.77854321427903,1.92370232747318));
#9513=CARTESIAN_POINT('Ctrl Pts',(5.99707609729567,1.77852998619227,1.92370045728329));
#9514=CARTESIAN_POINT('Ctrl Pts',(5.99708946505468,1.77852319714364,1.92369949747681));
#9515=CARTESIAN_POINT('Ctrl Pts',(6.00199921851898,1.77602962392392,1.92334697811698));
#9516=CARTESIAN_POINT('Ctrl Pts',(6.00688538425036,1.7735225946533,1.92299668092783));
#9517=CARTESIAN_POINT('Ctrl Pts',(6.02129243550442,1.76605519918921,1.92196519684877));
#9518=CARTESIAN_POINT('Ctrl Pts',(6.03078387972458,1.76103802376924,1.92128743908224));
#9519=CARTESIAN_POINT('Ctrl Pts',(6.05257600510387,1.74929264589705,1.91973439398466));
#9520=CARTESIAN_POINT('Ctrl Pts',(6.06484731532463,1.7425108294251,1.91886214259767));
#9521=CARTESIAN_POINT('Ctrl Pts',(6.20487975197366,1.66318229925407,1.90892301870525));
#9522=CARTESIAN_POINT('Ctrl Pts',(6.32433823506054,1.57685362073657,1.90055841904611));
#9523=CARTESIAN_POINT('Ctrl Pts',(6.52195257802618,1.39778997876207,1.88502988379646));
#9524=CARTESIAN_POINT('Ctrl Pts',(6.6032363949858,1.30959431306031,1.87796376276932));
#9525=CARTESIAN_POINT('Ctrl Pts',(6.68604408267547,1.20172312826808,1.86953146912589));
#9526=CARTESIAN_POINT('Ctrl Pts',(6.69580987867472,1.18867344144245,1.86851494178726));
#9527=CARTESIAN_POINT('Ctrl Pts',(6.71145056117932,1.16723048110878,1.86684953568607));
#9528=CARTESIAN_POINT('Ctrl Pts',(6.71742275809633,1.15890887976216,1.86620441025367));
#9529=CARTESIAN_POINT('Ctrl Pts',(6.72797773045962,1.14395995458449,1.86504742410944));
#9530=CARTESIAN_POINT('Ctrl Pts',(6.73258497235119,1.1373501193316,1.8645365103754));
#9531=CARTESIAN_POINT('Ctrl Pts',(6.7422540649355,1.12329751257589,1.86345159632207));
#9532=CARTESIAN_POINT('Ctrl Pts',(6.74730582398839,1.11584804789945,1.86287723032537));
#9533=CARTESIAN_POINT('Ctrl Pts',(6.76066844719456,1.0958531497276,1.86133746569626));
#9534=CARTESIAN_POINT('Ctrl Pts',(6.76888792355924,1.08324762647418,1.86036869013031));
#9535=CARTESIAN_POINT('Ctrl Pts',(6.80904631599262,1.0201099637075,1.85552495940285));
#9536=CARTESIAN_POINT('Ctrl Pts',(6.83884210141049,0.968257562903548,1.85157276357886));
#9537=CARTESIAN_POINT('Ctrl Pts',(6.93899042394852,0.774293234319279,1.83687300423142));
#9538=CARTESIAN_POINT('Ctrl Pts',(6.99466232358782,0.625277353532774,1.82568225382217));
#9539=CARTESIAN_POINT('Ctrl Pts',(7.04087087708038,0.435229225678174,1.8121777195781));
#9540=CARTESIAN_POINT('Ctrl Pts',(7.04862847668504,0.39894334917576,1.80963558122238));
#9541=CARTESIAN_POINT('Ctrl Pts',(7.06154546629564,0.329039949266209,1.80483084415302));
#9542=CARTESIAN_POINT('Ctrl Pts',(7.066866353894,0.295464524088075,1.80256344834977));
#9543=CARTESIAN_POINT('Ctrl Pts',(7.0724832565604,0.253032086363658,1.79976177479462));
#9544=CARTESIAN_POINT('Ctrl Pts',(7.07358169352563,0.244289130020815,1.79918790561487));
#9545=CARTESIAN_POINT('Ctrl Pts',(7.07523088605998,0.230420036124329,1.7982832545103));
#9546=CARTESIAN_POINT('Ctrl Pts',(7.07581975052471,0.225298671204406,1.79795042589789));
#9547=CARTESIAN_POINT('Ctrl Pts',(7.0768764662282,0.215783495205807,1.79733440074816));
#9548=CARTESIAN_POINT('Ctrl Pts',(7.07734956854153,0.211390451495288,1.79705092671119));
#9549=CARTESIAN_POINT('Ctrl Pts',(7.07826738932372,0.202593464129223,1.79648511417043));
#9550=CARTESIAN_POINT('Ctrl Pts',(7.07871204618241,0.198189618732565,1.79620278115165));
#9551=CARTESIAN_POINT('Ctrl Pts',(7.07970451006276,0.188021852125648,1.79555296146577));
#9552=CARTESIAN_POINT('Ctrl Pts',(7.08024189093331,0.182256920403751,1.79518603892067));
#9553=CARTESIAN_POINT('Ctrl Pts',(7.08156992230612,0.167305893814251,1.79423817719713));
#9554=CARTESIAN_POINT('Ctrl Pts',(7.08232200875522,0.158116396954387,1.7936592317831));
#9555=CARTESIAN_POINT('Ctrl Pts',(7.08668811633936,0.0997972873341222,1.790006340589));
#9556=CARTESIAN_POINT('Ctrl Pts',(7.08854511044351,0.0505497621316073,1.78701713277168));
#9557=CARTESIAN_POINT('Ctrl Pts',(7.08857674428943,0.0012807565402712,1.78407775478297));
#9558=CARTESIAN_POINT('Ctrl Pts',(7.08857697543068,0.000847466486718941,
1.62559580923438));
#9559=CARTESIAN_POINT('Ctrl Pts',(7.0885186478675,0.13813772867541,1.6346093415605));
#9560=CARTESIAN_POINT('Ctrl Pts',(7.0742870217937,0.275032186647476,1.64406239390923));
#9561=CARTESIAN_POINT('Ctrl Pts',(7.02136448036863,0.527429007289867,1.66203452124581));
#9562=CARTESIAN_POINT('Ctrl Pts',(6.98594482700694,0.643022062967079,1.67048117357389));
#9563=CARTESIAN_POINT('Ctrl Pts',(6.9342345859718,0.769535207729763,1.67953767511746));
#9564=CARTESIAN_POINT('Ctrl Pts',(6.92799797735193,0.784283992593526,1.6805901674866));
#9565=CARTESIAN_POINT('Ctrl Pts',(6.919177355224,0.80446275310561,1.68202402410278));
#9566=CARTESIAN_POINT('Ctrl Pts',(6.91674558763128,0.809958063607057,1.68241387742721));
#9567=CARTESIAN_POINT('Ctrl Pts',(6.91254014766623,0.819346639764221,1.68307874378594));
#9568=CARTESIAN_POINT('Ctrl Pts',(6.91077873336726,0.823245302745461,1.68335448156896));
#9569=CARTESIAN_POINT('Ctrl Pts',(6.90708649128147,0.831348028823863,1.68392677710576));
#9570=CARTESIAN_POINT('Ctrl Pts',(6.90515356693689,0.835551072967431,1.68422319329436));
#9571=CARTESIAN_POINT('Ctrl Pts',(6.9004273923886,0.84573442154125,1.68494036848763));
#9572=CARTESIAN_POINT('Ctrl Pts',(6.89761901556641,0.851707729337802,1.68536021027999));
#9573=CARTESIAN_POINT('Ctrl Pts',(6.88757187304332,0.87280500605721,1.68684047699931));
#9574=CARTESIAN_POINT('Ctrl Pts',(6.88017189635716,0.887852015034895,1.68789151483874));
#9575=CARTESIAN_POINT('Ctrl Pts',(6.86139847977402,0.924840444295633,1.69046780629416));
#9576=CARTESIAN_POINT('Ctrl Pts',(6.84980512988548,0.94666768205827,1.69198160424515));
#9577=CARTESIAN_POINT('Ctrl Pts',(6.79950021875832,1.03727298462176,1.6982614381187));
#9578=CARTESIAN_POINT('Ctrl Pts',(6.75712774792099,1.10394243196616,1.70287436838431));
#9579=CARTESIAN_POINT('Ctrl Pts',(6.61786958130527,1.29675573459564,1.7167033108207));
#9580=CARTESIAN_POINT('Ctrl Pts',(6.50977763753097,1.41398692410837,1.7258447971311));
#9581=CARTESIAN_POINT('Ctrl Pts',(6.37244731286415,1.53121767622822,1.73696642571239));
#9582=CARTESIAN_POINT('Ctrl Pts',(6.35573939200201,1.54501602901815,1.73831117597603));
#9583=CARTESIAN_POINT('Ctrl Pts',(6.3296140732491,1.56588530796427,1.74040318463983));
#9584=CARTESIAN_POINT('Ctrl Pts',(6.32035296875346,1.57314987326505,1.74114275003695));
#9585=CARTESIAN_POINT('Ctrl Pts',(6.30451665109693,1.58534730035983,1.74240426414843));
#9586=CARTESIAN_POINT('Ctrl Pts',(6.29797417678056,1.59032231493196,1.7429245419122));
#9587=CARTESIAN_POINT('Ctrl Pts',(6.28467472438383,1.60030633777818,1.74398045916568));
#9588=CARTESIAN_POINT('Ctrl Pts',(6.27791644277611,1.60531332245671,1.74451616273635));
#9589=CARTESIAN_POINT('Ctrl Pts',(6.26118376939706,1.61754684860185,1.74584047196962));
#9590=CARTESIAN_POINT('Ctrl Pts',(6.25117382988796,1.62472395670157,1.74663095544629));
#9591=CARTESIAN_POINT('Ctrl Pts',(6.21365723330576,1.65110065833184,1.74958760390165));
#9592=CARTESIAN_POINT('Ctrl Pts',(6.18573541055629,1.66969725532199,1.75177628304859));
#9593=CARTESIAN_POINT('Ctrl Pts',(6.11457383764612,1.71454408695528,1.7573285197755));
#9594=CARTESIAN_POINT('Ctrl Pts',(6.0707815794354,1.73986912475829,1.76072268879818));
#9595=CARTESIAN_POINT('Ctrl Pts',(5.92261414724874,1.81819574979078,1.77212382054799));
#9596=CARTESIAN_POINT('Ctrl Pts',(5.81454439380532,1.86367547879841,1.78032425845484));
#9597=CARTESIAN_POINT('Ctrl Pts',(5.61737875461597,1.92692241665534,1.79471975571545));
#9598=CARTESIAN_POINT('Ctrl Pts',(5.52985919385639,1.94859337517318,1.80091974923904));
#9599=CARTESIAN_POINT('Ctrl Pts',(5.4303822768349,1.96618364594338,1.80755949173854));
#9600=CARTESIAN_POINT('Ctrl Pts',(5.41958310089061,1.968001665715,1.80827493851534));
#9601=CARTESIAN_POINT('Ctrl Pts',(5.40320753263651,1.97061997041465,1.80935116098224));
#9602=CARTESIAN_POINT('Ctrl Pts',(5.39764202753576,1.97148568621826,1.80971542188362));
#9603=CARTESIAN_POINT('Ctrl Pts',(5.38762647144156,1.97300018924479,1.81036813128623));
#9604=CARTESIAN_POINT('Ctrl Pts',(5.38317784757979,1.9736575090386,1.81065704564296));
#9605=CARTESIAN_POINT('Ctrl Pts',(5.37339936030238,1.97506858575359,1.81128990674961));
#9606=CARTESIAN_POINT('Ctrl Pts',(5.36806866058057,1.9758158149631,1.81163348650117));
#9607=CARTESIAN_POINT('Ctrl Pts',(5.35272874880679,1.97790280455986,1.81261827241101));
#9608=CARTESIAN_POINT('Ctrl Pts',(5.34271213002741,1.97918817166451,1.81325652390456));
#9609=CARTESIAN_POINT('Ctrl Pts',(5.26998901477252,1.98795941837045,1.8178584752704));
#9610=CARTESIAN_POINT('Ctrl Pts',(5.20696135822694,1.99254059429888,1.82167541324663));
#9611=CARTESIAN_POINT('Ctrl Pts',(5.01315008934833,1.99739909857102,1.8331732542045));
#9612=CARTESIAN_POINT('Ctrl Pts',(4.88247521016737,1.98782419847057,1.84061123969016));
#9613=CARTESIAN_POINT('Ctrl Pts',(4.66583816701276,1.95033300652042,1.85354398893336));
#9614=CARTESIAN_POINT('Ctrl Pts',(4.57913208347251,1.92926397660002,1.85888463572897));
#9615=CARTESIAN_POINT('Ctrl Pts',(4.47919163793529,1.89776082036726,1.86538783022986));
#9616=CARTESIAN_POINT('Ctrl Pts',(4.46430778045187,1.89287566560678,1.86636544765753));
#9617=CARTESIAN_POINT('Ctrl Pts',(4.43997105879876,1.88456912625687,1.86797970652299));
#9618=CARTESIAN_POINT('Ctrl Pts',(4.43048360992003,1.88125062696164,1.86861297452493));
#9619=CARTESIAN_POINT('Ctrl Pts',(4.4134545918659,1.87514942076045,1.86975695979694));
#9620=CARTESIAN_POINT('Ctrl Pts',(4.40590394964709,1.87239254305697,1.87026681402807));
#9621=CARTESIAN_POINT('Ctrl Pts',(4.38982216108017,1.86641038127407,1.87135841618666));
#9622=CARTESIAN_POINT('Ctrl Pts',(4.38129608390681,1.86317208302679,1.87194058748928));
#9623=CARTESIAN_POINT('Ctrl Pts',(4.35825305961791,1.85423878810684,1.87352348600471));
#9624=CARTESIAN_POINT('Ctrl Pts',(4.34378044088254,1.84843194002899,1.87452792809919));
#9625=CARTESIAN_POINT('Ctrl Pts',(4.26708695076379,1.81661121241874,1.87990681093444));
#9626=CARTESIAN_POINT('Ctrl Pts',(4.20615370851447,1.78762685080172,1.88438068049406));
#9627=CARTESIAN_POINT('Ctrl Pts',(4.00331996138289,1.67821397657109,1.89997570611706));
#9628=CARTESIAN_POINT('Ctrl Pts',(3.86986483666516,1.58351324221346,1.91152928418664));
#9629=CARTESIAN_POINT('Ctrl Pts',(3.70846184219961,1.43626865884864,1.92652310852278));
#9630=CARTESIAN_POINT('Ctrl Pts',(3.66905407985949,1.39718559945625,1.93027437348577));
#9631=CARTESIAN_POINT('Ctrl Pts',(3.62500104265978,1.3496902802352,1.93452624992127));
#9632=CARTESIAN_POINT('Ctrl Pts',(3.61872611184866,1.34282944609183,1.93513334110161));
#9633=CARTESIAN_POINT('Ctrl Pts',(3.60863726499821,1.33164252140809,1.93611143232783));
#9634=CARTESIAN_POINT('Ctrl Pts',(3.60479382140584,1.32734341737144,1.93648452613418));
#9635=CARTESIAN_POINT('Ctrl Pts',(3.5979808863196,1.31965593960071,1.93714664064215));
#9636=CARTESIAN_POINT('Ctrl Pts',(3.59500418097798,1.31627411748113,1.93743618897301));
#9637=CARTESIAN_POINT('Ctrl Pts',(3.58856535921404,1.30890883548465,1.93806305069477));
#9638=CARTESIAN_POINT('Ctrl Pts',(3.58510758733448,1.3049217145677,1.93840004752316));
#9639=CARTESIAN_POINT('Ctrl Pts',(3.57540102253982,1.2936390191853,1.93934723192615));
#9640=CARTESIAN_POINT('Ctrl Pts',(3.56918894500103,1.28631184750864,1.93995480553468));
#9641=CARTESIAN_POINT('Ctrl Pts',(3.53026935687444,1.23972795543907,1.94377229797163));
#9642=CARTESIAN_POINT('Ctrl Pts',(3.49902441645861,1.19926794103641,1.94688661808404));
#9643=CARTESIAN_POINT('Ctrl Pts',(3.38111956289245,1.03381886743734,1.95904223294462));
#9644=CARTESIAN_POINT('Ctrl Pts',(3.30731812864984,0.900300008321492,1.96763354781027));
#9645=CARTESIAN_POINT('Ctrl Pts',(3.21843452097759,0.684500953130051,1.98141284969103));
#9646=CARTESIAN_POINT('Ctrl Pts',(3.19209697690137,0.607502350096773,1.98630303843298));
#9647=CARTESIAN_POINT('Ctrl Pts',(3.16645679492729,0.514302584381907,1.99230445155953));
#9648=CARTESIAN_POINT('Ctrl Pts',(3.16255247547667,0.499441432852979,1.99326367682759));
#9649=CARTESIAN_POINT('Ctrl Pts',(3.15640103345556,0.474875542138074,1.99485372265693));
#9650=CARTESIAN_POINT('Ctrl Pts',(3.15405418294834,0.465196268351635,1.995481343078));
#9651=CARTESIAN_POINT('Ctrl Pts',(3.14994612472778,0.447681353724132,1.99661923856131));
#9652=CARTESIAN_POINT('Ctrl Pts',(3.14815955378462,0.439851835090765,1.99712869056361));
#9653=CARTESIAN_POINT('Ctrl Pts',(3.14443145456124,0.423046448523216,1.99822397213832));
#9654=CARTESIAN_POINT('Ctrl Pts',(3.14250454089642,0.414067561573615,1.99881025480113));
#9655=CARTESIAN_POINT('Ctrl Pts',(3.13741443595816,0.389524182950732,2.00041595769839));
#9656=CARTESIAN_POINT('Ctrl Pts',(3.13437508182302,0.373934974472855,2.00143927698293));
#9657=CARTESIAN_POINT('Ctrl Pts',(3.11858288505755,0.287448481973071,2.00713669966753));
#9658=CARTESIAN_POINT('Ctrl Pts',(3.10949294634671,0.215944847970046,2.01192491895846));
#9659=CARTESIAN_POINT('Ctrl Pts',(3.0927320733747,-0.0154454677935332,2.02766691509111));
#9660=CARTESIAN_POINT('Ctrl Pts',(3.10041094744031,-0.175793402475635,2.03900417881268));
#9661=CARTESIAN_POINT('Ctrl Pts',(3.13610531763832,-0.386290889499241,2.05364054535397));
#9662=CARTESIAN_POINT('Ctrl Pts',(3.14718200608279,-0.438713127306731,2.05725798109177));
#9663=CARTESIAN_POINT('Ctrl Pts',(3.16262315696911,-0.49956342259038,2.06137780864298));
#9664=CARTESIAN_POINT('Ctrl Pts',(3.16495186141941,-0.508480682786174,2.06197951216228));
#9665=CARTESIAN_POINT('Ctrl Pts',(3.16883168362759,-0.522927306642616,2.06295065616983));
#9666=CARTESIAN_POINT('Ctrl Pts',(3.17034499137608,-0.528466556222705,2.0633221435079));
#9667=CARTESIAN_POINT('Ctrl Pts',(3.17308778898029,-0.53833830360861,2.06398252579143));
#9668=CARTESIAN_POINT('Ctrl Pts',(3.17430804920743,-0.542673239748834,2.0642719371742));
#9669=CARTESIAN_POINT('Ctrl Pts',(3.1769951491051,-0.552096607311319,2.06489979234198));
#9670=CARTESIAN_POINT('Ctrl Pts',(3.17846757229804,-0.557183338896319,2.0652379108631));
#9671=CARTESIAN_POINT('Ctrl Pts',(3.18269133641752,-0.571560427272183,2.06619146447219));
#9672=CARTESIAN_POINT('Ctrl Pts',(3.18549017834018,-0.580836837302783,2.06680422925057));
#9673=CARTESIAN_POINT('Ctrl Pts',(3.20399680543207,-0.640596656856699,2.07073784496737));
#9674=CARTESIAN_POINT('Ctrl Pts',(3.22164029738127,-0.690463806925515,2.07395624778665));
#9675=CARTESIAN_POINT('Ctrl Pts',(3.30339792252517,-0.89526053767156,2.08713139326545));
#9676=CARTESIAN_POINT('Ctrl Pts',(3.38492692698709,-1.04249459169457,2.09655560371181));
#9677=CARTESIAN_POINT('Ctrl Pts',(3.52262843973057,-1.23071542513694,2.11044626762472));
#9678=CARTESIAN_POINT('Ctrl Pts',(3.56392080412243,-1.28168291693147,2.11442014690451));
#9679=CARTESIAN_POINT('Ctrl Pts',(3.61826224435822,-1.34238189730793,2.11948455624988));
#9680=CARTESIAN_POINT('Ctrl Pts',(3.62902149384696,-1.35411421815771,2.12047976115093));
#9681=CARTESIAN_POINT('Ctrl Pts',(3.64627610461419,-1.3724830455099,2.12206475075751));
#9682=CARTESIAN_POINT('Ctrl Pts',(3.65267951429091,-1.37920528808382,2.12265062168663));
#9683=CARTESIAN_POINT('Ctrl Pts',(3.6647029454159,-1.39165222217593,2.12374650358928));
#9684=CARTESIAN_POINT('Ctrl Pts',(3.67031104633254,-1.3973882063366,2.12425599256076));
#9685=CARTESIAN_POINT('Ctrl Pts',(3.6828647725479,-1.41007420336093,2.12539290029009));
#9686=CARTESIAN_POINT('Ctrl Pts',(3.68982742128975,-1.41700700271386,2.12602106041877));
#9687=CARTESIAN_POINT('Ctrl Pts',(3.71033930501654,-1.4371313523716,2.12786484534362));
#9688=CARTESIAN_POINT('Ctrl Pts',(3.72402494247374,-1.45018171719798,2.12908652942289));
#9689=CARTESIAN_POINT('Ctrl Pts',(3.84308779334311,-1.56052855554241,2.13964612411791));
#9690=CARTESIAN_POINT('Ctrl Pts',(3.95846958813204,-1.64637379662709,2.14946996585542));
#9691=CARTESIAN_POINT('Ctrl Pts',(4.19245013777418,-1.78408608232134,2.16837758074954));
#9692=CARTESIAN_POINT('Ctrl Pts',(4.308883236307,-1.83829054360325,2.17737319557314));
#9693=CARTESIAN_POINT('Ctrl Pts',(4.44454878346505,-1.88618993949204,2.18690315290051));
#9694=CARTESIAN_POINT('Ctrl Pts',(4.459440288013,-1.89125044119926,2.18793661198135));
#9695=CARTESIAN_POINT('Ctrl Pts',(4.48006764284195,-1.89798906508824,2.18934932696208));
#9696=CARTESIAN_POINT('Ctrl Pts',(4.48575304725337,-1.89981817857702,2.1897367476822));
#9697=CARTESIAN_POINT('Ctrl Pts',(4.49551560608305,-1.90291068365749,2.19039854260204));
#9698=CARTESIAN_POINT('Ctrl Pts',(4.49958871743466,-1.90418656116014,2.19067362731709));
#9699=CARTESIAN_POINT('Ctrl Pts',(4.5080926791622,-1.90682043245434,2.19124576978082));
#9700=CARTESIAN_POINT('Ctrl Pts',(4.51252420228966,-1.90817607036028,2.19154267977607));
#9701=CARTESIAN_POINT('Ctrl Pts',(4.52331927003924,-1.91143727077997,2.19226301416058));
#9702=CARTESIAN_POINT('Ctrl Pts',(4.52968776085435,-1.91332653614393,2.1926855014915));
#9703=CARTESIAN_POINT('Ctrl Pts',(4.55242563418988,-1.91994851602255,2.19418553827451));
#9704=CARTESIAN_POINT('Ctrl Pts',(4.56884661151151,-1.92450341268009,2.1952533652806));
#9705=CARTESIAN_POINT('Ctrl Pts',(4.60973921928892,-1.93528394172807,2.19787887672789));
#9706=CARTESIAN_POINT('Ctrl Pts',(4.63427502756244,-1.94125655864457,2.19942453130822));
#9707=CARTESIAN_POINT('Ctrl Pts',(4.73883285779753,-1.96461487400764,2.205911347083));
#9708=CARTESIAN_POINT('Ctrl Pts',(4.81977685118149,-1.97753155351539,2.21068883075821));
#9709=CARTESIAN_POINT('Ctrl Pts',(5.0551081552201,-2.0003526178119,2.22442787810779));
#9710=CARTESIAN_POINT('Ctrl Pts',(5.21011862229985,-1.99734324320496,2.23333647179194));
#9711=CARTESIAN_POINT('Ctrl Pts',(5.38738925048083,-1.97318112629982,2.24435253024693));
#9712=CARTESIAN_POINT('Ctrl Pts',(5.41149302194494,-1.96944428143835,2.24586710710607));
#9713=CARTESIAN_POINT('Ctrl Pts',(5.44516517591006,-1.96358981742938,2.24800891909488));
#9714=CARTESIAN_POINT('Ctrl Pts',(5.45479630849116,-1.96184215492393,2.24862452705035));
#9715=CARTESIAN_POINT('Ctrl Pts',(5.47245683009992,-1.95850303310291,2.24975903973385));
#9716=CARTESIAN_POINT('Ctrl Pts',(5.48049007194776,-1.95693289281094,2.25027726067193));
#9717=CARTESIAN_POINT('Ctrl Pts',(5.4968009064896,-1.95364049941748,2.25133397254712));
#9718=CARTESIAN_POINT('Ctrl Pts',(5.50507766032501,-1.95191497346157,2.25187255784419));
#9719=CARTESIAN_POINT('Ctrl Pts',(5.52559180711936,-1.94750194406158,2.25321345953189));
#9720=CARTESIAN_POINT('Ctrl Pts',(5.537815188727,-1.94475169392781,2.25401775909664));
#9721=CARTESIAN_POINT('Ctrl Pts',(5.58417498885021,-1.93386093357323,2.25708899126347));
#9722=CARTESIAN_POINT('Ctrl Pts',(5.61811868939426,-1.92493564516567,2.25938076687164));
#9723=CARTESIAN_POINT('Ctrl Pts',(5.70347265611761,-1.90006731190146,2.26525703681875));
#9724=CARTESIAN_POINT('Ctrl Pts',(5.75450332920836,-1.88293111709827,2.26887691895692));
#9725=CARTESIAN_POINT('Ctrl Pts',(5.88853387054315,-1.83180378559905,2.27866089484497));
#9726=CARTESIAN_POINT('Ctrl Pts',(5.97003821806222,-1.79424526481523,2.28490700090815));
#9727=CARTESIAN_POINT('Ctrl Pts',(6.14002552152954,-1.70156050829027,2.29840405139285));
#9728=CARTESIAN_POINT('Ctrl Pts',(6.22729382693212,-1.64471783306534,2.30563689135189));
#9729=CARTESIAN_POINT('Ctrl Pts',(6.32267180790665,-1.57137982128751,2.31361265653518));
#9730=CARTESIAN_POINT('Ctrl Pts',(6.33548296428924,-1.56127659811982,2.31468534709351));
#9731=CARTESIAN_POINT('Ctrl Pts',(6.35339280035416,-1.54679251373565,2.31618524410383));
#9732=CARTESIAN_POINT('Ctrl Pts',(6.35859511472257,-1.5425416385639,2.31662095750045));
#9733=CARTESIAN_POINT('Ctrl Pts',(6.36732525972065,-1.5353342713384,2.31735205498524));
#9734=CARTESIAN_POINT('Ctrl Pts',(6.37086448313447,-1.53239172913787,2.31764841962198));
#9735=CARTESIAN_POINT('Ctrl Pts',(6.37801665717794,-1.52640335935194,2.31824721990174));
#9736=CARTESIAN_POINT('Ctrl Pts',(6.38162901330332,-1.52335690756484,2.3185496076446));
#9737=CARTESIAN_POINT('Ctrl Pts',(6.39057951192814,-1.51575398542618,2.31929882418905));
#9738=CARTESIAN_POINT('Ctrl Pts',(6.39590454750912,-1.51118208266376,2.31974454452688));
#9739=CARTESIAN_POINT('Ctrl Pts',(6.40757913073792,-1.5010511401374,2.32072198064465));
#9740=CARTESIAN_POINT('Ctrl Pts',(6.41391778924148,-1.49547968964539,2.321252833754));
#9741=CARTESIAN_POINT('Ctrl Pts',(6.43216608904699,-1.47923366526153,2.32278221880721));
#9742=CARTESIAN_POINT('Ctrl Pts',(6.44398323252484,-1.46845563078022,2.3237740050948));
#9743=CARTESIAN_POINT('Ctrl Pts',(6.48487055385752,-1.43025273929782,2.32721588207732));
#9744=CARTESIAN_POINT('Ctrl Pts',(6.51324659656555,-1.40209610231227,2.32962321679784));
#9745=CARTESIAN_POINT('Ctrl Pts',(6.59893849946325,-1.3117968006145,2.33702560471193));
#9746=CARTESIAN_POINT('Ctrl Pts',(6.65316530577674,-1.24685078707598,2.34190901336403));
#9747=CARTESIAN_POINT('Ctrl Pts',(6.77813788096399,-1.0762191893389,2.35419111760451));
#9748=CARTESIAN_POINT('Ctrl Pts',(6.84320402900208,-0.966863843601102,2.36160889506266));
#9749=CARTESIAN_POINT('Ctrl Pts',(6.90804051567228,-0.829622808686236,2.3709455829387));
#9750=CARTESIAN_POINT('Ctrl Pts',(6.91822659464173,-0.806976283978035,2.37248614457263));
#9751=CARTESIAN_POINT('Ctrl Pts',(6.93196805266002,-0.774834283425505,2.37467521152113));
#9752=CARTESIAN_POINT('Ctrl Pts',(6.93587811358629,-0.765492251020123,2.37531175571147));
#9753=CARTESIAN_POINT('Ctrl Pts',(6.94256794874434,-0.749160608642424,2.37642525400048));
#9754=CARTESIAN_POINT('Ctrl Pts',(6.94537966315552,-0.742184240624828,2.37690112584366));
#9755=CARTESIAN_POINT('Ctrl Pts',(6.95118552422492,-0.727540517259782,2.37790054457039));
#9756=CARTESIAN_POINT('Ctrl Pts',(6.95417179776423,-0.719870212470008,2.37842434380341));
#9757=CARTESIAN_POINT('Ctrl Pts',(6.96117797996114,-0.701539915944533,2.37967694818009));
#9758=CARTESIAN_POINT('Ctrl Pts',(6.9651541688795,-0.690863630097261,2.38040719054387));
#9759=CARTESIAN_POINT('Ctrl Pts',(6.97839082119528,-0.654369659089111,2.38290596348991));
#9760=CARTESIAN_POINT('Ctrl Pts',(6.98720981464392,-0.628396246926899,2.38468891210499));
#9761=CARTESIAN_POINT('Ctrl Pts',(7.00715082964822,-0.565430581908695,2.38902409113906));
#9762=CARTESIAN_POINT('Ctrl Pts',(7.01773902068331,-0.528282153670864,2.391592426768));
#9763=CARTESIAN_POINT('Ctrl Pts',(7.0679796882215,-0.330389330144033,2.4053291729097));
#9764=CARTESIAN_POINT('Ctrl Pts',(7.08857715545339,-0.165496138935671,2.41703857396203));
#9765=CARTESIAN_POINT('Ctrl Pts',(7.08857715545311,3.3222036233127E-12,
2.42843892255116));
#9766=CARTESIAN_POINT('Origin',(5.09382715545311,0.,-6.77268258743872));
#9767=CARTESIAN_POINT('',(7.08857715495384,-4.3655925271901E-5,3.38727862543405));
#9768=CARTESIAN_POINT('',(7.08857715545311,9.38914434820125E-11,3.22796126976449));
#9769=CARTESIAN_POINT('',(7.08857715545311,8.3550772080578E-14,-6.77268258743872));
#9770=CARTESIAN_POINT('Ctrl Pts',(7.08857715492703,-4.58127331705431E-5,
3.38727861359244));
#9771=CARTESIAN_POINT('Ctrl Pts',(7.08857709852051,-0.00250183082418328,
3.38712320877298));
#9772=CARTESIAN_POINT('Ctrl Pts',(7.08857250618887,-0.00495784000431415,
3.38696766332));
#9773=CARTESIAN_POINT('Ctrl Pts',(7.08854430155101,-0.0125464722495827,
3.38648661511498));
#9774=CARTESIAN_POINT('Ctrl Pts',(7.08850541512609,-0.0176789843406733,
3.38616063939049));
#9775=CARTESIAN_POINT('Ctrl Pts',(7.08834420420563,-0.031775294329847,3.38526361437851));
#9776=CARTESIAN_POINT('Ctrl Pts',(7.08818126235171,-0.0407384226304432,
3.38469130714592));
#9777=CARTESIAN_POINT('Ctrl Pts',(7.08758290455359,-0.0647465309243057,
3.38315303086674));
#9778=CARTESIAN_POINT('Ctrl Pts',(7.08703762158118,-0.0797879535402261,
3.38218366787627));
#9779=CARTESIAN_POINT('Ctrl Pts',(7.0836431288264,-0.151116869654046,3.37755920561389));
#9780=CARTESIAN_POINT('Ctrl Pts',(7.07857971239356,-0.207268340064208,3.37383612540531));
#9781=CARTESIAN_POINT('Ctrl Pts',(7.06586614929467,-0.302807314340294,3.36735657017158));
#9782=CARTESIAN_POINT('Ctrl Pts',(7.05939262223529,-0.342318791249575,3.36463416234251));
#9783=CARTESIAN_POINT('Ctrl Pts',(7.03693774861316,-0.457527846573419,3.35658050637764));
#9784=CARTESIAN_POINT('Ctrl Pts',(7.01773758018822,-0.532520541956035,3.35118747832221));
#9785=CARTESIAN_POINT('Ctrl Pts',(6.9704281920205,-0.680831781169107,3.34033565578518));
#9786=CARTESIAN_POINT('Ctrl Pts',(6.94224670858607,-0.753996021387809,3.33488630434343));
#9787=CARTESIAN_POINT('Ctrl Pts',(6.89965421953311,-0.847715453802603,3.32791491418379));
#9788=CARTESIAN_POINT('Ctrl Pts',(6.88906079774946,-0.869924801332104,3.32626381758821));
#9789=CARTESIAN_POINT('Ctrl Pts',(6.87058634868833,-0.906881251200297,3.32352458579133));
#9790=CARTESIAN_POINT('Ctrl Pts',(6.86292614477236,-0.921735127052531,3.32242588770936));
#9791=CARTESIAN_POINT('Ctrl Pts',(6.85198518917063,-0.942311701201185,3.32090888951387));
#9792=CARTESIAN_POINT('Ctrl Pts',(6.8488616202024,-0.948116577354574,3.320481488738));
#9793=CARTESIAN_POINT('Ctrl Pts',(6.84349781503736,-0.957967395749502,3.3197572878788));
#9794=CARTESIAN_POINT('Ctrl Pts',(6.84127219456565,-0.962021197932506,3.31945958339373));
#9795=CARTESIAN_POINT('Ctrl Pts',(6.83695957506552,-0.969811966024536,3.31888810504421));
#9796=CARTESIAN_POINT('Ctrl Pts',(6.83487463129223,-0.973549983031158,3.31861419937776));
#9797=CARTESIAN_POINT('Ctrl Pts',(6.82982980836454,-0.982526617793599,3.31795705875355));
#9798=CARTESIAN_POINT('Ctrl Pts',(6.82685820532529,-0.9877586486549,3.31757456135241));
#9799=CARTESIAN_POINT('Ctrl Pts',(6.8158634874209,-1.00691443052252,3.31617574350262));
#9800=CARTESIAN_POINT('Ctrl Pts',(6.80769562319996,-1.02075497187569,3.3151681812041));
#9801=CARTESIAN_POINT('Ctrl Pts',(6.73752655663979,-1.13644004665874,3.30675986233794));
#9802=CARTESIAN_POINT('Ctrl Pts',(6.66666750077952,-1.2326494397742,3.29984575532485));
#9803=CARTESIAN_POINT('Ctrl Pts',(6.51813664250263,-1.40048759101688,3.28683471699357));
#9804=CARTESIAN_POINT('Ctrl Pts',(6.442563525247,-1.47340803481055,3.28075881220056));
#9805=CARTESIAN_POINT('Ctrl Pts',(6.31953849316263,-1.57468390429232,3.27119210792828));
#9806=CARTESIAN_POINT('Ctrl Pts',(6.27606413925425,-1.60757973181704,3.26786738321616));
#9807=CARTESIAN_POINT('Ctrl Pts',(6.21929140428639,-1.64698861308956,3.26356259037007));
#9808=CARTESIAN_POINT('Ctrl Pts',(6.20719143362846,-1.65519220431611,3.26264720838283));
#9809=CARTESIAN_POINT('Ctrl Pts',(6.18867607129601,-1.66745044405147,3.26124913366752));
#9810=CARTESIAN_POINT('Ctrl Pts',(6.18232573140066,-1.6716028175036,3.26077009257741));
#9811=CARTESIAN_POINT('Ctrl Pts',(6.16935309855411,-1.67998012234839,3.25979235594394));
#9812=CARTESIAN_POINT('Ctrl Pts',(6.1627292362971,-1.68420236446147,3.2592935723595));
#9813=CARTESIAN_POINT('Ctrl Pts',(6.14813714804323,-1.69338302779993,3.25819566993454));
#9814=CARTESIAN_POINT('Ctrl Pts',(6.14015855464053,-1.69832453831343,3.25759594480215));
#9815=CARTESIAN_POINT('Ctrl Pts',(6.11772834641523,-1.71199854419326,3.2559113871023));
#9816=CARTESIAN_POINT('Ctrl Pts',(6.10320056127153,-1.72060395292479,3.2548219805004));
#9817=CARTESIAN_POINT('Ctrl Pts',(6.01538426104975,-1.7711262531708,3.24824511414507));
#9818=CARTESIAN_POINT('Ctrl Pts',(5.93961358814865,-1.80853467405239,3.24259917353566));
#9819=CARTESIAN_POINT('Ctrl Pts',(5.7241170264138,-1.8984171202113,3.22663956008988));
#9820=CARTESIAN_POINT('Ctrl Pts',(5.58053707097804,-1.9401963082779,3.21608165181089));
#9821=CARTESIAN_POINT('Ctrl Pts',(5.38367687892514,-1.97423064999869,3.20241605452096));
#9822=CARTESIAN_POINT('Ctrl Pts',(5.33338752889605,-1.98096221899896,3.19899844769956));
#9823=CARTESIAN_POINT('Ctrl Pts',(5.27334778529183,-1.98667859042588,3.19504538027708));
#9824=CARTESIAN_POINT('Ctrl Pts',(5.26379702098257,-1.98751848590658,3.19442036796973));
#9825=CARTESIAN_POINT('Ctrl Pts',(5.248983880856,-1.98871359510105,3.19345727616396));
#9826=CARTESIAN_POINT('Ctrl Pts',(5.24372568072868,-1.98911684082435,3.19311663695123));
#9827=CARTESIAN_POINT('Ctrl Pts',(5.23397198325351,-1.98982594502665,3.19248712201647));
#9828=CARTESIAN_POINT('Ctrl Pts',(5.22947707591475,-1.99013742338515,3.19219795052357));
#9829=CARTESIAN_POINT('Ctrl Pts',(5.21922143724784,-1.99081318894947,3.19154027227158));
#9830=CARTESIAN_POINT('Ctrl Pts',(5.21346015824319,-1.99116770409923,3.19117231121698));
#9831=CARTESIAN_POINT('Ctrl Pts',(5.19839681858278,-1.99202899839834,3.19021397959583));
#9832=CARTESIAN_POINT('Ctrl Pts',(5.18909247970869,-1.99249563883409,3.18962575503284));
#9833=CARTESIAN_POINT('Ctrl Pts',(5.12392116011475,-1.99530661507959,3.18552949407312));
#9834=CARTESIAN_POINT('Ctrl Pts',(5.06797502758653,-1.9953663918303,3.18213576354771));
#9835=CARTESIAN_POINT('Ctrl Pts',(4.84962392566178,-1.98641225485162,3.16911703124668));
#9836=CARTESIAN_POINT('Ctrl Pts',(4.68857411250159,-1.95990923518893,3.15995601572542));
#9837=CARTESIAN_POINT('Ctrl Pts',(4.46786717336476,-1.8951889669928,3.14626316818435));
#9838=CARTESIAN_POINT('Ctrl Pts',(4.40422149818246,-1.87296816013138,3.14217970589422));
#9839=CARTESIAN_POINT('Ctrl Pts',(4.32738670495393,-1.84169477419209,3.13701939913801));
#9840=CARTESIAN_POINT('Ctrl Pts',(4.31301685886521,-1.83564862230034,3.13604418342241));
#9841=CARTESIAN_POINT('Ctrl Pts',(4.2903559879828,-1.82579977272359,3.13448950528925));
#9842=CARTESIAN_POINT('Ctrl Pts',(4.28201744556825,-1.82210749340418,3.13391378715432));
#9843=CARTESIAN_POINT('Ctrl Pts',(4.26637710381656,-1.81505332962233,3.13282692284827));
#9844=CARTESIAN_POINT('Ctrl Pts',(4.2590697158949,-1.81170422291852,3.1323162216528));
#9845=CARTESIAN_POINT('Ctrl Pts',(4.24266997668752,-1.80406764586246,3.13116342234245));
#9846=CARTESIAN_POINT('Ctrl Pts',(4.23358944430854,-1.79975545228914,3.1305204837879));
#9847=CARTESIAN_POINT('Ctrl Pts',(4.2104388682996,-1.78854639967122,3.12886924426446));
#9848=CARTESIAN_POINT('Ctrl Pts',(4.19641700152983,-1.78155215532139,3.12785759782902));
#9849=CARTESIAN_POINT('Ctrl Pts',(4.10307121026518,-1.73360874231533,3.12104390016041));
#9850=CARTESIAN_POINT('Ctrl Pts',(4.02650162835934,-1.68754523144274,3.11506263111305));
#9851=CARTESIAN_POINT('Ctrl Pts',(3.84614174300541,-1.56184610571137,3.10000114368129));
#9852=CARTESIAN_POINT('Ctrl Pts',(3.74660107071103,-1.47684151982662,3.09079049378236));
#9853=CARTESIAN_POINT('Ctrl Pts',(3.61231596880704,-1.33721316506094,3.07744805969703));
#9854=CARTESIAN_POINT('Ctrl Pts',(3.57072795862261,-1.28964528920073,3.07316247995355));
#9855=CARTESIAN_POINT('Ctrl Pts',(3.52518485781038,-1.23227061743155,3.06835642938633));
#9856=CARTESIAN_POINT('Ctrl Pts',(3.51896668589212,-1.22431370334604,3.06769762919173));
#9857=CARTESIAN_POINT('Ctrl Pts',(3.50952695435974,-1.21204348445192,3.06669390928744));
#9858=CARTESIAN_POINT('Ctrl Pts',(3.50626209067189,-1.20776392648606,3.06634608441327));
#9859=CARTESIAN_POINT('Ctrl Pts',(3.50030144291197,-1.1998848230521,3.06570989861047));
#9860=CARTESIAN_POINT('Ctrl Pts',(3.49760051176691,-1.19628938300882,3.06542118910934));
#9861=CARTESIAN_POINT('Ctrl Pts',(3.49154399227421,-1.1881700010936,3.06477278318482));
#9862=CARTESIAN_POINT('Ctrl Pts',(3.48819539674085,-1.1836409691228,3.06441356926972));
#9863=CARTESIAN_POINT('Ctrl Pts',(3.47839281480679,-1.17026466187944,3.06335969819392));
#9864=CARTESIAN_POINT('Ctrl Pts',(3.47199232649376,-1.16137818478592,3.06266859060035));
#9865=CARTESIAN_POINT('Ctrl Pts',(3.41001149017844,-1.07381188205242,3.05594155443617));
#9866=CARTESIAN_POINT('Ctrl Pts',(3.3601185833546,-0.991245064867244,3.05024775519266));
#9867=CARTESIAN_POINT('Ctrl Pts',(3.25811809403412,-0.790998727362796,3.03713318581263));
#9868=CARTESIAN_POINT('Ctrl Pts',(3.21103261191144,-0.671260268431884,3.02978328090813));
#9869=CARTESIAN_POINT('Ctrl Pts',(3.15908950397202,-0.489398099386128,3.0184763793657));
#9870=CARTESIAN_POINT('Ctrl Pts',(3.14508067327121,-0.430239871078381,3.01478114614464));
#9871=CARTESIAN_POINT('Ctrl Pts',(3.13098495275062,-0.355677914969023,3.01005782073257));
#9872=CARTESIAN_POINT('Ctrl Pts',(3.12834476129221,-0.34078619450181,3.00911130865941));
#9873=CARTESIAN_POINT('Ctrl Pts',(3.12440111726925,-0.316969960479531,3.00759191887856));
#9874=CARTESIAN_POINT('Ctrl Pts',(3.12298838078027,-0.308063947360792,3.00702249511245));
#9875=CARTESIAN_POINT('Ctrl Pts',(3.1204282420379,-0.291185781348925,3.0059408561587));
#9876=CARTESIAN_POINT('Ctrl Pts',(3.11926864046898,-0.283215639618584,3.00542903666978));
#9877=CARTESIAN_POINT('Ctrl Pts',(3.11674790692168,-0.265121761263558,3.00426461682406));
#9878=CARTESIAN_POINT('Ctrl Pts',(3.11541621566462,-0.254994216013902,3.00361110521924));
#9879=CARTESIAN_POINT('Ctrl Pts',(3.11217314627363,-0.228774058520256,3.00191442383744));
#9880=CARTESIAN_POINT('Ctrl Pts',(3.11038001797486,-0.212667837621573,3.00086758918041));
#9881=CARTESIAN_POINT('Ctrl Pts',(3.09595363973842,-0.0669636060906816,
2.99135374193094));
#9882=CARTESIAN_POINT('Ctrl Pts',(3.09584453860064,0.0635354900294857,2.98248929467057));
#9883=CARTESIAN_POINT('Ctrl Pts',(3.11746786251759,0.285867328631664,2.96697124783214));
#9884=CARTESIAN_POINT('Ctrl Pts',(3.1329827000008,0.377896337761139,2.96043185371752));
#9885=CARTESIAN_POINT('Ctrl Pts',(3.16869435037146,0.525692624310654,2.94998233966712));
#9886=CARTESIAN_POINT('Ctrl Pts',(3.18503757925898,0.582248075434627,2.94599874786823));
#9887=CARTESIAN_POINT('Ctrl Pts',(3.20703853202009,0.647421863521953,2.94148705687845));
#9888=CARTESIAN_POINT('Ctrl Pts',(3.21028839902287,0.656816672823371,2.94083867070505));
#9889=CARTESIAN_POINT('Ctrl Pts',(3.2153949322283,0.67122914100788,2.93984745554976));
#9890=CARTESIAN_POINT('Ctrl Pts',(3.21720172264121,0.676264122610122,2.93950182987135));
#9891=CARTESIAN_POINT('Ctrl Pts',(3.22056535742885,0.68552026901011,2.9388677289042));
#9892=CARTESIAN_POINT('Ctrl Pts',(3.22211622294915,0.689743422617815,2.93857892107796));
#9893=CARTESIAN_POINT('Ctrl Pts',(3.22565493313783,0.699279837056318,2.93792787093746));
#9894=CARTESIAN_POINT('Ctrl Pts',(3.22765116042811,0.704589880881847,2.93756612945849));
#9895=CARTESIAN_POINT('Ctrl Pts',(3.23286804383442,0.718289286317735,2.93663469861728));
#9896=CARTESIAN_POINT('Ctrl Pts',(3.23612282643017,0.726665636302621,2.93606696301326));
#9897=CARTESIAN_POINT('Ctrl Pts',(3.25749507185824,0.780586003006086,2.93242206647504));
#9898=CARTESIAN_POINT('Ctrl Pts',(3.27723098210347,0.825475159389581,2.92943255026893));
#9899=CARTESIAN_POINT('Ctrl Pts',(3.37231660202252,1.02177341304041,2.91636802706252));
#9900=CARTESIAN_POINT('Ctrl Pts',(3.46508258026458,1.16396660454672,2.90687021929907));
#9901=CARTESIAN_POINT('Ctrl Pts',(3.61895713219339,1.34478741498196,2.89274301742363));
#9902=CARTESIAN_POINT('Ctrl Pts',(3.66587144617644,1.39450198536912,2.88860448416378));
#9903=CARTESIAN_POINT('Ctrl Pts',(3.72655178170956,1.45252558506473,2.88338228307836));
#9904=CARTESIAN_POINT('Ctrl Pts',(3.73799037163492,1.463208500751,2.8824032881618));
#9905=CARTESIAN_POINT('Ctrl Pts',(3.75630075950714,1.47991017023988,2.88084396455564));
#9906=CARTESIAN_POINT('Ctrl Pts',(3.76309037759503,1.48601836981163,2.88026741911284));
#9907=CARTESIAN_POINT('Ctrl Pts',(3.77593302540604,1.49741350722789,2.87917984546561));
#9908=CARTESIAN_POINT('Ctrl Pts',(3.78197654455625,1.50271092404523,2.87866926861631));
#9909=CARTESIAN_POINT('Ctrl Pts',(3.79563606257786,1.51453890628871,2.87751788732708));
#9910=CARTESIAN_POINT('Ctrl Pts',(3.80326960575692,1.52104878854996,2.87687625116742));
#9911=CARTESIAN_POINT('Ctrl Pts',(3.82290044704847,1.53753580025171,2.87523058519151));
#9912=CARTESIAN_POINT('Ctrl Pts',(3.83496612071126,1.54743009778423,2.87422324816928));
#9913=CARTESIAN_POINT('Ctrl Pts',(3.91518493465625,1.61165334281457,2.86755155803434));
#9914=CARTESIAN_POINT('Ctrl Pts',(3.98671096669044,1.66159984981628,2.86171672934004));
#9915=CARTESIAN_POINT('Ctrl Pts',(4.18664148247596,1.78255849078888,2.84572345620774));
#9916=CARTESIAN_POINT('Ctrl Pts',(4.31998406317598,1.84435992113757,2.8353491403926));
#9917=CARTESIAN_POINT('Ctrl Pts',(4.50664533268357,1.90703516887904,2.82188325092822));
#9918=CARTESIAN_POINT('Ctrl Pts',(4.55499925611224,1.92125767938949,2.81848891847914));
#9919=CARTESIAN_POINT('Ctrl Pts',(4.61312170891715,1.93598590843416,2.81455903386999));
#9920=CARTESIAN_POINT('Ctrl Pts',(4.62241636720697,1.93827011571675,2.81393510606344));
#9921=CARTESIAN_POINT('Ctrl Pts',(4.63685397554141,1.94170822945358,2.81297332097893));
#9922=CARTESIAN_POINT('Ctrl Pts',(4.64198551497529,1.94290876496222,2.81263291476507));
#9923=CARTESIAN_POINT('Ctrl Pts',(4.65151352693363,1.9450980751337,2.8120036089029));
#9924=CARTESIAN_POINT('Ctrl Pts',(4.6559085648697,1.94609228365405,2.81171441521704));
#9925=CARTESIAN_POINT('Ctrl Pts',(4.66594598226418,1.948327138278,2.81105640385118));
#9926=CARTESIAN_POINT('Ctrl Pts',(4.67159040391613,1.94955817142729,2.81068813409623));
#9927=CARTESIAN_POINT('Ctrl Pts',(4.68636655974522,1.95271362843127,2.80972846134835));
#9928=CARTESIAN_POINT('Ctrl Pts',(4.6955067127439,1.95459854818002,2.80913921416225));
#9929=CARTESIAN_POINT('Ctrl Pts',(4.75989782562752,1.96740710543544,2.80501667984474));
#9930=CARTESIAN_POINT('Ctrl Pts',(4.8155818987722,1.97605170724412,2.80159937169849));
#9931=CARTESIAN_POINT('Ctrl Pts',(5.03278783868504,2.00040550833585,2.78858259232941));
#9932=CARTESIAN_POINT('Ctrl Pts',(5.1956190018227,1.99874752598073,2.77944096667626));
#9933=CARTESIAN_POINT('Ctrl Pts',(5.42319181716855,1.968521876308,2.76577320499344));
#9934=CARTESIAN_POINT('Ctrl Pts',(5.4894274722456,1.95628689666896,2.76169307408302));
#9935=CARTESIAN_POINT('Ctrl Pts',(5.57007738013882,1.93712576051797,2.75653651207407));
#9936=CARTESIAN_POINT('Ctrl Pts',(5.58519827033156,1.93334551863264,2.75556152719567));
#9937=CARTESIAN_POINT('Ctrl Pts',(5.60909283176573,1.92707342748075,2.75400713282003));
#9938=CARTESIAN_POINT('Ctrl Pts',(5.61789658436368,1.92469788312874,2.75343146523104));
#9939=CARTESIAN_POINT('Ctrl Pts',(5.63442995422656,1.9201147864167,2.75234464410352));
#9940=CARTESIAN_POINT('Ctrl Pts',(5.64216314013123,1.91792070322963,2.75183393515021));
#9941=CARTESIAN_POINT('Ctrl Pts',(5.65953790316027,1.91287741073224,2.75068104842828));
#9942=CARTESIAN_POINT('Ctrl Pts',(5.66917157009502,1.91000194685948,2.75003802968309));
#9943=CARTESIAN_POINT('Ctrl Pts',(5.69376724371163,1.90245764920388,2.74838644681994));
#9944=CARTESIAN_POINT('Ctrl Pts',(5.70869648510636,1.89768514268986,2.747374534872));
#9945=CARTESIAN_POINT('Ctrl Pts',(5.80838310915044,1.8645179949319,2.74055292250614));
#9946=CARTESIAN_POINT('Ctrl Pts',(5.89119397304827,1.83063371061706,2.73456351267928));
#9947=CARTESIAN_POINT('Ctrl Pts',(6.08862499505134,1.73390653964181,2.71950039032983));
#9948=CARTESIAN_POINT('Ctrl Pts',(6.19988048016363,1.66514189927543,2.71029725601398));
#9949=CARTESIAN_POINT('Ctrl Pts',(6.35380942151657,1.54772632456468,2.69696348222466));
#9950=CARTESIAN_POINT('Ctrl Pts',(6.40215819008974,1.50707786112066,2.69267921460158));
#9951=CARTESIAN_POINT('Ctrl Pts',(6.45591381809099,1.45734328249231,2.68787443786638));
#9952=CARTESIAN_POINT('Ctrl Pts',(6.46327358152506,1.45042959702501,2.68721568019898));
#9953=CARTESIAN_POINT('Ctrl Pts',(6.47447565518848,1.43974520457679,2.68621201132708));
#9954=CARTESIAN_POINT('Ctrl Pts',(6.4783556027667,1.43601445471509,2.68586419540469));
#9955=CARTESIAN_POINT('Ctrl Pts',(6.48544936121748,1.42913799949735,2.6852280181593));
#9956=CARTESIAN_POINT('Ctrl Pts',(6.48866763111459,1.4259971365444,2.6849393083289));
#9957=CARTESIAN_POINT('Ctrl Pts',(6.49589303829415,1.4188976525757,2.68429089195976));
#9958=CARTESIAN_POINT('Ctrl Pts',(6.49989404108337,1.41493293244304,2.68393166800227));
#9959=CARTESIAN_POINT('Ctrl Pts',(6.51162481018724,1.40320964734802,2.68287773979697));
#9960=CARTESIAN_POINT('Ctrl Pts',(6.5193076839296,1.3954041636229,2.68218658569109));
#9961=CARTESIAN_POINT('Ctrl Pts',(6.58997112855875,1.3224203012347,2.67581665945378));
#9962=CARTESIAN_POINT('Ctrl Pts',(6.64851364673704,1.25307480858604,2.67044020763134));
#9963=CARTESIAN_POINT('Ctrl Pts',(6.77105887491358,1.08604530044307,2.6583279921024));
#9964=CARTESIAN_POINT('Ctrl Pts',(6.83161250615947,0.986256831199962,2.65165598822264));
#9965=CARTESIAN_POINT('Ctrl Pts',(6.9054471220186,0.83642926150532,2.64176352143123));
#9966=CARTESIAN_POINT('Ctrl Pts',(6.92605152991183,0.790274706547201,2.63873414397802));
#9967=CARTESIAN_POINT('Ctrl Pts',(6.95737388764499,0.712281517808107,2.63360407835666));
#9968=CARTESIAN_POINT('Ctrl Pts',(6.96908038201041,0.680864536925153,2.63153491007232));
#9969=CARTESIAN_POINT('Ctrl Pts',(6.98399671548727,0.637525085206788,2.62866991586266));
#9970=CARTESIAN_POINT('Ctrl Pts',(6.98789622605157,0.625844665196475,2.62789675047019));
#9971=CARTESIAN_POINT('Ctrl Pts',(6.99427660058254,0.606127217380235,2.62658954571154));
#9972=CARTESIAN_POINT('Ctrl Pts',(6.99681526420447,0.59810914688202,2.62605740915565));
#9973=CARTESIAN_POINT('Ctrl Pts',(7.00173461335333,0.582223546202908,2.62500190724928));
#9974=CARTESIAN_POINT('Ctrl Pts',(7.00411752627149,0.574356876437284,2.62447862666401));
#9975=CARTESIAN_POINT('Ctrl Pts',(7.00979504117397,0.555187558878182,2.62320197283816));
#9976=CARTESIAN_POINT('Ctrl Pts',(7.0130383001815,0.543870146993055,2.62244695243635));
#9977=CARTESIAN_POINT('Ctrl Pts',(7.02196835379593,0.511633674051969,2.62029237784176));
#9978=CARTESIAN_POINT('Ctrl Pts',(7.0274144415132,0.490650224892829,2.6188851642908));
#9979=CARTESIAN_POINT('Ctrl Pts',(7.06976555882728,0.315802071986491,2.60711631059225));
#9980=CARTESIAN_POINT('Ctrl Pts',(7.08857715545311,0.158164798835133,2.59616345434794));
#9981=CARTESIAN_POINT('Ctrl Pts',(7.08857715545311,-4.46165673850807E-12,
2.58513735103561));
#9982=CARTESIAN_POINT('',(7.08857712267632,0.00123466570667409,2.42852336023369));
#9983=CARTESIAN_POINT('Ctrl Pts',(7.08857715545311,3.31900585956301E-12,
2.42843892255116));
#9984=CARTESIAN_POINT('Ctrl Pts',(7.08857715545311,0.000410617190948955,
2.428467208281));
#9985=CARTESIAN_POINT('Ctrl Pts',(7.08857702866544,0.000821238121669504,
2.42849549165351));
#9986=CARTESIAN_POINT('Ctrl Pts',(7.08857677508315,0.00123186273744409,
2.4285237726487));
#9987=CARTESIAN_POINT('Ctrl Pts',(7.08857677337603,0.00123462397966759,
2.428523962824));
#9988=CARTESIAN_POINT('Ctrl Pts',(7.08854025465424,0.0602369660175714,2.43258763604517));
#9989=CARTESIAN_POINT('Ctrl Pts',(7.08588590411455,0.11921567211675,2.43659616672538));
#9990=CARTESIAN_POINT('Ctrl Pts',(7.07982904186567,0.186822369557015,2.44106952969729));
#9991=CARTESIAN_POINT('Ctrl Pts',(7.07897947661117,0.195643448811554,2.44165079025752));
#9992=CARTESIAN_POINT('Ctrl Pts',(7.0774927640007,0.210071789148959,2.44259727988455));
#9993=CARTESIAN_POINT('Ctrl Pts',(7.07689056797417,0.215682421341409,2.44296427802026));
#9994=CARTESIAN_POINT('Ctrl Pts',(7.07577889611734,0.225641366031836,2.44361373954427));
#9995=CARTESIAN_POINT('Ctrl Pts',(7.07527890133582,0.229990669398404,2.44389670823432));
#9996=CARTESIAN_POINT('Ctrl Pts',(7.07423565016347,0.23880960736887,2.44446907431109));
#9997=CARTESIAN_POINT('Ctrl Pts',(7.0736915773188,0.243279071926444,2.44475841505161));
#9998=CARTESIAN_POINT('Ctrl Pts',(7.07247342880585,0.253011135887692,2.44538682755914));
#9999=CARTESIAN_POINT('Ctrl Pts',(7.07179349041179,0.258272896908093,2.44572556924882));
#10000=CARTESIAN_POINT('Ctrl Pts',(7.06984161628269,0.272917698420617,2.44666569445789));
#10001=CARTESIAN_POINT('Ctrl Pts',(7.06852383276362,0.282294634217964,2.44726458370449));
#10002=CARTESIAN_POINT('Ctrl Pts',(7.06090677652683,0.333829722981961,2.45054092490055));
#10003=CARTESIAN_POINT('Ctrl Pts',(7.0533237140759,0.375790299831245,2.4531528836701));
#10004=CARTESIAN_POINT('Ctrl Pts',(7.03617895593015,0.455895236060439,2.45808706384697));
#10005=CARTESIAN_POINT('Ctrl Pts',(7.02682325599828,0.494062076019784,2.46041483374894));
#10006=CARTESIAN_POINT('Ctrl Pts',(6.97717417179435,0.673505670480455,2.47135044457464));
#10007=CARTESIAN_POINT('Ctrl Pts',(6.92248551594705,0.810317777363745,2.47969874679399));
#10008=CARTESIAN_POINT('Ctrl Pts',(6.82528461060875,0.992275397383697,2.49204252896068));
#10009=CARTESIAN_POINT('Ctrl Pts',(6.79497509402291,1.04338394583525,2.49565684294258));
#10010=CARTESIAN_POINT('Ctrl Pts',(6.75420306693964,1.10562423997621,2.50028890785388));
#10011=CARTESIAN_POINT('Ctrl Pts',(6.74583177967914,1.11809383757276,2.50122895193193));
#10012=CARTESIAN_POINT('Ctrl Pts',(6.73222337040408,1.13787798274131,2.50274038960131));
#10013=CARTESIAN_POINT('Ctrl Pts',(6.72707608773023,1.14525385033864,2.50330839331741));
#10014=CARTESIAN_POINT('Ctrl Pts',(6.71722294491025,1.15917151883042,2.50438889899884));
#10015=CARTESIAN_POINT('Ctrl Pts',(6.7125269701184,1.16572012343655,2.50490101658599));
#10016=CARTESIAN_POINT('Ctrl Pts',(6.7017655676926,1.18053664528241,2.50606827962637));
#10017=CARTESIAN_POINT('Ctrl Pts',(6.69567584613039,1.18878655532312,2.50672435350424));
#10018=CARTESIAN_POINT('Ctrl Pts',(6.67971996387891,1.21005720412223,2.50843210131766));
#10019=CARTESIAN_POINT('Ctrl Pts',(6.66975713222072,1.22300413701099,2.50948751994744));
#10020=CARTESIAN_POINT('Ctrl Pts',(6.58453981323938,1.33097563636166,2.51842675531303));
#10021=CARTESIAN_POINT('Ctrl Pts',(6.50094015791897,1.41906449691718,2.52665148109656));
#10022=CARTESIAN_POINT('Ctrl Pts',(6.30055901765953,1.59498853664329,2.54513649478515));
#10023=CARTESIAN_POINT('Ctrl Pts',(6.18106484259249,1.67872213949061,2.55542696833088));
#10024=CARTESIAN_POINT('Ctrl Pts',(6.04127764800335,1.75543733407049,2.56605223437323));
#10025=CARTESIAN_POINT('Ctrl Pts',(6.02896176303418,1.76202893267157,2.5669768994246));
#10026=CARTESIAN_POINT('Ctrl Pts',(6.0070920256358,1.77343996331735,2.56859741021253));
#10027=CARTESIAN_POINT('Ctrl Pts',(5.99756685486375,1.77831285054461,2.5692961234726));
#10028=CARTESIAN_POINT('Ctrl Pts',(5.98309796682004,1.78556856277171,2.57034628803498));
#10029=CARTESIAN_POINT('Ctrl Pts',(5.97818304460048,1.78800792262705,2.57070107958827));
#10030=CARTESIAN_POINT('Ctrl Pts',(5.97324458884348,1.79043361803056,2.57105558400338));
#10031=CARTESIAN_POINT('Ctrl Pts',(5.97323112840455,1.79044022940787,2.57105655023906));
#10032=CARTESIAN_POINT('Ctrl Pts',(5.97320487235439,1.7904531252509,2.57105843495803));
#10033=CARTESIAN_POINT('Ctrl Pts',(5.97319207673019,1.79045940974114,2.57105935344368));
#10034=CARTESIAN_POINT('Ctrl Pts',(5.97316632002369,1.7904720596426,2.57106120226492));
#10035=CARTESIAN_POINT('Ctrl Pts',(5.97315335899579,1.79047842502269,2.57106213259625));
#10036=CARTESIAN_POINT('Ctrl Pts',(5.9731272691552,1.79049123783319,2.57106400527479));
#10037=CARTESIAN_POINT('Ctrl Pts',(5.9731141402062,1.790497685326,2.57106494763144));
#10038=CARTESIAN_POINT('Ctrl Pts',(5.97308771195149,1.79051066361127,2.57106684454415));
#10039=CARTESIAN_POINT('Ctrl Pts',(5.97307441275842,1.79051719434375,2.57106779909176));
#10040=CARTESIAN_POINT('Ctrl Pts',(5.9730476414839,1.79053034033748,2.571069720567));
#10041=CARTESIAN_POINT('Ctrl Pts',(5.97303416942019,1.79053695558521,2.57107068749298));
#10042=CARTESIAN_POINT('Ctrl Pts',(5.97300704989647,1.79055027182643,2.57107263390383));
#10043=CARTESIAN_POINT('Ctrl Pts',(5.97299340243132,1.79055697281751,2.57107361338868));
#10044=CARTESIAN_POINT('Ctrl Pts',(5.97296592951168,1.79057046180373,2.57107558510219));
#10045=CARTESIAN_POINT('Ctrl Pts',(5.9729521040551,1.79057724979481,2.57107657733061));
#10046=CARTESIAN_POINT('Ctrl Pts',(5.97292427250901,1.79059091406369,2.57107857471978));
#10047=CARTESIAN_POINT('Ctrl Pts',(5.97291026641626,1.79059779033785,2.57107957988036));
#10048=CARTESIAN_POINT('Ctrl Pts',(5.97288207093768,1.79061163246313,2.57108160332353));
#10049=CARTESIAN_POINT('Ctrl Pts',(5.97286788150617,1.79061859833131,2.57108262160898));
#10050=CARTESIAN_POINT('Ctrl Pts',(5.97283931657448,1.79063262099103,2.57108467149981));
#10051=CARTESIAN_POINT('Ctrl Pts',(5.97282494111046,1.7906396777593,2.57108570310216));
#10052=CARTESIAN_POINT('Ctrl Pts',(5.97279600138937,1.79065388353995,2.57108777982099));
#10053=CARTESIAN_POINT('Ctrl Pts',(5.97278143704024,1.79066103259184,2.57108882494363));
#10054=CARTESIAN_POINT('Ctrl Pts',(5.97275211664794,1.7906754243466,2.57109092890986));
#10055=CARTESIAN_POINT('Ctrl Pts',(5.97273736068233,1.79068266700555,2.57109198774744));
#10056=CARTESIAN_POINT('Ctrl Pts',(5.9727076541774,1.79069724737028,2.57109411934879));
#10057=CARTESIAN_POINT('Ctrl Pts',(5.97269270363054,1.79070458507375,2.57109519211264));
#10058=CARTESIAN_POINT('Ctrl Pts',(5.9726626050891,1.79071935691996,2.57109735177134));
#10059=CARTESIAN_POINT('Ctrl Pts',(5.97264745704566,1.79072679108051,2.57109843866922));
#10060=CARTESIAN_POINT('Ctrl Pts',(5.97261696048989,1.79074175730498,2.57110062681131));
#10061=CARTESIAN_POINT('Ctrl Pts',(5.97260161200983,1.79074928934671,2.57110172805269));
#10062=CARTESIAN_POINT('Ctrl Pts',(5.97257071151941,1.79076445281675,2.57110394509994));
#10063=CARTESIAN_POINT('Ctrl Pts',(5.9725551595434,1.79077208422166,2.57110506090282));
#10064=CARTESIAN_POINT('Ctrl Pts',(5.97252384899427,1.79078744790328,2.57110730729155));
#10065=CARTESIAN_POINT('Ctrl Pts',(5.97250809042578,1.790795180171,2.57110843787653));
#10066=CARTESIAN_POINT('Ctrl Pts',(5.97247636356511,1.79081074709209,2.57111071405217));
#10067=CARTESIAN_POINT('Ctrl Pts',(5.97246039527237,1.79081858173883,2.57111185964233));
#10068=CARTESIAN_POINT('Ctrl Pts',(5.97242824583908,1.79083435492997,2.57111416605082));
#10069=CARTESIAN_POINT('Ctrl Pts',(5.9724120645942,1.79084229351844,2.57111532687608));
#10070=CARTESIAN_POINT('Ctrl Pts',(5.97237948594145,1.79085827619806,2.57111766399092));
#10071=CARTESIAN_POINT('Ctrl Pts',(5.97236308857734,1.79086632026042,2.57111884027678));
#10072=CARTESIAN_POINT('Ctrl Pts',(5.97233007431993,1.79088251551715,2.57112120855257));
#10073=CARTESIAN_POINT('Ctrl Pts',(5.97231345748322,1.79089066667623,2.57112240053785));
#10074=CARTESIAN_POINT('Ctrl Pts',(5.97228000099322,1.79090707771628,2.57112480044649));
#10075=CARTESIAN_POINT('Ctrl Pts',(5.97226316127134,1.79091533762317,2.57112600837418));
#10076=CARTESIAN_POINT('Ctrl Pts',(5.96821033339912,1.79290318438824,2.57141671562544));
#10077=CARTESIAN_POINT('Ctrl Pts',(5.96416771133279,1.79486910055042,2.57170535442568));
#10078=CARTESIAN_POINT('Ctrl Pts',(5.9550843520656,1.79924840843737,2.57235092071349));
#10079=CARTESIAN_POINT('Ctrl Pts',(5.95004010708574,1.80165428905277,2.57270738570606));
#10080=CARTESIAN_POINT('Ctrl Pts',(5.93526624459514,1.80862470384438,2.57374567213332));
#10081=CARTESIAN_POINT('Ctrl Pts',(5.92550959022008,1.81313193117825,2.57442409910285));
#10082=CARTESIAN_POINT('Ctrl Pts',(5.85112314628559,1.8467690249183,2.57954517206707));
#10083=CARTESIAN_POINT('Ctrl Pts',(5.78501070564641,1.87251719591821,2.58380417035013));
#10084=CARTESIAN_POINT('Ctrl Pts',(5.57591679250681,1.94136201753426,2.59679114563572));
#10085=CARTESIAN_POINT('Ctrl Pts',(5.42938558965196,1.97197852233778,2.60525083148297));
#10086=CARTESIAN_POINT('Ctrl Pts',(5.21596457167497,1.99207225382881,2.61803044648524));
#10087=CARTESIAN_POINT('Ctrl Pts',(5.15086762364297,1.99499736680657,2.62198219059259));
#10088=CARTESIAN_POINT('Ctrl Pts',(5.0703103922254,1.99467111801823,2.62699437735823));
#10089=CARTESIAN_POINT('Ctrl Pts',(5.05487370116904,1.99442937066823,2.62796026857337));
#10090=CARTESIAN_POINT('Ctrl Pts',(5.03035874410439,1.99376073910522,2.62950348399473));
#10091=CARTESIAN_POINT('Ctrl Pts',(5.02127770633231,1.99345095175818,2.63007715932044));
#10092=CARTESIAN_POINT('Ctrl Pts',(5.00416303744325,1.99275000866163,2.63116229374953));
#10093=CARTESIAN_POINT('Ctrl Pts',(4.99612901532178,1.99237228484056,2.63167332372166));
#10094=CARTESIAN_POINT('Ctrl Pts',(4.97800871792434,1.99141048610662,2.63282972919786));
#10095=CARTESIAN_POINT('Ctrl Pts',(4.96792421401502,1.99079835186766,2.6334759672314));
#10096=CARTESIAN_POINT('Ctrl Pts',(4.9420457067158,1.98903009924406,2.63514134963781));
#10097=CARTESIAN_POINT('Ctrl Pts',(4.92626027352336,1.98776247576293,2.63616393745795));
#10098=CARTESIAN_POINT('Ctrl Pts',(4.81660022527514,1.97764090637914,2.64331612899059));
#10099=CARTESIAN_POINT('Ctrl Pts',(4.72345497253705,1.96232978470293,2.64964664342784));
#10100=CARTESIAN_POINT('Ctrl Pts',(4.46558455054291,1.90092509648242,2.6678489034237));
#10101=CARTESIAN_POINT('Ctrl Pts',(4.30519573921176,1.84018037944455,2.68002429642541));
#10102=CARTESIAN_POINT('Ctrl Pts',(4.14103046651171,1.75255227848553,2.69245390366278));
#10103=CARTESIAN_POINT('Ctrl Pts',(4.12763389415773,1.74520246166273,2.69346737338104));
#10104=CARTESIAN_POINT('Ctrl Pts',(4.10422803508306,1.7320090711367,2.69523487934507));
#10105=CARTESIAN_POINT('Ctrl Pts',(4.09418289347302,1.72623092496356,2.69599239588305));
#10106=CARTESIAN_POINT('Ctrl Pts',(4.07928268657311,1.71748637199194,2.69711382419378));
#10107=CARTESIAN_POINT('Ctrl Pts',(4.0743892422171,1.71458632337467,2.69748175768301));
#10108=CARTESIAN_POINT('Ctrl Pts',(4.06601692985436,1.70957604591039,2.6981105561612));
#10109=CARTESIAN_POINT('Ctrl Pts',(4.06253204880839,1.70747606737805,2.69837207117033));
#10110=CARTESIAN_POINT('Ctrl Pts',(4.05463896535233,1.70268673908978,2.69896388618684));
#10111=CARTESIAN_POINT('Ctrl Pts',(4.05023476844239,1.6999909285477,2.69929376067777));
#10112=CARTESIAN_POINT('Ctrl Pts',(4.03831176358491,1.69262905642084,2.70018598949965));
#10113=CARTESIAN_POINT('Ctrl Pts',(4.03081335032637,1.68792995177575,2.7007462420798));
#10114=CARTESIAN_POINT('Ctrl Pts',(3.99430943582904,1.6647139447737,2.70347066497373));
#10115=CARTESIAN_POINT('Ctrl Pts',(3.96575326395656,1.64549729812261,2.70559259282032));
#10116=CARTESIAN_POINT('Ctrl Pts',(3.83372494170271,1.55159638194335,2.71543025918857));
#10117=CARTESIAN_POINT('Ctrl Pts',(3.73706923804305,1.46782937716243,2.72272767451616));
#10118=CARTESIAN_POINT('Ctrl Pts',(3.59226287767608,1.31572057686954,2.73495150690417));
#10119=CARTESIAN_POINT('Ctrl Pts',(3.53920861368146,1.25258753812167,2.73978622293921));
#10120=CARTESIAN_POINT('Ctrl Pts',(3.46224533861029,1.14855545618745,2.74759775881338));
#10121=CARTESIAN_POINT('Ctrl Pts',(3.43562538092258,1.10977709690693,2.75047789829529));
#10122=CARTESIAN_POINT('Ctrl Pts',(3.40293399785123,1.05834856148039,2.75427756756005));
#10123=CARTESIAN_POINT('Ctrl Pts',(3.395589492297,1.04652289604748,2.7551499121363));
#10124=CARTESIAN_POINT('Ctrl Pts',(3.38382936967621,1.02713765233417,2.75657817233989));
#10125=CARTESIAN_POINT('Ctrl Pts',(3.37933860295248,1.01962404032246,2.75713133916255));
#10126=CARTESIAN_POINT('Ctrl Pts',(3.37077639267072,1.00508188985476,2.75820127738248));
#10127=CARTESIAN_POINT('Ctrl Pts',(3.36669813326708,0.998057550430446,2.75871778881004));
#10128=CARTESIAN_POINT('Ctrl Pts',(3.35741724544162,0.981845036036596,2.75990932659627));
#10129=CARTESIAN_POINT('Ctrl Pts',(3.35224447945945,0.972640131799848,2.76058540502048));
#10130=CARTESIAN_POINT('Ctrl Pts',(3.33632015842499,0.943768554619699,2.76270485679206));
#10131=CARTESIAN_POINT('Ctrl Pts',(3.32582713832255,0.923962012769674,2.76415729338854));
#10132=CARTESIAN_POINT('Ctrl Pts',(3.23774751296958,0.750707328722994,2.77685355142233));
#10133=CARTESIAN_POINT('Ctrl Pts',(3.17998421767927,0.588026098904509,2.78881017708032));
#10134=CARTESIAN_POINT('Ctrl Pts',(3.1227904194247,0.322480041929148,2.80772939197737));
#10135=CARTESIAN_POINT('Ctrl Pts',(3.10912876871158,0.223508524924275,2.81463375820815));
#10136=CARTESIAN_POINT('Ctrl Pts',(3.10219040185798,0.112037327689403,2.82198497726712));
#10137=CARTESIAN_POINT('Ctrl Pts',(3.10155713214352,0.100147350484549,2.82276361774902));
#10138=CARTESIAN_POINT('Ctrl Pts',(3.10077591496193,0.0825068914882814,
2.82391003553255));
#10139=CARTESIAN_POINT('Ctrl Pts',(3.10054632860217,0.0767605476189505,
2.82428209422477));
#10140=CARTESIAN_POINT('Ctrl Pts',(3.10018124912889,0.0665120219008368,
2.82494309155892));
#10141=CARTESIAN_POINT('Ctrl Pts',(3.10003615021763,0.0620103027300323,
2.82523255062056));
#10142=CARTESIAN_POINT('Ctrl Pts',(3.09975381515558,0.052221162266119,2.82586004781252));
#10143=CARTESIAN_POINT('Ctrl Pts',(3.09962235961899,0.0469336777105539,
2.82619776379596));
#10144=CARTESIAN_POINT('Ctrl Pts',(3.09931575784451,0.0322512211414929,
2.82713231472387));
#10145=CARTESIAN_POINT('Ctrl Pts',(3.09918595962792,0.0228552961052907,
2.82772670261983));
#10146=CARTESIAN_POINT('Ctrl Pts',(3.0988423185119,-0.0280759391005415,
2.83093041953442));
#10147=CARTESIAN_POINT('Ctrl Pts',(3.09985939905145,-0.0696124771190814,
2.83347763134926));
#10148=CARTESIAN_POINT('Ctrl Pts',(3.10371476138736,-0.138732467783235,
2.83765157044059));
#10149=CARTESIAN_POINT('Ctrl Pts',(3.1058319548193,-0.166340697732581,2.83930143894376));
#10150=CARTESIAN_POINT('Ctrl Pts',(3.12099001510693,-0.321543636251902,
2.84852167327295));
#10151=CARTESIAN_POINT('Ctrl Pts',(3.14573828711977,-0.447692461286682,
2.85582655281387));
#10152=CARTESIAN_POINT('Ctrl Pts',(3.19907176998566,-0.626350773667581,
2.86680624526192));
#10153=CARTESIAN_POINT('Ctrl Pts',(3.21814648867054,-0.681347586354424,
2.87027496428726));
#10154=CARTESIAN_POINT('Ctrl Pts',(3.24875820866924,-0.758528614746119,
2.87532707307689));
#10155=CARTESIAN_POINT('Ctrl Pts',(3.25835044303736,-0.781453924566613,
2.87685148876626));
#10156=CARTESIAN_POINT('Ctrl Pts',(3.27621718781569,-0.822010104859998,
2.87959499248833));
#10157=CARTESIAN_POINT('Ctrl Pts',(3.28432643245261,-0.839710485126383,
2.88080857533339));
#10158=CARTESIAN_POINT('Ctrl Pts',(3.29696500487535,-0.866263683693215,
2.88265507955644));
#10159=CARTESIAN_POINT('Ctrl Pts',(3.30130372376113,-0.875206317940565,
2.88328145470455));
#10160=CARTESIAN_POINT('Ctrl Pts',(3.30926779326416,-0.891313589617056,
2.88441801729611));
#10161=CARTESIAN_POINT('Ctrl Pts',(3.31286993493676,-0.898489514592974,
2.8849273905006));
#10162=CARTESIAN_POINT('Ctrl Pts',(3.32069119114078,-0.91383861502776,2.88602353094389));
#10163=CARTESIAN_POINT('Ctrl Pts',(3.32492369564684,-0.922004722049179,
2.88661075804306));
#10164=CARTESIAN_POINT('Ctrl Pts',(3.33645959683618,-0.943890024705633,
2.88819563276008));
#10165=CARTESIAN_POINT('Ctrl Pts',(3.34386698759133,-0.957553394392518,
2.88919692392528));
#10166=CARTESIAN_POINT('Ctrl Pts',(3.38085762267307,-1.0239218124382,2.89411983999269));
#10167=CARTESIAN_POINT('Ctrl Pts',(3.41266341670061,-1.075345389917,2.89812008837174));
#10168=CARTESIAN_POINT('Ctrl Pts',(3.4618976697215,-1.14741214976728,2.90400392478264));
#10169=CARTESIAN_POINT('Ctrl Pts',(3.47748940346697,-1.16927356372593,2.90582767304293));
#10170=CARTESIAN_POINT('Ctrl Pts',(3.58241177300322,-1.31027666671523,2.91784219186277));
#10171=CARTESIAN_POINT('Ctrl Pts',(3.68439504589187,-1.41940055981079,2.92838763838404));
#10172=CARTESIAN_POINT('Ctrl Pts',(3.83609472731421,-1.54909857175908,2.9420397000156));
#10173=CARTESIAN_POINT('Ctrl Pts',(3.87586989730947,-1.58056266122812,2.94545574865899));
#10174=CARTESIAN_POINT('Ctrl Pts',(3.9245437356649,-1.6161360528959,2.94940726466923));
#10175=CARTESIAN_POINT('Ctrl Pts',(3.9323240830601,-1.62173674771662,2.9500322047835));
#10176=CARTESIAN_POINT('Ctrl Pts',(3.94444655995106,-1.63033113721861,2.95099520964631));
#10177=CARTESIAN_POINT('Ctrl Pts',(3.94876056917908,-1.6333639780689,2.95133583339078));
#10178=CARTESIAN_POINT('Ctrl Pts',(3.95678289645264,-1.63895644163596,2.9519653344907));
#10179=CARTESIAN_POINT('Ctrl Pts',(3.96048783734651,-1.64152059236494,2.95225450750159));
#10180=CARTESIAN_POINT('Ctrl Pts',(3.9689591545174,-1.64734114969213,2.9529122080171));
#10181=CARTESIAN_POINT('Ctrl Pts',(3.97373099550769,-1.65058943334688,2.95328018966935));
#10182=CARTESIAN_POINT('Ctrl Pts',(3.98624136165873,-1.65902624292279,2.95423861064149));
#10183=CARTESIAN_POINT('Ctrl Pts',(3.99400235845032,-1.66418141712181,2.9548269033059));
#10184=CARTESIAN_POINT('Ctrl Pts',(4.04861408001894,-1.69990786274216,2.9589248947721));
#10185=CARTESIAN_POINT('Ctrl Pts',(4.09670117803248,-1.72855376961531,2.96232017793692));
#10186=CARTESIAN_POINT('Ctrl Pts',(4.28898747099218,-1.83240114836662,2.97533877869482));
#10187=CARTESIAN_POINT('Ctrl Pts',(4.44095221852488,-1.89188281096374,2.98449851604059));
#10188=CARTESIAN_POINT('Ctrl Pts',(4.66372036696744,-1.94899326999315,2.99818971026618));
#10189=CARTESIAN_POINT('Ctrl Pts',(4.72978198092951,-1.96240574263226,3.0022729535877));
#10190=CARTESIAN_POINT('Ctrl Pts',(4.81180612790805,-1.97477460431549,3.00743301431891));
#10191=CARTESIAN_POINT('Ctrl Pts',(4.82724780242245,-1.97691831513816,3.00840821498446));
#10192=CARTESIAN_POINT('Ctrl Pts',(4.85175953858244,-1.98002878639194,3.00996287468294));
#10193=CARTESIAN_POINT('Ctrl Pts',(4.86081403844431,-1.98111473896125,3.01053858958855));
#10194=CARTESIAN_POINT('Ctrl Pts',(4.87786306924405,-1.9830410209908,3.01162545124521));
#10195=CARTESIAN_POINT('Ctrl Pts',(4.88585587654973,-1.98389518914881,3.0121361530462));
#10196=CARTESIAN_POINT('Ctrl Pts',(4.90385540343027,-1.9857087774684,3.01328895833554));
#10197=CARTESIAN_POINT('Ctrl Pts',(4.91386459368685,-1.98664090508373,3.01393190229928));
#10198=CARTESIAN_POINT('Ctrl Pts',(4.93949285661997,-1.98883232634621,3.01558316478169));
#10199=CARTESIAN_POINT('Ctrl Pts',(4.95512026702194,-1.98998328486813,3.01659482892399));
#10200=CARTESIAN_POINT('Ctrl Pts',(5.05986649364596,-1.99645803224626,3.02340905093284));
#10201=CARTESIAN_POINT('Ctrl Pts',(5.14923040694753,-1.9959770926576,3.02939085914628));
#10202=CARTESIAN_POINT('Ctrl Pts',(5.36849496993185,-1.98006007821124,3.04445245449078));
#10203=CARTESIAN_POINT('Ctrl Pts',(5.49748546654194,-1.95783991751101,3.05366260617979));
#10204=CARTESIAN_POINT('Ctrl Pts',(5.68424947629233,-1.90641437568253,3.06700446626609));
#10205=CARTESIAN_POINT('Ctrl Pts',(5.74430106366956,-1.88676963982752,3.07128995911322));
#10206=CARTESIAN_POINT('Ctrl Pts',(5.81276277897269,-1.86071521220755,3.07609592541344));
#10207=CARTESIAN_POINT('Ctrl Pts',(5.82217324975735,-1.85705183257374,3.07675472287846));
#10208=CARTESIAN_POINT('Ctrl Pts',(5.83655672417828,-1.85132636859108,3.07775843954569));
#10209=CARTESIAN_POINT('Ctrl Pts',(5.84154971322237,-1.84931541753976,3.07810626388341));
#10210=CARTESIAN_POINT('Ctrl Pts',(5.85069908350851,-1.84558735085988,3.07874244922983));
#10211=CARTESIAN_POINT('Ctrl Pts',(5.85485779200564,-1.84387639394661,3.07903115880679));
#10212=CARTESIAN_POINT('Ctrl Pts',(5.86421235132211,-1.83999074362486,3.0796795655577));
#10213=CARTESIAN_POINT('Ctrl Pts',(5.86940479118589,-1.83780810191284,3.08003878021826));
#10214=CARTESIAN_POINT('Ctrl Pts',(5.88466537792273,-1.83131712022219,3.08109265535501));
#10215=CARTESIAN_POINT('Ctrl Pts',(5.89470756246268,-1.82694774838943,3.08178376622395));
#10216=CARTESIAN_POINT('Ctrl Pts',(5.99276773422059,-1.78331765777382,3.08851369443884));
#10217=CARTESIAN_POINT('Ctrl Pts',(6.07787944457729,-1.73780383528504,3.09421005098518));
#10218=CARTESIAN_POINT('Ctrl Pts',(6.26786664299274,-1.61775420838623,3.10732500136062));
#10219=CARTESIAN_POINT('Ctrl Pts',(6.36948383709108,-1.53889451260489,3.11467295179483));
#10220=CARTESIAN_POINT('Ctrl Pts',(6.50701255032076,-1.4091225206863,3.12597722672863));
#10221=CARTESIAN_POINT('Ctrl Pts',(6.54927190348036,-1.36542987486289,3.12967195506992));
#10222=CARTESIAN_POINT('Ctrl Pts',(6.59947559741968,-1.30854080624874,3.13439471140967));
#10223=CARTESIAN_POINT('Ctrl Pts',(6.60935274254128,-1.29708845014935,3.1353411837816));
#10224=CARTESIAN_POINT('Ctrl Pts',(6.62490970612298,-1.27863016397478,3.1368605248164));
#10225=CARTESIAN_POINT('Ctrl Pts',(6.63067400923459,-1.27169596087608,3.13742993993294));
#10226=CARTESIAN_POINT('Ctrl Pts',(6.64149753611098,-1.25849466585887,3.13851157204442));
#10227=CARTESIAN_POINT('Ctrl Pts',(6.64656621782396,-1.25223553385189,3.13902339341002));
#10228=CARTESIAN_POINT('Ctrl Pts',(6.65797719607487,-1.2379687227946,3.14018783073169));
#10229=CARTESIAN_POINT('Ctrl Pts',(6.66429612700988,-1.22994272678768,3.14084135804056));
#10230=CARTESIAN_POINT('Ctrl Pts',(6.6804801035732,-1.20905857178749,3.14253810697932));
#10231=CARTESIAN_POINT('Ctrl Pts',(6.69025043562454,-1.19612829274047,3.14358499397311));
#10232=CARTESIAN_POINT('Ctrl Pts',(6.77707964881563,-1.07825743907066,3.15309774340971));
#10233=CARTESIAN_POINT('Ctrl Pts',(6.84383539292177,-0.966145859060132,
3.16196092255532));
#10234=CARTESIAN_POINT('Ctrl Pts',(6.93881071945174,-0.764030992167013,
3.17747451671486));
#10235=CARTESIAN_POINT('Ctrl Pts',(6.97247817385822,-0.677036552294206,
3.18401069335264));
#10236=CARTESIAN_POINT('Ctrl Pts',(7.01730257704336,-0.531731298182875,
3.1944613813244));
#10237=CARTESIAN_POINT('Ctrl Pts',(7.03216384096697,-0.474708524401591,
3.19844902578721));
#10238=CARTESIAN_POINT('Ctrl Pts',(7.04655994670518,-0.407383197353299,
3.20296468330791));
#10239=CARTESIAN_POINT('Ctrl Pts',(7.04856635010261,-0.397644457040907,
3.20361321800442));
#10240=CARTESIAN_POINT('Ctrl Pts',(7.05154018537318,-0.382643273280248,
3.20460461165063));
#10241=CARTESIAN_POINT('Ctrl Pts',(7.05255937194231,-0.377391425196362,
3.204950268831));
#10242=CARTESIAN_POINT('Ctrl Pts',(7.0543967409988,-0.367715519263763,3.20558439946568));
#10243=CARTESIAN_POINT('Ctrl Pts',(7.05522108325874,-0.363292806948913,
3.20587320568759));
#10244=CARTESIAN_POINT('Ctrl Pts',(7.05705093917638,-0.353287575604664,
3.20652421702005));
#10245=CARTESIAN_POINT('Ctrl Pts',(7.05804760793636,-0.347703540396118,
3.20688592156302));
#10246=CARTESIAN_POINT('Ctrl Pts',(7.06056132531484,-0.333264135557118,
3.2078171931973));
#10247=CARTESIAN_POINT('Ctrl Pts',(7.06204241067935,-0.324402520241099,
3.20838480764394));
#10248=CARTESIAN_POINT('Ctrl Pts',(7.07121065860102,-0.267171646286709,
3.2120271465433));
#10249=CARTESIAN_POINT('Ctrl Pts',(7.07717478455331,-0.218538906957556,
3.21501436720786));
#10250=CARTESIAN_POINT('Ctrl Pts',(7.08249696326586,-0.156217553636739,
3.21876095816004));
#10251=CARTESIAN_POINT('Ctrl Pts',(7.08351321701481,-0.142691686145127,
3.21956921403908));
#10252=CARTESIAN_POINT('Ctrl Pts',(7.08714366116788,-0.0867390665351364,
3.22289626608107));
#10253=CARTESIAN_POINT('Ctrl Pts',(7.08853944685439,-0.0442432801139429,
3.22538421847911));
#10254=CARTESIAN_POINT('Ctrl Pts',(7.08857690420624,-0.00115606523612509,
3.22789393898319));
#10255=CARTESIAN_POINT('Ctrl Pts',(7.08857715545314,-0.000578028495419831,
3.22792760577034));
#10256=CARTESIAN_POINT('Ctrl Pts',(7.08857715545311,9.38914434820126E-11,
3.22796126976449));
#10257=CARTESIAN_POINT('Origin',(5.09382715545311,0.,-6.77268258743872));
#10258=CARTESIAN_POINT('',(7.08857715545311,-9.37345802482419E-11,4.18476380915572));
#10259=CARTESIAN_POINT('',(7.08857715495348,4.36882467403433E-5,4.02544645345466));
#10260=CARTESIAN_POINT('',(7.08857715545311,8.3550772080578E-14,-6.77268258743872));
#10261=CARTESIAN_POINT('Ctrl Pts',(7.08857715545311,-9.37346381069126E-11,
4.18476380915572));
#10262=CARTESIAN_POINT('Ctrl Pts',(7.08857715544518,-0.168685457521296,
4.17493968220012));
#10263=CARTESIAN_POINT('Ctrl Pts',(7.06718218732477,-0.336672456479282,
4.16528040244134));
#10264=CARTESIAN_POINT('Ctrl Pts',(7.01913649669845,-0.522246467177999,
4.15346024509175));
#10265=CARTESIAN_POINT('Ctrl Pts',(7.01298196055782,-0.544428322291977,
4.15202940146003));
#10266=CARTESIAN_POINT('Ctrl Pts',(7.00345982020135,-0.576577096447058,
4.14992716976473));
#10267=CARTESIAN_POINT('Ctrl Pts',(7.00039492180035,-0.586632259583106,
4.14926556326834));
#10268=CARTESIAN_POINT('Ctrl Pts',(6.99482333892916,-0.604406262242485,
4.14808859976392));
#10269=CARTESIAN_POINT('Ctrl Pts',(6.99234873746499,-0.612134967879349,
4.14757429812032));
#10270=CARTESIAN_POINT('Ctrl Pts',(6.9871005811178,-0.628188096590249,4.14650069997607));
#10271=CARTESIAN_POINT('Ctrl Pts',(6.98431912905566,-0.636509734986001,
4.14594115391338));
#10272=CARTESIAN_POINT('Ctrl Pts',(6.97695221431537,-0.658075997784857,
4.14448306267339));
#10273=CARTESIAN_POINT('Ctrl Pts',(6.9722819618218,-0.671290942913361,4.14358174434966));
#10274=CARTESIAN_POINT('Ctrl Pts',(6.95101157132762,-0.729517064067628,
4.13957482989187));
#10275=CARTESIAN_POINT('Ctrl Pts',(6.93293123839276,-0.77396681090106,4.13642065378434));
#10276=CARTESIAN_POINT('Ctrl Pts',(6.8784200460391,-0.895255297385321,4.12754012092097));
#10277=CARTESIAN_POINT('Ctrl Pts',(6.83865537915418,-0.970476976769931,
4.1217134399807));
#10278=CARTESIAN_POINT('Ctrl Pts',(6.72375825304741,-1.15780573846782,4.10646249844511));
#10279=CARTESIAN_POINT('Ctrl Pts',(6.64183531549823,-1.26525226317017,4.09695183356967));
#10280=CARTESIAN_POINT('Ctrl Pts',(6.53240339601693,-1.38208762899703,4.08622313576878));
#10281=CARTESIAN_POINT('Ctrl Pts',(6.51475521064603,-1.40022548848324,4.08454598131497));
#10282=CARTESIAN_POINT('Ctrl Pts',(6.49107387052963,-1.42365490501938,4.08236976319191));
#10283=CARTESIAN_POINT('Ctrl Pts',(6.48534804172971,-1.42925200704962,4.08184912665446));
#10284=CARTESIAN_POINT('Ctrl Pts',(6.47604534064768,-1.43823666896614,4.08101238754025));
#10285=CARTESIAN_POINT('Ctrl Pts',(6.47248941970006,-1.44164565336273,4.08069467512534));
#10286=CARTESIAN_POINT('Ctrl Pts',(6.46559061582683,-1.44821051806986,4.08008244921019));
#10287=CARTESIAN_POINT('Ctrl Pts',(6.46224942286905,-1.45136804232795,4.07978781585456));
#10288=CARTESIAN_POINT('Ctrl Pts',(6.45420045771056,-1.45892204460257,4.07908245599499));
#10289=CARTESIAN_POINT('Ctrl Pts',(6.44948219682547,-1.4633073721104,4.07867257283375));
#10290=CARTESIAN_POINT('Ctrl Pts',(6.43314007578034,-1.47834946449639,4.07726489955268));
#10291=CARTESIAN_POINT('Ctrl Pts',(6.42141079337622,-1.48889152006443,4.07627531843306));
#10292=CARTESIAN_POINT('Ctrl Pts',(6.35004396862921,-1.5515206630299,4.07036895487261));
#10293=CARTESIAN_POINT('Ctrl Pts',(6.2874667488758,-1.60016386009697,4.06566405075377));
#10294=CARTESIAN_POINT('Ctrl Pts',(6.17740011583619,-1.67566190638798,4.05784717117237));
#10295=CARTESIAN_POINT('Ctrl Pts',(6.13140862784903,-1.70452282664882,4.05470348376064));
#10296=CARTESIAN_POINT('Ctrl Pts',(5.97266525032127,-1.795330209042,4.04408462587772));
#10297=CARTESIAN_POINT('Ctrl Pts',(5.85513409613194,-1.84823520537275,4.03657709673123));
#10298=CARTESIAN_POINT('Ctrl Pts',(5.70989220393536,-1.89739400630095,4.02714428438091));
#10299=CARTESIAN_POINT('Ctrl Pts',(5.68630315111657,-1.90489166883283,4.02560859093979));
#10300=CARTESIAN_POINT('Ctrl Pts',(5.65288771636854,-1.91483188195549,4.02342532564944));
#10301=CARTESIAN_POINT('Ctrl Pts',(5.64317230833253,-1.91764171417169,4.02278962940731));
#10302=CARTESIAN_POINT('Ctrl Pts',(5.62619808557777,-1.92241131926098,4.02167718938542));
#10303=CARTESIAN_POINT('Ctrl Pts',(5.61894871880877,-1.92440417502588,4.02120152256362));
#10304=CARTESIAN_POINT('Ctrl Pts',(5.60373652000043,-1.92849366178767,4.0202021118443));
#10305=CARTESIAN_POINT('Ctrl Pts',(5.59577164076622,-1.93058206091953,4.01967811325639));
#10306=CARTESIAN_POINT('Ctrl Pts',(5.57674034621484,-1.93544635205272,4.01842424269346));
#10307=CARTESIAN_POINT('Ctrl Pts',(5.56566269481705,-1.93817670669019,4.01769292588816));
#10308=CARTESIAN_POINT('Ctrl Pts',(5.52777782491709,-1.94717031191082,4.01518652123842));
#10309=CARTESIAN_POINT('Ctrl Pts',(5.50086564947327,-1.95297336040285,4.01339689600016));
#10310=CARTESIAN_POINT('Ctrl Pts',(5.43574479166177,-1.96561085538815,4.0090423952495));
#10311=CARTESIAN_POINT('Ctrl Pts',(5.39744111586407,-1.97189044755189,4.0064612248424));
#10312=CARTESIAN_POINT('Ctrl Pts',(5.2455210928835,-1.99226532840329,3.99614645484045));
#10313=CARTESIAN_POINT('Ctrl Pts',(5.13097330789122,-1.99768542385434,3.98818313822186));
#10314=CARTESIAN_POINT('Ctrl Pts',(4.91229044824469,-1.98921346808849,3.9729268045579));
#10315=CARTESIAN_POINT('Ctrl Pts',(4.80844168670823,-1.97698892824479,3.96566390672439));
#10316=CARTESIAN_POINT('Ctrl Pts',(4.69003769705261,-1.95352170824858,3.95766231752985));
#10317=CARTESIAN_POINT('Ctrl Pts',(4.67409535379721,-1.95015851834441,3.9565911257986));
#10318=CARTESIAN_POINT('Ctrl Pts',(4.65164316753662,-1.94513391963992,3.95509294647673));
#10319=CARTESIAN_POINT('Ctrl Pts',(4.64509825687946,-1.94363448807067,3.95465747746288));
#10320=CARTESIAN_POINT('Ctrl Pts',(4.6340805167136,-1.94105171695287,3.95392667055196));
#10321=CARTESIAN_POINT('Ctrl Pts',(4.62960367671393,-1.93998590278659,3.95363035383835));
#10322=CARTESIAN_POINT('Ctrl Pts',(4.62044218307069,-1.93777127003361,3.95302531542296));
#10323=CARTESIAN_POINT('Ctrl Pts',(4.61575795031524,-1.93662093950825,3.9527166816312));
#10324=CARTESIAN_POINT('Ctrl Pts',(4.60375933652997,-1.93362819294203,3.95192785812466));
#10325=CARTESIAN_POINT('Ctrl Pts',(4.59645107011538,-1.93176124036041,3.95144905152288));
#10326=CARTESIAN_POINT('Ctrl Pts',(4.56615890249008,-1.9238395684421,3.9494706670552));
#10327=CARTESIAN_POINT('Ctrl Pts',(4.54327248161798,-1.91741548414262,3.94799087193066));
#10328=CARTESIAN_POINT('Ctrl Pts',(4.48229704888695,-1.89911816583587,3.94407497193255));
#10329=CARTESIAN_POINT('Ctrl Pts',(4.44443901521083,-1.88650849878358,3.94167181058319));
#10330=CARTESIAN_POINT('Ctrl Pts',(4.3197300874655,-1.84077110655513,3.93377266870492));
#10331=CARTESIAN_POINT('Ctrl Pts',(4.23481667842238,-1.80271106885129,3.92841814638109));
#10332=CARTESIAN_POINT('Ctrl Pts',(4.03814722745226,-1.6974962820613,3.91545385079092));
#10333=CARTESIAN_POINT('Ctrl Pts',(3.92972636592304,-1.62505898083826,3.90781322595053));
#10334=CARTESIAN_POINT('Ctrl Pts',(3.8166014520879,-1.5323135312837,3.89874153182216));
#10335=CARTESIAN_POINT('Ctrl Pts',(3.8041935596417,-1.52188548189055,3.89773059888617));
#10336=CARTESIAN_POINT('Ctrl Pts',(3.78417475979877,-1.50464032906498,3.89607253990372));
#10337=CARTESIAN_POINT('Ctrl Pts',(3.77648657129276,-1.49791378136283,3.89542911145248));
#10338=CARTESIAN_POINT('Ctrl Pts',(3.76282980752074,-1.48577874924235,3.89427400228424));
#10339=CARTESIAN_POINT('Ctrl Pts',(3.75684164299108,-1.48039257235171,3.8937632565234));
#10340=CARTESIAN_POINT('Ctrl Pts',(3.74421894405368,-1.46889977333143,3.89267746432896));
#10341=CARTESIAN_POINT('Ctrl Pts',(3.73759288562572,-1.46278414994466,3.89210204431425));
#10342=CARTESIAN_POINT('Ctrl Pts',(3.71996612297027,-1.44629253587602,3.89055646449893));
#10343=CARTESIAN_POINT('Ctrl Pts',(3.70904173682172,-1.43583618823217,3.88958288298789));
#10344=CARTESIAN_POINT('Ctrl Pts',(3.65483582539958,-1.38275859321155,3.8846714526289));
#10345=CARTESIAN_POINT('Ctrl Pts',(3.61340224691981,-1.33830421396426,3.88065372563191));
#10346=CARTESIAN_POINT('Ctrl Pts',(3.49097837554367,-1.19430225816004,3.86791789930762));
#10347=CARTESIAN_POINT('Ctrl Pts',(3.41752069534814,-1.08879380085662,3.85894855513481));
#10348=CARTESIAN_POINT('Ctrl Pts',(3.30746079226101,-0.892876529603085,
3.84330737973299));
#10349=CARTESIAN_POINT('Ctrl Pts',(3.26637131767857,-0.805445724567154,
3.83664549145883));
#10350=CARTESIAN_POINT('Ctrl Pts',(3.22784032555064,-0.705152915714656,
3.82958381177159));
#10351=CARTESIAN_POINT('Ctrl Pts',(3.22399716649293,-0.694898056723149,
3.82886835104965));
#10352=CARTESIAN_POINT('Ctrl Pts',(3.21830548518843,-0.679321536867135,
3.827792111869));
#10353=CARTESIAN_POINT('Ctrl Pts',(3.21639480392385,-0.674023036248907,
3.82742784804097));
#10354=CARTESIAN_POINT('Ctrl Pts',(3.21299902101718,-0.664479731489126,
3.82677513562387));
#10355=CARTESIAN_POINT('Ctrl Pts',(3.21150581490721,-0.660237954796991,
3.82648622115841));
#10356=CARTESIAN_POINT('Ctrl Pts',(3.20825677698235,-0.65090773813331,3.82585336244394));
#10357=CARTESIAN_POINT('Ctrl Pts',(3.20650719348742,-0.645817233071268,
3.82550978517489));
#10358=CARTESIAN_POINT('Ctrl Pts',(3.20153464902753,-0.63115656197493,3.82452501337038));
#10359=CARTESIAN_POINT('Ctrl Pts',(3.19836367000329,-0.621568758081545,
3.82388677336884));
#10360=CARTESIAN_POINT('Ctrl Pts',(3.17589339637236,-0.551856025009419,
3.81928516677135));
#10361=CARTESIAN_POINT('Ctrl Pts',(3.15938385495189,-0.490862314019932,
3.81546853706149));
#10362=CARTESIAN_POINT('Ctrl Pts',(3.11767874775922,-0.301565207734443,
3.80397275165978));
#10363=CARTESIAN_POINT('Ctrl Pts',(3.10217018004465,-0.171491505671629,
3.79653640939479));
#10364=CARTESIAN_POINT('Ctrl Pts',(3.0976697843183,0.0483230484799643,3.78360365164448));
#10365=CARTESIAN_POINT('Ctrl Pts',(3.10182483649588,0.137488995768343,3.77826108998273));
#10366=CARTESIAN_POINT('Ctrl Pts',(3.11370470858484,0.241636260315474,3.77175576153798));
#10367=CARTESIAN_POINT('Ctrl Pts',(3.11566344872655,0.257179537500163,3.77077807323617));
#10368=CARTESIAN_POINT('Ctrl Pts',(3.1191791299521,0.282654858790892,3.76916372116944));
#10369=CARTESIAN_POINT('Ctrl Pts',(3.12062845818183,0.292601245675392,3.76853043151641));
#10370=CARTESIAN_POINT('Ctrl Pts',(3.12337200629763,0.310481369968122,3.76738642284655));
#10371=CARTESIAN_POINT('Ctrl Pts',(3.12463913625113,0.318419091580993,3.76687656702241));
#10372=CARTESIAN_POINT('Ctrl Pts',(3.12744628079598,0.335346082279987,3.76578497859009));
#10373=CARTESIAN_POINT('Ctrl Pts',(3.12900003363533,0.344332856328137,3.76520282271844));
#10374=CARTESIAN_POINT('Ctrl Pts',(3.13337713565051,0.368654879339487,3.76362000936851));
#10375=CARTESIAN_POINT('Ctrl Pts',(3.13631871328186,0.383967936436851,3.76261563768816));
#10376=CARTESIAN_POINT('Ctrl Pts',(3.15293405522157,0.465303592599773,3.75723789065463));
#10377=CARTESIAN_POINT('Ctrl Pts',(3.16976768337267,0.530628732653149,3.7527651368445));
#10378=CARTESIAN_POINT('Ctrl Pts',(3.23847015368414,0.750482087264382,3.73717866371862));
#10379=CARTESIAN_POINT('Ctrl Pts',(3.30593618002157,0.899449104254594,3.72563317947668));
#10380=CARTESIAN_POINT('Ctrl Pts',(3.41968622368333,1.08598794387326,3.71063775818693));
#10381=CARTESIAN_POINT('Ctrl Pts',(3.45060167785383,1.13222299687918,3.70687834761051));
#10382=CARTESIAN_POINT('Ctrl Pts',(3.48890050399811,1.18461999645955,3.70261844692349));
#10383=CARTESIAN_POINT('Ctrl Pts',(3.49444233434071,1.19209156297615,3.70201103372938));
#10384=CARTESIAN_POINT('Ctrl Pts',(3.50350488786465,1.20413284879238,3.70103252747815));
#10385=CARTESIAN_POINT('Ctrl Pts',(3.50699344657215,1.20872644328681,3.70065933784227));
#10386=CARTESIAN_POINT('Ctrl Pts',(3.51324231964693,1.21688102855489,3.69999711976966));
#10387=CARTESIAN_POINT('Ctrl Pts',(3.51599481817817,1.22044785945556,3.69970756303625));
#10388=CARTESIAN_POINT('Ctrl Pts',(3.52199718116999,1.22817178588013,3.69908075946758));
#10389=CARTESIAN_POINT('Ctrl Pts',(3.52525146044897,1.23232531998495,3.69874382868134));
#10390=CARTESIAN_POINT('Ctrl Pts',(3.53447341856897,1.24399986427066,3.69779701864955));
#10391=CARTESIAN_POINT('Ctrl Pts',(3.54047906477935,1.25149089368089,3.69718975007611));
#10392=CARTESIAN_POINT('Ctrl Pts',(3.57872284560016,1.29849411340336,3.6933789089183));
#10393=CARTESIAN_POINT('Ctrl Pts',(3.61241507634537,1.33680486857441,3.69027055031326));
#10394=CARTESIAN_POINT('Ctrl Pts',(3.75170794502934,1.48344876530115,3.67816825642467));
#10395=CARTESIAN_POINT('Ctrl Pts',(3.86801266812822,1.58091393616315,3.66962013751421));
#10396=CARTESIAN_POINT('Ctrl Pts',(4.0627695384565,1.7095898487232,3.65584430977834));
#10397=CARTESIAN_POINT('Ctrl Pts',(4.13404099634435,1.75059573212043,3.65090531944602));
#10398=CARTESIAN_POINT('Ctrl Pts',(4.22142951305117,1.79393063080244,3.64484952544176));
#10399=CARTESIAN_POINT('Ctrl Pts',(4.23530570976769,1.8006125794268,3.64388810540857));
#10400=CARTESIAN_POINT('Ctrl Pts',(4.25829045132254,1.81135457392184,3.6422951691027));
#10401=CARTESIAN_POINT('Ctrl Pts',(4.26735470073241,1.81550826277797,3.64166687343972));
#10402=CARTESIAN_POINT('Ctrl Pts',(4.28377595232894,1.8228848339123,3.64052825375207));
#10403=CARTESIAN_POINT('Ctrl Pts',(4.29112204619071,1.82613158723095,3.64001875756983));
#10404=CARTESIAN_POINT('Ctrl Pts',(4.30690215139824,1.83299230544158,3.63892393459924));
#10405=CARTESIAN_POINT('Ctrl Pts',(4.315341866255,1.83659260689268,3.63833815835825));
#10406=CARTESIAN_POINT('Ctrl Pts',(4.33842464417495,1.84625180688925,3.6367352678884));
#10407=CARTESIAN_POINT('Ctrl Pts',(4.35311529890635,1.85219453894624,3.63571427752956));
#10408=CARTESIAN_POINT('Ctrl Pts',(4.43441984209327,1.88396226987241,3.63005769140693));
#10409=CARTESIAN_POINT('Ctrl Pts',(4.50230593188078,1.90636628290309,3.62530992539184));
#10410=CARTESIAN_POINT('Ctrl Pts',(4.76307851271704,1.9771561872093,3.60698129078445));
#10411=CARTESIAN_POINT('Ctrl Pts',(4.96159393700057,2.00026075941747,3.59271506159357));
#10412=CARTESIAN_POINT('Ctrl Pts',(5.18100717846272,1.992952397945,3.57807725593972));
#10413=CARTESIAN_POINT('Ctrl Pts',(5.20177048993695,1.99193572563543,3.57670475659522));
#10414=CARTESIAN_POINT('Ctrl Pts',(5.22991413163123,1.99011629619296,3.57486496418902));
#10415=CARTESIAN_POINT('Ctrl Pts',(5.23731061286233,1.98959670262184,3.57438337592298));
#10416=CARTESIAN_POINT('Ctrl Pts',(5.24901022677738,1.98870923609749,3.57362484649662));
#10417=CARTESIAN_POINT('Ctrl Pts',(5.25331526730577,1.98836861632971,3.57334642906661));
#10418=CARTESIAN_POINT('Ctrl Pts',(5.2622008664577,1.98763653366105,3.57277325673427));
#10419=CARTESIAN_POINT('Ctrl Pts',(5.26678120130415,1.98724321483594,3.57247861914212));
#10420=CARTESIAN_POINT('Ctrl Pts',(5.27777636997539,1.9862607445281,3.57177323029626));
#10421=CARTESIAN_POINT('Ctrl Pts',(5.28418985840642,1.9856563405711,3.57136332256596));
#10422=CARTESIAN_POINT('Ctrl Pts',(5.30629533251938,1.98346504565613,3.56995547363347));
#10423=CARTESIAN_POINT('Ctrl Pts',(5.32197182585846,1.98172307839815,3.56896574418144));
#10424=CARTESIAN_POINT('Ctrl Pts',(5.41623778925947,1.9701148139321,3.56305770284072));
#10425=CARTESIAN_POINT('Ctrl Pts',(5.49421189549902,1.95575966508944,3.5583513995742));
#10426=CARTESIAN_POINT('Ctrl Pts',(5.59267232724365,1.93149505940367,3.55241251324111));
#10427=CARTESIAN_POINT('Ctrl Pts',(5.61412160184396,1.92582797289528,3.55111910548171));
#10428=CARTESIAN_POINT('Ctrl Pts',(5.79247323985027,1.87550864180013,3.54033729976511));
#10429=CARTESIAN_POINT('Ctrl Pts',(5.94342959345671,1.81212826871002,3.53097196477376));
#10430=CARTESIAN_POINT('Ctrl Pts',(6.10509183627556,1.71956631779482,3.51949302039675));
#10431=CARTESIAN_POINT('Ctrl Pts',(6.12499941118154,1.70770263392336,3.51805349302589));
#10432=CARTESIAN_POINT('Ctrl Pts',(6.15379969465358,1.6898522166908,3.51593031143604));
#10433=CARTESIAN_POINT('Ctrl Pts',(6.16285847219723,1.68413607965307,3.51525649647807));
#10434=CARTESIAN_POINT('Ctrl Pts',(6.17861062085973,1.67401808998066,3.51407406421678));
#10435=CARTESIAN_POINT('Ctrl Pts',(6.18532438700091,1.66964832311669,3.51356663997991));
#10436=CARTESIAN_POINT('Ctrl Pts',(6.19828736545144,1.66109955202571,3.51258008721594));
#10437=CARTESIAN_POINT('Ctrl Pts',(6.20453964092166,1.65692542055978,3.51210114654019));
#10438=CARTESIAN_POINT('Ctrl Pts',(6.22092866919317,1.64584936409896,3.51083740566849));
#10439=CARTESIAN_POINT('Ctrl Pts',(6.23102550445284,1.63888921392634,3.51005042298985));
#10440=CARTESIAN_POINT('Ctrl Pts',(6.26818543475536,1.61276466483037,3.50712219344519));
#10441=CARTESIAN_POINT('Ctrl Pts',(6.29483228988954,1.59302030171959,3.5049589910087));
#10442=CARTESIAN_POINT('Ctrl Pts',(6.36022367553467,1.54199418225084,3.49948585862434));
#10443=CARTESIAN_POINT('Ctrl Pts',(6.3983106728703,1.50991002685388,3.49614642308244));
#10444=CARTESIAN_POINT('Ctrl Pts',(6.51607246560829,1.40292462004297,3.48533020141262));
#10445=CARTESIAN_POINT('Ctrl Pts',(6.59080392461046,1.32288934194362,3.47768858874758));
#10446=CARTESIAN_POINT('Ctrl Pts',(6.72001423243646,1.15946105250098,3.46318190124743));
#10447=CARTESIAN_POINT('Ctrl Pts',(6.77556957581477,1.07730282279316,3.45633483650199));
#10448=CARTESIAN_POINT('Ctrl Pts',(6.83024285758485,0.981839176404877,3.44910403192548));
#10449=CARTESIAN_POINT('Ctrl Pts',(6.83561086552789,0.972284515571788,3.44838804159841));
#10450=CARTESIAN_POINT('Ctrl Pts',(6.84361906219759,0.957751318688625,3.44731116621229));
#10451=CARTESIAN_POINT('Ctrl Pts',(6.84631724651666,0.952805220369281,3.44694678979151));
#10452=CARTESIAN_POINT('Ctrl Pts',(6.8511313235749,0.943890802064821,3.44629395944234));
#10453=CARTESIAN_POINT('Ctrl Pts',(6.85325477585697,0.939926718030011,3.44600503884596));
#10454=CARTESIAN_POINT('Ctrl Pts',(6.8578897959809,0.931203264826867,3.44537226539275));
#10455=CARTESIAN_POINT('Ctrl Pts',(6.86039551493203,0.926440906401836,3.4450287788303));
#10456=CARTESIAN_POINT('Ctrl Pts',(6.86754463320332,0.91271885399775,3.44404452895397));
#10457=CARTESIAN_POINT('Ctrl Pts',(6.87213943539684,0.903733833824589,3.44340671531134));
#10458=CARTESIAN_POINT('Ctrl Pts',(6.90490003060749,0.83845391932637,3.43881795304588));
#10459=CARTESIAN_POINT('Ctrl Pts',(6.93045833880855,0.780882535163358,3.43501281075605));
#10460=CARTESIAN_POINT('Ctrl Pts',(7.00707875344604,0.583608389057448,3.42246005125068));
#10461=CARTESIAN_POINT('Ctrl Pts',(7.04524375895339,0.439439501650824,3.41404333454195));
#10462=CARTESIAN_POINT('Ctrl Pts',(7.0772801406051,0.223220693816843,3.40107997807778));
#10463=CARTESIAN_POINT('Ctrl Pts',(7.08388258814698,0.15359383560584,3.3968617862632));
#10464=CARTESIAN_POINT('Ctrl Pts',(7.0875124804748,0.0672331879277639,3.39150336582134));
#10465=CARTESIAN_POINT('Ctrl Pts',(7.08800166959783,0.050689824531779,3.39047131458294));
#10466=CARTESIAN_POINT('Ctrl Pts',(7.08840915873896,0.026886180326674,3.38897753977713));
#10467=CARTESIAN_POINT('Ctrl Pts',(7.08849377643241,0.0196291480183904,
3.38852095762822));
#10468=CARTESIAN_POINT('Ctrl Pts',(7.08856446090382,0.00823273870908804,
3.3878020387734));
#10469=CARTESIAN_POINT('Ctrl Pts',(7.08857724960592,0.00409354651653826,
3.38754053199994));
#10470=CARTESIAN_POINT('Ctrl Pts',(7.08857715493132,-4.56255882934932E-5,
3.38727862543405));
#10471=CARTESIAN_POINT('Ctrl Pts',(7.08857715545311,9.38937122496597E-11,
3.22796126976449));
#10472=CARTESIAN_POINT('Ctrl Pts',(7.08857715544517,0.168685454855076,3.2377853965787));
#10473=CARTESIAN_POINT('Ctrl Pts',(7.06718218800094,0.336672451181935,3.24744467620048));
#10474=CARTESIAN_POINT('Ctrl Pts',(7.01913649848504,0.522246460643926,3.25926483344194));
#10475=CARTESIAN_POINT('Ctrl Pts',(7.01298196209565,0.544428316921216,3.26069567714573));
#10476=CARTESIAN_POINT('Ctrl Pts',(7.00345982108771,0.576577093536144,3.26279790899861));
#10477=CARTESIAN_POINT('Ctrl Pts',(7.00039492230318,0.586632257973225,3.26345951558006));
#10478=CARTESIAN_POINT('Ctrl Pts',(6.99482333860884,0.604406263268823,3.26463647925897));
#10479=CARTESIAN_POINT('Ctrl Pts',(6.99234873670921,0.612134970242019,3.26515078099188));
#10480=CARTESIAN_POINT('Ctrl Pts',(6.98710057930681,0.628188102074734,3.2662243793466));
#10481=CARTESIAN_POINT('Ctrl Pts',(6.98431912661748,0.636509742253686,3.2667839255307));
#10482=CARTESIAN_POINT('Ctrl Pts',(6.97695220991413,0.658076010461559,3.26824201714204));
#10483=CARTESIAN_POINT('Ctrl Pts',(6.97228195603154,0.671290959196758,3.2691433357174));
#10484=CARTESIAN_POINT('Ctrl Pts',(6.95101155575453,0.729517105215765,3.27315025192122));
#10485=CARTESIAN_POINT('Ctrl Pts',(6.93293121296876,0.773966872729414,3.27630442957034));
#10486=CARTESIAN_POINT('Ctrl Pts',(6.87841998155473,0.895255431543577,3.28518496806801));
#10487=CARTESIAN_POINT('Ctrl Pts',(6.83865528022506,0.970477159813528,3.29101165325064));
#10488=CARTESIAN_POINT('Ctrl Pts',(6.72375800552674,1.15780610754,3.306262611492));
#10489=CARTESIAN_POINT('Ctrl Pts',(6.64183493106537,1.26525275239806,3.31577328896848));
#10490=CARTESIAN_POINT('Ctrl Pts',(6.53240299116342,1.38208804644868,3.32650198171037));
#10491=CARTESIAN_POINT('Ctrl Pts',(6.51475495195988,1.4002257470951,3.32817912157778));
#10492=CARTESIAN_POINT('Ctrl Pts',(6.49107378136203,1.4236549923912,3.3303553238341));
#10493=CARTESIAN_POINT('Ctrl Pts',(6.48534797027268,1.42925207647901,3.33087595870867));
#10494=CARTESIAN_POINT('Ctrl Pts',(6.47604529059742,1.43823671704978,3.33171269584108));
#10495=CARTESIAN_POINT('Ctrl Pts',(6.47248937315868,1.44164569785363,3.33203040792309));
#10496=CARTESIAN_POINT('Ctrl Pts',(6.46559057005701,1.44821056143531,3.33264263373642));
#10497=CARTESIAN_POINT('Ctrl Pts',(6.46224937431774,1.45136808811623,3.33293726731979));
#10498=CARTESIAN_POINT('Ctrl Pts',(6.4542003936161,1.45892210444373,3.33364262849662));
#10499=CARTESIAN_POINT('Ctrl Pts',(6.44948211987209,1.46330744347849,3.33405251273967));
#10500=CARTESIAN_POINT('Ctrl Pts',(6.43313991047296,1.47834961534023,3.3354601934806));
#10501=CARTESIAN_POINT('Ctrl Pts',(6.42141055106612,1.48889173719833,3.33644978086266));
#10502=CARTESIAN_POINT('Ctrl Pts',(6.35004285449729,1.55152161820794,3.34235621452919));
#10503=CARTESIAN_POINT('Ctrl Pts',(6.28746476248122,1.60016539335824,3.34706117706064));
#10504=CARTESIAN_POINT('Ctrl Pts',(6.17741057557539,1.67565461476364,3.35487715953641));
#10505=CARTESIAN_POINT('Ctrl Pts',(6.13143321066452,1.70450734343938,3.35801991298445));
#10506=CARTESIAN_POINT('Ctrl Pts',(5.97269202358152,1.79531825991671,3.36863875155969));
#10507=CARTESIAN_POINT('Ctrl Pts',(5.85514660269822,1.84823117735319,3.37614716843463));
#10508=CARTESIAN_POINT('Ctrl Pts',(5.70988998249731,1.89739471872135,3.38558093914143));
#10509=CARTESIAN_POINT('Ctrl Pts',(5.68630156940592,1.90489215196905,3.38711659121429));
#10510=CARTESIAN_POINT('Ctrl Pts',(5.65288689141644,1.91483212219995,3.38929980726434));
#10511=CARTESIAN_POINT('Ctrl Pts',(5.64317159339087,1.91764191837016,3.38993549636044));
#10512=CARTESIAN_POINT('Ctrl Pts',(5.62619750690776,1.92241147940399,3.3910479275253));
#10513=CARTESIAN_POINT('Ctrl Pts',(5.61894816599453,1.92440432576779,3.39152359268106));
#10514=CARTESIAN_POINT('Ctrl Pts',(5.6037359661584,1.92849380834459,3.39252300352889));
#10515=CARTESIAN_POINT('Ctrl Pts',(5.59577105987582,1.93058221206542,3.39304700393154));
#10516=CARTESIAN_POINT('Ctrl Pts',(5.57673959783384,1.93544653962978,3.39430088562208));
#10517=CARTESIAN_POINT('Ctrl Pts',(5.56566180549297,1.93817692403709,3.39503221180626));
#10518=CARTESIAN_POINT('Ctrl Pts',(5.52777593983032,1.94717074438924,3.39753868266361));
#10519=CARTESIAN_POINT('Ctrl Pts',(5.50086290237092,1.95297394527661,3.39932836576618));
#10520=CARTESIAN_POINT('Ctrl Pts',(5.43573957227161,1.96561179528322,3.4036830339539));
#10521=CARTESIAN_POINT('Ctrl Pts',(5.397434277516,1.9718915323255,3.40626431558079));
#10522=CARTESIAN_POINT('Ctrl Pts',(5.24550388666742,1.99226714138722,3.41657980066685));
#10523=CARTESIAN_POINT('Ctrl Pts',(5.13094725159728,1.99768640957115,3.42454375649992));
#10524=CARTESIAN_POINT('Ctrl Pts',(4.91226739539063,1.98921075493262,3.43979988447141));
#10525=CARTESIAN_POINT('Ctrl Pts',(4.80843032309346,1.97698667467482,3.44706194007859));
#10526=CARTESIAN_POINT('Ctrl Pts',(4.69003771629629,1.95352171227245,3.45506276007776));
#10527=CARTESIAN_POINT('Ctrl Pts',(4.67409536758635,1.95015852135857,3.45613395218003));
#10528=CARTESIAN_POINT('Ctrl Pts',(4.65164317429171,1.9451339211812,3.45763213197464));
#10529=CARTESIAN_POINT('Ctrl Pts',(4.64509826203054,1.94363448926557,3.45806760109595));
#10530=CARTESIAN_POINT('Ctrl Pts',(4.63408051936311,1.94105171758261,3.45879840817356));
#10531=CARTESIAN_POINT('Ctrl Pts',(4.62960367846387,1.93998590320752,3.45909472494692));
#10532=CARTESIAN_POINT('Ctrl Pts',(4.62044218313054,1.93777127005026,3.4596997634741));
#10533=CARTESIAN_POINT('Ctrl Pts',(4.61575794958448,1.93662093932988,3.46000839731793));
#10534=CARTESIAN_POINT('Ctrl Pts',(4.60375933397472,1.93362819229858,3.46079722094412));
#10535=CARTESIAN_POINT('Ctrl Pts',(4.59645106652795,1.93176123944092,3.46127602761315));
#10536=CARTESIAN_POINT('Ctrl Pts',(4.56615889609478,1.9238395667109,3.46325441226205));
#10537=CARTESIAN_POINT('Ctrl Pts',(4.54327247346199,1.91741548182374,3.46473420749827));
#10538=CARTESIAN_POINT('Ctrl Pts',(4.48229703683551,1.89911816200378,3.46865010774123));
#10539=CARTESIAN_POINT('Ctrl Pts',(4.44443900105115,1.88650849395834,3.47105326922216));
#10540=CARTESIAN_POINT('Ctrl Pts',(4.31973007500538,1.84077110112843,3.47895241099657));
#10541=CARTESIAN_POINT('Ctrl Pts',(4.23481666957667,1.80271106444529,3.4843069331157));
#10542=CARTESIAN_POINT('Ctrl Pts',(4.03814722747321,1.69749628161576,3.49727122816487));
#10543=CARTESIAN_POINT('Ctrl Pts',(3.92972637085183,1.62505898389022,3.50491185266703));
#10544=CARTESIAN_POINT('Ctrl Pts',(3.81660145956486,1.53231353753691,3.5139835465249));
#10545=CARTESIAN_POINT('Ctrl Pts',(3.80419356555638,1.52188548692369,3.51499447958252));
#10546=CARTESIAN_POINT('Ctrl Pts',(3.78417476297861,1.50464033184335,3.51665253878526));
#10547=CARTESIAN_POINT('Ctrl Pts',(3.77648657328467,1.49791378312528,3.51729596733447));
#10548=CARTESIAN_POINT('Ctrl Pts',(3.76282980725424,1.48577874901147,3.51845107669293));
#10549=CARTESIAN_POINT('Ctrl Pts',(3.75684164164996,1.48039257114839,3.51896182254581));
#10550=CARTESIAN_POINT('Ctrl Pts',(3.74421894028102,1.4688997698766,3.52004761495186));
#10551=CARTESIAN_POINT('Ctrl Pts',(3.73759288050139,1.46278414520507,3.52062303508637));
#10552=CARTESIAN_POINT('Ctrl Pts',(3.71996611381691,1.44629252722031,3.52216861526454));
#10553=CARTESIAN_POINT('Ctrl Pts',(3.70904172503282,1.43583617690194,3.52314219702043));
#10554=CARTESIAN_POINT('Ctrl Pts',(3.65483579272347,1.38275856035883,3.52805362934279));
#10555=CARTESIAN_POINT('Ctrl Pts',(3.61340219766025,1.33830416066351,3.53207135812795));
#10556=CARTESIAN_POINT('Ctrl Pts',(3.49097824925787,1.19430209981282,3.54480719343686));
#10557=CARTESIAN_POINT('Ctrl Pts',(3.41752052282418,1.08879354745196,3.55377654524543));
#10558=CARTESIAN_POINT('Ctrl Pts',(3.30746067700814,0.892876284046156,3.56941771786359));
#10559=CARTESIAN_POINT('Ctrl Pts',(3.26637127044077,0.805445600785516,3.57607959613874));
#10560=CARTESIAN_POINT('Ctrl Pts',(3.22784032729168,0.705152920340156,3.58314126680652));
#10561=CARTESIAN_POINT('Ctrl Pts',(3.22399716779749,0.694898060252058,3.58385672760659));
#10562=CARTESIAN_POINT('Ctrl Pts',(3.21830548577588,0.67932153849607,3.58493296692));
#10563=CARTESIAN_POINT('Ctrl Pts',(3.21639480421915,0.674023037078554,3.58529723080324));
#10564=CARTESIAN_POINT('Ctrl Pts',(3.21299902075027,0.664479730739243,3.58594994332835));
#10565=CARTESIAN_POINT('Ctrl Pts',(3.21150581436864,0.660237953267188,3.58623885784671));
#10566=CARTESIAN_POINT('Ctrl Pts',(3.20825677578016,0.650907734660911,3.58687171669202));
#10567=CARTESIAN_POINT('Ctrl Pts',(3.20650719189738,0.645817228434815,3.58721529403877));
#10568=CARTESIAN_POINT('Ctrl Pts',(3.20153464612462,0.631156553319627,3.58820006610978));
#10569=CARTESIAN_POINT('Ctrl Pts',(3.19836366620917,0.621568746560217,3.58883830629828));
#10570=CARTESIAN_POINT('Ctrl Pts',(3.17589337706522,0.551855963548858,3.59343991615476));
#10571=CARTESIAN_POINT('Ctrl Pts',(3.15938382546428,0.490862204156248,3.59725654871097));
#10572=CARTESIAN_POINT('Ctrl Pts',(3.11767866472496,0.301564781234179,3.60875235275822));
#10573=CARTESIAN_POINT('Ctrl Pts',(3.10217010175756,0.171490803308188,3.61618870989906));
#10574=CARTESIAN_POINT('Ctrl Pts',(3.09766981425869,-0.0483237159697841,
3.62912146723118));
#10575=CARTESIAN_POINT('Ctrl Pts',(3.1018248749594,-0.137489353042398,3.63446401120191));
#10576=CARTESIAN_POINT('Ctrl Pts',(3.11370471374329,-0.241636302010408,
3.64096932003552));
#10577=CARTESIAN_POINT('Ctrl Pts',(3.11566345306548,-0.257179570332415,
3.6419470077915));
#10578=CARTESIAN_POINT('Ctrl Pts',(3.11917913314574,-0.282654881039812,
3.64356135920014));
#10579=CARTESIAN_POINT('Ctrl Pts',(3.12062846123137,-0.292601266180397,
3.64419464874659));
#10580=CARTESIAN_POINT('Ctrl Pts',(3.12337200942936,-0.310481389873712,
3.64533865738518));
#10581=CARTESIAN_POINT('Ctrl Pts',(3.12463913964924,-0.31841911262524,3.64584851328592));
#10582=CARTESIAN_POINT('Ctrl Pts',(3.12744628524539,-0.335346108481486,
3.64694010205887));
#10583=CARTESIAN_POINT('Ctrl Pts',(3.12900003891108,-0.344332886540949,
3.64752225819586));
#10584=CARTESIAN_POINT('Ctrl Pts',(3.13337714454712,-0.368654927240598,
3.64910507271514));
#10585=CARTESIAN_POINT('Ctrl Pts',(3.1363187252391,-0.383967997962829,3.65010944530784));
#10586=CARTESIAN_POINT('Ctrl Pts',(3.15293410991627,-0.465303847400993,
3.65548720525991));
#10587=CARTESIAN_POINT('Ctrl Pts',(3.16976779559368,-0.530629162928124,
3.65995997164014));
#10588=CARTESIAN_POINT('Ctrl Pts',(3.23847074818011,-0.750483817708959,
3.6755465402418));
#10589=CARTESIAN_POINT('Ctrl Pts',(3.30593745665356,-0.899451859374783,
3.68709211468425));
#10590=CARTESIAN_POINT('Ctrl Pts',(3.41968783916793,-1.08599036734191,3.70208751766366));
#10591=CARTESIAN_POINT('Ctrl Pts',(3.45060261776856,-1.13222429677065,3.70584683697757));
#10592=CARTESIAN_POINT('Ctrl Pts',(3.48890064838236,-1.18462019165321,3.71010664784652));
#10593=CARTESIAN_POINT('Ctrl Pts',(3.49444244778048,-1.1920917147581,3.71071405750844));
#10594=CARTESIAN_POINT('Ctrl Pts',(3.50350496079102,-1.20413294503375,3.71169255924212));
#10595=CARTESIAN_POINT('Ctrl Pts',(3.50699351042237,-1.20872652703664,3.71206574786143));
#10596=CARTESIAN_POINT('Ctrl Pts',(3.51324237418476,-1.21688109939131,3.71272796488251));
#10597=CARTESIAN_POINT('Ctrl Pts',(3.51599487258273,-1.22044792978967,3.7130175215736));
#10598=CARTESIAN_POINT('Ctrl Pts',(3.52199724358281,-1.22817186581259,3.71364432591847));
#10599=CARTESIAN_POINT('Ctrl Pts',(3.52525153108682,-1.23232540995246,3.71398125751727));
#10600=CARTESIAN_POINT('Ctrl Pts',(3.53447353362177,-1.24400000893292,3.71492807198143));
#10601=CARTESIAN_POINT('Ctrl Pts',(3.54047921659056,-1.25149108254966,3.7155353441363));
#10602=CARTESIAN_POINT('Ctrl Pts',(3.57872377603487,-1.29849524480288,3.71934626172196));
#10603=CARTESIAN_POINT('Ctrl Pts',(3.61241681643663,-1.33680684136023,3.72245468876477));
#10604=CARTESIAN_POINT('Ctrl Pts',(3.75171710117433,-1.48345798689375,3.73455759135895));
#10605=CARTESIAN_POINT('Ctrl Pts',(3.86802979852114,-1.58092809878593,3.74310620313579));
#10606=CARTESIAN_POINT('Ctrl Pts',(4.06278830165982,-1.70960070047408,3.75688206918397));
#10607=CARTESIAN_POINT('Ctrl Pts',(4.13405170903037,-1.7506011522757,3.76182050195941));
#10608=CARTESIAN_POINT('Ctrl Pts',(4.22143126178332,-1.79393147774978,3.76787567467788));
#10609=CARTESIAN_POINT('Ctrl Pts',(4.23530710024496,-1.80061323894182,3.76883706989948));
#10610=CARTESIAN_POINT('Ctrl Pts',(4.25829137088769,-1.81135499742174,3.77042997358977));
#10611=CARTESIAN_POINT('Ctrl Pts',(4.26735551090812,-1.8155086309207,3.77105826168098));
#10612=CARTESIAN_POINT('Ctrl Pts',(4.28377664625156,-1.82288514224108,3.77219687332661));
#10613=CARTESIAN_POINT('Ctrl Pts',(4.29112273397342,-1.82613188952116,3.77270636909272));
#10614=CARTESIAN_POINT('Ctrl Pts',(4.30690291655853,-1.83299263438238,3.77380119745486));
#10615=CARTESIAN_POINT('Ctrl Pts',(4.31534271545483,-1.83659296729466,3.77438697954499));
#10616=CARTESIAN_POINT('Ctrl Pts',(4.33842595595339,-1.84625234709807,3.77598990219368));
#10617=CARTESIAN_POINT('Ctrl Pts',(4.3531169923676,-1.85219521965553,3.77701091914311));
#10618=CARTESIAN_POINT('Ctrl Pts',(4.4344281634835,-1.88396543543093,3.78266796694263));
#10619=CARTESIAN_POINT('Ctrl Pts',(4.5023207381432,-1.90637112691631,3.78741618992693));
#10620=CARTESIAN_POINT('Ctrl Pts',(4.76318759513982,-1.97718350268646,3.80575146708481));
#10621=CARTESIAN_POINT('Ctrl Pts',(4.96179591185586,-2.00028306631814,3.82002462665903));
#10622=CARTESIAN_POINT('Ctrl Pts',(5.18122283748945,-1.99294216699515,3.83466209118415));
#10623=CARTESIAN_POINT('Ctrl Pts',(5.20191068399526,-1.9919273374996,3.83602951847649));
#10624=CARTESIAN_POINT('Ctrl Pts',(5.2299686486106,-1.99011252900006,3.83786366725163));
#10625=CARTESIAN_POINT('Ctrl Pts',(5.23735480239263,-1.98959347681001,3.83834457417821));
#10626=CARTESIAN_POINT('Ctrl Pts',(5.24904206210842,-1.98870674724812,3.83910229275337));
#10627=CARTESIAN_POINT('Ctrl Pts',(5.25334506921535,-1.9883662212601,3.83938057530421));
#10628=CARTESIAN_POINT('Ctrl Pts',(5.26222994919408,-1.98763407289399,3.83995369487418));
#10629=CARTESIAN_POINT('Ctrl Pts',(5.26681159701087,-1.98724057226022,3.84024841340139));
#10630=CARTESIAN_POINT('Ctrl Pts',(5.27781551482398,-1.98625714316381,3.84095435480886));
#10631=CARTESIAN_POINT('Ctrl Pts',(5.28423643385009,-1.98565189915354,3.84136473072139));
#10632=CARTESIAN_POINT('Ctrl Pts',(5.30639495046331,-1.98345473748275,3.84277592973379));
#10633=CARTESIAN_POINT('Ctrl Pts',(5.32211694904346,-1.98170673159543,3.84376848854349));
#10634=CARTESIAN_POINT('Ctrl Pts',(5.41690021275341,-1.97002550684214,3.84970859685526));
#10635=CARTESIAN_POINT('Ctrl Pts',(5.4953376592896,-1.95554822630603,3.85444163959602));
#10636=CARTESIAN_POINT('Ctrl Pts',(5.58586114571642,-1.93316159423466,3.85990172187665));
#10637=CARTESIAN_POINT('Ctrl Pts',(5.59898264065211,-1.92977437499375,3.86069306372408));
#10638=CARTESIAN_POINT('Ctrl Pts',(5.77900740569764,-1.88134030198174,3.87156010179077));
#10639=CARTESIAN_POINT('Ctrl Pts',(5.93938070271494,-1.81492346102197,3.88143896606319));
#10640=CARTESIAN_POINT('Ctrl Pts',(6.10835299924791,-1.71763041237996,3.8934674576784));
#10641=CARTESIAN_POINT('Ctrl Pts',(6.12733808787899,-1.70627430781312,3.89484274368384));
#10642=CARTESIAN_POINT('Ctrl Pts',(6.15505287621803,-1.68906419510839,3.89688782061571));
#10643=CARTESIAN_POINT('Ctrl Pts',(6.1639318823387,-1.68345292549688,3.89754877663661));
#10644=CARTESIAN_POINT('Ctrl Pts',(6.17947418317278,-1.67345800741364,3.8987161631305));
#10645=CARTESIAN_POINT('Ctrl Pts',(6.18615632842068,-1.66910399503938,3.89922149054561));
#10646=CARTESIAN_POINT('Ctrl Pts',(6.19908220481033,-1.66057077126476,3.90020576446135));
#10647=CARTESIAN_POINT('Ctrl Pts',(6.20532879698651,-1.65639612075254,3.90068453472512));
#10648=CARTESIAN_POINT('Ctrl Pts',(6.22191913656929,-1.64517255136957,3.90196450605855));
#10649=CARTESIAN_POINT('Ctrl Pts',(6.23222023851879,-1.63806148183562,3.90276803785077));
#10650=CARTESIAN_POINT('Ctrl Pts',(6.27107327470375,-1.6106969104163,3.90583279846002));
#10651=CARTESIAN_POINT('Ctrl Pts',(6.2991558376273,-1.5897910160843,3.90811873547069));
#10652=CARTESIAN_POINT('Ctrl Pts',(6.36883122861123,-1.5350140298848,3.9139764836569));
#10653=CARTESIAN_POINT('Ctrl Pts',(6.40963297870938,-1.50018587978312,3.91758339883017));
#10654=CARTESIAN_POINT('Ctrl Pts',(6.51495750668446,-1.40267611630217,3.92737147528454));
#10655=CARTESIAN_POINT('Ctrl Pts',(6.57672621637369,-1.33720609366694,3.9336360307158));
#10656=CARTESIAN_POINT('Ctrl Pts',(6.69998997885088,-1.1874734670786,3.94715606273761));
#10657=CARTESIAN_POINT('Ctrl Pts',(6.75973657549667,-1.10208997928839,3.95439336778145));
#10658=CARTESIAN_POINT('Ctrl Pts',(6.82082241454186,-0.998388902066491,
3.96237164322743));
#10659=CARTESIAN_POINT('Ctrl Pts',(6.82891987929916,-0.984249107201606,
3.96344290339751));
#10660=CARTESIAN_POINT('Ctrl Pts',(6.84010861807734,-0.964144024554281,
3.96494116119756));
#10661=CARTESIAN_POINT('Ctrl Pts',(6.84334416331121,-0.958260345174318,
3.96537664141484));
#10662=CARTESIAN_POINT('Ctrl Pts',(6.84874709657984,-0.9483167931981,3.96610746168287));
#10663=CARTESIAN_POINT('Ctrl Pts',(6.85093023728254,-0.944265588357725,
3.96640378062932));
#10664=CARTESIAN_POINT('Ctrl Pts',(6.85537278959444,-0.93595288632395,3.96700881824968));
#10665=CARTESIAN_POINT('Ctrl Pts',(6.85763079299438,-0.931690697589313,
3.96731744904535));
#10666=CARTESIAN_POINT('Ctrl Pts',(6.86338009900063,-0.920742543993711,
3.96810625556856));
#10667=CARTESIAN_POINT('Ctrl Pts',(6.86684901822192,-0.914044818825352,
3.96858504829917));
#10668=CARTESIAN_POINT('Ctrl Pts',(6.88109002063351,-0.886162417382578,
3.970563298827));
#10669=CARTESIAN_POINT('Ctrl Pts',(6.8915215668731,-0.864804775530169,3.9720429772356));
#10670=CARTESIAN_POINT('Ctrl Pts',(6.91843124332041,-0.807117362150341,
3.97595848727869));
#10671=CARTESIAN_POINT('Ctrl Pts',(6.93420612063805,-0.77047009790331,3.97836138347411));
#10672=CARTESIAN_POINT('Ctrl Pts',(7.00351062640271,-0.595166244652166,
3.98957139501167));
#10673=CARTESIAN_POINT('Ctrl Pts',(7.04253450382315,-0.451284364024468,
3.99798163952158));
#10674=CARTESIAN_POINT('Ctrl Pts',(7.07639767614088,-0.231973801152632,
4.01111595482023));
#10675=CARTESIAN_POINT('Ctrl Pts',(7.08357992194477,-0.158996585193538,
4.01553010832341));
#10676=CARTESIAN_POINT('Ctrl Pts',(7.08746223093588,-0.0688155482614963,
4.02112309351378));
#10677=CARTESIAN_POINT('Ctrl Pts',(7.08797615278786,-0.051828010141138,
4.0221825172722));
#10678=CARTESIAN_POINT('Ctrl Pts',(7.08840213305802,-0.027439866292334,
4.02371272051326));
#10679=CARTESIAN_POINT('Ctrl Pts',(7.08849017770342,-0.0200427758340486,
4.02417806009595));
#10680=CARTESIAN_POINT('Ctrl Pts',(7.08856389118241,-0.00841511051592803,
4.02491151845259));
#10681=CARTESIAN_POINT('Ctrl Pts',(7.08857725168938,-0.00418473261553051,
4.02517877714476));
#10682=CARTESIAN_POINT('Ctrl Pts',(7.08857715493134,4.56245408300607E-5,
4.02544645345466));
#10683=CARTESIAN_POINT('Origin',(5.09382715545311,0.,-6.77268258743872));
#10684=CARTESIAN_POINT('',(7.08857715545311,-3.14645820945244E-12,4.98428615635939));
#10685=CARTESIAN_POINT('',(7.08857715545311,4.63564351804039E-12,4.82758772788682));
#10686=CARTESIAN_POINT('',(7.08857715545311,8.3550772080578E-14,-6.77268258743872));
#10687=CARTESIAN_POINT('',(7.08857712267089,-0.00123466680453736,4.98420171859293));
#10688=CARTESIAN_POINT('Ctrl Pts',(7.08857715545311,-3.14645820945244E-12,
4.98428615635939));
#10689=CARTESIAN_POINT('Ctrl Pts',(7.08857715545311,-0.000410617569554449,
4.98425787060343));
#10690=CARTESIAN_POINT('Ctrl Pts',(7.0885770286652,-0.000821238879055287,
4.9842295872048));
#10691=CARTESIAN_POINT('Ctrl Pts',(7.08857677508245,-0.00123186387362816,
4.98420130618351));
#10692=CARTESIAN_POINT('Ctrl Pts',(7.08857677337535,-0.0012346250781053,
4.9842011160108));
#10693=CARTESIAN_POINT('Ctrl Pts',(7.08854025461787,-0.0602369722889442,
4.98013744242997));
#10694=CARTESIAN_POINT('Ctrl Pts',(7.08588590358347,-0.119215683551362,
4.97612891140116));
#10695=CARTESIAN_POINT('Ctrl Pts',(7.07982904051931,-0.186822383758213,
4.97165554826758));
#10696=CARTESIAN_POINT('Ctrl Pts',(7.07897947543163,-0.195643460673842,
4.97107428786379));
#10697=CARTESIAN_POINT('Ctrl Pts',(7.07749276312789,-0.210071797355168,
4.97012779847945));
#10698=CARTESIAN_POINT('Ctrl Pts',(7.07689056722123,-0.215682428229593,
4.96976080043087));
#10699=CARTESIAN_POINT('Ctrl Pts',(7.07577889558268,-0.225641370710706,
4.96911133905215));
#10700=CARTESIAN_POINT('Ctrl Pts',(7.07527890089432,-0.229990673185066,
4.96882837042057));
#10701=CARTESIAN_POINT('Ctrl Pts',(7.07423564991491,-0.238809609413973,
4.96825600445741));
#10702=CARTESIAN_POINT('Ctrl Pts',(7.07369157716984,-0.243279073122874,
4.96796666377202));
#10703=CARTESIAN_POINT('Ctrl Pts',(7.0724734288636,-0.253011135418825,4.96733825137212));
#10704=CARTESIAN_POINT('Ctrl Pts',(7.07179349057742,-0.258272895622735,
4.96699950973492));
#10705=CARTESIAN_POINT('Ctrl Pts',(7.06984161671701,-0.27291769523819,4.96605938464704));
#10706=CARTESIAN_POINT('Ctrl Pts',(7.06852383336751,-0.282294629957024,
4.96546049546868));
#10707=CARTESIAN_POINT('Ctrl Pts',(7.06090677739358,-0.333829717906222,
4.96218415431966));
#10708=CARTESIAN_POINT('Ctrl Pts',(7.05332371500427,-0.375790295018537,
4.95957219553235));
#10709=CARTESIAN_POINT('Ctrl Pts',(7.0361789592161,-0.45589522114539,4.95463801597854));
#10710=CARTESIAN_POINT('Ctrl Pts',(7.02682326220819,-0.494062050879139,
4.95231024669574));
#10711=CARTESIAN_POINT('Ctrl Pts',(6.97721082332847,-0.67337321319461,4.94138270652834));
#10712=CARTESIAN_POINT('Ctrl Pts',(6.92258770274573,-0.810062229424848,
4.93304200405361));
#10713=CARTESIAN_POINT('Ctrl Pts',(6.82543272284463,-0.992024066641868,
4.92070027154727));
#10714=CARTESIAN_POINT('Ctrl Pts',(6.79506813422487,-1.04323904280439,4.91707890843787));
#10715=CARTESIAN_POINT('Ctrl Pts',(6.75422723196292,-1.105588074991,4.91243889070054));
#10716=CARTESIAN_POINT('Ctrl Pts',(6.74585102741146,-1.11806552254119,4.91149827621661));
#10717=CARTESIAN_POINT('Ctrl Pts',(6.73223646878752,-1.13785913859887,4.90998613732503));
#10718=CARTESIAN_POINT('Ctrl Pts',(6.7270881048697,-1.14523672843157,4.909418008423));
#10719=CARTESIAN_POINT('Ctrl Pts',(6.71723414447937,-1.15915583120775,4.90833740366725));
#10720=CARTESIAN_POINT('Ctrl Pts',(6.71253845968714,-1.16570416636264,4.90782531319366));
#10721=CARTESIAN_POINT('Ctrl Pts',(6.70177949998019,-1.18051763818208,4.90665830471736));
#10722=CARTESIAN_POINT('Ctrl Pts',(6.695691970849,-1.18876479720094,4.906002459825));
#10723=CARTESIAN_POINT('Ctrl Pts',(6.67974554243104,-1.21002352246016,4.90429570169942));
#10724=CARTESIAN_POINT('Ctrl Pts',(6.66979015629161,-1.22296142574569,4.90324105094155));
#10725=CARTESIAN_POINT('Ctrl Pts',(6.58483031207992,-1.33061398973457,4.8943285919645));
#10726=CARTESIAN_POINT('Ctrl Pts',(6.50153550920894,-1.41843997195227,4.8861322351878));
#10727=CARTESIAN_POINT('Ctrl Pts',(6.30126932224092,-1.59448675528496,4.86764966304606));
#10728=CARTESIAN_POINT('Ctrl Pts',(6.18147907553477,-1.67848784591336,4.85733007374101));
#10729=CARTESIAN_POINT('Ctrl Pts',(6.04133884055726,-1.75540441676685,4.84667745020489));
#10730=CARTESIAN_POINT('Ctrl Pts',(6.02901085423549,-1.76200298910028,4.84575184107523));
#10731=CARTESIAN_POINT('Ctrl Pts',(6.00712143869961,-1.7734248675481,4.84412982981531));
#10732=CARTESIAN_POINT('Ctrl Pts',(5.9975887663511,-1.77830176613695,4.84343055316382));
#10733=CARTESIAN_POINT('Ctrl Pts',(5.98311076227342,-1.78556219556864,4.84237971579656));
#10734=CARTESIAN_POINT('Ctrl Pts',(5.97819428164566,-1.78800237009174,4.84202480854908));
#10735=CARTESIAN_POINT('Ctrl Pts',(5.97325426947437,-1.79042886310762,4.84167018981195));
#10736=CARTESIAN_POINT('Ctrl Pts',(5.97324081758061,-1.79043547037812,4.8416692241826));
#10737=CARTESIAN_POINT('Ctrl Pts',(5.97321461181638,-1.79044834169904,4.84166734305946));
#10738=CARTESIAN_POINT('Ctrl Pts',(5.97320185797123,-1.79045460575605,4.841666427566));
#10739=CARTESIAN_POINT('Ctrl Pts',(5.97317618545032,-1.79046721448624,4.84166458477392));
#10740=CARTESIAN_POINT('Ctrl Pts',(5.97316326678685,-1.79047355914897,4.84166365747654));
#10741=CARTESIAN_POINT('Ctrl Pts',(5.97313726220864,-1.7904863302662,4.8416617909039));
#10742=CARTESIAN_POINT('Ctrl Pts',(5.97312417631221,-1.79049275670717,4.84166085163032));
#10743=CARTESIAN_POINT('Ctrl Pts',(5.97309783483001,-1.79050569256458,4.84165896093136));
#10744=CARTESIAN_POINT('Ctrl Pts',(5.97308457922809,-1.7905122019843,4.84165800950519));
#10745=CARTESIAN_POINT('Ctrl Pts',(5.97305789585658,-1.79052530500224,4.84165609432428));
#10746=CARTESIAN_POINT('Ctrl Pts',(5.97304446805399,-1.79053189861188,4.84165513056754));
#10747=CARTESIAN_POINT('Ctrl Pts',(5.97301743774316,-1.79054517124153,4.84165319054445));
#10748=CARTESIAN_POINT('Ctrl Pts',(5.97300383520166,-1.79055185027297,4.8416522142761));
#10749=CARTESIAN_POINT('Ctrl Pts',(5.97297645274663,-1.79056529504064,4.84165024903959));
#10750=CARTESIAN_POINT('Ctrl Pts',(5.97296267291844,-1.79057206072993,4.84164926007794));
#10751=CARTESIAN_POINT('Ctrl Pts',(5.97293493329572,-1.79058568007188,4.84164726926984));
#10752=CARTESIAN_POINT('Ctrl Pts',(5.97292097347083,-1.79059253373426,4.84164626742161));
#10753=CARTESIAN_POINT('Ctrl Pts',(5.97289287121183,-1.7906063303043,4.84164425065191));
#10754=CARTESIAN_POINT('Ctrl Pts',(5.97287872875385,-1.79061327321834,4.84164323572913));
#10755=CARTESIAN_POINT('Ctrl Pts',(5.97285025849024,-1.79062724962001,4.84164119261506));
#10756=CARTESIAN_POINT('Ctrl Pts',(5.97283593068016,-1.79063428310434,4.84164016442388));
#10757=CARTESIAN_POINT('Ctrl Pts',(5.97280708694354,-1.79064844198926,4.84163809457561));
#10758=CARTESIAN_POINT('Ctrl Pts',(5.97279257100046,-1.79065556739233,4.84163705291778));
#10759=CARTESIAN_POINT('Ctrl Pts',(5.97276334814837,-1.79066991149647,4.84163495593306));
#10760=CARTESIAN_POINT('Ctrl Pts',(5.97274864127561,-1.79067713017394,4.84163390060922));
#10761=CARTESIAN_POINT('Ctrl Pts',(5.972719033695,-1.79069166221769,4.84163177608799));
#10762=CARTESIAN_POINT('Ctrl Pts',(5.97270413299984,-1.79069897557178,4.84163070689197));
#10763=CARTESIAN_POINT('Ctrl Pts',(5.97267413494835,-1.79071369833788,4.841628554425));
#10764=CARTESIAN_POINT('Ctrl Pts',(5.97265903748002,-1.79072110779872,4.84162747114649));
#10765=CARTESIAN_POINT('Ctrl Pts',(5.97262864285379,-1.7907360242461,4.84162529029869));
#10766=CARTESIAN_POINT('Ctrl Pts',(5.97261334573714,-1.79074353120609,4.84162419273285));
#10767=CARTESIAN_POINT('Ctrl Pts',(5.97258254877119,-1.79075864412614,4.84162198309354));
#10768=CARTESIAN_POINT('Ctrl Pts',(5.97256704892172,-1.7907662500798,4.84162087102057));
#10769=CARTESIAN_POINT('Ctrl Pts',(5.97253584340905,-1.79078156247958,4.84161863214748));
#10770=CARTESIAN_POINT('Ctrl Pts',(5.97252013777952,-1.7907892689025,4.8416175053503));
#10771=CARTESIAN_POINT('Ctrl Pts',(5.97248851759955,-1.79080478374535,4.84161523680743));
#10772=CARTESIAN_POINT('Ctrl Pts',(5.97247260303742,-1.79081259216413,4.84161409506145));
#10773=CARTESIAN_POINT('Ctrl Pts',(5.97244056176071,-1.79082831256356,4.84161179639079));
#10774=CARTESIAN_POINT('Ctrl Pts',(5.97242443513319,-1.79083622449442,4.8416106394729));
#10775=CARTESIAN_POINT('Ctrl Pts',(5.97239196658779,-1.79085215343624,4.84160831023497));
#10776=CARTESIAN_POINT('Ctrl Pts',(5.97237562455932,-1.79086017049419,4.84160713790757));
#10777=CARTESIAN_POINT('Ctrl Pts',(5.97234272188251,-1.79087631130167,4.84160477761348));
#10778=CARTESIAN_POINT('Ctrl Pts',(5.97232616127637,-1.79088443502304,4.84160358965042));
#10779=CARTESIAN_POINT('Ctrl Pts',(5.97229281805885,-1.79090079079554,4.84160119784393));
#10780=CARTESIAN_POINT('Ctrl Pts',(5.9722760354639,-1.79090902283092,4.84159999400228));
#10781=CARTESIAN_POINT('Ctrl Pts',(5.97224224488607,-1.79092559686754,4.84159757019782));
#10782=CARTESIAN_POINT('Ctrl Pts',(5.97222523689052,-1.79093393886708,4.84159635023471));
#10783=CARTESIAN_POINT('Ctrl Pts',(5.97219099203734,-1.79095073451215,4.84159389393999));
#10784=CARTESIAN_POINT('Ctrl Pts',(5.97217375518661,-1.79095918814617,4.84159265760952));
#10785=CARTESIAN_POINT('Ctrl Pts',(5.97213904914235,-1.79097620874276,4.84159016833233));
#10786=CARTESIAN_POINT('Ctrl Pts',(5.9721215798687,-1.79098477573626,4.84158891538053));
#10787=CARTESIAN_POINT('Ctrl Pts',(5.97208640533138,-1.79100202481519,4.8415863926011));
#10788=CARTESIAN_POINT('Ctrl Pts',(5.97206870011,-1.79101070687127,4.84158512277717));
#10789=CARTESIAN_POINT('Ctrl Pts',(5.97203305003128,-1.79102818783726,4.84158256599404));
#10790=CARTESIAN_POINT('Ctrl Pts',(5.97201510513642,-1.79103698675669,4.84158127903284));
#10791=CARTESIAN_POINT('Ctrl Pts',(5.97197897197081,-1.79105470325643,4.84157868770903));
#10792=CARTESIAN_POINT('Ctrl Pts',(5.97196078372762,-1.79106362081412,4.84157738334913));
#10793=CARTESIAN_POINT('Ctrl Pts',(5.97192416011175,-1.79108157640323,4.8415747569609));
#10794=CARTESIAN_POINT('Ctrl Pts',(5.97190572468066,-1.7910906144539,4.84157343492912));
#10795=CARTESIAN_POINT('Ctrl Pts',(5.97186860280112,-1.79110881290672,4.84157077292057));
#10796=CARTESIAN_POINT('Ctrl Pts',(5.97184991638432,-1.79111797328368,4.84156943294682));
#10797=CARTESIAN_POINT('Ctrl Pts',(5.96779173482544,-1.79310727927813,4.84127843327595));
#10798=CARTESIAN_POINT('Ctrl Pts',(5.96374560892815,-1.79507372718939,4.84098963761113));
#10799=CARTESIAN_POINT('Ctrl Pts',(5.95458621933872,-1.79948701771378,4.84033887643599));
#10800=CARTESIAN_POINT('Ctrl Pts',(5.94946916404042,-1.80192576096321,4.83997740977135));
#10801=CARTESIAN_POINT('Ctrl Pts',(5.93622638961938,-1.80816801881361,4.83904716244677));
#10802=CARTESIAN_POINT('Ctrl Pts',(5.9280851787687,-1.81193863350361,4.83848032727813));
#10803=CARTESIAN_POINT('Ctrl Pts',(5.87556718820647,-1.83583341608546,4.83485436532135));
#10804=CARTESIAN_POINT('Ctrl Pts',(5.83048717443688,-1.85438256021371,4.83188184274893));
#10805=CARTESIAN_POINT('Ctrl Pts',(5.77122186882622,-1.87626557697511,4.8280968443184));
#10806=CARTESIAN_POINT('Ctrl Pts',(5.75762042331226,-1.88112057705133,4.82723640218582));
#10807=CARTESIAN_POINT('Ctrl Pts',(5.63162341461277,-1.92455811420703,4.81933128304467));
#10808=CARTESIAN_POINT('Ctrl Pts',(5.51603999125919,-1.95317367974293,4.81254496577493));
#10809=CARTESIAN_POINT('Ctrl Pts',(5.30724346848137,-1.98545339295984,4.80017396451355));
#10810=CARTESIAN_POINT('Ctrl Pts',(5.21503321011211,-1.99320793024042,4.79467512054944));
#10811=CARTESIAN_POINT('Ctrl Pts',(5.09975311288965,-1.99487233749274,4.78756487535699));
#10812=CARTESIAN_POINT('Ctrl Pts',(5.0768787692345,-1.99480912505917,4.7861429138952));
#10813=CARTESIAN_POINT('Ctrl Pts',(5.04341392610554,-1.99414102243853,4.7840441928695));
#10814=CARTESIAN_POINT('Ctrl Pts',(5.03281859943143,-1.99384499403104,4.78337701766936));
#10815=CARTESIAN_POINT('Ctrl Pts',(5.01412969635665,-1.99317372976244,4.78219522791565));
#10816=CARTESIAN_POINT('Ctrl Pts',(5.00603504223436,-1.99283359659311,4.78168171726847));
#10817=CARTESIAN_POINT('Ctrl Pts',(4.98913692104654,-1.99202039147902,4.78060619342338));
#10818=CARTESIAN_POINT('Ctrl Pts',(4.98033408592948,-1.99153825078043,4.78004390837229));
#10819=CARTESIAN_POINT('Ctrl Pts',(4.95735472159103,-1.99012679796126,4.77857071282173));
#10820=CARTESIAN_POINT('Ctrl Pts',(4.94318461503148,-1.98910437255734,4.77765692097764));
#10821=CARTESIAN_POINT('Ctrl Pts',(4.88429038086476,-1.98422201786818,4.77383597582742));
#10822=CARTESIAN_POINT('Ctrl Pts',(4.83969500769983,-1.97900454641532,4.77088701057705));
#10823=CARTESIAN_POINT('Ctrl Pts',(4.60755187933135,-1.94386908882395,4.75523365450591));
#10824=CARTESIAN_POINT('Ctrl Pts',(4.42481948914022,-1.88878180565106,4.74174447563576));
#10825=CARTESIAN_POINT('Ctrl Pts',(4.20295810335114,-1.78560546430026,4.72496613757666));
#10826=CARTESIAN_POINT('Ctrl Pts',(4.15420544056685,-1.76043936465509,4.7212617997646));
#10827=CARTESIAN_POINT('Ctrl Pts',(4.09805239799195,-1.72845473708438,4.71702453683944));
#10828=CARTESIAN_POINT('Ctrl Pts',(4.08959265983707,-1.72355337396047,4.71638699834109));
#10829=CARTESIAN_POINT('Ctrl Pts',(4.07659057567029,-1.71589205500446,4.7154088254445));
#10830=CARTESIAN_POINT('Ctrl Pts',(4.07202278983582,-1.71317589396691,4.71506550544436));
#10831=CARTESIAN_POINT('Ctrl Pts',(4.06360577520608,-1.70812521069914,4.71443355061349));
#10832=CARTESIAN_POINT('Ctrl Pts',(4.05975361115117,-1.70579592372634,4.71414460017078));
#10833=CARTESIAN_POINT('Ctrl Pts',(4.05102688093056,-1.70047870819988,4.7134906001621));
#10834=CARTESIAN_POINT('Ctrl Pts',(4.04615725891464,-1.6974828539401,4.71312607157251));
#10835=CARTESIAN_POINT('Ctrl Pts',(4.03354203295897,-1.68964683896085,4.71218261373066));
#10836=CARTESIAN_POINT('Ctrl Pts',(4.02581657081383,-1.68477428159878,4.71160572315657));
#10837=CARTESIAN_POINT('Ctrl Pts',(3.97429964627373,-1.65178507098262,4.70776271936707));
#10838=CARTESIAN_POINT('Ctrl Pts',(3.93158538720874,-1.62201444338199,4.70459551910765));
#10839=CARTESIAN_POINT('Ctrl Pts',(3.84716859039364,-1.55812903618492,4.69826996929578));
#10840=CARTESIAN_POINT('Ctrl Pts',(3.80558608938803,-1.52392885665618,4.69511807250601));
#10841=CARTESIAN_POINT('Ctrl Pts',(3.6914377605992,-1.42203051817702,4.68620774371435));
#10842=CARTESIAN_POINT('Ctrl Pts',(3.6224719221804,-1.35054804798122,4.68049863373865));
#10843=CARTESIAN_POINT('Ctrl Pts',(3.52541315284806,-1.23364812816854,4.67151574501245));
#10844=CARTESIAN_POINT('Ctrl Pts',(3.49334164844884,-1.19174482408826,4.66835854377184));
#10845=CARTESIAN_POINT('Ctrl Pts',(3.44305203555003,-1.1203417164278,4.66303285188453));
#10846=CARTESIAN_POINT('Ctrl Pts',(3.42387407191304,-1.09154960281792,4.66089921627786));
#10847=CARTESIAN_POINT('Ctrl Pts',(3.39881922910334,-1.05172761184657,4.65795906685079));
#10848=CARTESIAN_POINT('Ctrl Pts',(3.39228238712628,-1.04111873967821,4.65717682544423));
#10849=CARTESIAN_POINT('Ctrl Pts',(3.38148521452398,-1.02322230441606,4.65585862376941));
#10850=CARTESIAN_POINT('Ctrl Pts',(3.37717091296617,-1.01596759225094,4.65532463938377));
#10851=CARTESIAN_POINT('Ctrl Pts',(3.36875849814875,-1.00161512576402,4.65426885629764));
#10852=CARTESIAN_POINT('Ctrl Pts',(3.36465782584373,-0.994519059057538,
4.65374716349192));
#10853=CARTESIAN_POINT('Ctrl Pts',(3.35573528511954,-0.978856904206022,
4.652596267491));
#10854=CARTESIAN_POINT('Ctrl Pts',(3.35093279482576,-0.970280078440811,
4.65196638692575));
#10855=CARTESIAN_POINT('Ctrl Pts',(3.33430996787674,-0.940071527132777,
4.64974893019714));
#10856=CARTESIAN_POINT('Ctrl Pts',(3.32282778476937,-0.918257234436943,
4.64814950040768));
#10857=CARTESIAN_POINT('Ctrl Pts',(3.244279143585,-0.762071361410633,4.63670607687237));
#10858=CARTESIAN_POINT('Ctrl Pts',(3.19218384871628,-0.620739336039943,
4.62633888902752));
#10859=CARTESIAN_POINT('Ctrl Pts',(3.13621271217059,-0.392417245021813,
4.60994954107252));
#10860=CARTESIAN_POINT('Ctrl Pts',(3.12127590716206,-0.30868878652656,4.6040235406184));
#10861=CARTESIAN_POINT('Ctrl Pts',(3.1088239824134,-0.198632994791531,4.59651213476653));
#10862=CARTESIAN_POINT('Ctrl Pts',(3.10642169745108,-0.172951839554206,
4.59477921863489));
#10863=CARTESIAN_POINT('Ctrl Pts',(3.10324022679456,-0.129965196569153,
4.59191916817871));
#10864=CARTESIAN_POINT('Ctrl Pts',(3.10218719938283,-0.112683658375299,
4.59078030468028));
#10865=CARTESIAN_POINT('Ctrl Pts',(3.10103960740373,-0.0887131984822156,
4.5892177649745));
#10866=CARTESIAN_POINT('Ctrl Pts',(3.10075351456413,-0.082034799494594,
4.58878426757865));
#10867=CARTESIAN_POINT('Ctrl Pts',(3.10032562681002,-0.0707161060020321,
4.58805282830292));
#10868=CARTESIAN_POINT('Ctrl Pts',(3.10016645157353,-0.0660765598743967,
4.58775393910452));
#10869=CARTESIAN_POINT('Ctrl Pts',(3.09989230295485,-0.0571795792539851,
4.5871826085624));
#10870=CARTESIAN_POINT('Ctrl Pts',(3.09977476597956,-0.0529222935228022,
4.5869100210713));
#10871=CARTESIAN_POINT('Ctrl Pts',(3.09952602345727,-0.0427294365643947,
4.58625923195428));
#10872=CARTESIAN_POINT('Ctrl Pts',(3.09940767935907,-0.0367935503396157,
4.58588173664157));
#10873=CARTESIAN_POINT('Ctrl Pts',(3.09907660892048,-0.0153941640765726,
4.58452594373036));
#10874=CARTESIAN_POINT('Ctrl Pts',(3.09901720150257,7.16218653557497E-5,
4.58355570142605));
#10875=CARTESIAN_POINT('Ctrl Pts',(3.10016409170935,0.147312245682319,4.57439692124935));
#10876=CARTESIAN_POINT('Ctrl Pts',(3.11424635515854,0.278680929092709,4.56680859138581));
#10877=CARTESIAN_POINT('Ctrl Pts',(3.16964955494612,0.54401935990359,4.55107124596365));
#10878=CARTESIAN_POINT('Ctrl Pts',(3.21229905976571,0.676950336641671,4.54294362226343));
#10879=CARTESIAN_POINT('Ctrl Pts',(3.27627359279887,0.822133984055138,4.53312161123617));
#10880=CARTESIAN_POINT('Ctrl Pts',(3.28436926009618,0.839801955480722,4.53191018164853));
#10881=CARTESIAN_POINT('Ctrl Pts',(3.29699056000783,0.866316608245543,4.53006629907485));
#10882=CARTESIAN_POINT('Ctrl Pts',(3.30132641995931,0.875252720065993,4.52944036382479));
#10883=CARTESIAN_POINT('Ctrl Pts',(3.30928746784373,0.891352975719818,4.52830427127814));
#10884=CARTESIAN_POINT('Ctrl Pts',(3.3128895369032,0.89852836334888,4.5277949251043));
#10885=CARTESIAN_POINT('Ctrl Pts',(3.32071323456913,0.913881436945375,4.5266984772613));
#10886=CARTESIAN_POINT('Ctrl Pts',(3.32494832199605,0.922052018655944,4.52611091332138));
#10887=CARTESIAN_POINT('Ctrl Pts',(3.33649777280483,0.94396146965767,4.52452424259157));
#10888=CARTESIAN_POINT('Ctrl Pts',(3.34391652981032,0.957644294547188,4.52352147819668));
#10889=CARTESIAN_POINT('Ctrl Pts',(3.38106899637459,1.02429316675204,4.51857743566589));
#10890=CARTESIAN_POINT('Ctrl Pts',(3.4130484331492,1.07596403141138,4.51455670711693));
#10891=CARTESIAN_POINT('Ctrl Pts',(3.46230162440845,1.14797871692089,4.50867389836942));
#10892=CARTESIAN_POINT('Ctrl Pts',(3.47770542095237,1.16956451007768,4.50687264275241));
#10893=CARTESIAN_POINT('Ctrl Pts',(3.58242573665211,1.31029180932618,4.49488144139735));
#10894=CARTESIAN_POINT('Ctrl Pts',(3.68440405461566,1.41940861574163,4.48433660699607));
#10895=CARTESIAN_POINT('Ctrl Pts',(3.83609668502084,1.54910012507296,4.47068521047233));
#10896=CARTESIAN_POINT('Ctrl Pts',(3.87587101771571,1.58056348912742,4.46726923857692));
#10897=CARTESIAN_POINT('Ctrl Pts',(3.92454392406315,1.6161361888765,4.463317799071));
#10898=CARTESIAN_POINT('Ctrl Pts',(3.93232422734655,1.62173685073044,4.46269286259712));
#10899=CARTESIAN_POINT('Ctrl Pts',(3.94444664968546,1.63033120044091,4.46172986215833));
#10900=CARTESIAN_POINT('Ctrl Pts',(3.9487606488812,1.6333640339037,4.46138923923341));
#10901=CARTESIAN_POINT('Ctrl Pts',(3.95678296653972,1.63895649026087,4.46075973892991));
#10902=CARTESIAN_POINT('Ctrl Pts',(3.96048790790836,1.64152064108349,4.46047056590162));
#10903=CARTESIAN_POINT('Ctrl Pts',(3.96895923789559,1.64734120667784,4.45981286443535));
#10904=CARTESIAN_POINT('Ctrl Pts',(3.97373109129877,1.65058949840283,4.45944488185673));
#10905=CARTESIAN_POINT('Ctrl Pts',(3.98624151273063,1.65902634406777,4.45848645674469));
#10906=CARTESIAN_POINT('Ctrl Pts',(3.99400255271682,1.66418154579543,4.45789816089755));
#10907=CARTESIAN_POINT('Ctrl Pts',(4.04861538771135,1.69990870869614,4.45380008672563));
#10908=CARTESIAN_POINT('Ctrl Pts',(4.09670361270046,1.72855521529318,4.45040472929386));
#10909=CARTESIAN_POINT('Ctrl Pts',(4.28899021322516,1.83240224929677,4.43738613443141));
#10910=CARTESIAN_POINT('Ctrl Pts',(4.44095393201731,1.89188330190286,4.42822645789346));
#10911=CARTESIAN_POINT('Ctrl Pts',(4.66372079266504,1.9489933577245,4.4145353423935));
#10912=CARTESIAN_POINT('Ctrl Pts',(4.72978223251753,1.96240578313709,4.41045210959053));
#10913=CARTESIAN_POINT('Ctrl Pts',(4.81180618877112,1.97477461289938,4.40529206079465));
#10914=CARTESIAN_POINT('Ctrl Pts',(4.82724784978449,1.9769183214168,4.40431686097244));
#10915=CARTESIAN_POINT('Ctrl Pts',(4.85175956841584,1.98002879002063,4.40276220237625));
#10916=CARTESIAN_POINT('Ctrl Pts',(4.86081406428668,1.98111474198218,4.40218648772142));
#10917=CARTESIAN_POINT('Ctrl Pts',(4.87786308993262,1.98304102323914,4.4010996263888));
#10918=CARTESIAN_POINT('Ctrl Pts',(4.8858558960803,1.98389519119144,4.4005889246598));
#10919=CARTESIAN_POINT('Ctrl Pts',(4.90385542346344,1.98570877939338,4.39943611933404));
#10920=CARTESIAN_POINT('Ctrl Pts',(4.91386461538426,1.98664090705762,4.39879317526066));
#10921=CARTESIAN_POINT('Ctrl Pts',(4.93949288858385,1.98883232889451,4.3971419121087));
#10922=CARTESIAN_POINT('Ctrl Pts',(4.95512030760072,1.98998328776442,4.39613024740096));
#10923=CARTESIAN_POINT('Ctrl Pts',(5.05986684368127,1.9964580516727,4.38931600518865));
#10924=CARTESIAN_POINT('Ctrl Pts',(5.14923105906543,1.99597708802232,4.38333417607024));
#10925=CARTESIAN_POINT('Ctrl Pts',(5.368495650465,1.98005996633097,4.36827257613832));
#10926=CARTESIAN_POINT('Ctrl Pts',(5.49748587795039,1.95783981502472,4.35906244333095));
#10927=CARTESIAN_POINT('Ctrl Pts',(5.68424958192619,1.90641434137607,4.34572060510302));
#10928=CARTESIAN_POINT('Ctrl Pts',(5.74430112269613,1.88676961786906,4.34143511563473));
#10929=CARTESIAN_POINT('Ctrl Pts',(5.8127627901207,1.86071520788417,4.33662915270703));
#10930=CARTESIAN_POINT('Ctrl Pts',(5.8221732581293,1.85705182927412,4.33597035543761));
#10931=CARTESIAN_POINT('Ctrl Pts',(5.83655672865267,1.85132636679246,4.33496663904351));
#10932=CARTESIAN_POINT('Ctrl Pts',(5.84154971656284,1.84931541618558,4.33461881478507));
#10933=CARTESIAN_POINT('Ctrl Pts',(5.85069908495199,1.8455873502659,4.33398262957089));
#10934=CARTESIAN_POINT('Ctrl Pts',(5.85485779268381,1.84387639366469,4.33369392004714));
#10935=CARTESIAN_POINT('Ctrl Pts',(5.86421235044143,1.83999074399096,4.33304551340429));
#10936=CARTESIAN_POINT('Ctrl Pts',(5.86940478951236,1.83780810261645,4.33268629879851));
#10937=CARTESIAN_POINT('Ctrl Pts',(5.88466537433436,1.83131712176445,4.33163242379357));
#10938=CARTESIAN_POINT('Ctrl Pts',(5.89470755775693,1.82694775044492,4.33094131300108));
#10939=CARTESIAN_POINT('Ctrl Pts',(5.99276781497663,1.78331762217945,4.32421137891598));
#10940=CARTESIAN_POINT('Ctrl Pts',(6.0778796060278,1.73780374911271,4.31851501711611));
#10941=CARTESIAN_POINT('Ctrl Pts',(6.26786680947022,1.61775408209795,4.30540006562914));
#10942=CARTESIAN_POINT('Ctrl Pts',(6.3694839418109,1.53889442004371,4.29805211889814));
#10943=CARTESIAN_POINT('Ctrl Pts',(6.50701258713228,1.40912248299074,4.28674784902604));
#10944=CARTESIAN_POINT('Ctrl Pts',(6.54927192677593,1.36542984922908,4.28305312174268));
#10945=CARTESIAN_POINT('Ctrl Pts',(6.59947560623293,1.3085407960717,4.27833036670315));
#10946=CARTESIAN_POINT('Ctrl Pts',(6.60935274923855,1.29708844228768,4.27738389452483));
#10947=CARTESIAN_POINT('Ctrl Pts',(6.6249097096193,1.27863015977595,4.27586455379365));
#10948=CARTESIAN_POINT('Ctrl Pts',(6.63067401160961,1.2716959579936,4.27529513878569));
#10949=CARTESIAN_POINT('Ctrl Pts',(6.64149753644228,1.25849466544202,4.27421350687661));
#10950=CARTESIAN_POINT('Ctrl Pts',(6.64656621722854,1.25223553458073,4.27370168560467));
#10951=CARTESIAN_POINT('Ctrl Pts',(6.65797719345753,1.23796872608678,4.27253724849171));
#10952=CARTESIAN_POINT('Ctrl Pts',(6.6642961233049,1.22994273150356,4.27188372129819));
#10953=CARTESIAN_POINT('Ctrl Pts',(6.68048009717417,1.20905858014824,4.27018697265338));
#10954=CARTESIAN_POINT('Ctrl Pts',(6.69025042765089,1.19612830334546,4.26914008583931));
#10955=CARTESIAN_POINT('Ctrl Pts',(6.77707965361206,1.07825743432101,4.2596273351404));
#10956=CARTESIAN_POINT('Ctrl Pts',(6.84383540839038,0.966145834093963,4.25076415439392));
#10957=CARTESIAN_POINT('Ctrl Pts',(6.93881075892006,0.76403090248282,4.23525055538052));
#10958=CARTESIAN_POINT('Ctrl Pts',(6.97247822476205,0.677036417394026,4.22871437547163));
#10959=CARTESIAN_POINT('Ctrl Pts',(7.01730261076583,0.531731169832178,4.21826368859593));
#10960=CARTESIAN_POINT('Ctrl Pts',(7.032163857205,0.474708450966558,4.21427604815709));
#10961=CARTESIAN_POINT('Ctrl Pts',(7.04655994959518,0.407383183415082,4.20976039466402));
#10962=CARTESIAN_POINT('Ctrl Pts',(7.04856635222556,0.397644446517391,4.20911186019882));
#10963=CARTESIAN_POINT('Ctrl Pts',(7.05154018650171,0.382643267487679,4.20812046686881));
#10964=CARTESIAN_POINT('Ctrl Pts',(7.05255937280284,0.377391420711163,4.20777480977541));
#10965=CARTESIAN_POINT('Ctrl Pts',(7.05439674144263,0.367715516887429,4.20714067928));
#10966=CARTESIAN_POINT('Ctrl Pts',(7.05522108354875,0.363292805373047,4.20685187311068));
#10967=CARTESIAN_POINT('Ctrl Pts',(7.0570509391888,0.353287575524319,4.20620086187582));
#10968=CARTESIAN_POINT('Ctrl Pts',(7.0580476078255,0.347703541010868,4.20583915737786));
#10969=CARTESIAN_POINT('Ctrl Pts',(7.06056132499627,0.333264137421996,4.20490788582372));
#10970=CARTESIAN_POINT('Ctrl Pts',(7.06204241027792,0.32440252266112,4.20434027141216));
#10971=CARTESIAN_POINT('Ctrl Pts',(7.07121065976443,0.267171639492199,4.20069793192226));
#10972=CARTESIAN_POINT('Ctrl Pts',(7.07717478663549,0.218538890282222,4.19771071067118));
#10973=CARTESIAN_POINT('Ctrl Pts',(7.0824969622721,0.156217563139525,4.19396412132613));
#10974=CARTESIAN_POINT('Ctrl Pts',(7.08351321349206,0.142691731819713,4.19315586760225));
#10975=CARTESIAN_POINT('Ctrl Pts',(7.0871436593937,0.0867391208870799,4.18982881601366));
#10976=CARTESIAN_POINT('Ctrl Pts',(7.08853944685373,0.0442433067737386,
4.18734086199011));
#10977=CARTESIAN_POINT('Ctrl Pts',(7.08857690420654,0.00115606453166728,
4.18483113989589));
#10978=CARTESIAN_POINT('Ctrl Pts',(7.08857715545314,0.000578028143273556,
4.18479747312931));
#10979=CARTESIAN_POINT('Ctrl Pts',(7.08857715545311,-9.37345802482418E-11,
4.18476380915572));
#10980=CARTESIAN_POINT('Ctrl Pts',(7.08857715492705,4.58116840822842E-5,
4.02544646529617));
#10981=CARTESIAN_POINT('Ctrl Pts',(7.08857709852169,0.00250183564861334,
4.02560187048724));
#10982=CARTESIAN_POINT('Ctrl Pts',(7.08857250616951,0.00495785070224662,
4.02575741631251));
#10983=CARTESIAN_POINT('Ctrl Pts',(7.08854430144895,0.0125464882364174,
4.02623846485478));
#10984=CARTESIAN_POINT('Ctrl Pts',(7.08850541498808,0.0176789997428494,
4.02656444054343));
#10985=CARTESIAN_POINT('Ctrl Pts',(7.0883442039336,0.0317753122926986,4.02746146572168));
#10986=CARTESIAN_POINT('Ctrl Pts',(7.08818126193469,0.0407384437379774,
4.02803377315785));
#10987=CARTESIAN_POINT('Ctrl Pts',(7.08758290353538,0.0647465644321104,
4.02957205024097));
#10988=CARTESIAN_POINT('Ctrl Pts',(7.08703761993958,0.0797879962970355,
4.03054141383691));
#10989=CARTESIAN_POINT('Ctrl Pts',(7.08364312076721,0.151117008065387,4.03516588236312));
#10990=CARTESIAN_POINT('Ctrl Pts',(7.07857969142872,0.20726856435142,4.03888896844737));
#10991=CARTESIAN_POINT('Ctrl Pts',(7.06586609534288,0.302807672359106,4.04536853327583));
#10992=CARTESIAN_POINT('Ctrl Pts',(7.05939255246803,0.342319197734179,4.048090944713));
#10993=CARTESIAN_POINT('Ctrl Pts',(7.03694388477639,0.457496270064081,4.05614236579636));
#10994=CARTESIAN_POINT('Ctrl Pts',(7.01775365014093,0.532457742289129,4.06153308152317));
#10995=CARTESIAN_POINT('Ctrl Pts',(6.97045390472378,0.680763747804374,4.07238436832725));
#10996=CARTESIAN_POINT('Ctrl Pts',(6.94226572929044,0.753951958449263,4.07783549493542));
#10997=CARTESIAN_POINT('Ctrl Pts',(6.89966222109006,0.847698540996847,4.0848089072685));
#10998=CARTESIAN_POINT('Ctrl Pts',(6.88906701568782,0.869912098662336,4.0864603185018));
#10999=CARTESIAN_POINT('Ctrl Pts',(6.87058965905482,0.906874808492847,4.08920001644525));
#11000=CARTESIAN_POINT('Ctrl Pts',(6.86292843116922,0.921730781025356,4.09029887041223));
#11001=CARTESIAN_POINT('Ctrl Pts',(6.85198623558389,0.942309751363044,4.09181604578255));
#11002=CARTESIAN_POINT('Ctrl Pts',(6.84886249949088,0.948114952263243,4.09224347059474));
#11003=CARTESIAN_POINT('Ctrl Pts',(6.8434984938801,0.957966156216981,4.09296769996346));
#11004=CARTESIAN_POINT('Ctrl Pts',(6.84127284285697,0.962020020688211,4.09326540909022));
#11005=CARTESIAN_POINT('Ctrl Pts',(6.8369602364849,0.969810776813559,4.09383688668179));
#11006=CARTESIAN_POINT('Ctrl Pts',(6.83487533728708,0.973548720086075,4.09411078700596));
#11007=CARTESIAN_POINT('Ctrl Pts',(6.82983072216348,0.982525001238606,4.09476790189424));
#11008=CARTESIAN_POINT('Ctrl Pts',(6.82685928442083,0.987756753396547,4.09515037902927));
#11009=CARTESIAN_POINT('Ctrl Pts',(6.81586595085718,1.00691017907661,4.09654902526836));
#11010=CARTESIAN_POINT('Ctrl Pts',(6.80769935346212,1.02074867073847,4.09755643906983));
#11011=CARTESIAN_POINT('Ctrl Pts',(6.73749862823314,1.13648721328408,4.10596864954574));
#11012=CARTESIAN_POINT('Ctrl Pts',(6.66659686688781,1.23274581067569,4.11288624743041));
#11013=CARTESIAN_POINT('Ctrl Pts',(6.51803786695324,1.40058464061019,4.12589836657878));
#11014=CARTESIAN_POINT('Ctrl Pts',(6.4424933612927,1.47346902791223,4.13197178641174));
#11015=CARTESIAN_POINT('Ctrl Pts',(6.31951146787305,1.57470446990719,4.14153503950475));
#11016=CARTESIAN_POINT('Ctrl Pts',(6.27604751175241,1.60759149946494,4.14485895894372));
#11017=CARTESIAN_POINT('Ctrl Pts',(6.21928675888488,1.64699177714022,4.14916284017094));
#11018=CARTESIAN_POINT('Ctrl Pts',(6.20718773365005,1.65519468279194,4.1500781502127));
#11019=CARTESIAN_POINT('Ctrl Pts',(6.18867338735697,1.66745220598004,4.151476147814));
#11020=CARTESIAN_POINT('Ctrl Pts',(6.18232310417629,1.6716045279285,4.1519551845026));
#11021=CARTESIAN_POINT('Ctrl Pts',(6.16935051152475,1.67998177862438,4.15293291787599));
#11022=CARTESIAN_POINT('Ctrl Pts',(6.16272663220396,1.68420401724034,4.15343170263343));
#11023=CARTESIAN_POINT('Ctrl Pts',(6.14813415832408,1.69338489157496,4.15452963383762));
#11024=CARTESIAN_POINT('Ctrl Pts',(6.1401551932842,1.69832661158322,4.15512938675838));
#11025=CARTESIAN_POINT('Ctrl Pts',(6.1177229848562,1.71200176934391,4.15681409422844));
#11026=CARTESIAN_POINT('Ctrl Pts',(6.10319354997353,1.72060808446585,4.15790362410002));
#11027=CARTESIAN_POINT('Ctrl Pts',(6.01532393436398,1.77116047061669,4.16448448015018));
#11028=CARTESIAN_POINT('Ctrl Pts',(5.93949805313887,1.80859147009762,4.17013452134775));
#11029=CARTESIAN_POINT('Ctrl Pts',(5.72398909994932,1.89845526580207,4.18609488797693));
#11030=CARTESIAN_POINT('Ctrl Pts',(5.5804602603567,1.9402113496441,4.19664882535676));
#11031=CARTESIAN_POINT('Ctrl Pts',(5.38366091572784,1.97423281006533,4.21031010996969));
#11032=CARTESIAN_POINT('Ctrl Pts',(5.33337861411253,1.98096311405979,4.21372722070526));
#11033=CARTESIAN_POINT('Ctrl Pts',(5.27334632543013,1.98667872066863,4.21767979426143));
#11034=CARTESIAN_POINT('Ctrl Pts',(5.26379590596213,1.98751857958875,4.21830478364355));
#11035=CARTESIAN_POINT('Ctrl Pts',(5.24898318488842,1.98871364920272,4.21926784786616));
#11036=CARTESIAN_POINT('Ctrl Pts',(5.24372505857129,1.989116887513,4.21960848219264));
#11037=CARTESIAN_POINT('Ctrl Pts',(5.23397142564024,1.98982598432062,4.22023799279811));
#11038=CARTESIAN_POINT('Ctrl Pts',(5.22947650899357,1.99013746204794,4.22052716481127));
#11039=CARTESIAN_POINT('Ctrl Pts',(5.21922075557577,1.99081323219154,4.22118485024384));
#11040=CARTESIAN_POINT('Ctrl Pts',(5.21345937107045,1.9911677516999,4.22155281791148));
#11041=CARTESIAN_POINT('Ctrl Pts',(5.1983955756887,1.99202906528167,4.22251117814042));
#11042=CARTESIAN_POINT('Ctrl Pts',(5.18909088638598,1.99249571665251,4.2230994244898));
#11043=CARTESIAN_POINT('Ctrl Pts',(5.12391072845345,1.99530701041735,4.22719623764638));
#11044=CARTESIAN_POINT('Ctrl Pts',(5.06795608949343,1.99536638452538,4.23059046356859));
#11045=CARTESIAN_POINT('Ctrl Pts',(4.84960444696433,1.98640921900876,4.24360915360744));
#11046=CARTESIAN_POINT('Ctrl Pts',(4.68856265971034,1.95990621663879,4.25276976107664));
#11047=CARTESIAN_POINT('Ctrl Pts',(4.46786451647704,1.89518804706262,4.26646208085342));
#11048=CARTESIAN_POINT('Ctrl Pts',(4.40421999358698,1.87296756328339,4.27054547331167));
#11049=CARTESIAN_POINT('Ctrl Pts',(4.32738638211132,1.84169463918865,4.27570570168349));
#11050=CARTESIAN_POINT('Ctrl Pts',(4.31301660765079,1.83564851479277,4.27668091267777));
#11051=CARTESIAN_POINT('Ctrl Pts',(4.29035582247543,1.82579969981102,4.27823558507285));
#11052=CARTESIAN_POINT('Ctrl Pts',(4.2820172947541,1.82210742613277,4.2788113022401));
#11053=CARTESIAN_POINT('Ctrl Pts',(4.26637696442575,1.81505326609324,4.27989816582913));
#11054=CARTESIAN_POINT('Ctrl Pts',(4.25906957334082,1.81170415725227,4.28040886728339));
#11055=CARTESIAN_POINT('Ctrl Pts',(4.24266980595346,1.80406756546632,4.28156166866341));
#11056=CARTESIAN_POINT('Ctrl Pts',(4.23358924872094,1.79975535895956,4.28220460904056));
#11057=CARTESIAN_POINT('Ctrl Pts',(4.2104385688693,1.78854625255723,4.28385585616723));
#11058=CARTESIAN_POINT('Ctrl Pts',(4.19641662386367,1.78155196586377,4.28486750843468));
#11059=CARTESIAN_POINT('Ctrl Pts',(4.1030685211369,1.73360733542049,4.29168137655293));
#11060=CARTESIAN_POINT('Ctrl Pts',(4.02649686933588,1.68754235487881,4.29766282078443));
#11061=CARTESIAN_POINT('Ctrl Pts',(3.84613728877387,1.56184235729986,4.31272434301702));
#11062=CARTESIAN_POINT('Ctrl Pts',(3.74659855618972,1.47683902506872,4.3219348307558));
#11063=CARTESIAN_POINT('Ctrl Pts',(3.61231539684048,1.33721251239724,4.33527707808051));
#11064=CARTESIAN_POINT('Ctrl Pts',(3.57072766755594,1.289644925758,4.33956262959613));
#11065=CARTESIAN_POINT('Ctrl Pts',(3.52518482629187,1.23227057720689,4.34436865285197));
#11066=CARTESIAN_POINT('Ctrl Pts',(3.51896666226061,1.22431367284508,4.34502745221803));
#11067=CARTESIAN_POINT('Ctrl Pts',(3.50952693977512,1.21204346537878,4.34603117116648));
#11068=CARTESIAN_POINT('Ctrl Pts',(3.50626207738366,1.20776390900997,4.34637899590437));
#11069=CARTESIAN_POINT('Ctrl Pts',(3.50030143034232,1.19988480636251,4.34701518163334));
#11070=CARTESIAN_POINT('Ctrl Pts',(3.49760049863815,1.19628936549466,4.34730389119559));
#11071=CARTESIAN_POINT('Ctrl Pts',(3.49154397581996,1.18816997892694,4.34795229747965));
#11072=CARTESIAN_POINT('Ctrl Pts',(3.48819537754692,1.18364094310834,4.34831151169133));
#11073=CARTESIAN_POINT('Ctrl Pts',(3.47839278168777,1.17026461634209,4.3493653842746));
#11074=CARTESIAN_POINT('Ctrl Pts',(3.4719922824136,1.16137812341069,4.35005649306461));
#11075=CARTESIAN_POINT('Ctrl Pts',(3.4100020041262,1.07379847226471,4.35678455420889));
#11076=CARTESIAN_POINT('Ctrl Pts',(3.36010163269945,0.991217005556853,4.36247925978546));
#11077=CARTESIAN_POINT('Ctrl Pts',(3.25810450965683,0.790965105692136,4.37559396395353));
#11078=CARTESIAN_POINT('Ctrl Pts',(3.21102556893558,0.671238044025972,4.38294317599498));
#11079=CARTESIAN_POINT('Ctrl Pts',(3.15908778847075,0.489390940519344,4.39424914646893));
#11080=CARTESIAN_POINT('Ctrl Pts',(3.14507983140447,0.430235629294735,4.39794420079618));
#11081=CARTESIAN_POINT('Ctrl Pts',(3.13098476502849,0.355676869345259,4.40266732463889));
#11082=CARTESIAN_POINT('Ctrl Pts',(3.12834462031343,0.340785371325787,4.40361382271666));
#11083=CARTESIAN_POINT('Ctrl Pts',(3.12440102863109,0.316969408356208,4.40513319535612));
#11084=CARTESIAN_POINT('Ctrl Pts',(3.1229883021754,0.308063443057399,4.40570261611588));
#11085=CARTESIAN_POINT('Ctrl Pts',(3.12042817308161,0.291185314314506,4.40678425276645));
#11086=CARTESIAN_POINT('Ctrl Pts',(3.11926857190762,0.283215161912105,4.40729607298309));
#11087=CARTESIAN_POINT('Ctrl Pts',(3.11674782939329,0.265121186462534,4.40846049917843));
#11088=CARTESIAN_POINT('Ctrl Pts',(3.11541612997236,0.254993554637581,4.40911401644258));
#11089=CARTESIAN_POINT('Ctrl Pts',(3.11217302480051,0.228773026521777,4.4108107220397));
#11090=CARTESIAN_POINT('Ctrl Pts',(3.11037987447228,0.212666520978772,4.41185757542553));
#11091=CARTESIAN_POINT('Ctrl Pts',(3.09595422304999,0.0669684310689805,
4.42137102453675));
#11092=CARTESIAN_POINT('Ctrl Pts',(3.09584459922837,-0.0635241515526198,
4.43023501217895));
#11093=CARTESIAN_POINT('Ctrl Pts',(3.11746372222519,-0.285833321325941,
4.44575144367755));
#11094=CARTESIAN_POINT('Ctrl Pts',(3.13297384668399,-0.377846324009289,
4.45228967009824));
#11095=CARTESIAN_POINT('Ctrl Pts',(3.16868157619853,-0.525648194615674,
4.46273960996431));
#11096=CARTESIAN_POINT('Ctrl Pts',(3.18502963653073,-0.58222416125124,4.46672467228651));
#11097=CARTESIAN_POINT('Ctrl Pts',(3.20703743763096,-0.647418686649058,
4.47123780265506));
#11098=CARTESIAN_POINT('Ctrl Pts',(3.21028755744028,-0.656814271779177,
4.47188624280263));
#11099=CARTESIAN_POINT('Ctrl Pts',(3.21539440881028,-0.671227677611153,
4.47287752284728));
#11100=CARTESIAN_POINT('Ctrl Pts',(3.21720125436617,-0.676262824528884,
4.47322315999818));
#11101=CARTESIAN_POINT('Ctrl Pts',(3.22056493929564,-0.685519126340224,
4.47385727180544));
#11102=CARTESIAN_POINT('Ctrl Pts',(3.22211579843322,-0.689742270564241,
4.47414607908291));
#11103=CARTESIAN_POINT('Ctrl Pts',(3.22565442465368,-0.699278476875247,
4.47479711521682));
#11104=CARTESIAN_POINT('Ctrl Pts',(3.22765057272135,-0.704588322562702,
4.47515884333502));
#11105=CARTESIAN_POINT('Ctrl Pts',(3.23286711612269,-0.718286873948393,
4.47609021651312));
#11106=CARTESIAN_POINT('Ctrl Pts',(3.23612163073709,-0.726662570803931,
4.47665790821851));
#11107=CARTESIAN_POINT('Ctrl Pts',(3.25748829360405,-0.78056916844642,4.48030187689446));
#11108=CARTESIAN_POINT('Ctrl Pts',(3.27721793429671,-0.825445604307218,
4.48329056028528));
#11109=CARTESIAN_POINT('Ctrl Pts',(3.37229867655185,-1.02174543722544,4.49635519451998));
#11110=CARTESIAN_POINT('Ctrl Pts',(3.46507021711557,-1.16395126086564,4.5058536988342));
#11111=CARTESIAN_POINT('Ctrl Pts',(3.61895413196227,-1.34478421876155,4.51998179647415));
#11112=CARTESIAN_POINT('Ctrl Pts',(3.66586963526371,-1.39450022184614,4.52412043826137));
#11113=CARTESIAN_POINT('Ctrl Pts',(3.72655137947403,-1.45252520774829,4.52934276141503));
#11114=CARTESIAN_POINT('Ctrl Pts',(3.73799005573561,-1.46320820933447,4.53032176382666));
#11115=CARTESIAN_POINT('Ctrl Pts',(3.75630055136633,-1.47990998229503,4.53188109671129));
#11116=CARTESIAN_POINT('Ctrl Pts',(3.76309018918098,-1.48601820125571,4.53245764386057));
#11117=CARTESIAN_POINT('Ctrl Pts',(3.77593285504474,-1.49741335728102,4.53354521908515));
#11118=CARTESIAN_POINT('Ctrl Pts',(3.78197637225338,-1.50271077361714,4.53405579579285));
#11119=CARTESIAN_POINT('Ctrl Pts',(3.79563585994884,-1.5145387323627,4.53520717457566));
#11120=CARTESIAN_POINT('Ctrl Pts',(3.803269374401,-1.52104859201148,4.53584880835404));
#11121=CARTESIAN_POINT('Ctrl Pts',(3.82290009062851,-1.53753550438551,4.53749446394439));
#11122=CARTESIAN_POINT('Ctrl Pts',(3.83496566647921,-1.5474297270172,4.53850179289028));
#11123=CARTESIAN_POINT('Ctrl Pts',(3.91517720073498,-1.61164719073418,4.54517287835131));
#11124=CARTESIAN_POINT('Ctrl Pts',(3.98669532784684,-1.66158894882174,4.5510070727885));
#11125=CARTESIAN_POINT('Ctrl Pts',(4.18662332889657,-1.78254992827892,4.5670002139327));
#11126=CARTESIAN_POINT('Ctrl Pts',(4.31997294583062,-1.84435590972678,4.57737512345643));
#11127=CARTESIAN_POINT('Ctrl Pts',(4.50664294086914,-1.90703446154237,4.59084165991703));
#11128=CARTESIAN_POINT('Ctrl Pts',(4.55499790894734,-1.92125733047917,4.5942360688566));
#11129=CARTESIAN_POINT('Ctrl Pts',(4.61312148182262,-1.93598585232027,4.59816602976758));
#11130=CARTESIAN_POINT('Ctrl Pts',(4.62241619364844,-1.93827007377864,4.59878996123502));
#11131=CARTESIAN_POINT('Ctrl Pts',(4.63685386782449,-1.94170820413684,4.59975175076874));
#11132=CARTESIAN_POINT('Ctrl Pts',(4.64198541939511,-1.94290874276813,4.60009215780698));
#11133=CARTESIAN_POINT('Ctrl Pts',(4.65151344300547,-1.9450980560474,4.60072146446842));
#11134=CARTESIAN_POINT('Ctrl Pts',(4.65590848043457,-1.94609226465297,4.60101065813491));
#11135=CARTESIAN_POINT('Ctrl Pts',(4.66594588263913,-1.94832711635444,4.6016686685364));
#11136=CARTESIAN_POINT('Ctrl Pts',(4.67159028958026,-1.94955814661992,4.60203693735338));
#11137=CARTESIAN_POINT('Ctrl Pts',(4.68636637983322,-1.95271359064234,4.6029966059093));
#11138=CARTESIAN_POINT('Ctrl Pts',(4.69550648184458,-1.95459850087827,4.60358584987261));
#11139=CARTESIAN_POINT('Ctrl Pts',(4.75989625093131,-1.96740680047743,4.60770829874435));
#11140=CARTESIAN_POINT('Ctrl Pts',(4.81557901150069,-1.97605126315098,4.61112553013966));
#11141=CARTESIAN_POINT('Ctrl Pts',(5.03278478737302,-2.00040551285652,4.62414231536013));
#11142=CARTESIAN_POINT('Ctrl Pts',(5.19561717009188,-1.99874771707183,4.63328400376623));
#11143=CARTESIAN_POINT('Ctrl Pts',(5.42319137411066,-1.96852195680953,4.64695184671766));
#11144=CARTESIAN_POINT('Ctrl Pts',(5.48942721489577,-1.95628695511843,4.65103198853302));
#11145=CARTESIAN_POINT('Ctrl Pts',(5.57007731849368,-1.93712577578741,4.65618856291183));
#11146=CARTESIAN_POINT('Ctrl Pts',(5.58519822250771,-1.93334553090129,4.65716354866106));
#11147=CARTESIAN_POINT('Ctrl Pts',(5.6090928017212,-1.92707343553369,4.65871794417281));
#11148=CARTESIAN_POINT('Ctrl Pts',(5.61789655834378,-1.92469789023318,4.65929361201861));
#11149=CARTESIAN_POINT('Ctrl Pts',(5.63442993335875,-1.92011479229683,4.66038043347526));
#11150=CARTESIAN_POINT('Ctrl Pts',(5.64216312040221,-1.91792070887504,4.66089114249958));
#11151=CARTESIAN_POINT('Ctrl Pts',(5.65953788285447,-1.91287741672792,4.66204402917443));
#11152=CARTESIAN_POINT('Ctrl Pts',(5.66917154808532,-1.91000195347986,4.66268704780022));
#11153=CARTESIAN_POINT('Ctrl Pts',(5.69376721135482,-1.90245765933255,4.664338629952));
#11154=CARTESIAN_POINT('Ctrl Pts',(5.70869644416392,-1.8976851558804,4.66535054130215));
#11155=CARTESIAN_POINT('Ctrl Pts',(5.80838276081461,-1.86451811328965,4.67217213248661));
#11156=CARTESIAN_POINT('Ctrl Pts',(5.89119334047811,-1.83063397073732,4.6781615204004));
#11157=CARTESIAN_POINT('Ctrl Pts',(6.08862437713143,-1.73390691508636,4.69322463796165));
#11158=CARTESIAN_POINT('Ctrl Pts',(6.19988012040535,-1.66514216001331,4.70242779208748));
#11159=CARTESIAN_POINT('Ctrl Pts',(6.353809332506,-1.54772639908053,4.71576158880403));
#11160=CARTESIAN_POINT('Ctrl Pts',(6.40215814154306,-1.5070779053753,4.72004585996782));
#11161=CARTESIAN_POINT('Ctrl Pts',(6.45591380912792,-1.45734329089058,4.7248506402328));
#11162=CARTESIAN_POINT('Ctrl Pts',(6.46327357481374,-1.45042960338276,4.72550939810109));
#11163=CARTESIAN_POINT('Ctrl Pts',(6.47447565160237,-1.43974520802031,4.72651306725245));
#11164=CARTESIAN_POINT('Ctrl Pts',(6.47835560007893,-1.43601445731111,4.72686088325526));
#11165=CARTESIAN_POINT('Ctrl Pts',(6.48544936001788,-1.42913800066806,4.727497060634));
#11166=CARTESIAN_POINT('Ctrl Pts',(6.48866763050755,-1.42599713714078,4.72778577051755));
#11167=CARTESIAN_POINT('Ctrl Pts',(6.49589303887598,-1.41889765200411,4.72843418699341));
#11168=CARTESIAN_POINT('Ctrl Pts',(6.49989404226039,-1.41493293127675,4.7287934110044));
#11169=CARTESIAN_POINT('Ctrl Pts',(6.51162481274837,-1.40320964476914,4.72984733933442));
#11170=CARTESIAN_POINT('Ctrl Pts',(6.51930768727117,-1.39540416021821,4.73053849351095));
#11171=CARTESIAN_POINT('Ctrl Pts',(6.58997102679856,-1.32242040595063,4.73690841028084));
#11172=CARTESIAN_POINT('Ctrl Pts',(6.64851345431889,-1.25307503632279,4.74228485360505));
#11173=CARTESIAN_POINT('Ctrl Pts',(6.77105869299919,-1.0860455927663,4.7543970671153));
#11174=CARTESIAN_POINT('Ctrl Pts',(6.83161239416044,-0.986257041083104,
4.76106907678195));
#11175=CARTESIAN_POINT('Ctrl Pts',(6.9054470777902,-0.8364293587969,4.77096155112508));
#11176=CARTESIAN_POINT('Ctrl Pts',(6.92605149798289,-0.790274782157797,
4.77399093000325));
#11177=CARTESIAN_POINT('Ctrl Pts',(6.95737387210527,-0.712281559085304,
4.77912099787863));
#11178=CARTESIAN_POINT('Ctrl Pts',(6.96908037166673,-0.68086456606297,4.78119016695826));
#11179=CARTESIAN_POINT('Ctrl Pts',(6.98399671085792,-0.637525098993796,
4.78405516217971));
#11180=CARTESIAN_POINT('Ctrl Pts',(6.98789622250901,-0.625844675980574,
4.78482832777026));
#11181=CARTESIAN_POINT('Ctrl Pts',(6.99427659863734,-0.60612722350328,4.78613553283714));
#11182=CARTESIAN_POINT('Ctrl Pts',(6.99681526280512,-0.598109151358696,
4.78666766950205));
#11183=CARTESIAN_POINT('Ctrl Pts',(7.00173461289452,-0.582223547725681,
4.78772317160442));
#11184=CARTESIAN_POINT('Ctrl Pts',(7.00411752621209,-0.574356876654398,
4.78824645227647));
#11185=CARTESIAN_POINT('Ctrl Pts',(7.00979504188972,-0.555187556437833,
4.78952310627933));
#11186=CARTESIAN_POINT('Ctrl Pts',(7.01303830126534,-0.543870143198756,
4.7902781267716));
#11187=CARTESIAN_POINT('Ctrl Pts',(7.02196835550385,-0.511633667668831,
4.79243270153997));
#11188=CARTESIAN_POINT('Ctrl Pts',(7.02741444346134,-0.490650217271119,
4.79383991517465));
#11189=CARTESIAN_POINT('Ctrl Pts',(7.0697655595526,-0.315802065917204,4.80560876877572));
#11190=CARTESIAN_POINT('Ctrl Pts',(7.08857715545348,-0.158164795785966,
4.81656162480003));
#11191=CARTESIAN_POINT('Ctrl Pts',(7.08857715545311,4.63462601629772E-12,
4.82758772788682));
#11192=CARTESIAN_POINT('Origin',(5.09382715545311,0.,-6.77268258743872));
#11193=CARTESIAN_POINT('',(7.08857697542999,-0.000847468688046533,5.78712926957393));
#11194=CARTESIAN_POINT('',(7.09089102510648,-0.00118553947171295,5.62731851852589));
#11195=CARTESIAN_POINT('',(7.08857715545311,8.3550772080578E-14,-6.77268258743872));
#11196=CARTESIAN_POINT('Ctrl Pts',(7.08857697543024,-0.000847467537915952,
5.78712926964943));
#11197=CARTESIAN_POINT('Ctrl Pts',(7.08851864778083,-0.138137762372735,
5.77811573517358));
#11198=CARTESIAN_POINT('Ctrl Pts',(7.07428701488024,-0.275032252711523,
5.7686626804473));
#11199=CARTESIAN_POINT('Ctrl Pts',(7.02136446103858,-0.527429070389755,
5.7506905530694));
#11200=CARTESIAN_POINT('Ctrl Pts',(6.98594481453895,-0.643022093466309,
5.74224390314858));
#11201=CARTESIAN_POINT('Ctrl Pts',(6.93423458573705,-0.769535208304726,
5.73318740374307));
#11202=CARTESIAN_POINT('Ctrl Pts',(6.92799797685692,-0.784283993764439,
5.73213491133118));
#11203=CARTESIAN_POINT('Ctrl Pts',(6.91917735469631,-0.804462754298365,
5.73070105471366));
#11204=CARTESIAN_POINT('Ctrl Pts',(6.91674558735057,-0.809958064234257,
5.73031120142937));
#11205=CARTESIAN_POINT('Ctrl Pts',(6.91254014790502,-0.819346639230769,
5.72964633515278));
#11206=CARTESIAN_POINT('Ctrl Pts',(6.91077873387739,-0.823245301616172,
5.72937059741184));
#11207=CARTESIAN_POINT('Ctrl Pts',(6.90708649247861,-0.831348026207296,
5.72879830197985));
#11208=CARTESIAN_POINT('Ctrl Pts',(6.90515356855211,-0.835551069460491,
5.72850188585384));
#11209=CARTESIAN_POINT('Ctrl Pts',(6.9004273952516,-0.845734415410518,5.72778471084471));
#11210=CARTESIAN_POINT('Ctrl Pts',(6.89761901927022,-0.851707721478765,
5.72736486917326));
#11211=CARTESIAN_POINT('Ctrl Pts',(6.88757188100193,-0.872804989552912,
5.72588460305805));
#11212=CARTESIAN_POINT('Ctrl Pts',(6.88017190788738,-0.887851991690589,
5.72483356569295));
#11213=CARTESIAN_POINT('Ctrl Pts',(6.86139850173605,-0.924840401948595,
5.72225727555241));
#11214=CARTESIAN_POINT('Ctrl Pts',(6.84980515899305,-0.946667627702199,
5.72074347842823));
#11215=CARTESIAN_POINT('Ctrl Pts',(6.7995002922786,-1.03727285836511,5.71446364953517));
#11216=CARTESIAN_POINT('Ctrl Pts',(6.75712786539693,-1.10394224992717,5.70985072318407));
#11217=CARTESIAN_POINT('Ctrl Pts',(6.61786970184766,-1.296755606723,5.69602177809838));
#11218=CARTESIAN_POINT('Ctrl Pts',(6.50977768791325,-1.41398688631044,5.6868802858042));
#11219=CARTESIAN_POINT('Ctrl Pts',(6.37244728192596,-1.53121770192777,5.67575865074876));
#11220=CARTESIAN_POINT('Ctrl Pts',(6.35573936817078,-1.54501604834893,5.67441390106552));
#11221=CARTESIAN_POINT('Ctrl Pts',(6.32961405947582,-1.56588531880682,5.67232189321447));
#11222=CARTESIAN_POINT('Ctrl Pts',(6.32035295777391,-1.57314988179829,5.67158232804223));
#11223=CARTESIAN_POINT('Ctrl Pts',(6.30451664434112,-1.5853473055098,5.67032081426914));
#11224=CARTESIAN_POINT('Ctrl Pts',(6.29797417142884,-1.5903223189749,5.66980053661757));
#11225=CARTESIAN_POINT('Ctrl Pts',(6.28467472141519,-1.60030633998083,5.66874461955397));
#11226=CARTESIAN_POINT('Ctrl Pts',(6.2779164407825,-1.6053133239208,5.66820891606077));
#11227=CARTESIAN_POINT('Ctrl Pts',(6.26118376894454,-1.61754684892312,5.66688460694955));
#11228=CARTESIAN_POINT('Ctrl Pts',(6.25117382999982,-1.62472395661662,5.66609412351733));
#11229=CARTESIAN_POINT('Ctrl Pts',(6.21365723014178,-1.6511006605735,5.66313747480288));
#11230=CARTESIAN_POINT('Ctrl Pts',(6.18573540341013,-1.66969726008991,5.66094879534436));
#11231=CARTESIAN_POINT('Ctrl Pts',(6.11457381596717,-1.71454410021904,5.65539655748736));
#11232=CARTESIAN_POINT('Ctrl Pts',(6.07078154686166,-1.73986914340071,5.65200238762648));
#11233=CARTESIAN_POINT('Ctrl Pts',(5.92261401824319,-1.81819581469486,5.64060124850046));
#11234=CARTESIAN_POINT('Ctrl Pts',(5.81454417257815,-1.86367557030014,5.63240080369409));
#11235=CARTESIAN_POINT('Ctrl Pts',(5.61737853591381,-1.92692247100687,5.61800530770726));
#11236=CARTESIAN_POINT('Ctrl Pts',(5.52985907899718,-1.94859339585833,5.61180532197608));
#11237=CARTESIAN_POINT('Ctrl Pts',(5.4303822703508,-1.96618364704437,5.60516558673266));
#11238=CARTESIAN_POINT('Ctrl Pts',(5.41958309597748,-1.96800166651936,5.60445014006174));
#11239=CARTESIAN_POINT('Ctrl Pts',(5.40320753022592,-1.97061997079041,5.60337391776093));
#11240=CARTESIAN_POINT('Ctrl Pts',(5.3976420260537,-1.97148568644396,5.60300965692064));
#11241=CARTESIAN_POINT('Ctrl Pts',(5.38762647170969,-1.97300018920297,5.60235694763225));
#11242=CARTESIAN_POINT('Ctrl Pts',(5.38317784866881,-1.97365750887705,5.60206803332873));
#11243=CARTESIAN_POINT('Ctrl Pts',(5.3733993633529,-1.97506858531866,5.60143517234842));
#11244=CARTESIAN_POINT('Ctrl Pts',(5.36806866477218,-1.97581581437817,5.6010915926698));
#11245=CARTESIAN_POINT('Ctrl Pts',(5.35272875676186,-1.97790280350508,5.60010680699909));
#11246=CARTESIAN_POINT('Ctrl Pts',(5.34271214060866,-1.97918817032043,5.59946855567015));
#11247=CARTESIAN_POINT('Ctrl Pts',(5.26998906660551,-1.98795941254316,5.5948666068882));
#11248=CARTESIAN_POINT('Ctrl Pts',(5.20696144904454,-1.99254058791037,5.59104967115456));
#11249=CARTESIAN_POINT('Ctrl Pts',(5.01315043191117,-1.99739909849227,5.5795518448154));
#11250=CARTESIAN_POINT('Ctrl Pts',(4.88247576416099,-1.98782424339013,5.57211387098648));
#11251=CARTESIAN_POINT('Ctrl Pts',(4.66583867661601,-1.95033312945932,5.55918112134196));
#11252=CARTESIAN_POINT('Ctrl Pts',(4.57913235188481,-1.92926405943375,5.55384046060544));
#11253=CARTESIAN_POINT('Ctrl Pts',(4.47919166765882,-1.89776083004868,5.54733725067333));
#11254=CARTESIAN_POINT('Ctrl Pts',(4.46430780380629,-1.8928756734287,5.54635963283881));
#11255=CARTESIAN_POINT('Ctrl Pts',(4.43997107480193,-1.88456913181486,5.5447453734981));
#11256=CARTESIAN_POINT('Ctrl Pts',(4.43048362489725,-1.88125063224838,5.54411210543214));
#11257=CARTESIAN_POINT('Ctrl Pts',(4.41345460695683,-1.87514942623074,5.54296812017506));
#11258=CARTESIAN_POINT('Ctrl Pts',(4.4059039658673,-1.87239254901107,5.54245826602385));
#11259=CARTESIAN_POINT('Ctrl Pts',(4.38982218180117,-1.86641038907222,5.54136666417947));
#11260=CARTESIAN_POINT('Ctrl Pts',(4.38129610798701,-1.86317209221796,5.54078449311225));
#11261=CARTESIAN_POINT('Ctrl Pts',(4.35825309801326,-1.85423880323849,5.53920159560043));
#11262=CARTESIAN_POINT('Ctrl Pts',(4.34378049014782,-1.84843195991956,5.53819715428113));
#11263=CARTESIAN_POINT('Ctrl Pts',(4.26708715046856,-1.81661129765646,5.53281828215199));
#11264=CARTESIAN_POINT('Ctrl Pts',(4.20615404158314,-1.7876270104557,5.52834442298922));
#11265=CARTESIAN_POINT('Ctrl Pts',(4.00332127348718,-1.67821473273237,5.5127494763014));
#11266=CARTESIAN_POINT('Ctrl Pts',(3.86986687261089,-1.58351471368963,5.50119597280198));
#11267=CARTESIAN_POINT('Ctrl Pts',(3.70846355491796,-1.43627035264085,5.48620213325376));
#11268=CARTESIAN_POINT('Ctrl Pts',(3.66905498685675,-1.3971865673288,5.48245079280582));
#11269=CARTESIAN_POINT('Ctrl Pts',(3.62500117812364,-1.34969042795929,5.47819884208006));
#11270=CARTESIAN_POINT('Ctrl Pts',(3.61872621701148,-1.34282956191797,5.47759174798476));
#11271=CARTESIAN_POINT('Ctrl Pts',(3.60863733160063,-1.33164259574499,5.47661365303636));
#11272=CARTESIAN_POINT('Ctrl Pts',(3.60479387937749,-1.32734348245983,5.47624055839702));
#11273=CARTESIAN_POINT('Ctrl Pts',(3.59798093544976,-1.31965599529119,5.47557844303638));
#11274=CARTESIAN_POINT('Ctrl Pts',(3.59500422981552,-1.31627417309262,5.47528889467969));
#11275=CARTESIAN_POINT('Ctrl Pts',(3.58856541483381,-1.30890889940386,5.47466203362447));
#11276=CARTESIAN_POINT('Ctrl Pts',(3.58510764996193,-1.30492178693169,5.47432503748345));
#11277=CARTESIAN_POINT('Ctrl Pts',(3.57540112315549,-1.29363913692636,5.47337785680347));
#11278=CARTESIAN_POINT('Ctrl Pts',(3.56918907613332,-1.28631200257696,5.47277028619838));
#11279=CARTESIAN_POINT('Ctrl Pts',(3.53027013863521,-1.23972890118846,5.46895285777323));
#11280=CARTESIAN_POINT('Ctrl Pts',(3.49902576058154,-1.19926968687474,5.4658385949702));
#11281=CARTESIAN_POINT('Ctrl Pts',(3.38112572229012,-1.03382792794735,5.45368349415277));
#11282=CARTESIAN_POINT('Ctrl Pts',(3.3073270949795,-0.900316487034451,5.44509259584546));
#11283=CARTESIAN_POINT('Ctrl Pts',(3.21844048613116,-0.684518264250985,
5.43131332792379));
#11284=CARTESIAN_POINT('Ctrl Pts',(3.19209974908524,-0.607512118360447,
5.42642266848376));
#11285=CARTESIAN_POINT('Ctrl Pts',(3.1664572208232,-0.51430419075007,5.42042073103093));
#11286=CARTESIAN_POINT('Ctrl Pts',(3.16255280260136,-0.49944270841317,5.41946148457612));
#11287=CARTESIAN_POINT('Ctrl Pts',(3.15640123941935,-0.474876384633146,
5.41787141090199));
#11288=CARTESIAN_POINT('Ctrl Pts',(3.15405436032711,-0.465197010221756,
5.41724378402069));
#11289=CARTESIAN_POINT('Ctrl Pts',(3.14994627097088,-0.44768198884405,5.4161058816988));
#11290=CARTESIAN_POINT('Ctrl Pts',(3.14815969603198,-0.439852464435022,
5.41559642936443));
#11291=CARTESIAN_POINT('Ctrl Pts',(3.14443160680815,-0.423047148392428,
5.41450115248068));
#11292=CARTESIAN_POINT('Ctrl Pts',(3.14250470601428,-0.414068337982984,
5.41391487487658));
#11293=CARTESIAN_POINT('Ctrl Pts',(3.13741467739742,-0.389525381279098,
5.41230919977965));
#11294=CARTESIAN_POINT('Ctrl Pts',(3.13437537952753,-0.37393651955715,5.41128590346255));
#11295=CARTESIAN_POINT('Ctrl Pts',(3.1185842089205,-0.287456119014403,5.40558888371829));
#11296=CARTESIAN_POINT('Ctrl Pts',(3.10949462434862,-0.215958324588518,
5.4008010636791));
#11297=CARTESIAN_POINT('Ctrl Pts',(3.09265206787229,0.0165283067286086,
5.38498452533375));
#11298=CARTESIAN_POINT('Ctrl Pts',(3.10051650234774,0.177985539301892,5.37356500852506));
#11299=CARTESIAN_POINT('Ctrl Pts',(3.13657367484361,0.388519350413989,5.35893076200216));
#11300=CARTESIAN_POINT('Ctrl Pts',(3.14748733273616,0.439944104046039,5.35538353792883));
#11301=CARTESIAN_POINT('Ctrl Pts',(3.16267678199651,0.499769825089018,5.35133333449026));
#11302=CARTESIAN_POINT('Ctrl Pts',(3.16499459449813,0.508641919632829,5.3507347084816));
#11303=CARTESIAN_POINT('Ctrl Pts',(3.16885961096554,0.523029948401436,5.34976753521139));
#11304=CARTESIAN_POINT('Ctrl Pts',(3.17036951024386,0.528555638806814,5.34939696769402));
#11305=CARTESIAN_POINT('Ctrl Pts',(3.17310868553862,0.538412846588221,5.34873757318475));
#11306=CARTESIAN_POINT('Ctrl Pts',(3.17432884120676,0.542746770566812,5.34844823617108));
#11307=CARTESIAN_POINT('Ctrl Pts',(3.17701889960714,0.552179161052406,5.34781979385125));
#11308=CARTESIAN_POINT('Ctrl Pts',(3.17849447269919,0.557275902517075,5.34748101887947));
#11309=CARTESIAN_POINT('Ctrl Pts',(3.18273574494844,0.571709726251058,5.34652373073608));
#11310=CARTESIAN_POINT('Ctrl Pts',(3.18554954915867,0.581032681353897,5.34590792116906));
#11311=CARTESIAN_POINT('Ctrl Pts',(3.20439890485507,0.641871842668362,5.34190350623619));
#11312=CARTESIAN_POINT('Ctrl Pts',(3.22245220902761,0.692744915447949,5.33862164795559));
#11313=CARTESIAN_POINT('Ctrl Pts',(3.30920633196461,0.908953947022581,5.32471425094573));
#11314=CARTESIAN_POINT('Ctrl Pts',(3.39792147487279,1.06535440925857,5.3146837187225));
#11315=CARTESIAN_POINT('Ctrl Pts',(3.53943388099586,1.25135128905305,5.30066396719669));
#11316=CARTESIAN_POINT('Ctrl Pts',(3.5743218737062,1.29349193818094,5.29733057835285));
#11317=CARTESIAN_POINT('Ctrl Pts',(3.62108074417206,1.34546553701348,5.29297954516331));
#11318=CARTESIAN_POINT('Ctrl Pts',(3.63139581736244,1.3566702121026,5.29202651557373));
#11319=CARTESIAN_POINT('Ctrl Pts',(3.64803688835665,1.37433613003269,5.29049911268272));
#11320=CARTESIAN_POINT('Ctrl Pts',(3.65428039951754,1.38087451561727,5.28992825838498));
#11321=CARTESIAN_POINT('Ctrl Pts',(3.66560701718082,1.39257577487941,5.28889646843536));
#11322=CARTESIAN_POINT('Ctrl Pts',(3.67067424258776,1.39775385404223,5.28843622612792));
#11323=CARTESIAN_POINT('Ctrl Pts',(3.68265166352345,1.40986064924029,5.28735143663487));
#11324=CARTESIAN_POINT('Ctrl Pts',(3.68958480950051,1.41676629954124,5.28672588704078));
#11325=CARTESIAN_POINT('Ctrl Pts',(3.70992532846668,1.43673016446754,5.28489733311379));
#11326=CARTESIAN_POINT('Ctrl Pts',(3.72346571649023,1.44965075772637,5.28368842104235));
#11327=CARTESIAN_POINT('Ctrl Pts',(3.83912906095041,1.55695109141519,5.27342807270738));
#11328=CARTESIAN_POINT('Ctrl Pts',(3.95066263302172,1.64058686049391,5.26392182413216));
#11329=CARTESIAN_POINT('Ctrl Pts',(4.18426046130562,1.78029588055611,5.24497833906629));
#11330=CARTESIAN_POINT('Ctrl Pts',(4.30512693710624,1.83704176675259,5.2356107904843));
#11331=CARTESIAN_POINT('Ctrl Pts',(4.44533202950561,1.88645713430267,5.22576750428409));
#11332=CARTESIAN_POINT('Ctrl Pts',(4.45996881529259,1.89142541156067,5.22475210914947));
#11333=CARTESIAN_POINT('Ctrl Pts',(4.48030490032262,1.89806565675324,5.22335956639989));
#11334=CARTESIAN_POINT('Ctrl Pts',(4.48595568860229,1.89988291134891,5.22297455559995));
#11335=CARTESIAN_POINT('Ctrl Pts',(4.49567440435848,1.90296058388496,5.22231580030969));
#11336=CARTESIAN_POINT('Ctrl Pts',(4.49973837143314,1.90423323544996,5.22204135933294));
#11337=CARTESIAN_POINT('Ctrl Pts',(4.50824122589562,1.90686607676153,5.22146934156337));
#11338=CARTESIAN_POINT('Ctrl Pts',(4.51268082488346,1.90822379678429,5.22117191874408));
#11339=CARTESIAN_POINT('Ctrl Pts',(4.52352551970217,1.91149896879319,5.22044834556641));
#11340=CARTESIAN_POINT('Ctrl Pts',(4.52993566868948,1.91339976420366,5.22002315266412));
#11341=CARTESIAN_POINT('Ctrl Pts',(4.55298724124787,1.92010932092578,5.218502678237));
#11342=CARTESIAN_POINT('Ctrl Pts',(4.5696821353629,1.92473366020924,5.21741747241571));
#11343=CARTESIAN_POINT('Ctrl Pts',(4.61139626035668,1.93570506969996,5.2147407512475));
#11344=CARTESIAN_POINT('Ctrl Pts',(4.63648298079526,1.9417852914853,5.21316187996794));
#11345=CARTESIAN_POINT('Ctrl Pts',(4.74473267047711,1.9658071403892,5.20645367954117));
#11346=CARTESIAN_POINT('Ctrl Pts',(4.82888411952969,1.9789067901642,5.20149969730753));
#11347=CARTESIAN_POINT('Ctrl Pts',(5.06300988690219,2.00014466767902,5.18784552468283));
#11348=CARTESIAN_POINT('Ctrl Pts',(5.21343257149962,1.99680167224567,5.17917935503643));
#11349=CARTESIAN_POINT('Ctrl Pts',(5.38648827413168,1.9733182970053,5.16842906757464));
#11350=CARTESIAN_POINT('Ctrl Pts',(5.41085891551759,1.96954979926487,5.16689811242441));
#11351=CARTESIAN_POINT('Ctrl Pts',(5.44483886518325,1.96364838887499,5.16473699090043));
#11352=CARTESIAN_POINT('Ctrl Pts',(5.45451238569607,1.96189458806115,5.16411873839884));
#11353=CARTESIAN_POINT('Ctrl Pts',(5.47222599575718,1.95854769048859,5.16298091078681));
#11354=CARTESIAN_POINT('Ctrl Pts',(5.48027002686475,1.956976403063,5.16246203495747));
#11355=CARTESIAN_POINT('Ctrl Pts',(5.49657754744652,1.95368649505009,5.16140561620808));
#11356=CARTESIAN_POINT('Ctrl Pts',(5.50484026204032,1.95196491305983,5.16086798882051));
#11357=CARTESIAN_POINT('Ctrl Pts',(5.52527221945312,1.94757232000018,5.15953258079778));
#11358=CARTESIAN_POINT('Ctrl Pts',(5.53742770432753,1.94483966595977,5.15873285203241));
#11359=CARTESIAN_POINT('Ctrl Pts',(5.58321642052769,1.93409438480144,5.15569996350098));
#11360=CARTESIAN_POINT('Ctrl Pts',(5.61666334983906,1.9253220534628,5.15344275373732));
#11361=CARTESIAN_POINT('Ctrl Pts',(5.70049141713316,1.9009905661415,5.14767583470599));
#11362=CARTESIAN_POINT('Ctrl Pts',(5.75051269653897,1.8842956181932,5.14413239413984));
#11363=CARTESIAN_POINT('Ctrl Pts',(5.88471487483561,1.83351169718912,5.1343542243994));
#11364=CARTESIAN_POINT('Ctrl Pts',(5.96732140419943,1.79562641506956,5.12803060411832));
#11365=CARTESIAN_POINT('Ctrl Pts',(6.1389545685334,1.70225765673671,5.11440966658794));
#11366=CARTESIAN_POINT('Ctrl Pts',(6.22678803790127,1.64510679896248,5.10713048330254));
#11367=CARTESIAN_POINT('Ctrl Pts',(6.32267230170687,1.57137943306154,5.09911238102685));
#11368=CARTESIAN_POINT('Ctrl Pts',(6.33548329912968,1.56127632974721,5.09803970376784));
#11369=CARTESIAN_POINT('Ctrl Pts',(6.35339295260509,1.54679238961031,5.09653982204586));
#11370=CARTESIAN_POINT('Ctrl Pts',(6.35859524052958,1.54254153526504,5.09610411086431));
#11371=CARTESIAN_POINT('Ctrl Pts',(6.36732535362666,1.53533419342582,5.09537301605208));
#11372=CARTESIAN_POINT('Ctrl Pts',(6.37086457140157,1.53239165555807,5.09507665188825));
#11373=CARTESIAN_POINT('Ctrl Pts',(6.3780167456839,1.5264032849146,5.09447785158997));
#11374=CARTESIAN_POINT('Ctrl Pts',(6.38162910761804,1.52335682785821,5.0941754633614));
#11375=CARTESIAN_POINT('Ctrl Pts',(6.39057964103947,1.51575387514746,5.09342624390475));
#11376=CARTESIAN_POINT('Ctrl Pts',(6.39590470538112,1.51118194681546,5.09298052115921));
#11377=CARTESIAN_POINT('Ctrl Pts',(6.4075793589996,1.50105094067484,5.09200307914271));
#11378=CARTESIAN_POINT('Ctrl Pts',(6.41391805892647,1.49547945190704,5.091472222558));
#11379=CARTESIAN_POINT('Ctrl Pts',(6.43216651201427,1.47923328423941,5.0899428246219));
#11380=CARTESIAN_POINT('Ctrl Pts',(6.44398376534353,1.46845514255627,5.08895102906392));
#11381=CARTESIAN_POINT('Ctrl Pts',(6.48487159682627,1.43025174078433,5.08550910875932));
#11382=CARTESIAN_POINT('Ctrl Pts',(6.51324801847542,1.40209467902018,5.08310174116355));
#11383=CARTESIAN_POINT('Ctrl Pts',(6.59893997211107,1.31179509003635,5.07569934300571));
#11384=CARTESIAN_POINT('Ctrl Pts',(6.65316650157718,1.246849269565,5.07081595364142));
#11385=CARTESIAN_POINT('Ctrl Pts',(6.77813840689327,1.07621829823807,5.05853390122981));
#11386=CARTESIAN_POINT('Ctrl Pts',(6.84320421747374,0.966863426912216,5.05111615554143));
#11387=CARTESIAN_POINT('Ctrl Pts',(6.90804047792998,0.829622892047224,5.04177950168581));
#11388=CARTESIAN_POINT('Ctrl Pts',(6.91822656910962,0.80697634255003,5.04023893836912));
#11389=CARTESIAN_POINT('Ctrl Pts',(6.93196804001188,0.774834313478809,5.03804986948117));
#11390=CARTESIAN_POINT('Ctrl Pts',(6.93587810250327,0.765492277738563,5.03741332506443));
#11391=CARTESIAN_POINT('Ctrl Pts',(6.94256793925524,0.749160632058954,5.03629982655155));
#11392=CARTESIAN_POINT('Ctrl Pts',(6.94537965374703,0.742184264096279,5.03582395471267));
#11393=CARTESIAN_POINT('Ctrl Pts',(6.95118551398956,0.72754054335906,5.03482453616651));
#11394=CARTESIAN_POINT('Ctrl Pts',(6.95417178665268,0.719870241154159,5.03430073711077));
#11395=CARTESIAN_POINT('Ctrl Pts',(6.96117796504693,0.701539955500313,5.03304813347918));
#11396=CARTESIAN_POINT('Ctrl Pts',(6.96515415114846,0.690863677980075,5.03231789168681));
#11397=CARTESIAN_POINT('Ctrl Pts',(6.97839078583096,0.654369759003233,5.02981912231209));
#11398=CARTESIAN_POINT('Ctrl Pts',(6.987209766122,0.62839639111193,5.02803617675052));
#11399=CARTESIAN_POINT('Ctrl Pts',(7.00715074819199,0.565430851827448,5.02370100643216));
#11400=CARTESIAN_POINT('Ctrl Pts',(7.0177389223077,0.528282505822011,5.02113267654849));
#11401=CARTESIAN_POINT('Ctrl Pts',(7.06797965083055,0.330389628924655,5.00739592710424));
#11402=CARTESIAN_POINT('Ctrl Pts',(7.08857715545311,0.165496289135984,4.99568651530648));
#11403=CARTESIAN_POINT('Ctrl Pts',(7.08857715545311,-3.14833228931555E-12,
4.98428615635939));
#11404=CARTESIAN_POINT('Ctrl Pts',(7.08857715545311,4.63564351804039E-12,
4.82758772788682));
#11405=CARTESIAN_POINT('Ctrl Pts',(7.08857715545311,0.000573719257101207,
4.82762772343443));
#11406=CARTESIAN_POINT('Ctrl Pts',(7.08857690794847,0.00114744551234271,
4.82766771905986));
#11407=CARTESIAN_POINT('Ctrl Pts',(7.08848669692276,0.105696976420473,4.83495600109056));
#11408=CARTESIAN_POINT('Ctrl Pts',(7.08026752389154,0.209517214713461,4.84218852636164));
#11409=CARTESIAN_POINT('Ctrl Pts',(7.06143895786786,0.328324282050292,4.85016246565267));
#11410=CARTESIAN_POINT('Ctrl Pts',(7.05869142249721,0.344385673291137,4.85123375556096));
#11411=CARTESIAN_POINT('Ctrl Pts',(7.05453410036983,0.367016244780663,4.85273204744083));
#11412=CARTESIAN_POINT('Ctrl Pts',(7.05328755320094,0.37361424031373,4.85316753250585));
#11413=CARTESIAN_POINT('Ctrl Pts',(7.05113055114468,0.384723481699219,4.85389835853669));
#11414=CARTESIAN_POINT('Ctrl Pts',(7.05023776506502,0.389238061165263,4.85419467843257));
#11415=CARTESIAN_POINT('Ctrl Pts',(7.04837726814135,0.398477958442519,4.85479971565694));
#11416=CARTESIAN_POINT('Ctrl Pts',(7.04740803109899,0.403202914030322,4.85510834512106));
#11417=CARTESIAN_POINT('Ctrl Pts',(7.04487923215159,0.415307410094315,4.8558971441728));
#11418=CARTESIAN_POINT('Ctrl Pts',(7.04329491966233,0.422681785173675,4.8563759308144));
#11419=CARTESIAN_POINT('Ctrl Pts',(7.03654529535589,0.453253315835352,4.85835412275427));
#11420=CARTESIAN_POINT('Ctrl Pts',(7.03100723390141,0.476367295760992,4.85983375012937));
#11421=CARTESIAN_POINT('Ctrl Pts',(7.01507214287535,0.537992613721132,4.86374908972714));
#11422=CARTESIAN_POINT('Ctrl Pts',(7.00393062331271,0.576301561377695,4.86615187004281));
#11423=CARTESIAN_POINT('Ctrl Pts',(6.96302692821696,0.702679239000464,4.87405110996139));
#11424=CARTESIAN_POINT('Ctrl Pts',(6.92826017460389,0.789001306990145,4.87940605376871));
#11425=CARTESIAN_POINT('Ctrl Pts',(6.83068644838862,0.989582887833457,4.89237094102702));
#11426=CARTESIAN_POINT('Ctrl Pts',(6.76247293580302,1.100713112585,4.90001172681703));
#11427=CARTESIAN_POINT('Ctrl Pts',(6.67414691277301,1.21732481932324,4.90908359471025));
#11428=CARTESIAN_POINT('Ctrl Pts',(6.66420405686953,1.23012463374942,4.91009451936571));
#11429=CARTESIAN_POINT('Ctrl Pts',(6.64774200029192,1.25079197769677,4.91175256753217));
#11430=CARTESIAN_POINT('Ctrl Pts',(6.64131625956643,1.2587332453353,4.91239599353068));
#11431=CARTESIAN_POINT('Ctrl Pts',(6.62971568124969,1.27284675754089,4.91355110007175));
#11432=CARTESIAN_POINT('Ctrl Pts',(6.62456388791828,1.27903771822497,4.91406184567603));
#11433=CARTESIAN_POINT('Ctrl Pts',(6.61356523961786,1.29209327232376,4.91514763942081));
#11434=CARTESIAN_POINT('Ctrl Pts',(6.60770906364544,1.2989497421019,4.9157230611546));
#11435=CARTESIAN_POINT('Ctrl Pts',(6.59190775368478,1.3171980718919,4.91726865015813));
#11436=CARTESIAN_POINT('Ctrl Pts',(6.58187938420923,1.32851676055405,4.91824223920823));
#11437=CARTESIAN_POINT('Ctrl Pts',(6.53092555234893,1.38472587740811,4.9231537752426));
#11438=CARTESIAN_POINT('Ctrl Pts',(6.48809711819846,1.42784016355731,4.92717160452332));
#11439=CARTESIAN_POINT('Ctrl Pts',(6.34890589818336,1.55571883139408,4.93990797492455));
#11440=CARTESIAN_POINT('Ctrl Pts',(6.24629614124813,1.63318466892481,4.94887778886495));
#11441=CARTESIAN_POINT('Ctrl Pts',(6.05475850589738,1.75069776380793,4.96451882559785));
#11442=CARTESIAN_POINT('Ctrl Pts',(5.96898029257621,1.79511645302358,4.97118013028009));
#11443=CARTESIAN_POINT('Ctrl Pts',(5.8702516617401,1.83747448139454,4.97824127769598));
#11444=CARTESIAN_POINT('Ctrl Pts',(5.86015226828568,1.84170934680892,4.97895673789953));
#11445=CARTESIAN_POINT('Ctrl Pts',(5.84480627712942,1.84799611603437,4.98003297649632));
#11446=CARTESIAN_POINT('Ctrl Pts',(5.8395852140434,1.8501092416391,4.98039724025271));
#11447=CARTESIAN_POINT('Ctrl Pts',(5.83017962832406,1.85386968812512,4.98104995264498));
#11448=CARTESIAN_POINT('Ctrl Pts',(5.82599844271205,1.85552499097945,4.98133886715646));
#11449=CARTESIAN_POINT('Ctrl Pts',(5.81680013763755,1.85913060401638,4.98197172609797));
#11450=CARTESIAN_POINT('Ctrl Pts',(5.81178071420334,1.86107474994281,4.98231530354701));
#11451=CARTESIAN_POINT('Ctrl Pts',(5.79732220399448,1.86660768574782,4.9833000762067));
#11452=CARTESIAN_POINT('Ctrl Pts',(5.78786349236886,1.87014521065981,4.98393831687609));
#11453=CARTESIAN_POINT('Ctrl Pts',(5.71906665149869,1.89528113580518,4.98853994125855));
#11454=CARTESIAN_POINT('Ctrl Pts',(5.65875303971482,1.91412525036457,4.99235658680572));
#11455=CARTESIAN_POINT('Ctrl Pts',(5.47119892407446,1.96308304804697,5.00385247749157));
#11456=CARTESIAN_POINT('Ctrl Pts',(5.34181666355457,1.98358474727842,5.01128890389283));
#11457=CARTESIAN_POINT('Ctrl Pts',(5.1223381643693,1.99653855049845,5.02422166087855));
#11458=CARTESIAN_POINT('Ctrl Pts',(5.03308009599025,1.99581711373973,5.02956412415536));
#11459=CARTESIAN_POINT('Ctrl Pts',(4.92855463808832,1.98795321375761,5.03606934305721));
#11460=CARTESIAN_POINT('Ctrl Pts',(4.91294756484843,1.98659395373497,5.03704702782196));
#11461=CARTESIAN_POINT('Ctrl Pts',(4.8873559147632,1.98406104247023,5.03866137529451));
#11462=CARTESIAN_POINT('Ctrl Pts',(4.87736114625361,1.98299547513656,5.03929466392463));
#11463=CARTESIAN_POINT('Ctrl Pts',(4.85938871986587,1.98094189613123,5.04043867156936));
#11464=CARTESIAN_POINT('Ctrl Pts',(4.85140812304315,1.97998110737837,5.04094852739906));
#11465=CARTESIAN_POINT('Ctrl Pts',(4.83438564732956,1.97782730369345,5.04204011674125));
#11466=CARTESIAN_POINT('Ctrl Pts',(4.82534573307707,1.97662046449783,5.0426222735232));
#11467=CARTESIAN_POINT('Ctrl Pts',(4.80087323803033,1.97318237989198,5.04420509161456));
#11468=CARTESIAN_POINT('Ctrl Pts',(4.78545828402121,1.97083213855456,5.04520946716294));
#11469=CARTESIAN_POINT('Ctrl Pts',(4.70354266184363,1.95735831959495,5.05058727486061));
#11470=CARTESIAN_POINT('Ctrl Pts',(4.63761737715697,1.9430502977452,5.05506008814791));
#11471=CARTESIAN_POINT('Ctrl Pts',(4.41527720522925,1.88285549072507,5.07064701610538));
#11472=CARTESIAN_POINT('Ctrl Pts',(4.26381972627475,1.8211678573861,5.08219293059166));
#11473=CARTESIAN_POINT('Ctrl Pts',(4.07304397351016,1.71467742696865,5.09718826647046));
#11474=CARTESIAN_POINT('Ctrl Pts',(4.02565914161774,1.68556675578075,5.1009472434908));
#11475=CARTESIAN_POINT('Ctrl Pts',(3.97183278668838,1.64931583519805,5.10520671719149));
#11476=CARTESIAN_POINT('Ctrl Pts',(3.96415374596918,1.64406571755524,5.10581411333155));
#11477=CARTESIAN_POINT('Ctrl Pts',(3.95177297190206,1.63547334838524,5.10679259763656));
#11478=CARTESIAN_POINT('Ctrl Pts',(3.94704862021085,1.63216415368232,5.10716578223072));
#11479=CARTESIAN_POINT('Ctrl Pts',(3.93865971602439,1.62623370020206,5.10782799489912));
#11480=CARTESIAN_POINT('Ctrl Pts',(3.93498962880865,1.62362047566312,5.10811755123467));
#11481=CARTESIAN_POINT('Ctrl Pts',(3.92704043991007,1.61791970280442,5.10874435801259));
#11482=CARTESIAN_POINT('Ctrl Pts',(3.92276472743715,1.61482760551296,5.10908129237846));
#11483=CARTESIAN_POINT('Ctrl Pts',(3.91074375715549,1.60606146107707,5.11002812253459));
#11484=CARTESIAN_POINT('Ctrl Pts',(3.90302699910572,1.60034831847765,5.1106354074763));
#11485=CARTESIAN_POINT('Ctrl Pts',(3.85458264159906,1.56393785663435,5.11444660358583));
#11486=CARTESIAN_POINT('Ctrl Pts',(3.81499989376728,1.5317409676805,5.11755528027043));
#11487=CARTESIAN_POINT('Ctrl Pts',(3.66307025707052,1.39816017047473,5.12966040661471));
#11488=CARTESIAN_POINT('Ctrl Pts',(3.56117802808255,1.28565533322423,5.13821081917022));
#11489=CARTESIAN_POINT('Ctrl Pts',(3.42511921671253,1.09598526195555,5.15198682669929));
#11490=CARTESIAN_POINT('Ctrl Pts',(3.38142821501397,1.02638071854155,5.15692322378292));
#11491=CARTESIAN_POINT('Ctrl Pts',(3.33478599823343,0.940765062971582,5.16297612776706));
#11492=CARTESIAN_POINT('Ctrl Pts',(3.32757604994052,0.927157865778961,5.16393743197347));
#11493=CARTESIAN_POINT('Ctrl Pts',(3.31595885969982,0.90460559798098,5.16553021580144));
#11494=CARTESIAN_POINT('Ctrl Pts',(3.3114597793325,0.89570837647937,5.16615847589545));
#11495=CARTESIAN_POINT('Ctrl Pts',(3.30345716701127,0.879583636267798,5.16729705748947));
#11496=CARTESIAN_POINT('Ctrl Pts',(3.29993020862832,0.872367932585918,5.16780655139943));
#11497=CARTESIAN_POINT('Ctrl Pts',(3.29246729917109,0.856863133478572,5.16890139866501));
#11498=CARTESIAN_POINT('Ctrl Pts',(3.28854478756427,0.848567810433568,5.16948720166505));
#11499=CARTESIAN_POINT('Ctrl Pts',(3.27800372110959,0.825871662698205,5.17109024042847));
#11500=CARTESIAN_POINT('Ctrl Pts',(3.27149945132605,0.811418796162326,5.17211135352792));
#11501=CARTESIAN_POINT('Ctrl Pts',(3.2366143682867,0.731366474942204,5.17777007852239));
#11502=CARTESIAN_POINT('Ctrl Pts',(3.21160610153351,0.664362914660169,5.18251996210409));
#11503=CARTESIAN_POINT('Ctrl Pts',(3.13071396009952,0.406072623288723,5.20087951253324));
#11504=CARTESIAN_POINT('Ctrl Pts',(3.09999535566019,0.208160048299562,5.21517801258646));
#11505=CARTESIAN_POINT('Ctrl Pts',(3.09900529884054,-0.0114417586268873,
5.22981424448838));
#11506=CARTESIAN_POINT('Ctrl Pts',(3.09922718580167,-0.0318777711936141,
5.23116315961155));
#11507=CARTESIAN_POINT('Ctrl Pts',(3.09995626350637,-0.0596715369501025,
5.2329767035658));
#11508=CARTESIAN_POINT('Ctrl Pts',(3.10019022271175,-0.0670343984942129,
5.23345512036498));
#11509=CARTESIAN_POINT('Ctrl Pts',(3.1006256754827,-0.0787019057856752,
5.23420987584505));
#11510=CARTESIAN_POINT('Ctrl Pts',(3.10080033609171,-0.0830073966191989,
5.23448766587285));
#11511=CARTESIAN_POINT('Ctrl Pts',(3.10119044618907,-0.0919113652062631,
5.2350605998534));
#11512=CARTESIAN_POINT('Ctrl Pts',(3.10140786360553,-0.0965096888198008,
5.23535562096739));
#11513=CARTESIAN_POINT('Ctrl Pts',(3.10196949429675,-0.107575885532921,
5.23606361356053));
#11514=CARTESIAN_POINT('Ctrl Pts',(3.10232929867243,-0.114042986133909,
5.23647572527738));
#11515=CARTESIAN_POINT('Ctrl Pts',(3.1036865249775,-0.136467844747534,5.23789939891494));
#11516=CARTESIAN_POINT('Ctrl Pts',(3.10484433154464,-0.152415766437448,
5.23890249934234));
#11517=CARTESIAN_POINT('Ctrl Pts',(3.11306995331485,-0.249532804671289,
5.24496318374307));
#11518=CARTESIAN_POINT('Ctrl Pts',(3.12491439625332,-0.330229119892889,
5.24979673567846));
#11519=CARTESIAN_POINT('Ctrl Pts',(3.16927041597079,-0.54143367631716,5.26242333219809));
#11520=CARTESIAN_POINT('Ctrl Pts',(3.21008188501042,-0.669755414624781,
5.27009147803214));
#11521=CARTESIAN_POINT('Ctrl Pts',(3.28779897839909,-0.849136199244131,
5.2817676140239));
#11522=CARTESIAN_POINT('Ctrl Pts',(3.31468648912195,-0.904116948512592,
5.2854838992962));
#11523=CARTESIAN_POINT('Ctrl Pts',(3.35154438108733,-0.971453322727717,
5.29025782289212));
#11524=CARTESIAN_POINT('Ctrl Pts',(3.35919318010695,-0.98504607710563,5.29123322526791));
#11525=CARTESIAN_POINT('Ctrl Pts',(3.37161103414365,-1.00652075258717,5.29279366562318));
#11526=CARTESIAN_POINT('Ctrl Pts',(3.37627674951127,-1.01446192257436,5.29337499424073));
#11527=CARTESIAN_POINT('Ctrl Pts',(3.38511186516823,-1.02926384820683,5.2944667611415));
#11528=CARTESIAN_POINT('Ctrl Pts',(3.38926802650402,-1.03613232037234,5.29497671156523));
#11529=CARTESIAN_POINT('Ctrl Pts',(3.39865347031188,-1.05143339875253,5.29612033991878));
#11530=CARTESIAN_POINT('Ctrl Pts',(3.40390440985147,-1.05985240616255,5.29675480150723));
#11531=CARTESIAN_POINT('Ctrl Pts',(3.4195983574244,-1.08460187604915,5.29863560582476));
#11532=CARTESIAN_POINT('Ctrl Pts',(3.430216595198,-1.10081931199353,5.29988838397706));
#11533=CARTESIAN_POINT('Ctrl Pts',(3.51810027325618,-1.23086961571095,5.3101040733299));
#11534=CARTESIAN_POINT('Ctrl Pts',(3.60670284975215,-1.33656400974577,5.31951011421758));
#11535=CARTESIAN_POINT('Ctrl Pts',(3.80141070555066,-1.52530226383815,5.33838164596255));
#11536=CARTESIAN_POINT('Ctrl Pts',(3.90647946539576,-1.60844591030783,5.34778283294266));
#11537=CARTESIAN_POINT('Ctrl Pts',(4.03205134424048,-1.68875597179244,5.35765168775827));
#11538=CARTESIAN_POINT('Ctrl Pts',(4.0451178311414,-1.69690111473951,5.35866309905567));
#11539=CARTESIAN_POINT('Ctrl Pts',(4.06334363836582,-1.70797143251194,5.36005115918856));
#11540=CARTESIAN_POINT('Ctrl Pts',(4.06842326122865,-1.7110258762293,5.3604356056916));
#11541=CARTESIAN_POINT('Ctrl Pts',(4.07717383709986,-1.71623474749747,5.36109364991638));
#11542=CARTESIAN_POINT('Ctrl Pts',(4.08083817431937,-1.71840012894711,5.36136794084873));
#11543=CARTESIAN_POINT('Ctrl Pts',(4.08851556189541,-1.72290386676248,5.36193993376229));
#11544=CARTESIAN_POINT('Ctrl Pts',(4.09252988387002,-1.72523995685392,5.36223748030058));
#11545=CARTESIAN_POINT('Ctrl Pts',(4.10235163576087,-1.73090978837254,5.36296182860558));
#11546=CARTESIAN_POINT('Ctrl Pts',(4.1081678316498,-1.73422838810453,5.36338766802693));
#11547=CARTESIAN_POINT('Ctrl Pts',(4.12914829898174,-1.74605975904956,5.36491305902834));
#11548=CARTESIAN_POINT('Ctrl Pts',(4.14440753268719,-1.75440371820867,5.36600244892579));
#11549=CARTESIAN_POINT('Ctrl Pts',(4.18269937689515,-1.77469627757084,5.36869153897599));
#11550=CARTESIAN_POINT('Ctrl Pts',(4.20586017025401,-1.78639734336619,5.37027844413264));
#11551=CARTESIAN_POINT('Ctrl Pts',(4.30661741675954,-1.83485691438885,5.37704108281297));
#11552=CARTESIAN_POINT('Ctrl Pts',(4.38631915362615,-1.86703876795166,5.38203854311386));
#11553=CARTESIAN_POINT('Ctrl Pts',(4.60923548360172,-1.94071411020311,5.39567334601262));
#11554=CARTESIAN_POINT('Ctrl Pts',(4.75538865892204,-1.97145979331053,5.40428070599617));
#11555=CARTESIAN_POINT('Ctrl Pts',(4.92819698062149,-1.98801534501321,5.41496622959319));
#11556=CARTESIAN_POINT('Ctrl Pts',(4.95283958021462,-1.98991476875213,5.41650056308381));
#11557=CARTESIAN_POINT('Ctrl Pts',(4.98733357024458,-1.9919295933272,5.41866566577576));
#11558=CARTESIAN_POINT('Ctrl Pts',(4.99716081289375,-1.99243067662212,5.41928446153285));
#11559=CARTESIAN_POINT('Ctrl Pts',(5.01518176750561,-1.99321591350688,5.42042297107007));
#11560=CARTESIAN_POINT('Ctrl Pts',(5.02337433408403,-1.99352230276203,5.42094198238258));
#11561=CARTESIAN_POINT('Ctrl Pts',(5.04000160084478,-1.99404151396235,5.42199834563052));
#11562=CARTESIAN_POINT('Ctrl Pts',(5.04843622069285,-1.99425134052624,5.4225357800192));
#11563=CARTESIAN_POINT('Ctrl Pts',(5.06931433635182,-1.99463820121408,5.42387007832624));
#11564=CARTESIAN_POINT('Ctrl Pts',(5.08175850535056,-1.99475230746542,5.42466888331444));
#11565=CARTESIAN_POINT('Ctrl Pts',(5.12867284228941,-1.9947434750988,5.42769407472404));
#11566=CARTESIAN_POINT('Ctrl Pts',(5.16313511938344,-1.99384350320989,5.4299443536146));
#11567=CARTESIAN_POINT('Ctrl Pts',(5.2499826175256,-1.98932127430707,5.43568943326603));
#11568=CARTESIAN_POINT('Ctrl Pts',(5.30227789606448,-1.98452290892568,5.43921763996204));
#11569=CARTESIAN_POINT('Ctrl Pts',(5.45861817953614,-1.96393024284312,5.44996168642467));
#11570=CARTESIAN_POINT('Ctrl Pts',(5.56166039276611,-1.9419638435852,5.4573161005389));
#11571=CARTESIAN_POINT('Ctrl Pts',(5.75719993620534,-1.88380715312217,5.4715205431783));
#11572=CARTESIAN_POINT('Ctrl Pts',(5.84970623669408,-1.84863307327996,5.47835207330984));
#11573=CARTESIAN_POINT('Ctrl Pts',(5.94910254938537,-1.80212383121095,5.48556420722634));
#11574=CARTESIAN_POINT('Ctrl Pts',(5.95893455942866,-1.79742468404907,5.48627608306903));
#11575=CARTESIAN_POINT('Ctrl Pts',(5.97377911412428,-1.79017979712449,5.48734801468233));
#11576=CARTESIAN_POINT('Ctrl Pts',(5.97882003274639,-1.78769314050534,5.48771151537912));
#11577=CARTESIAN_POINT('Ctrl Pts',(5.98787450052443,-1.78317893809211,5.48836342997736));
#11578=CARTESIAN_POINT('Ctrl Pts',(5.99189174453633,-1.78115911009823,5.48865230438652));
#11579=CARTESIAN_POINT('Ctrl Pts',(5.99591982727087,-1.77911673994173,5.48894159134309));
#11580=CARTESIAN_POINT('Ctrl Pts',(5.99593739984907,-1.77910782974053,5.48894285335541));
#11581=CARTESIAN_POINT('Ctrl Pts',(5.99597231062825,-1.77909012752922,5.48894536053409));
#11582=CARTESIAN_POINT('Ctrl Pts',(5.99598964882855,-1.77908133552812,5.4889466057006));
#11583=CARTESIAN_POINT('Ctrl Pts',(5.99602409448578,-1.7790638679002,5.4889490794492));
#11584=CARTESIAN_POINT('Ctrl Pts',(5.99604120190241,-1.77905519230222,5.48895030802856));
#11585=CARTESIAN_POINT('Ctrl Pts',(5.99607518929048,-1.7790379558331,5.48895274884028));
#11586=CARTESIAN_POINT('Ctrl Pts',(5.99609206933451,-1.77902939493332,5.488953961078));
#11587=CARTESIAN_POINT('Ctrl Pts',(5.99612560553281,-1.77901238608183,5.48895636946228));
#11588=CARTESIAN_POINT('Ctrl Pts',(5.99614226165779,-1.77900393815293,5.48895756560689));
#11589=CARTESIAN_POINT('Ctrl Pts',(5.99617535341753,-1.77898715354271,5.48895994204957));
#11590=CARTESIAN_POINT('Ctrl Pts',(5.99619178901208,-1.77897881688951,5.48896112234492));
#11591=CARTESIAN_POINT('Ctrl Pts',(5.9962244429254,-1.77896225322332,5.4889634673204));
#11592=CARTESIAN_POINT('Ctrl Pts',(5.99624066126477,-1.77895402620737,5.48896463200216));
#11593=CARTESIAN_POINT('Ctrl Pts',(5.99627288399326,-1.77893768015119,5.48896694598978));
#11594=CARTESIAN_POINT('Ctrl Pts',(5.99628888836769,-1.7789295611257,5.48896809529472));
#11595=CARTESIAN_POINT('Ctrl Pts',(5.99632068622825,-1.77891342951889,5.48897037874903));
#11596=CARTESIAN_POINT('Ctrl Pts',(5.9963364797822,-1.77890541691027,5.48897151290341));
#11597=CARTESIAN_POINT('Ctrl Pts',(5.99636785921738,-1.77888949652702,5.48897376628796));
#11598=CARTESIAN_POINT('Ctrl Pts',(5.99638344509576,-1.77888158876074,5.48897488551807));
#11599=CARTESIAN_POINT('Ctrl Pts',(5.99641441239506,-1.77886587645148,5.48897710928539));
#11600=CARTESIAN_POINT('Ctrl Pts',(5.99642979375325,-1.77885807194704,5.48897821381824));
#11601=CARTESIAN_POINT('Ctrl Pts',(5.99646035482178,-1.77884256475587,5.48898040839322));
#11602=CARTESIAN_POINT('Ctrl Pts',(5.99647553461199,-1.77883486203515,5.48898149844123));
#11603=CARTESIAN_POINT('Ctrl Pts',(5.9965056956834,-1.77881955683817,5.48898366427235));
#11604=CARTESIAN_POINT('Ctrl Pts',(5.99652067693711,-1.77881195438221,5.48898474005361));
#11605=CARTESIAN_POINT('Ctrl Pts',(5.99655044380506,-1.7787968482775,5.48898687755769));
#11606=CARTESIAN_POINT('Ctrl Pts',(5.9965652294263,-1.77878934463137,5.48898793928114));
#11607=CARTESIAN_POINT('Ctrl Pts',(5.99659460802554,-1.77877443464417,5.48899004888513));
#11608=CARTESIAN_POINT('Ctrl Pts',(5.99660920095602,-1.77876702833322,5.48899109676238));
#11609=CARTESIAN_POINT('Ctrl Pts',(5.99663819683887,-1.77875231168166,5.48899317886573));
#11610=CARTESIAN_POINT('Ctrl Pts',(5.99665259986189,-1.77874500131103,5.48899421309703));
#11611=CARTESIAN_POINT('Ctrl Pts',(5.99668121873968,-1.77873047513138,5.4889962681106));
#11612=CARTESIAN_POINT('Ctrl Pts',(5.99669543462644,-1.77872325931179,5.48899728889529));
#11613=CARTESIAN_POINT('Ctrl Pts',(5.99672368212086,-1.77870892078466,5.48899931722346));
#11614=CARTESIAN_POINT('Ctrl Pts',(5.99673771367204,-1.77870179811131,5.489000324763));
#11615=CARTESIAN_POINT('Ctrl Pts',(5.99676559505476,-1.7786876445939,5.48900232678501));
#11616=CARTESIAN_POINT('Ctrl Pts',(5.99677944492023,-1.77868061373799,5.48900332127002));
#11617=CARTESIAN_POINT('Ctrl Pts',(5.99680696561645,-1.77866664250849,5.48900529737609));
#11618=CARTESIAN_POINT('Ctrl Pts',(5.99682063643611,-1.77865970214577,5.48900627899647));
#11619=CARTESIAN_POINT('Ctrl Pts',(5.99684780177849,-1.77864591052832,5.48900822957017));
#11620=CARTESIAN_POINT('Ctrl Pts',(5.99686129621501,-1.77863905932245,5.48900919851742));
#11621=CARTESIAN_POINT('Ctrl Pts',(5.99688811124726,-1.77862544478689,5.48901112392156));
#11622=CARTESIAN_POINT('Ctrl Pts',(5.99690143185286,-1.77861868145712,5.48901208037926));
#11623=CARTESIAN_POINT('Ctrl Pts',(5.99692790160734,-1.77860524147804,5.4890139809758));
#11624=CARTESIAN_POINT('Ctrl Pts',(5.99694105083226,-1.77859856479493,5.48901492512019));
#11625=CARTESIAN_POINT('Ctrl Pts',(5.99696718052759,-1.77858529675144,5.48901680128443));
#11626=CARTESIAN_POINT('Ctrl Pts',(5.99698016093245,-1.77857870542902,5.48901773329967));
#11627=CARTESIAN_POINT('Ctrl Pts',(5.99700595525111,-1.77856560697152,5.48901958536842));
#11628=CARTESIAN_POINT('Ctrl Pts',(5.99701876920665,-1.7785590998198,5.48902050542503));
#11629=CARTESIAN_POINT('Ctrl Pts',(5.99704423317913,-1.7785461684211,5.48902233376005));
#11630=CARTESIAN_POINT('Ctrl Pts',(5.99705688314776,-1.77853974420308,5.4890232420351));
#11631=CARTESIAN_POINT('Ctrl Pts',(5.99708289483485,-1.77852653395965,5.48902510968199));
#11632=CARTESIAN_POINT('Ctrl Pts',(5.99709625660383,-1.77851974788894,5.48902606905706));
#11633=CARTESIAN_POINT('Ctrl Pts',(6.0020071055388,-1.77602559473077,5.48937866658172));
#11634=CARTESIAN_POINT('Ctrl Pts',(6.00689436806657,-1.77351797336801,5.48972904182116));
#11635=CARTESIAN_POINT('Ctrl Pts',(6.0213078336732,-1.7660471492128,5.49076098323373));
#11636=CARTESIAN_POINT('Ctrl Pts',(6.03080455503388,-1.76102706011105,5.49143911571422));
#11637=CARTESIAN_POINT('Ctrl Pts',(6.0526105316357,-1.74927380163278,5.49299314230048));
#11638=CARTESIAN_POINT('Ctrl Pts',(6.06489036143997,-1.74248692086713,5.49386599515891));
#11639=CARTESIAN_POINT('Ctrl Pts',(6.20517424038399,-1.66301045399931,5.50382292478515));
#11640=CARTESIAN_POINT('Ctrl Pts',(6.32484238670365,-1.57648637434162,5.51220221617603));
#11641=CARTESIAN_POINT('Ctrl Pts',(6.52236952541922,-1.39733901816774,5.52773127436068));
#11642=CARTESIAN_POINT('Ctrl Pts',(6.60343485634565,-1.30933903869002,5.53478130645898));
#11643=CARTESIAN_POINT('Ctrl Pts',(6.68606044956264,-1.20170136284439,5.54319530638623));
#11644=CARTESIAN_POINT('Ctrl Pts',(6.6958225566121,-1.18865627435675,5.54421147237901));
#11645=CARTESIAN_POINT('Ctrl Pts',(6.71145855825071,-1.16721938263567,5.54587640405648));
#11646=CARTESIAN_POINT('Ctrl Pts',(6.71742966952308,-1.15889918136026,5.54652142002283));
#11647=CARTESIAN_POINT('Ctrl Pts',(6.72798343430515,-1.14395180522961,5.54767828501758));
#11648=CARTESIAN_POINT('Ctrl Pts',(6.73259053399238,-1.13734210440813,5.54818918784432));
#11649=CARTESIAN_POINT('Ctrl Pts',(6.74226003692117,-1.12328875699047,5.54927415805731));
#11650=CARTESIAN_POINT('Ctrl Pts',(6.74731233500627,-1.1158384080682,5.54984859162818));
#11651=CARTESIAN_POINT('Ctrl Pts',(6.76067802194942,-1.09583865062556,5.55138872870582));
#11652=CARTESIAN_POINT('Ctrl Pts',(6.76889994529216,-1.08322910206195,5.55235781200575));
#11653=CARTESIAN_POINT('Ctrl Pts',(6.80909284730965,-1.02003530861282,5.55720583872655));
#11654=CARTESIAN_POINT('Ctrl Pts',(6.83891606812381,-0.968128023894585,
5.56116218872616));
#11655=CARTESIAN_POINT('Ctrl Pts',(6.93903973707845,-0.774161308408252,
5.57586192382845));
#11656=CARTESIAN_POINT('Ctrl Pts',(6.99467892489336,-0.625209072407786,
5.58704767703248));
#11657=CARTESIAN_POINT('Ctrl Pts',(7.04087087724725,-0.435229225625189,
5.60054735933996));
#11658=CARTESIAN_POINT('Ctrl Pts',(7.04862847847864,-0.398943341144046,
5.60308949825052));
#11659=CARTESIAN_POINT('Ctrl Pts',(7.06154546789643,-0.329039939068891,
5.60789423543807));
#11660=CARTESIAN_POINT('Ctrl Pts',(7.06686635442532,-0.295464519844523,
5.61016163083061));
#11661=CARTESIAN_POINT('Ctrl Pts',(7.07248325639656,-0.253032087660945,
5.61296330402136));
#11662=CARTESIAN_POINT('Ctrl Pts',(7.07358169342412,-0.244289130860153,
5.61353717323134));
#11663=CARTESIAN_POINT('Ctrl Pts',(7.07523088609569,-0.230420035832409,
5.61444182440976));
#11664=CARTESIAN_POINT('Ctrl Pts',(7.07581975063605,-0.225298670240397,
5.61477465306572));
#11665=CARTESIAN_POINT('Ctrl Pts',(7.07687646647887,-0.215783492915587,
5.6153906783008));
#11666=CARTESIAN_POINT('Ctrl Pts',(7.07734956885683,-0.211390448550495,
5.61567415237963));
#11667=CARTESIAN_POINT('Ctrl Pts',(7.07826738978968,-0.202593459585779,
5.61623996502225));
#11668=CARTESIAN_POINT('Ctrl Pts',(7.07871204673247,-0.198189613244848,
5.61652229810091));
#11669=CARTESIAN_POINT('Ctrl Pts',(7.07970451081397,-0.188021844236451,
5.61717211793837));
#11670=CARTESIAN_POINT('Ctrl Pts',(7.08024189179518,-0.182256911056624,
5.61753904057486));
#11671=CARTESIAN_POINT('Ctrl Pts',(7.08156992345348,-0.167305880330492,
5.61848690255623));
#11672=CARTESIAN_POINT('Ctrl Pts',(7.08232201005302,-0.158116380789593,
5.61906584813554));
#11673=CARTESIAN_POINT('Ctrl Pts',(7.08668811678998,-0.0997972750626993,
5.62271873905821));
#11674=CARTESIAN_POINT('Ctrl Pts',(7.0885451104228,-0.0505497564851107,
5.62570794647002));
#11675=CARTESIAN_POINT('Ctrl Pts',(7.0885767442888,-0.00128075752557987,
5.62864732406692));
#11676=CARTESIAN_POINT('Origin',(5.09382715545311,0.,-6.77268258743872));
#11677=CARTESIAN_POINT('',(7.08799995208786,0.00180011744721413,6.58540798502574));
#11678=CARTESIAN_POINT('',(7.08575281161347,-0.000877199754626239,6.42728338101755));
#11679=CARTESIAN_POINT('',(7.08857715545311,8.3550772080578E-14,-6.77268258743872));
#11680=CARTESIAN_POINT('Ctrl Pts',(7.08857636475715,0.00177608583532361,
6.58573943276249));
#11681=CARTESIAN_POINT('Ctrl Pts',(7.08868588516143,-0.121227957941686,
6.5785857802516));
#11682=CARTESIAN_POINT('Ctrl Pts',(7.07741849417107,-0.243966358813522,
6.57135126467452));
#11683=CARTESIAN_POINT('Ctrl Pts',(7.05234423754484,-0.378730559112279,
6.56287097820885));
#11684=CARTESIAN_POINT('Ctrl Pts',(7.04962091214582,-0.392551605440979,
6.56199514662556));
#11685=CARTESIAN_POINT('Ctrl Pts',(7.0448388108166,-0.415534888572078,6.56052792503132));
#11686=CARTESIAN_POINT('Ctrl Pts',(7.0428612841997,-0.424713648469547,6.55993908502373));
#11687=CARTESIAN_POINT('Ctrl Pts',(7.03885051728125,-0.44271163642731,6.55877863065602));
#11688=CARTESIAN_POINT('Ctrl Pts',(7.03682191011819,-0.45153167117863,6.55820717536531));
#11689=CARTESIAN_POINT('Ctrl Pts',(7.03287599826177,-0.468168693386053,
6.55712388466846));
#11690=CARTESIAN_POINT('Ctrl Pts',(7.03097126126369,-0.475988498272161,
6.55661246101819));
#11691=CARTESIAN_POINT('Ctrl Pts',(7.02655505291837,-0.493653388630137,
6.555451960513));
#11692=CARTESIAN_POINT('Ctrl Pts',(7.02401559601967,-0.503491182999488,
6.55480199617546));
#11693=CARTESIAN_POINT('Ctrl Pts',(7.01727740803145,-0.528794374278642,
6.55312060014303));
#11694=CARTESIAN_POINT('Ctrl Pts',(7.01296733249796,-0.54422910661841,6.55208561250086));
#11695=CARTESIAN_POINT('Ctrl Pts',(6.98028977524964,-0.656031838053373,
6.54451880485529));
#11696=CARTESIAN_POINT('Ctrl Pts',(6.94486879497236,-0.750172211367793,
6.53775761723513));
#11697=CARTESIAN_POINT('Ctrl Pts',(6.86897249569128,-0.913352557611503,
6.525367791711));
#11698=CARTESIAN_POINT('Ctrl Pts',(6.83114694481671,-0.983398666759867,
6.51980985448184));
#11699=CARTESIAN_POINT('Ctrl Pts',(6.74579068808271,-1.12109116298879,6.50852702427869));
#11700=CARTESIAN_POINT('Ctrl Pts',(6.69802966842602,-1.18842984258498,6.50281429888683));
#11701=CARTESIAN_POINT('Ctrl Pts',(6.63098314635375,-1.27152222488384,6.49566930776576));
#11702=CARTESIAN_POINT('Ctrl Pts',(6.6153886349375,-1.29014266664258,6.49406171368352));
#11703=CARTESIAN_POINT('Ctrl Pts',(6.59570284993209,-1.31279462133187,6.49210278028014));
#11704=CARTESIAN_POINT('Ctrl Pts',(6.59192992287261,-1.31709848516167,6.49173043477878));
#11705=CARTESIAN_POINT('Ctrl Pts',(6.58459340172728,-1.32539511129628,6.49101247095633));
#11706=CARTESIAN_POINT('Ctrl Pts',(6.58103216444069,-1.32938988447384,6.49066669086063));
#11707=CARTESIAN_POINT('Ctrl Pts',(6.57444766450176,-1.33671639097868,6.49003244467795));
#11708=CARTESIAN_POINT('Ctrl Pts',(6.57142921669363,-1.34005221953726,6.48974364492419));
#11709=CARTESIAN_POINT('Ctrl Pts',(6.56458100281913,-1.34756923025407,6.48909278569706));
#11710=CARTESIAN_POINT('Ctrl Pts',(6.56074468459922,-1.3517443080906,6.48873122574483));
#11711=CARTESIAN_POINT('Ctrl Pts',(6.55078883132367,-1.36248699708177,6.48780057671447));
#11712=CARTESIAN_POINT('Ctrl Pts',(6.54464259499581,-1.36902984249187,6.48723343593178));
#11713=CARTESIAN_POINT('Ctrl Pts',(6.50478443476463,-1.41089010897879,6.4836010639108));
#11714=CARTESIAN_POINT('Ctrl Pts',(6.46982666332094,-1.44500434442088,6.48062278840586));
#11715=CARTESIAN_POINT('Ctrl Pts',(6.42479727779275,-1.48582934945199,6.47698159327014));
#11716=CARTESIAN_POINT('Ctrl Pts',(6.41587342408448,-1.49377508158908,6.47626906459009));
#11717=CARTESIAN_POINT('Ctrl Pts',(6.39518572186291,-1.51186464509181,6.47463654951614));
#11718=CARTESIAN_POINT('Ctrl Pts',(6.38337364797385,-1.52195226014561,6.47371850038589));
#11719=CARTESIAN_POINT('Ctrl Pts',(6.27208399766122,-1.61476871193656,6.46518659431576));
#11720=CARTESIAN_POINT('Ctrl Pts',(6.16489715164525,-1.68777293012297,6.4578142807614));
#11721=CARTESIAN_POINT('Ctrl Pts',(6.00527869533838,-1.7751188799328,6.44705544387477));
#11722=CARTESIAN_POINT('Ctrl Pts',(5.95818713694719,-1.79851943863914,6.44390874471338));
#11723=CARTESIAN_POINT('Ctrl Pts',(5.88907060725803,-1.82952265885987,6.43928907392226));
#11724=CARTESIAN_POINT('Ctrl Pts',(5.8677492108992,-1.83864349276188,6.43786393305834));
#11725=CARTESIAN_POINT('Ctrl Pts',(5.8293914936377,-1.8542666961672,6.43529680069524));
#11726=CARTESIAN_POINT('Ctrl Pts',(5.81241568696985,-1.86091116506232,6.43415956034687));
#11727=CARTESIAN_POINT('Ctrl Pts',(5.78618742895198,-1.87076472328597,6.43239969182188));
#11728=CARTESIAN_POINT('Ctrl Pts',(5.77699814618326,-1.87414001348626,6.43178258936295));
#11729=CARTESIAN_POINT('Ctrl Pts',(5.7602360182227,-1.88015720423062,6.43065582822823));
#11730=CARTESIAN_POINT('Ctrl Pts',(5.75267133417024,-1.88282134843125,6.43014691797857));
#11731=CARTESIAN_POINT('Ctrl Pts',(5.73628836582741,-1.88848031093389,6.42904378788189));
#11732=CARTESIAN_POINT('Ctrl Pts',(5.72746479346409,-1.8914591273617,6.42844905501003));
#11733=CARTESIAN_POINT('Ctrl Pts',(5.70338303223282,-1.89940165380783,6.42682406630561));
#11734=CARTESIAN_POINT('Ctrl Pts',(5.68808555667229,-1.90424314022985,6.4257898474097));
#11735=CARTESIAN_POINT('Ctrl Pts',(5.60833989468399,-1.92842729848641,6.42038701336388));
#11736=CARTESIAN_POINT('Ctrl Pts',(5.54300826095254,-1.94468244149756,6.41591991230863));
#11737=CARTESIAN_POINT('Ctrl Pts',(5.32520046092084,-1.98731363355628,6.40089315838238));
#11738=CARTESIAN_POINT('Ctrl Pts',(5.17048024289048,-1.99926598901546,6.38995959937071));
#11739=CARTESIAN_POINT('Ctrl Pts',(4.95285321576843,-1.99076432141499,6.37495926291303));
#11740=CARTESIAN_POINT('Ctrl Pts',(4.88989105248304,-1.98530299760848,6.37067268747268));
#11741=CARTESIAN_POINT('Ctrl Pts',(4.81728023758988,-1.97551293202631,6.36586567029279));
#11742=CARTESIAN_POINT('Ctrl Pts',(4.80728242356727,-1.97408755359546,6.3652068378418));
#11743=CARTESIAN_POINT('Ctrl Pts',(4.79197267560127,-1.9717860962818,6.36420307923019));
#11744=CARTESIAN_POINT('Ctrl Pts',(4.78665291825287,-1.97096436450418,6.36385524756638));
#11745=CARTESIAN_POINT('Ctrl Pts',(4.7768950489558,-1.96941662045992,6.36321905527266));
#11746=CARTESIAN_POINT('Ctrl Pts',(4.7724560724592,-1.96869713589493,6.36293034602091));
#11747=CARTESIAN_POINT('Ctrl Pts',(4.76246277379203,-1.96704268680219,6.36228194801662));
#11748=CARTESIAN_POINT('Ctrl Pts',(4.7569099637623,-1.96609920729975,6.36192274171707));
#11749=CARTESIAN_POINT('Ctrl Pts',(4.74057326154863,-1.96325219006401,6.36086891396389));
#11750=CARTESIAN_POINT('Ctrl Pts',(4.72980075722238,-1.96128332208228,6.36017784164154));
#11751=CARTESIAN_POINT('Ctrl Pts',(4.62539686936041,-1.94131178911723,6.35351258287231));
#11752=CARTESIAN_POINT('Ctrl Pts',(4.53314055242254,-1.91670389972308,6.34787347598419));
#11753=CARTESIAN_POINT('Ctrl Pts',(4.32090649469527,-1.84344807320631,6.33476699576689));
#11754=CARTESIAN_POINT('Ctrl Pts',(4.20321101028993,-1.78955552884023,6.32737533679035));
#11755=CARTESIAN_POINT('Ctrl Pts',(4.03885400356676,-1.69404076667453,6.31601234957295));
#11756=CARTESIAN_POINT('Ctrl Pts',(3.98759223501989,-1.66101947040291,6.31230637370615));
#11757=CARTESIAN_POINT('Ctrl Pts',(3.92558874230334,-1.61693404851766,6.30757093813506));
#11758=CARTESIAN_POINT('Ctrl Pts',(3.91335230062993,-1.60802232711629,6.30662358057183));
#11759=CARTESIAN_POINT('Ctrl Pts',(3.89398806826986,-1.59357933436011,6.30510315128279));
#11760=CARTESIAN_POINT('Ctrl Pts',(3.88679416880441,-1.58813736649715,6.30453354190998));
#11761=CARTESIAN_POINT('Ctrl Pts',(3.87324778896266,-1.57774472973173,6.30345175350529));
#11762=CARTESIAN_POINT('Ctrl Pts',(3.86688788061656,-1.57280400395455,6.30293997164572));
#11763=CARTESIAN_POINT('Ctrl Pts',(3.85253358851301,-1.56151275388631,6.30177591697387));
#11764=CARTESIAN_POINT('Ctrl Pts',(3.84455774113881,-1.55513913330964,6.30112273512344));
#11765=CARTESIAN_POINT('Ctrl Pts',(3.8240625180685,-1.53850167475167,6.29942747639795));
#11766=CARTESIAN_POINT('Ctrl Pts',(3.8116187314131,-1.5281463180425,6.29838174484567));
#11767=CARTESIAN_POINT('Ctrl Pts',(3.69886274464726,-1.43196718413306,6.28875199764492));
#11768=CARTESIAN_POINT('Ctrl Pts',(3.60719451270669,-1.33655050243019,6.2797586371305));
#11769=CARTESIAN_POINT('Ctrl Pts',(3.46360698416528,-1.15389882219337,6.26361266981048));
#11770=CARTESIAN_POINT('Ctrl Pts',(3.40762260822076,-1.0704276645956,6.25656698823341));
#11771=CARTESIAN_POINT('Ctrl Pts',(3.33324589751594,-0.939114562229729,
6.24624510340067));
#11772=CARTESIAN_POINT('Ctrl Pts',(3.31001269947785,-0.894197667815707,
6.24283914849803));
#11773=CARTESIAN_POINT('Ctrl Pts',(3.28443493076994,-0.839773242290625,
6.23889768494268));
#11774=CARTESIAN_POINT('Ctrl Pts',(3.28042298910728,-0.83107440069057,6.23827321423748));
#11775=CARTESIAN_POINT('Ctrl Pts',(3.27430045197504,-0.817543839487553,
6.23731077499121));
#11776=CARTESIAN_POINT('Ctrl Pts',(3.27214614987967,-0.812732225052388,
6.23697025212102));
#11777=CARTESIAN_POINT('Ctrl Pts',(3.26818592381283,-0.803792236454992,
6.23634084164352));
#11778=CARTESIAN_POINT('Ctrl Pts',(3.26637492334548,-0.799666309176151,
6.23605165913068));
#11779=CARTESIAN_POINT('Ctrl Pts',(3.2622749027994,-0.790238731888157,6.23539381482357));
#11780=CARTESIAN_POINT('Ctrl Pts',(3.25999491422456,-0.784933258699513,
6.2350256998411));
#11781=CARTESIAN_POINT('Ctrl Pts',(3.25409385332693,-0.771035585981555,
6.23406669956338));
#11782=CARTESIAN_POINT('Ctrl Pts',(3.25050987935621,-0.762427652525928,
6.23347796515679));
#11783=CARTESIAN_POINT('Ctrl Pts',(3.22578059290626,-0.701839463813795,
6.22936867649569));
#11784=CARTESIAN_POINT('Ctrl Pts',(3.20677456883366,-0.649007220919063,
6.22596325599426));
#11785=CARTESIAN_POINT('Ctrl Pts',(3.1415365774367,-0.440420674228292,6.21294550242712));
#11786=CARTESIAN_POINT('Ctrl Pts',(3.11216592957644,-0.280058874966243,
6.20379410462717));
#11787=CARTESIAN_POINT('Ctrl Pts',(3.09858391842104,-0.0506729573932457,
6.1901136990173));
#11788=CARTESIAN_POINT('Ctrl Pts',(3.09801085941084,0.0167095540782358,
6.18603188695777));
#11789=CARTESIAN_POINT('Ctrl Pts',(3.10150236693872,0.0995614616089712,
6.1808734351888));
#11790=CARTESIAN_POINT('Ctrl Pts',(3.10234120444189,0.115127029242017,6.17989833378868));
#11791=CARTESIAN_POINT('Ctrl Pts',(3.10395977553171,0.13978029173327,6.17834379617816));
#11792=CARTESIAN_POINT('Ctrl Pts',(3.10461956890376,0.148875427108541,6.17776810307447));
#11793=CARTESIAN_POINT('Ctrl Pts',(3.10597825894061,0.16597874206437,6.17668126015351));
#11794=CARTESIAN_POINT('Ctrl Pts',(3.1066632474555,0.173987866953295,6.17617055511855));
#11795=CARTESIAN_POINT('Ctrl Pts',(3.10831381495862,0.192003647838789,6.1750177125317));
#11796=CARTESIAN_POINT('Ctrl Pts',(3.10930666443292,0.202007526326784,6.17437473427432));
#11797=CARTESIAN_POINT('Ctrl Pts',(3.11204063258,0.227585874381187,6.17272332476387));
#11798=CARTESIAN_POINT('Ctrl Pts',(3.11388972210581,0.243147875414463,6.17171154687424));
#11799=CARTESIAN_POINT('Ctrl Pts',(3.12750624921126,0.347259377547065,6.16489393125444));
#11800=CARTESIAN_POINT('Ctrl Pts',(3.14502533871208,0.434941982325944,6.15890863244901));
#11801=CARTESIAN_POINT('Ctrl Pts',(3.20246218588092,0.647153052977282,6.14384633564044));
#11802=CARTESIAN_POINT('Ctrl Pts',(3.24885096834211,0.769498702300583,6.13463940615336));
#11803=CARTESIAN_POINT('Ctrl Pts',(3.33491070833416,0.942987915869029,6.12130125916831));
#11804=CARTESIAN_POINT('Ctrl Pts',(3.36563797546309,0.998186919040296,6.11701632895041));
#11805=CARTESIAN_POINT('Ctrl Pts',(3.40425965165985,1.06042028283198,6.11221090894979));
#11806=CARTESIAN_POINT('Ctrl Pts',(3.40964942157835,1.06895972659542,6.11155212980415));
#11807=CARTESIAN_POINT('Ctrl Pts',(3.41801132295856,1.08198790668985,6.11054843515846));
#11808=CARTESIAN_POINT('Ctrl Pts',(3.4209370710774,1.0865060063837,6.11020061471496));
#11809=CARTESIAN_POINT('Ctrl Pts',(3.42634068867206,1.09477699475915,6.10956443314773));
#11810=CARTESIAN_POINT('Ctrl Pts',(3.42881295634264,1.09853334164469,6.1092757234837));
#11811=CARTESIAN_POINT('Ctrl Pts',(3.43441044857961,1.10697582645171,6.10862731238993));
#11812=CARTESIAN_POINT('Ctrl Pts',(3.43754282604389,1.111657100647,6.1082680935046));
#11813=CARTESIAN_POINT('Ctrl Pts',(3.44682379130446,1.12540100159068,6.10721419415414));
#11814=CARTESIAN_POINT('Ctrl Pts',(3.45302734729278,1.13442650629275,6.10652306354062));
#11815=CARTESIAN_POINT('Ctrl Pts',(3.51468984352989,1.22257470407039,6.09977767926405));
#11816=CARTESIAN_POINT('Ctrl Pts',(3.57576204010148,1.29763128039524,6.09406766015992));
#11817=CARTESIAN_POINT('Ctrl Pts',(3.7299196840154,1.46123369403699,6.08095066807389));
#11818=CARTESIAN_POINT('Ctrl Pts',(3.82657408992542,1.54580595301847,6.07361316082865));
#11819=CARTESIAN_POINT('Ctrl Pts',(3.97999409974984,1.65592560037629,6.06232292310008));
#11820=CARTESIAN_POINT('Ctrl Pts',(4.03090360349148,1.68905479899823,6.05863089631575));
#11821=CARTESIAN_POINT('Ctrl Pts',(4.09627672521156,1.72746904656913,6.05391118574962));
#11822=CARTESIAN_POINT('Ctrl Pts',(4.10939881743706,1.73498040198418,6.05296492662961));
#11823=CARTESIAN_POINT('Ctrl Pts',(4.13048032360395,1.74673173127524,6.051445847848));
#11824=CARTESIAN_POINT('Ctrl Pts',(4.13838546285367,1.7510682531575,6.0508764796131));
#11825=CARTESIAN_POINT('Ctrl Pts',(4.15340724356758,1.75917674571198,6.04979488531505));
#11826=CARTESIAN_POINT('Ctrl Pts',(4.16051787950756,1.76295950766066,6.04928305450948));
#11827=CARTESIAN_POINT('Ctrl Pts',(4.17669941756333,1.7714425327052,6.04811852512529));
#11828=CARTESIAN_POINT('Ctrl Pts',(4.18578385535764,1.77611635121095,6.04746491463593));
#11829=CARTESIAN_POINT('Ctrl Pts',(4.20937489597057,1.78802532030028,6.04576780656778));
#11830=CARTESIAN_POINT('Ctrl Pts',(4.22393428015434,1.79515367175058,6.04472064104634));
#11831=CARTESIAN_POINT('Ctrl Pts',(4.35612029080565,1.85788696661597,6.03521321890788));
#11832=CARTESIAN_POINT('Ctrl Pts',(4.47881571118974,1.90202653371074,6.02635622128806));
#11833=CARTESIAN_POINT('Ctrl Pts',(4.69502459895472,1.95668684785514,6.01086416603617));
#11834=CARTESIAN_POINT('Ctrl Pts',(4.78662006503553,1.97314244917739,6.00434350250644));
#11835=CARTESIAN_POINT('Ctrl Pts',(4.9378577813625,1.98952316765853,5.99388713425263));
#11836=CARTESIAN_POINT('Ctrl Pts',(4.99694638159507,1.99327480085813,5.98987992319688));
#11837=CARTESIAN_POINT('Ctrl Pts',(5.06607175913961,1.994581729572,5.98534512179595));
#11838=CARTESIAN_POINT('Ctrl Pts',(5.07602516429889,1.99469539953001,5.98469587396475));
#11839=CARTESIAN_POINT('Ctrl Pts',(5.09133122782593,1.99475561836228,5.98370362356004));
#11840=CARTESIAN_POINT('Ctrl Pts',(5.09668334776992,1.99475513545624,5.98335781538285));
#11841=CARTESIAN_POINT('Ctrl Pts',(5.10653421220646,1.99471459917883,5.9827235427726));
#11842=CARTESIAN_POINT('Ctrl Pts',(5.11103281022762,1.9946808686242,5.98243474446747));
#11843=CARTESIAN_POINT('Ctrl Pts',(5.12120040404407,1.99457023169572,5.98178391987169));
#11844=CARTESIAN_POINT('Ctrl Pts',(5.12686920255847,1.99448437670734,5.98142239286366));
#11845=CARTESIAN_POINT('Ctrl Pts',(5.14151083432827,1.99420018498417,5.98049188569986));
#11846=CARTESIAN_POINT('Ctrl Pts',(5.15048294642272,1.99396545593045,5.979924852849));
#11847=CARTESIAN_POINT('Ctrl Pts',(5.20821639025844,1.99206502771256,5.97629474655348));
#11848=CARTESIAN_POINT('Ctrl Pts',(5.25690860341288,1.988671231944,5.97331850450749));
#11849=CARTESIAN_POINT('Ctrl Pts',(5.31728010108539,1.98223064538762,5.96968121249203));
#11850=CARTESIAN_POINT('Ctrl Pts',(5.32911734907688,1.98086044023108,5.96897058481451));
#11851=CARTESIAN_POINT('Ctrl Pts',(5.38520518403725,1.97385819977351,5.96561267370825));
#11852=CARTESIAN_POINT('Ctrl Pts',(5.42927237319543,1.96684878227665,5.96300148241768));
#11853=CARTESIAN_POINT('Ctrl Pts',(5.57133238201177,1.93933858352787,5.95457363347082));
#11854=CARTESIAN_POINT('Ctrl Pts',(5.66802158756929,1.91294160767607,5.94881451204955));
#11855=CARTESIAN_POINT('Ctrl Pts',(5.81198766609175,1.86173359992015,5.9397804558131));
#11856=CARTESIAN_POINT('Ctrl Pts',(5.860932154065,1.84210635805048,5.9366252556888));
#11857=CARTESIAN_POINT('Ctrl Pts',(5.94059426360093,1.80643526784675,5.9313026189406));
#11858=CARTESIAN_POINT('Ctrl Pts',(5.9717747813277,1.79148839166356,5.92916998370932));
#11859=CARTESIAN_POINT('Ctrl Pts',(6.01364067741499,1.77006380354809,5.92623099915262));
#11860=CARTESIAN_POINT('Ctrl Pts',(6.02467794644827,1.76428443782323,5.92544889679229));
#11861=CARTESIAN_POINT('Ctrl Pts',(6.04310029870376,1.75441708226857,5.92413086376869));
#11862=CARTESIAN_POINT('Ctrl Pts',(6.05051497820353,1.75038487348025,5.92359690786228));
#11863=CARTESIAN_POINT('Ctrl Pts',(6.06507902678555,1.74234455283601,5.9225411301326));
#11864=CARTESIAN_POINT('Ctrl Pts',(6.07222972860703,1.73833919012566,5.92201941388445));
#11865=CARTESIAN_POINT('Ctrl Pts',(6.08790301402524,1.72943268253098,5.92086840419036));
#11866=CARTESIAN_POINT('Ctrl Pts',(6.09641441671951,1.72451239306663,5.92023843287208));
#11867=CARTESIAN_POINT('Ctrl Pts',(6.12614593860835,1.70703062995768,5.91802031641588));
#11868=CARTESIAN_POINT('Ctrl Pts',(6.14716847600234,1.69413919559536,5.91642030829377));
#11869=CARTESIAN_POINT('Ctrl Pts',(6.29419953114322,1.60018215093131,5.90499886780564));
#11870=CARTESIAN_POINT('Ctrl Pts',(6.41093889171826,1.50554890790296,5.89465691854766));
#11871=CARTESIAN_POINT('Ctrl Pts',(6.57572233686878,1.3380119975311,5.87827382636505));
#11872=CARTESIAN_POINT('Ctrl Pts',(6.63152697466188,1.27348745365528,5.87232928307388));
#11873=CARTESIAN_POINT('Ctrl Pts',(6.6986495627327,1.18500633203405,5.8647969850376));
#11874=CARTESIAN_POINT('Ctrl Pts',(6.71386269417006,1.16412196502821,5.86306099067059));
#11875=CARTESIAN_POINT('Ctrl Pts',(6.73859882267876,1.12874009896752,5.86019640978647));
#11876=CARTESIAN_POINT('Ctrl Pts',(6.74834591644032,1.11440377182698,5.85905604912421));
#11877=CARTESIAN_POINT('Ctrl Pts',(6.7615930255724,1.09436250448009,5.8574918155903));
#11878=CARTESIAN_POINT('Ctrl Pts',(6.76525276657489,1.08876476721394,5.85705809418005));
#11879=CARTESIAN_POINT('Ctrl Pts',(6.77140541029616,1.07924988643152,5.85632638830238));
#11880=CARTESIAN_POINT('Ctrl Pts',(6.77391289635154,1.07534228193641,5.85602745493481));
#11881=CARTESIAN_POINT('Ctrl Pts',(6.77869388944691,1.06783415500849,5.85545612710434));
#11882=CARTESIAN_POINT('Ctrl Pts',(6.78096953232191,1.06423507502839,5.85518358597631));
#11883=CARTESIAN_POINT('Ctrl Pts',(6.78638888631956,1.05560293832246,5.85453302162247));
#11884=CARTESIAN_POINT('Ctrl Pts',(6.78952171943477,1.05056305094438,5.85415570360883));
#11885=CARTESIAN_POINT('Ctrl Pts',(6.80072717097473,1.03235577319717,5.85280134377055));
#11886=CARTESIAN_POINT('Ctrl Pts',(6.80866953204444,1.01910831764367,5.85183233459209));
#11887=CARTESIAN_POINT('Ctrl Pts',(6.88317649851434,0.891496609000298,5.84264060976615));
#11888=CARTESIAN_POINT('Ctrl Pts',(6.93836916982898,0.77085149699917,5.83502325095135));
#11889=CARTESIAN_POINT('Ctrl Pts',(7.01224752832938,0.554876165668998,5.82177037532876));
#11890=CARTESIAN_POINT('Ctrl Pts',(7.03670057593788,0.462023006619127,5.81618658301961));
#11891=CARTESIAN_POINT('Ctrl Pts',(7.06068878825422,0.334146261795293,5.80835987917839));
#11892=CARTESIAN_POINT('Ctrl Pts',(7.06613090174208,0.300360025497406,5.80628023153093));
#11893=CARTESIAN_POINT('Ctrl Pts',(7.07404047656506,0.241676884494521,5.80263652542301));
#11894=CARTESIAN_POINT('Ctrl Pts',(7.07691360873699,0.216842214571727,5.80108484087109));
#11895=CARTESIAN_POINT('Ctrl Pts',(7.08037599338972,0.18103004777908,5.79883057628999));
#11896=CARTESIAN_POINT('Ctrl Pts',(7.08134250808545,0.170090796509527,5.79813975591724));
#11897=CARTESIAN_POINT('Ctrl Pts',(7.08286965557643,0.151010206342768,5.7969306891822));
#11898=CARTESIAN_POINT('Ctrl Pts',(7.08347075476179,0.142872300440119,5.79641371751136));
#11899=CARTESIAN_POINT('Ctrl Pts',(7.08453639554149,0.127131066677307,5.79541112337759));
#11900=CARTESIAN_POINT('Ctrl Pts',(7.08500735035069,0.119528304160802,5.79492571048008));
#11901=CARTESIAN_POINT('Ctrl Pts',(7.08602425909707,0.10143299692379,5.79376750146164));
#11902=CARTESIAN_POINT('Ctrl Pts',(7.08653087782553,0.0909385534460679,
5.79309349118482));
#11903=CARTESIAN_POINT('Ctrl Pts',(7.08804761810333,0.0533573994625538,
5.7906713111105));
#11904=CARTESIAN_POINT('Ctrl Pts',(7.08858849020073,0.0262557374264677,
5.78890867927665));
#11905=CARTESIAN_POINT('Ctrl Pts',(7.08857697543024,-0.000847467537911379,
5.78712926964944));
#11906=CARTESIAN_POINT('Ctrl Pts',(7.09089102510648,-0.00118553947171295,
5.62731851852589));
#11907=CARTESIAN_POINT('Ctrl Pts',(7.0866941324795,0.587071456722144,5.66499078781088));
#11908=CARTESIAN_POINT('Ctrl Pts',(6.50103913263564,1.84272192090518,5.74493881493197));
#11909=CARTESIAN_POINT('Ctrl Pts',(4.36834791099822,2.24206777668213,5.8671625998891));
#11910=CARTESIAN_POINT('Ctrl Pts',(2.81757555877128,0.60980875524591,5.99398987339733));
#11911=CARTESIAN_POINT('Ctrl Pts',(3.34465352606379,-1.57910723626363,6.12081714690552));
#11912=CARTESIAN_POINT('Ctrl Pts',(5.46844469940953,-2.32655318983495,6.24764442041377));
#11913=CARTESIAN_POINT('Ctrl Pts',(6.90380566236945,-1.21784869222614,6.34981092595642));
#11914=CARTESIAN_POINT('Ctrl Pts',(7.08678277106929,-0.277777213867225,
6.40970167366304));
#11915=CARTESIAN_POINT('Ctrl Pts',(7.08569500892407,-0.000879430567275395,
6.42731666353357));
#11916=CARTESIAN_POINT('Origin',(5.09382715545311,0.,-6.77268258743872));
#11917=CARTESIAN_POINT('',(7.08880671528828,-0.000547014378622251,7.38540769406316));
#11918=CARTESIAN_POINT('',(7.08857715545311,1.12756902441053E-10,7.22671373997843));
#11919=CARTESIAN_POINT('',(7.08857715545311,8.3550772080578E-14,-6.77268258743872));
#11920=CARTESIAN_POINT('Ctrl Pts',(7.08799995208786,0.00180011744721413,
6.58540798502575));
#11921=CARTESIAN_POINT('Ctrl Pts',(7.08953512162655,0.175492382420182,6.59648979094105));
#11922=CARTESIAN_POINT('Ctrl Pts',(6.98930587567619,1.01005559039421,6.64984735469243));
#11923=CARTESIAN_POINT('Ctrl Pts',(5.82074642522589,2.24160127242978,6.74548067627989));
#11924=CARTESIAN_POINT('Ctrl Pts',(3.6074629237785,1.8286359014643,6.8723079497881));
#11925=CARTESIAN_POINT('Ctrl Pts',(2.75099006585116,-0.253578904704738,
6.99913522329632));
#11926=CARTESIAN_POINT('Ctrl Pts',(4.03314933554441,-2.10431709865207,7.12596249680453));
#11927=CARTESIAN_POINT('Ctrl Pts',(6.28353626083478,-2.03415341945925,7.25278977031275));
#11928=CARTESIAN_POINT('Ctrl Pts',(7.07750672725613,-0.720147580231949,
7.33927148796819));
#11929=CARTESIAN_POINT('Ctrl Pts',(7.09175163085572,-0.0306588661273706,
7.38347744778755));
#11930=CARTESIAN_POINT('Ctrl Pts',(7.09164127533163,-0.000548482464498706,
7.38540764977084));
#11931=CARTESIAN_POINT('Ctrl Pts',(7.08857700753049,-0.000768203926909726,
6.42565722232425));
#11932=CARTESIAN_POINT('Ctrl Pts',(7.088589330516,0.0312301661132295,6.42760907927267));
#11933=CARTESIAN_POINT('Ctrl Pts',(7.08783171184399,0.063223026411317,6.42958181074859));
#11934=CARTESIAN_POINT('Ctrl Pts',(7.08582640600588,0.105200426417907,6.43220396661624));
#11935=CARTESIAN_POINT('Ctrl Pts',(7.08527231960211,0.11521413248421,6.43283199971842));
#11936=CARTESIAN_POINT('Ctrl Pts',(7.08415202477829,0.133024748424536,6.43395371348444));
#11937=CARTESIAN_POINT('Ctrl Pts',(7.08361544750926,0.14082336152514,6.43444646876064));
#11938=CARTESIAN_POINT('Ctrl Pts',(7.08245151325584,0.156402205302053,6.43543410627943));
#11939=CARTESIAN_POINT('Ctrl Pts',(7.08182430166488,0.164182307533372,6.43592897552786));
#11940=CARTESIAN_POINT('Ctrl Pts',(7.0803849649628,0.180816726927487,6.43699064321805));
#11941=CARTESIAN_POINT('Ctrl Pts',(7.07955927010025,0.18966967052163,6.43755785561866));
#11942=CARTESIAN_POINT('Ctrl Pts',(7.07722641192135,0.212994497171477,6.43905819699522));
#11943=CARTESIAN_POINT('Ctrl Pts',(7.07562006807252,0.227455708516326,6.43999440567719));
#11944=CARTESIAN_POINT('Ctrl Pts',(7.06803439219472,0.289547461014513,6.44404084680819));
#11945=CARTESIAN_POINT('Ctrl Pts',(7.06049540060659,0.336967817662538,6.44719931815086));
#11946=CARTESIAN_POINT('Ctrl Pts',(7.01788942838625,0.554112428174759,6.46198743990834));
#11947=CARTESIAN_POINT('Ctrl Pts',(6.96250985046776,0.719071621946716,6.47423393457015));
#11948=CARTESIAN_POINT('Ctrl Pts',(6.8572288289548,0.934831185141043,6.49079698832607));
#11949=CARTESIAN_POINT('Ctrl Pts',(6.82491453567728,0.993394802674202,6.49534261866924));
#11950=CARTESIAN_POINT('Ctrl Pts',(6.78433695249872,1.05891860529282,6.50040028558089));
#11951=CARTESIAN_POINT('Ctrl Pts',(6.77888995813123,1.06756514938461,6.50106708023694));
#11952=CARTESIAN_POINT('Ctrl Pts',(6.77045892410519,1.08072324061857,6.50208038869031));
#11953=CARTESIAN_POINT('Ctrl Pts',(6.7675226794871,1.0852649929698,6.50242989212538));
#11954=CARTESIAN_POINT('Ctrl Pts',(6.76211176379092,1.09356035053195,6.50306769244988));
#11955=CARTESIAN_POINT('Ctrl Pts',(6.75964287557799,1.09731753020336,6.50335635008455));
#11956=CARTESIAN_POINT('Ctrl Pts',(6.75406853295796,1.10573845155242,6.50400284181164));
#11957=CARTESIAN_POINT('Ctrl Pts',(6.7509561245584,1.11039746776133,6.50436020684622));
#11958=CARTESIAN_POINT('Ctrl Pts',(6.74177939564698,1.12400974665107,6.50540358419423));
#11959=CARTESIAN_POINT('Ctrl Pts',(6.73566174026383,1.13292705190093,6.50608615174947));
#11960=CARTESIAN_POINT('Ctrl Pts',(6.68512509943597,1.20532185563022,6.5116237084101));
#11961=CARTESIAN_POINT('Ctrl Pts',(6.63710946745687,1.26621977734296,6.51625863451744));
#11962=CARTESIAN_POINT('Ctrl Pts',(6.5108401767444,1.40847696402522,6.5274421148469));
#11963=CARTESIAN_POINT('Ctrl Pts',(6.42900242764555,1.48628434538825,6.53389097054297));
#11964=CARTESIAN_POINT('Ctrl Pts',(6.29320798742841,1.59507614532385,6.5441168470746));
#11965=CARTESIAN_POINT('Ctrl Pts',(6.24364977083468,1.6311619721759,6.54776175521778));
#11966=CARTESIAN_POINT('Ctrl Pts',(6.17103591330139,1.67908038347948,6.55304922787306));
#11967=CARTESIAN_POINT('Ctrl Pts',(6.14928828952595,1.69283529873874,6.55462620792526));
#11968=CARTESIAN_POINT('Ctrl Pts',(6.11524711434376,1.71345463574606,6.55708845322561));
#11969=CARTESIAN_POINT('Ctrl Pts',(6.10313629898589,1.72061633097482,6.55796325596448));
#11970=CARTESIAN_POINT('Ctrl Pts',(6.08282489038284,1.73233919086986,6.55942901299348));
#11971=CARTESIAN_POINT('Ctrl Pts',(6.07466593590645,1.73697175392102,6.56001742514646));
#11972=CARTESIAN_POINT('Ctrl Pts',(6.05871510179123,1.74588023820364,6.56116722657081));
#11973=CARTESIAN_POINT('Ctrl Pts',(6.05092671750115,1.75016198660145,6.56172839267283));
#11974=CARTESIAN_POINT('Ctrl Pts',(6.03610105416949,1.75818399829576,6.56279625593172));
#11975=CARTESIAN_POINT('Ctrl Pts',(6.02906944931659,1.76193442580175,6.56330258036936));
#11976=CARTESIAN_POINT('Ctrl Pts',(6.01312146941879,1.77031819018743,6.56445070783866));
#11977=CARTESIAN_POINT('Ctrl Pts',(6.00419223193426,1.77492646372661,6.56509337539839));
#11978=CARTESIAN_POINT('Ctrl Pts',(5.98126269392423,1.78654158256391,6.5667434545896));
#11979=CARTESIAN_POINT('Ctrl Pts',(5.96721423557539,1.79345132254698,6.56775420370496));
#11980=CARTESIAN_POINT('Ctrl Pts',(5.87317938406065,1.83833551935137,6.57451969383595));
#11981=CARTESIAN_POINT('Ctrl Pts',(5.79083298736072,1.87110833829854,6.58045060811876));
#11982=CARTESIAN_POINT('Ctrl Pts',(5.58170905287068,1.93861280681789,6.59550082587848));
#11983=CARTESIAN_POINT('Ctrl Pts',(5.45316275616061,1.9665001945574,6.60475674092297));
#11984=CARTESIAN_POINT('Ctrl Pts',(5.25997853114852,1.98882437221507,6.61815134042512));
#11985=CARTESIAN_POINT('Ctrl Pts',(5.19682558758413,1.99309349605632,6.62244482279055));
#11986=CARTESIAN_POINT('Ctrl Pts',(5.12347059201432,1.99455530814901,6.62725854454443));
#11987=CARTESIAN_POINT('Ctrl Pts',(5.11336907237617,1.99467985760589,6.62791760047651));
#11988=CARTESIAN_POINT('Ctrl Pts',(5.09788338736835,1.9947531404102,6.62892162729713));
#11989=CARTESIAN_POINT('Ctrl Pts',(5.09249982487867,1.99475682328346,6.62926950603586));
#11990=CARTESIAN_POINT('Ctrl Pts',(5.08261934727396,1.9947235823004,6.62990574339872));
#11991=CARTESIAN_POINT('Ctrl Pts',(5.07812257863614,1.99469324754727,6.63019445098651));
#11992=CARTESIAN_POINT('Ctrl Pts',(5.0679946493747,1.99459067412349,6.63084279431774));
#11993=CARTESIAN_POINT('Ctrl Pts',(5.06236367733891,1.99450979618571,6.63120194799081));
#11994=CARTESIAN_POINT('Ctrl Pts',(5.04578838650649,1.99420151089887,6.6322554762103));
#11995=CARTESIAN_POINT('Ctrl Pts',(5.03484530242939,1.99390785723189,6.63294630463898));
#11996=CARTESIAN_POINT('Ctrl Pts',(4.93508607267919,1.99040883252325,6.63920551728749));
#11997=CARTESIAN_POINT('Ctrl Pts',(4.8465625446466,1.9813607383178,6.64448338156183));
#11998=CARTESIAN_POINT('Ctrl Pts',(4.64395070552254,1.94685436265891,6.65650785784992));
#11999=CARTESIAN_POINT('Ctrl Pts',(4.53091477043828,1.9172272535737,6.66318493386606));
#12000=CARTESIAN_POINT('Ctrl Pts',(4.3726003549376,1.86051475586336,6.67313652737869));
#12001=CARTESIAN_POINT('Ctrl Pts',(4.32478052515999,1.84126314390431,6.67622371435591));
#12002=CARTESIAN_POINT('Ctrl Pts',(4.25688872568664,1.8108243706271,6.68076313422834));
#12003=CARTESIAN_POINT('Ctrl Pts',(4.23617861310828,1.80110792326424,6.68216946389145));
#12004=CARTESIAN_POINT('Ctrl Pts',(4.19926988472657,1.78301073778736,6.6847179516348));
#12005=CARTESIAN_POINT('Ctrl Pts',(4.18301025760501,1.77475985586078,6.68585568532457));
#12006=CARTESIAN_POINT('Ctrl Pts',(4.15829028429042,1.76178663089958,6.68760966345852));
#12007=CARTESIAN_POINT('Ctrl Pts',(4.14974716043247,1.75722347122054,6.68822033007702));
#12008=CARTESIAN_POINT('Ctrl Pts',(4.13426132758719,1.74880645955735,6.68933564428653));
#12009=CARTESIAN_POINT('Ctrl Pts',(4.12730771570866,1.74497300283502,6.68983956132312));
#12010=CARTESIAN_POINT('Ctrl Pts',(4.11219751411522,1.736524872572,6.69094146254863));
#12011=CARTESIAN_POINT('Ctrl Pts',(4.10405021751505,1.73189404814822,6.69154001530179));
#12012=CARTESIAN_POINT('Ctrl Pts',(4.08181994219555,1.71905053370222,6.69318550902097));
#12013=CARTESIAN_POINT('Ctrl Pts',(4.06780478633334,1.71072248160849,6.69423658091199));
#12014=CARTESIAN_POINT('Ctrl Pts',(3.99314426638532,1.66511039494194,6.69991095572775));
#12015=CARTESIAN_POINT('Ctrl Pts',(3.93443216758976,1.62477588077883,6.7046450834709));
#12016=CARTESIAN_POINT('Ctrl Pts',(3.76155603451837,1.4918638012132,6.71944374798924));
#12017=CARTESIAN_POINT('Ctrl Pts',(3.65535616137471,1.38974742759567,6.72981331261377));
#12018=CARTESIAN_POINT('Ctrl Pts',(3.51886054351958,1.2259330602287,6.74452104307906));
#12019=CARTESIAN_POINT('Ctrl Pts',(3.47894450916726,1.17285448677464,6.74903328608398));
#12020=CARTESIAN_POINT('Ctrl Pts',(3.43602710302209,1.10942808261533,6.75405874102827));
#12021=CARTESIAN_POINT('Ctrl Pts',(3.43037345108991,1.10093299902366,6.75472455620501));
#12022=CARTESIAN_POINT('Ctrl Pts',(3.42182511642405,1.08787221595719,6.75573669039174));
#12023=CARTESIAN_POINT('Ctrl Pts',(3.41888348863311,1.08333766269633,6.75608598863347));
#12024=CARTESIAN_POINT('Ctrl Pts',(3.41352882446706,1.07500943934847,6.7567235905653));
#12025=CARTESIAN_POINT('Ctrl Pts',(3.41111018312187,1.07121957023783,6.75701225351547));
#12026=CARTESIAN_POINT('Ctrl Pts',(3.40570420658077,1.0626852328549,6.75765897463491));
#12027=CARTESIAN_POINT('Ctrl Pts',(3.40272405249047,1.05793633628343,6.75801656212584));
#12028=CARTESIAN_POINT('Ctrl Pts',(3.3940459127365,1.04397728923754,6.75906119949848));
#12029=CARTESIAN_POINT('Ctrl Pts',(3.38840275810082,1.03473305291156,6.75974479211849));
#12030=CARTESIAN_POINT('Ctrl Pts',(3.34245167747488,0.958061866202165,6.76535101036473));
#12031=CARTESIAN_POINT('Ctrl Pts',(3.30607881586456,0.888345361085753,6.77004731096961));
#12032=CARTESIAN_POINT('Ctrl Pts',(3.23491930187805,0.729766656506672,6.7802611830524));
#12033=CARTESIAN_POINT('Ctrl Pts',(3.20220093285155,0.640194297382251,6.78573181649191));
#12034=CARTESIAN_POINT('Ctrl Pts',(3.1490691440313,0.454462518042895,6.79701942217045));
#12035=CARTESIAN_POINT('Ctrl Pts',(3.12910648613203,0.358454003972758,6.8028280116879));
#12036=CARTESIAN_POINT('Ctrl Pts',(3.1131899422585,0.238030016388062,6.81031398040511));
#12037=CARTESIAN_POINT('Ctrl Pts',(3.11051816884492,0.214633292099132,6.81177712254252));
#12038=CARTESIAN_POINT('Ctrl Pts',(3.10723347154922,0.18052169912609,6.81392534033777));
#12039=CARTESIAN_POINT('Ctrl Pts',(3.10629176475914,0.169839960976826,6.81460016488108));
#12040=CARTESIAN_POINT('Ctrl Pts',(3.10478841379868,0.151057524783607,6.81579071296601));
#12041=CARTESIAN_POINT('Ctrl Pts',(3.10419001777288,0.142959955203459,6.81630527769629));
#12042=CARTESIAN_POINT('Ctrl Pts',(3.10312109258738,0.127185263389626,6.81731029282065));
#12043=CARTESIAN_POINT('Ctrl Pts',(3.10264549443576,0.119508619201005,6.81780057551906));
#12044=CARTESIAN_POINT('Ctrl Pts',(3.10148772739044,0.0988895192001237,
6.81912076480896));
#12045=CARTESIAN_POINT('Ctrl Pts',(3.1008872873851,0.0859430206096428,6.81995320150754));
#12046=CARTESIAN_POINT('Ctrl Pts',(3.09912397962355,0.0377869164479501,
6.82306309524128));
#12047=CARTESIAN_POINT('Ctrl Pts',(3.09876780363548,0.00255601406838469,
6.82536533871372));
#12048=CARTESIAN_POINT('Ctrl Pts',(3.10264189845513,-0.233997828987448,
6.84101425760592));
#12049=CARTESIAN_POINT('Ctrl Pts',(3.13640900401216,-0.433655522898617,
6.85531829962411));
#12050=CARTESIAN_POINT('Ctrl Pts',(3.21687633452901,-0.677625253041591,
6.87294230081636));
#12051=CARTESIAN_POINT('Ctrl Pts',(3.2364987396808,-0.72969359935644,6.87670082602437));
#12052=CARTESIAN_POINT('Ctrl Pts',(3.26211397568363,-0.789905453433661,
6.88099151569122));
#12053=CARTESIAN_POINT('Ctrl Pts',(3.2660208929067,-0.798904296097861,6.88163125799971));
#12054=CARTESIAN_POINT('Ctrl Pts',(3.27214929079101,-0.812739587393907,
6.88261208196265));
#12055=CARTESIAN_POINT('Ctrl Pts',(3.27432393918432,-0.817596432905007,
6.88295587163263));
#12056=CARTESIAN_POINT('Ctrl Pts',(3.27837384508788,-0.826545280148521,
6.88358826024913));
#12057=CARTESIAN_POINT('Ctrl Pts',(3.2802435086024,-0.830639620305563,6.88387717826503));
#12058=CARTESIAN_POINT('Ctrl Pts',(3.28451566175652,-0.839911937439372,
6.88453056215311));
#12059=CARTESIAN_POINT('Ctrl Pts',(3.28692652539578,-0.845085947648634,
6.88489451123191));
#12060=CARTESIAN_POINT('Ctrl Pts',(3.29323957955067,-0.8584840147509,6.88583546459706));
#12061=CARTESIAN_POINT('Ctrl Pts',(3.29717596348398,-0.86669194287413,6.88641044802648));
#12062=CARTESIAN_POINT('Ctrl Pts',(3.32372071894968,-0.921083489930184,
6.89021281952478));
#12063=CARTESIAN_POINT('Ctrl Pts',(3.34805349585162,-0.966409285495142,
6.89334365658083));
#12064=CARTESIAN_POINT('Ctrl Pts',(3.40261655431234,-1.05924436249546,6.89978093537112));
#12065=CARTESIAN_POINT('Ctrl Pts',(3.43316006067346,-1.10651584807978,6.90307357280106));
#12066=CARTESIAN_POINT('Ctrl Pts',(3.46775923923249,-1.15539771051408,6.90655958852362));
#12067=CARTESIAN_POINT('Ctrl Pts',(3.46986435755691,-1.15835468174972,6.90677078977692));
#12068=CARTESIAN_POINT('Ctrl Pts',(3.53986360352071,-1.25611380871563,6.91376450064198));
#12069=CARTESIAN_POINT('Ctrl Pts',(3.61592801456458,-1.3447814324059,6.92047591178594));
#12070=CARTESIAN_POINT('Ctrl Pts',(3.72732839054369,-1.4537005618482,6.9297986652576));
#12071=CARTESIAN_POINT('Ctrl Pts',(3.75615763737576,-1.48027165674936,6.93217054853875));
#12072=CARTESIAN_POINT('Ctrl Pts',(3.80669213948574,-1.5241655065836,6.93627819135072));
#12073=CARTESIAN_POINT('Ctrl Pts',(3.8280109015467,-1.54191638398348,6.93799671527219));
#12074=CARTESIAN_POINT('Ctrl Pts',(3.85863696109675,-1.56635363132014,6.94044947902455));
#12075=CARTESIAN_POINT('Ctrl Pts',(3.86764293220926,-1.57341372707795,6.94116883620664));
#12076=CARTESIAN_POINT('Ctrl Pts',(3.8832376895765,-1.585423795647,6.9424114818964));
#12077=CARTESIAN_POINT('Ctrl Pts',(3.88979738686526,-1.59041119832056,6.94293328459356));
#12078=CARTESIAN_POINT('Ctrl Pts',(3.90239520124193,-1.59986683277711,6.94393378909102));
#12079=CARTESIAN_POINT('Ctrl Pts',(3.90842803551236,-1.60434189250607,6.94441221306948));
#12080=CARTESIAN_POINT('Ctrl Pts',(3.92415907502342,-1.61587375637479,6.94565802220415));
#12081=CARTESIAN_POINT('Ctrl Pts',(3.93389579415364,-1.62287727250695,6.94642743959259));
#12082=CARTESIAN_POINT('Ctrl Pts',(3.9620854506607,-1.6427705008603,6.9486505903565));
#12083=CARTESIAN_POINT('Ctrl Pts',(3.98069369025704,-1.65543590183602,6.95011270753178));
#12084=CARTESIAN_POINT('Ctrl Pts',(4.11851657998183,-1.74586834887584,6.96090644211711));
#12085=CARTESIAN_POINT('Ctrl Pts',(4.2455163743465,-1.81097820009745,6.97070492623463));
#12086=CARTESIAN_POINT('Ctrl Pts',(4.48669904769094,-1.90365425472071,6.98871272511691));
#12087=CARTESIAN_POINT('Ctrl Pts',(4.59849973863503,-1.93575808473208,6.99683561542773));
#12088=CARTESIAN_POINT('Ctrl Pts',(4.73094334588759,-1.96155480881843,7.00580634979991));
#12089=CARTESIAN_POINT('Ctrl Pts',(4.74947153372208,-1.9648921585735,7.0070464839901));
#12090=CARTESIAN_POINT('Ctrl Pts',(4.77485914782911,-1.9690948880131,7.00872301792543));
#12091=CARTESIAN_POINT('Ctrl Pts',(4.78167925345538,-1.97018754400765,7.0091711682355));
#12092=CARTESIAN_POINT('Ctrl Pts',(4.79313652147584,-1.9719621372078,7.00992012792961));
#12093=CARTESIAN_POINT('Ctrl Pts',(4.79777061262188,-1.9726631878765,7.0102219888622));
#12094=CARTESIAN_POINT('Ctrl Pts',(4.80657662619298,-1.97396364179228,7.01079352182552));
#12095=CARTESIAN_POINT('Ctrl Pts',(4.8107480330261,-1.9745661642311,7.01106337251019));
#12096=CARTESIAN_POINT('Ctrl Pts',(4.82172835384005,-1.97611666245945,7.01177144401466));
#12097=CARTESIAN_POINT('Ctrl Pts',(4.82854038533407,-1.97704267895438,7.01220844554638));
#12098=CARTESIAN_POINT('Ctrl Pts',(4.85246390663301,-1.98016892756954,7.01373562138544));
#12099=CARTESIAN_POINT('Ctrl Pts',(4.8695995845821,-1.9821824444351,7.01481594844347));
#12100=CARTESIAN_POINT('Ctrl Pts',(5.08690251218825,-2.00486234532082,7.02836913206812));
#12101=CARTESIAN_POINT('Ctrl Pts',(5.28908143376296,-1.99535046974311,7.03950502141961));
#12102=CARTESIAN_POINT('Ctrl Pts',(5.55844892346884,-1.94127494580665,7.05580352201697));
#12103=CARTESIAN_POINT('Ctrl Pts',(5.62959721699718,-1.92285476564722,7.06024139690932));
#12104=CARTESIAN_POINT('Ctrl Pts',(5.71477494156892,-1.89570734080917,7.06579975861128));
#12105=CARTESIAN_POINT('Ctrl Pts',(5.72992787543424,-1.89067668465797,7.06679813131708));
#12106=CARTESIAN_POINT('Ctrl Pts',(5.75371584306949,-1.88246092927145,7.0683812700384));
#12107=CARTESIAN_POINT('Ctrl Pts',(5.76239222626734,-1.87939697025274,7.06896205030836));
#12108=CARTESIAN_POINT('Ctrl Pts',(5.77859904737152,-1.87354729920393,7.07005332889127));
#12109=CARTESIAN_POINT('Ctrl Pts',(5.78613449217919,-1.87077592852671,7.07056334349911));
#12110=CARTESIAN_POINT('Ctrl Pts',(5.80295594089279,-1.8644738191269,7.0717078239135));
#12111=CARTESIAN_POINT('Ctrl Pts',(5.81223266141324,-1.86091906854542,7.07234307869535));
#12112=CARTESIAN_POINT('Ctrl Pts',(5.83571199155859,-1.8517202856674,7.07396150768721));
#12113=CARTESIAN_POINT('Ctrl Pts',(5.84987680044445,-1.84598213404487,7.07494780498331));
#12114=CARTESIAN_POINT('Ctrl Pts',(5.93720829072673,-1.80943046351508,7.08109164187705));
#12115=CARTESIAN_POINT('Ctrl Pts',(6.0085381787257,-1.7744382999037,7.0863895355258));
#12116=CARTESIAN_POINT('Ctrl Pts',(6.19895612433764,-1.66648802149252,7.10131223445727));
#12117=CARTESIAN_POINT('Ctrl Pts',(6.31276882181629,-1.58513988391596,7.11115899329005));
#12118=CARTESIAN_POINT('Ctrl Pts',(6.46561003801874,-1.44963223084906,7.1252380157083));
#12119=CARTESIAN_POINT('Ctrl Pts',(6.51195451302183,-1.40432847990216,7.12963760838606));
#12120=CARTESIAN_POINT('Ctrl Pts',(6.56292253160599,-1.34940335437977,7.13455417946827));
#12121=CARTESIAN_POINT('Ctrl Pts',(6.56977164816174,-1.34190852963138,7.13521658941542));
#12122=CARTESIAN_POINT('Ctrl Pts',(6.58017177448727,-1.33035195834597,7.13622464005901));
#12123=CARTESIAN_POINT('Ctrl Pts',(6.58376390796898,-1.32632768755214,7.13657322393231));
#12124=CARTESIAN_POINT('Ctrl Pts',(6.59032031342916,-1.31892229042792,7.13721013740142));
#12125=CARTESIAN_POINT('Ctrl Pts',(6.59328947514359,-1.31554571668826,7.13749882108049));
#12126=CARTESIAN_POINT('Ctrl Pts',(6.59994345535824,-1.30792691920996,7.13814635079389));
#12127=CARTESIAN_POINT('Ctrl Pts',(6.60362177615879,-1.30367915530447,7.13850472045696));
#12128=CARTESIAN_POINT('Ctrl Pts',(6.61437491097847,-1.29115476927748,7.13955379369074));
#12129=CARTESIAN_POINT('Ctrl Pts',(6.6214000992721,-1.28283554242252,7.1402409958054));
#12130=CARTESIAN_POINT('Ctrl Pts',(6.69210058800496,-1.19770764831555,7.14718058172315));
#12131=CARTESIAN_POINT('Ctrl Pts',(6.7500054196207,-1.11627086405036,7.1530652823694));
#12132=CARTESIAN_POINT('Ctrl Pts',(6.86656150814653,-0.923175627275076,
7.1662148909185));
#12133=CARTESIAN_POINT('Ctrl Pts',(6.92121670711533,-0.809621173809221,
7.17342389070417));
#12134=CARTESIAN_POINT('Ctrl Pts',(6.98567243080275,-0.635268491632854,
7.18454110637366));
#12135=CARTESIAN_POINT('Ctrl Pts',(7.00396303706933,-0.57794849676137,7.18819944472896));
#12136=CARTESIAN_POINT('Ctrl Pts',(7.02356493399509,-0.505338463935615,
7.19288116930449));
#12137=CARTESIAN_POINT('Ctrl Pts',(7.027329056784,-0.490739477737561,7.19382475428593));
#12138=CARTESIAN_POINT('Ctrl Pts',(7.03307700289468,-0.467352882771846,
7.1953405453573));
#12139=CARTESIAN_POINT('Ctrl Pts',(7.03516745610395,-0.458591888955015,
7.19590932656078));
#12140=CARTESIAN_POINT('Ctrl Pts',(7.03901510286803,-0.441968675865347,
7.19699045056201));
#12141=CARTESIAN_POINT('Ctrl Pts',(7.04078414514752,-0.434109362240635,
7.19750240277374));
#12142=CARTESIAN_POINT('Ctrl Pts',(7.04469197740838,-0.416243571726668,
7.1986680985766));
#12143=CARTESIAN_POINT('Ctrl Pts',(7.04680146308794,-0.406230983354801,
7.19932276112979));
#12144=CARTESIAN_POINT('Ctrl Pts',(7.05206423515512,-0.380262576897724,
7.20102441064051));
#12145=CARTESIAN_POINT('Ctrl Pts',(7.05509952620938,-0.364283885888679,
7.20207509821028));
#12146=CARTESIAN_POINT('Ctrl Pts',(7.0783285424351,-0.233281060990239,7.21072084935811));
#12147=CARTESIAN_POINT('Ctrl Pts',(7.08857715545971,-0.116744608515098,
7.21863090442123));
#12148=CARTESIAN_POINT('Ctrl Pts',(7.08857715545311,1.12752272796168E-10,
7.22671373997843));
#12149=CARTESIAN_POINT('Origin',(5.09382715545311,0.,-6.77268258743872));
#12150=CARTESIAN_POINT('',(7.08857666516212,-0.001398576294443,8.18540764972207));
#12151=CARTESIAN_POINT('',(7.08857712104368,-0.000272444087889267,8.02912895344979));
#12152=CARTESIAN_POINT('',(7.08857715545311,8.3550772080578E-14,-6.77268258743872));
#12153=CARTESIAN_POINT('Ctrl Pts',(7.08857708048265,-0.000546895445309948,
7.38540769765139));
#12154=CARTESIAN_POINT('Ctrl Pts',(7.08859597015781,0.0683514258463495,
7.38983115855148));
#12155=CARTESIAN_POINT('Ctrl Pts',(7.08504098529914,0.137392907239248,7.39425461945158));
#12156=CARTESIAN_POINT('Ctrl Pts',(7.0778937658154,0.206172859866408,7.39867808035167));
#12157=CARTESIAN_POINT('Ctrl Pts',(7.07063861570019,0.275991463081629,7.40316834022573));
#12158=CARTESIAN_POINT('Ctrl Pts',(7.0596817423248,0.345540058892286,7.40765860009979));
#12159=CARTESIAN_POINT('Ctrl Pts',(7.04505896197384,0.414393532432477,7.41214885997386));
#12160=CARTESIAN_POINT('Ctrl Pts',(7.03069092698795,0.482047500623273,7.41656089444458));
#12161=CARTESIAN_POINT('Ctrl Pts',(7.01278379571535,0.549029864948614,7.42097292891529));
#12162=CARTESIAN_POINT('Ctrl Pts',(6.99142365607376,0.614943154553544,7.42538496338601));
#12163=CARTESIAN_POINT('Ctrl Pts',(6.97007562037212,0.680819093723832,7.42979449773261));
#12164=CARTESIAN_POINT('Ctrl Pts',(6.94527860959919,0.745626687791695,7.43420403207922));
#12165=CARTESIAN_POINT('Ctrl Pts',(6.9171689403589,0.808982260569757,7.43861356642582));
#12166=CARTESIAN_POINT('Ctrl Pts',(6.88906532116135,0.87232419733101,7.44302215170856));
#12167=CARTESIAN_POINT('Ctrl Pts',(6.85765066061639,0.934214279254919,7.4474307369913));
#12168=CARTESIAN_POINT('Ctrl Pts',(6.82310921374251,0.99428925639292,7.45183932227404));
#12169=CARTESIAN_POINT('Ctrl Pts',(6.78745651537521,1.05629693798031,7.45638973852863));
#12170=CARTESIAN_POINT('Ctrl Pts',(6.74847263775237,1.11637021703044,7.46094015478322));
#12171=CARTESIAN_POINT('Ctrl Pts',(6.70641005089121,1.1741396713511,7.46549057103781));
#12172=CARTESIAN_POINT('Ctrl Pts',(6.6656075964235,1.23017843894577,7.46990466360539));
#12173=CARTESIAN_POINT('Ctrl Pts',(6.62190868633854,1.28404912791569,7.47431875617297));
#12174=CARTESIAN_POINT('Ctrl Pts',(6.57558479862159,1.33544818297521,7.47873284874055));
#12175=CARTESIAN_POINT('Ctrl Pts',(6.52711492855147,1.38922833061058,7.48335142683865));
#12176=CARTESIAN_POINT('Ctrl Pts',(6.4757713805736,1.44030182872507,7.48797000493674));
#12177=CARTESIAN_POINT('Ctrl Pts',(6.42190616946195,1.48836611593025,7.49258858303484));
#12178=CARTESIAN_POINT('Ctrl Pts',(6.36804095835031,1.53643040313543,7.49720716113293));
#12179=CARTESIAN_POINT('Ctrl Pts',(6.31165461331486,1.58148515758602,7.50182573923103));
#12180=CARTESIAN_POINT('Ctrl Pts',(6.25313367068357,1.62327938637938,7.50644431732912));
#12181=CARTESIAN_POINT('Ctrl Pts',(6.19667905707053,1.66359789342479,7.51089981702284));
#12182=CARTESIAN_POINT('Ctrl Pts',(6.13800773522275,1.70104701606772,7.51535531671655));
#12183=CARTESIAN_POINT('Ctrl Pts',(6.07744329185307,1.7353751348667,7.51981081641027));
#12184=CARTESIAN_POINT('Ctrl Pts',(6.01696941005075,1.76965192308176,7.52425965382801));
#12185=CARTESIAN_POINT('Ctrl Pts',(5.9546084474191,1.80081673092069,7.52870849124575));
#12186=CARTESIAN_POINT('Ctrl Pts',(5.89071401831209,1.82866040868795,7.5331573286635));
#12187=CARTESIAN_POINT('Ctrl Pts',(5.82689437395095,1.85647149703552,7.53760095897351));
#12188=CARTESIAN_POINT('Ctrl Pts',(5.76154527427762,1.88096898145218,7.54204458928353));
#12189=CARTESIAN_POINT('Ctrl Pts',(5.69504447026208,1.90198982722671,7.54648821959354));
#12190=CARTESIAN_POINT('Ctrl Pts',(5.62858524851718,1.92299752888199,7.5509290713471));
#12191=CARTESIAN_POINT('Ctrl Pts',(5.56097621645697,1.94053275748656,7.55536992310066));
#12192=CARTESIAN_POINT('Ctrl Pts',(5.49261319300565,1.95448132729713,7.55981077485422));
#12193=CARTESIAN_POINT('Ctrl Pts',(5.42426973105243,1.96842590584301,7.5642503558958));
#12194=CARTESIAN_POINT('Ctrl Pts',(5.35517318508442,1.97878576531309,7.56868993693738));
#12195=CARTESIAN_POINT('Ctrl Pts',(5.28573082354445,1.9854975559474,7.57312951797895));
#12196=CARTESIAN_POINT('Ctrl Pts',(5.21628478183528,1.99220970227993,7.57756933430068));
#12197=CARTESIAN_POINT('Ctrl Pts',(5.14649337530007,1.9952733512989,7.58200915062242));
#12198=CARTESIAN_POINT('Ctrl Pts',(5.07676849415664,1.99467705771505,7.58644896694415));
#12199=CARTESIAN_POINT('Ctrl Pts',(5.00697001312695,1.99408013469822,7.59089346982785));
#12200=CARTESIAN_POINT('Ctrl Pts',(4.9372386877492,1.98981556252933,7.59533797271155));
#12201=CARTESIAN_POINT('Ctrl Pts',(4.86798493486115,1.98192402828617,7.59978247559525));
#12202=CARTESIAN_POINT('Ctrl Pts',(4.79869055616879,1.97402786469207,7.604229585724));
#12203=CARTESIAN_POINT('Ctrl Pts',(4.72987479015126,1.96250058497032,7.60867669585275));
#12204=CARTESIAN_POINT('Ctrl Pts',(4.6619387061976,1.94743419141692,7.6131238059815));
#12205=CARTESIAN_POINT('Ctrl Pts',(4.59388533034977,1.93234178568066,7.61757859406194));
#12206=CARTESIAN_POINT('Ctrl Pts',(4.52671513938015,1.91369820030049,7.62203338214238));
#12207=CARTESIAN_POINT('Ctrl Pts',(4.46081408778557,1.89164532052447,7.62648817022282));
#12208=CARTESIAN_POINT('Ctrl Pts',(4.42736434458515,1.88045182440432,7.62874931042768));
#12209=CARTESIAN_POINT('Ctrl Pts',(4.39424125548785,1.86838075483627,7.63101045063254));
#12210=CARTESIAN_POINT('Ctrl Pts',(4.36149303308614,1.85545527990221,7.6332715908374));
#12211=CARTESIAN_POINT('Ctrl Pts',(4.29696377719709,1.82998607216092,7.63772709053111));
#12212=CARTESIAN_POINT('Ctrl Pts',(4.23363799911903,1.80109651306259,7.64218259022482));
#12213=CARTESIAN_POINT('Ctrl Pts',(4.17190279286082,1.76892143187842,7.64663808991853));
#12214=CARTESIAN_POINT('Ctrl Pts',(4.11025989880295,1.73679446185675,7.65108692733629));
#12215=CARTESIAN_POINT('Ctrl Pts',(4.05020328625875,1.70139194502923,7.65553576475404));
#12216=CARTESIAN_POINT('Ctrl Pts',(3.99210072440856,1.66289700030935,7.65998460217179));
#12217=CARTESIAN_POINT('Ctrl Pts',(3.93406616825767,1.62444711170322,7.66442823248181));
#12218=CARTESIAN_POINT('Ctrl Pts',(3.8779815260734,1.58291225306713,7.66887186279182));
#12219=CARTESIAN_POINT('Ctrl Pts',(3.82418898030399,1.5385208697655,7.67331549310184));
#12220=CARTESIAN_POINT('Ctrl Pts',(3.77043007046165,1.49415724394051,7.6777563448554));
#12221=CARTESIAN_POINT('Ctrl Pts',(3.7189607901727,1.44694094754962,7.68219719660896));
#12222=CARTESIAN_POINT('Ctrl Pts',(3.67009214155776,1.39714214477569,7.68663804836252));
#12223=CARTESIAN_POINT('Ctrl Pts',(3.6212374762912,1.34735759150583,7.6910776294041));
#12224=CARTESIAN_POINT('Ctrl Pts',(3.57498230781504,1.29499234785888,7.69551721044568));
#12225=CARTESIAN_POINT('Ctrl Pts',(3.53160119245343,1.24035382170964,7.69995679148727));
#12226=CARTESIAN_POINT('Ctrl Pts',(3.4882177780651,1.18571239993566,7.704396607809));
#12227=CARTESIAN_POINT('Ctrl Pts',(3.44770902145391,1.12879784108382,7.70883642413074));
#12228=CARTESIAN_POINT('Ctrl Pts',(3.41030842487547,1.06994964661626,7.71327624045247));
#12229=CARTESIAN_POINT('Ctrl Pts',(3.37286834913832,1.01103933342808,7.71772074333617));
#12230=CARTESIAN_POINT('Ctrl Pts',(3.33854324457653,0.950191724505961,7.72216524621986));
#12231=CARTESIAN_POINT('Ctrl Pts',(3.30752205488232,0.887773422768894,7.72660974910356));
#12232=CARTESIAN_POINT('Ctrl Pts',(3.27648266746263,0.825318505056366,7.73105685923231));
#12233=CARTESIAN_POINT('Ctrl Pts',(3.24875124706848,0.761291509552212,7.73550396936107));
#12234=CARTESIAN_POINT('Ctrl Pts',(3.22446858451634,0.696079087291983,7.73995107948982));
#12235=CARTESIAN_POINT('Ctrl Pts',(3.20014399785965,0.630754075549302,7.74440586757026));
#12236=CARTESIAN_POINT('Ctrl Pts',(3.17928020063015,0.564240018419293,7.7488606556507));
#12237=CARTESIAN_POINT('Ctrl Pts',(3.16196789788011,0.496937995558288,7.75331544373114));
#12238=CARTESIAN_POINT('Ctrl Pts',(3.1531806013624,0.462777154007605,7.75557658393598));
#12239=CARTESIAN_POINT('Ctrl Pts',(3.14530746504828,0.428413459846191,7.75783772414082));
#12240=CARTESIAN_POINT('Ctrl Pts',(3.1383552500829,0.393899974368878,7.76009886434566));
#12241=CARTESIAN_POINT('Ctrl Pts',(3.1246561474874,0.325892327764686,7.76455436403937));
#12242=CARTESIAN_POINT('Ctrl Pts',(3.11448212774918,0.257035591591292,7.76900986373308));
#12243=CARTESIAN_POINT('Ctrl Pts',(3.10793043782018,0.187727966469484,7.77346536342679));
#12244=CARTESIAN_POINT('Ctrl Pts',(3.101388544585,0.118523976530287,7.77791420084455));
#12245=CARTESIAN_POINT('Ctrl Pts',(3.09845827621122,0.0488709189142223,
7.7823630382623));
#12246=CARTESIAN_POINT('Ctrl Pts',(3.09918584280205,-0.0208229768686858,
7.78681187568006));
#12247=CARTESIAN_POINT('Ctrl Pts',(3.09991255781813,-0.0904352999641432,
7.79125550599008));
#12248=CARTESIAN_POINT('Ctrl Pts',(3.10428859934531,-0.160087879467095,
7.79569913630009));
#12249=CARTESIAN_POINT('Ctrl Pts',(3.11230822396324,-0.229369323684002,
7.80014276661011));
#12250=CARTESIAN_POINT('Ctrl Pts',(3.12032283399215,-0.29860744692438,7.80458361836366));
#12251=CARTESIAN_POINT('Ctrl Pts',(3.13197645120835,-0.367474410441749,
7.80902447011722));
#12252=CARTESIAN_POINT('Ctrl Pts',(3.14721136618868,-0.435562316421431,
7.81346532187078));
#12253=CARTESIAN_POINT('Ctrl Pts',(3.16244192182759,-0.503630739625652,
7.81790490291236));
#12254=CARTESIAN_POINT('Ctrl Pts',(3.18125163405266,-0.57092007071881,7.82234448395394));
#12255=CARTESIAN_POINT('Ctrl Pts',(3.20353172145893,-0.637032757965206,
7.82678406499552));
#12256=CARTESIAN_POINT('Ctrl Pts',(3.22581298962126,-0.703148948921208,
7.83122388131724));
#12257=CARTESIAN_POINT('Ctrl Pts',(3.25156483958468,-0.768087909452814,
7.83566369763897));
#12258=CARTESIAN_POINT('Ctrl Pts',(3.28062923577066,-0.831469101385753,
7.8401035139607));
#12259=CARTESIAN_POINT('Ctrl Pts',(3.30972431162534,-0.894917196961157,
7.84454801684439));
#12260=CARTESIAN_POINT('Ctrl Pts',(3.34213870825378,-0.956803796527888,
7.84899251972809));
#12261=CARTESIAN_POINT('Ctrl Pts',(3.37766742110722,-1.01677103062088,7.85343702261179));
#12262=CARTESIAN_POINT('Ctrl Pts',(3.41321697590028,-1.07677344283803,7.85788413274054));
#12263=CARTESIAN_POINT('Ctrl Pts',(3.45188421208295,-1.13485384122124,7.86233124286929));
#12264=CARTESIAN_POINT('Ctrl Pts',(3.49342112260742,-1.19068387598519,7.86677835299803));
#12265=CARTESIAN_POINT('Ctrl Pts',(3.53502974675788,-1.24661030150574,7.87123314107848));
#12266=CARTESIAN_POINT('Ctrl Pts',(3.57951762271077,-1.30027823163097,7.87568792915892));
#12267=CARTESIAN_POINT('Ctrl Pts',(3.62659740700095,-1.35139351328804,7.88014271723936));
#12268=CARTESIAN_POINT('Ctrl Pts',(3.65049394061156,-1.37733836551178,7.88240385744417));
#12269=CARTESIAN_POINT('Ctrl Pts',(3.6750576598063,-1.40262617781603,7.88466499764899));
#12270=CARTESIAN_POINT('Ctrl Pts',(3.70024770244873,-1.42722243209109,7.8869261378538));
#12271=CARTESIAN_POINT('Ctrl Pts',(3.74988382277378,-1.47568851267988,7.89138163754751));
#12272=CARTESIAN_POINT('Ctrl Pts',(3.80214879930399,-1.52165733931686,7.89583713724122));
#12273=CARTESIAN_POINT('Ctrl Pts',(3.856761261163,-1.56483083292866,7.90029263693493));
#12274=CARTESIAN_POINT('Ctrl Pts',(3.91129206140881,-1.60793976953249,7.90474147435267));
#12275=CARTESIAN_POINT('Ctrl Pts',(3.96816299928352,-1.64826136837502,7.9091903117704));
#12276=CARTESIAN_POINT('Ctrl Pts',(4.02705654344727,-1.68553493700389,7.91363914918814));
#12277=CARTESIAN_POINT('Ctrl Pts',(4.08588115611273,-1.72276487906945,7.91808277949815));
#12278=CARTESIAN_POINT('Ctrl Pts',(4.1467232617324,-1.75695361631742,7.92252640980815));
#12279=CARTESIAN_POINT('Ctrl Pts',(4.20923443383318,-1.78788234494249,7.92697004011816));
#12280=CARTESIAN_POINT('Ctrl Pts',(4.27170651833915,-1.81879173415075,7.9314108918717));
#12281=CARTESIAN_POINT('Ctrl Pts',(4.33584516144208,-1.84644494226885,7.93585174362526));
#12282=CARTESIAN_POINT('Ctrl Pts',(4.401276621564,-1.87066868272014,7.94029259537881));
#12283=CARTESIAN_POINT('Ctrl Pts',(4.46668935903,-1.89488549175409,7.94473217642039));
#12284=CARTESIAN_POINT('Ctrl Pts',(4.53339372059257,-1.91567461154033,7.94917175746196));
#12285=CARTESIAN_POINT('Ctrl Pts',(4.60099688698302,-1.93291124705189,7.95361133850354));
#12286=CARTESIAN_POINT('Ctrl Pts',(4.66860363607269,-1.95014879603665,7.95805115482528));
#12287=CARTESIAN_POINT('Ctrl Pts',(4.73710880995683,-1.96383336846661,7.96249097114702));
#12288=CARTESIAN_POINT('Ctrl Pts',(4.80610709619892,-1.97389075938938,7.96693078746875));
#12289=CARTESIAN_POINT('Ctrl Pts',(4.87517821535117,-1.983958766649,7.97137529035244));
#12290=CARTESIAN_POINT('Ctrl Pts',(4.94474300074929,-1.99039187998696,7.97581979323614));
#12291=CARTESIAN_POINT('Ctrl Pts',(5.01438963566877,-1.99316764045338,7.98026429611983));
#12292=CARTESIAN_POINT('Ctrl Pts',(5.08407712686621,-1.99594502924315,7.98471140624858));
#12293=CARTESIAN_POINT('Ctrl Pts',(5.15384607390411,-1.9950608009897,7.98915851637734));
#12294=CARTESIAN_POINT('Ctrl Pts',(5.22328606227653,-1.9905446375161,7.9936056265061));
#12295=CARTESIAN_POINT('Ctrl Pts',(5.29284593903943,-1.98602067686996,7.99806041458654));
#12296=CARTESIAN_POINT('Ctrl Pts',(5.3620752377972,-1.9778523218194,8.00251520266698));
#12297=CARTESIAN_POINT('Ctrl Pts',(5.43057086477357,-1.9661208601541,8.00696999074742));
#12298=CARTESIAN_POINT('Ctrl Pts',(5.46533755024061,-1.96016626048415,8.00923113095231));
#12299=CARTESIAN_POINT('Ctrl Pts',(5.49991541391814,-1.95329449976434,8.01149227115719));
#12300=CARTESIAN_POINT('Ctrl Pts',(5.53425327092352,-1.945521112533,8.01375341136208));
#12301=CARTESIAN_POINT('Ctrl Pts',(5.60191484760934,-1.93020391798067,8.01820891105579));
#12302=CARTESIAN_POINT('Ctrl Pts',(5.66890933243172,-1.91132271575537,8.0226644107495));
#12303=CARTESIAN_POINT('Ctrl Pts',(5.73483358288269,-1.88895164641501,8.02711991044321));
#12304=CARTESIAN_POINT('Ctrl Pts',(5.8006592572862,-1.8666140283703,8.03156874786096));
#12305=CARTESIAN_POINT('Ctrl Pts',(5.8654174141304,-1.84079705662434,8.03601758527871));
#12306=CARTESIAN_POINT('Ctrl Pts',(5.928716635496,-1.81162554591552,8.04046642269646));
#12307=CARTESIAN_POINT('Ctrl Pts',(5.99194176877194,-1.78248817877837,8.04491005300647));
#12308=CARTESIAN_POINT('Ctrl Pts',(6.0537109160025,-1.75000427474488,8.04935368331648));
#12309=CARTESIAN_POINT('Ctrl Pts',(6.11365102479551,-1.71434735045716,8.05379731362648));
#12310=CARTESIAN_POINT('Ctrl Pts',(6.17355365365331,-1.67871272207847,8.05823816538004));
#12311=CARTESIAN_POINT('Ctrl Pts',(6.23162909350217,-1.63990925902836,8.06267901713359));
#12312=CARTESIAN_POINT('Ctrl Pts',(6.28752873634795,-1.59815646864416,8.06711986888714));
#12313=CARTESIAN_POINT('Ctrl Pts',(6.3434123839861,-1.556415625466,8.07155944992872));
#12314=CARTESIAN_POINT('Ctrl Pts',(6.39712107889992,-1.51172742295573,8.0759990309703));
#12315=CARTESIAN_POINT('Ctrl Pts',(6.44833654454803,-1.46435374051276,8.08043861201187));
#12316=CARTESIAN_POINT('Ctrl Pts',(6.49955472441234,-1.41697754745283,8.0848784283336));
#12317=CARTESIAN_POINT('Ctrl Pts',(6.5482790552334,-1.36691592584987,8.08931824465534));
#12318=CARTESIAN_POINT('Ctrl Pts',(6.59422693255357,-1.3144687411182,8.09375806097707));
#12319=CARTESIAN_POINT('Ctrl Pts',(6.64022331133381,-1.26196619441589,8.09820256386076));
#12320=CARTESIAN_POINT('Ctrl Pts',(6.68343706422757,-1.20707342735552,8.10264706674445));
#12321=CARTESIAN_POINT('Ctrl Pts',(6.7236254845366,-1.15012389289879,8.10709156962815));
#12322=CARTESIAN_POINT('Ctrl Pts',(6.76383748027423,-1.09314095056801,8.1115386797569));
#12323=CARTESIAN_POINT('Ctrl Pts',(6.80102035026782,-1.03409925335822,8.11598578988566));
#12324=CARTESIAN_POINT('Ctrl Pts',(6.83497591475613,-0.973359419987069,
8.12043290001441));
#12325=CARTESIAN_POINT('Ctrl Pts',(6.868990103649,-0.912514719074521,8.12488768809484));
#12326=CARTESIAN_POINT('Ctrl Pts',(6.89976564909241,-0.849966468632431,
8.12934247617528));
#12327=CARTESIAN_POINT('Ctrl Pts',(6.92715166655712,-0.786097194680931,
8.13379726425571));
#12328=CARTESIAN_POINT('Ctrl Pts',(6.94105213141024,-0.753678731539992,
8.13605840446056));
#12329=CARTESIAN_POINT('Ctrl Pts',(6.95408013091807,-0.720920206227092,
8.13831954466541));
#12330=CARTESIAN_POINT('Ctrl Pts',(6.96622088098836,-0.687873025402394,
8.14058068487025));
#12331=CARTESIAN_POINT('Ctrl Pts',(6.99377560713267,-0.612868926628099,
8.1457125835386));
#12332=CARTESIAN_POINT('Ctrl Pts',(7.01684654224403,-0.536134208834767,
8.15084448220696));
#12333=CARTESIAN_POINT('Ctrl Pts',(7.0352446347772,-0.458176530907991,8.15597638087531));
#12334=CARTESIAN_POINT('Ctrl Pts',(7.05348683700635,-0.380879402225201,
8.16106479605523));
#12335=CARTESIAN_POINT('Ctrl Pts',(7.06713495375901,-0.302380129726197,
8.16615321123516));
#12336=CARTESIAN_POINT('Ctrl Pts',(7.07605109270582,-0.223194590172708,
8.17124162641508));
#12337=CARTESIAN_POINT('Ctrl Pts',(7.0843251968989,-0.149711055566642,8.17596363418408));
#12338=CARTESIAN_POINT('Ctrl Pts',(7.08852461457797,-0.0756368410426775,
8.18068564195308));
#12339=CARTESIAN_POINT('Ctrl Pts',(7.08857666516212,-0.001398576294443,
8.18540764972207));
#12340=CARTESIAN_POINT('Ctrl Pts',(7.08857715545311,1.12756902441053E-10,
7.22671373997843));
#12341=CARTESIAN_POINT('Ctrl Pts',(7.08857715545308,0.000600191909874145,
7.22675529437358));
#12342=CARTESIAN_POINT('Ctrl Pts',(7.08857688458501,0.001200389246813,7.2267968527846));
#12343=CARTESIAN_POINT('Ctrl Pts',(7.08846930109933,0.120384606063082,7.23505003639251));
#12344=CARTESIAN_POINT('Ctrl Pts',(7.07778833453187,0.238722052384156,7.24340464028335));
#12345=CARTESIAN_POINT('Ctrl Pts',(7.0483933295436,0.401062417775733,7.2546634015799));
#12346=CARTESIAN_POINT('Ctrl Pts',(7.03853620442267,0.446416242704073,7.25778379811172));
#12347=CARTESIAN_POINT('Ctrl Pts',(7.02492514741938,0.499966438045238,7.26140695740263));
#12348=CARTESIAN_POINT('Ctrl Pts',(7.02268779594919,0.508529773151547,7.26198445172257));
#12349=CARTESIAN_POINT('Ctrl Pts',(7.01893366488793,0.522517180831181,7.26292431479112));
#12350=CARTESIAN_POINT('Ctrl Pts',(7.01745080708027,0.527950116687992,7.26328852514501));
#12351=CARTESIAN_POINT('Ctrl Pts',(7.01474251371937,0.537709931944364,7.2639411816215));
#12352=CARTESIAN_POINT('Ctrl Pts',(7.01352544340598,0.542038992091794,7.26423009324422));
#12353=CARTESIAN_POINT('Ctrl Pts',(7.01081919381303,0.551541537905058,7.26486299271094));
#12354=CARTESIAN_POINT('Ctrl Pts',(7.00932370929607,0.556713119141431,7.26520661324837));
#12355=CARTESIAN_POINT('Ctrl Pts',(7.00496192540704,0.571571073988756,7.26619163387933));
#12356=CARTESIAN_POINT('Ctrl Pts',(7.00204291190497,0.581241979285742,7.26683007711997));
#12357=CARTESIAN_POINT('Ctrl Pts',(6.98031705892309,0.651293198308156,7.2714378283084));
#12358=CARTESIAN_POINT('Ctrl Pts',(6.95871963766281,0.71077756033698,7.27525995311493));
#12359=CARTESIAN_POINT('Ctrl Pts',(6.88373654286131,0.890207073890386,7.28679238951352));
#12360=CARTESIAN_POINT('Ctrl Pts',(6.82132055658072,1.00598883967134,7.29425803174684));
#12361=CARTESIAN_POINT('Ctrl Pts',(6.6984808400835,1.18825925284503,7.30719065598847));
#12362=CARTESIAN_POINT('Ctrl Pts',(6.64414592038585,1.25832522383765,7.31249906724981));
#12363=CARTESIAN_POINT('Ctrl Pts',(6.57495116503624,1.33624249689079,7.31896634895358));
#12364=CARTESIAN_POINT('Ctrl Pts',(6.56442532463618,1.347817994155,7.31994277350658));
#12365=CARTESIAN_POINT('Ctrl Pts',(6.54691962807049,1.36662018644199,7.32155546264852));
#12366=CARTESIAN_POINT('Ctrl Pts',(6.54001928463785,1.37392022604434,7.32218836516292));
#12367=CARTESIAN_POINT('Ctrl Pts',(6.52749887922954,1.38696703480958,7.32333195418898));
#12368=CARTESIAN_POINT('Ctrl Pts',(6.52189862729725,1.39273257857758,7.32384178024818));
#12369=CARTESIAN_POINT('Ctrl Pts',(6.50986694905094,1.40497050447237,7.32493361021595));
#12370=CARTESIAN_POINT('Ctrl Pts',(6.50342567147932,1.41143290118953,7.32551603937571));
#12371=CARTESIAN_POINT('Ctrl Pts',(6.48584348276125,1.42883233524096,7.32710036618503));
#12372=CARTESIAN_POINT('Ctrl Pts',(6.47461832589639,1.43968295761348,7.3281059901386));
#12373=CARTESIAN_POINT('Ctrl Pts',(6.41403096413897,1.49688837313351,7.33350402032759));
#12374=CARTESIAN_POINT('Ctrl Pts',(6.36246492436985,1.54083397270196,7.3379967066575));
#12375=CARTESIAN_POINT('Ctrl Pts',(6.17799495329815,1.682496773064,7.35373829720515));
#12376=CARTESIAN_POINT('Ctrl Pts',(6.03529388424404,1.76630838208587,7.3654295189683));
#12377=CARTESIAN_POINT('Ctrl Pts',(5.83481356114489,1.85278898690861,7.38039672863195));
#12378=CARTESIAN_POINT('Ctrl Pts',(5.7848687125538,1.87199106464918,7.38400924316252));
#12379=CARTESIAN_POINT('Ctrl Pts',(5.72548266043479,1.89212149819018,7.38812420732276));
#12380=CARTESIAN_POINT('Ctrl Pts',(5.71673678756077,1.89501874366896,7.38872570927152));
#12381=CARTESIAN_POINT('Ctrl Pts',(5.70250861971097,1.89962296236539,7.38969659325848));
#12382=CARTESIAN_POINT('Ctrl Pts',(5.69703859263579,1.90136700510846,7.39006802040016));
#12383=CARTESIAN_POINT('Ctrl Pts',(5.68726464021795,1.90443687060614,7.3907283379507));
#12384=CARTESIAN_POINT('Ctrl Pts',(5.68296368896756,1.90577175670558,7.39101774437718));
#12385=CARTESIAN_POINT('Ctrl Pts',(5.67359471356587,1.90864485699751,7.39164563756338));
#12386=CARTESIAN_POINT('Ctrl Pts',(5.66852507578857,1.91017745602564,7.39198379872935));
#12387=CARTESIAN_POINT('Ctrl Pts',(5.65416064776527,1.91445759412602,7.39293759477621));
#12388=CARTESIAN_POINT('Ctrl Pts',(5.64485170124714,1.91715765163288,7.39355055719189));
#12389=CARTESIAN_POINT('Ctrl Pts',(5.58457301697503,1.93416614183261,7.39748870606577));
#12390=CARTESIAN_POINT('Ctrl Pts',(5.53306566810787,1.94650989444179,7.40071117194312));
#12391=CARTESIAN_POINT('Ctrl Pts',(5.316016896263,1.98946911779409,7.41393018360304));
#12392=CARTESIAN_POINT('Ctrl Pts',(5.1474344918077,2.00112184492285,7.42339052563864));
#12393=CARTESIAN_POINT('Ctrl Pts',(4.91459359733022,1.98774101111655,7.43728752965647));
#12394=CARTESIAN_POINT('Ctrl Pts',(4.8500310272001,1.98085869272376,7.44122235796352));
#12395=CARTESIAN_POINT('Ctrl Pts',(4.77024006774156,1.96839297826526,7.44624286507685));
#12396=CARTESIAN_POINT('Ctrl Pts',(4.75458730219337,1.96575578833853,7.44723527352566));
#12397=CARTESIAN_POINT('Ctrl Pts',(4.72984233003675,1.96128238897049,7.44881679696032));
#12398=CARTESIAN_POINT('Ctrl Pts',(4.72072837970652,1.95956904988819,7.44940202732317));
#12399=CARTESIAN_POINT('Ctrl Pts',(4.70375271560743,1.95625505967262,7.45049732163637));
#12400=CARTESIAN_POINT('Ctrl Pts',(4.69588804213954,1.95467040345492,7.45100686837202));
#12401=CARTESIAN_POINT('Ctrl Pts',(4.67840016082486,1.95103684660869,7.4521446887413));
#12402=CARTESIAN_POINT('Ctrl Pts',(4.66878217230397,1.94896411492892,7.45277370952778));
#12403=CARTESIAN_POINT('Ctrl Pts',(4.64066144006187,1.94268588033353,7.45462252927555));
#12404=CARTESIAN_POINT('Ctrl Pts',(4.62220331534612,1.93828751932807,7.45584843802616));
#12405=CARTESIAN_POINT('Ctrl Pts',(4.48260811133525,1.90291157444481,7.46521664367364));
#12406=CARTESIAN_POINT('Ctrl Pts',(4.36458306180081,1.86087455792052,7.4737202764263));
#12407=CARTESIAN_POINT('Ctrl Pts',(4.1273376369796,1.75032134594481,7.49188857337727));
#12408=CARTESIAN_POINT('Ctrl Pts',(4.00965262147061,1.67996900407864,7.50154024703534));
#12409=CARTESIAN_POINT('Ctrl Pts',(3.88165289119638,1.58435807810279,7.51222073634554));
#12410=CARTESIAN_POINT('Ctrl Pts',(3.8634576690243,1.57027004122678,7.51374293388061));
#12411=CARTESIAN_POINT('Ctrl Pts',(3.83948962705213,1.55103980990285,7.51574901237472));
#12412=CARTESIAN_POINT('Ctrl Pts',(3.83349783549211,1.54617500206067,7.51625059187154));
#12413=CARTESIAN_POINT('Ctrl Pts',(3.82415117335156,1.53849590005424,7.51703293252671));
#12414=CARTESIAN_POINT('Ctrl Pts',(3.82077715485614,1.53570519009544,7.51731533063023));
#12415=CARTESIAN_POINT('Ctrl Pts',(3.81390526705266,1.52998312058331,7.51789041106131));
#12416=CARTESIAN_POINT('Ctrl Pts',(3.81040825976877,1.5270508597377,7.51818300937065));
#12417=CARTESIAN_POINT('Ctrl Pts',(3.80215239364931,1.5200798759383,7.51887372916558));
#12418=CARTESIAN_POINT('Ctrl Pts',(3.79740232621506,1.51603073324984,7.51927109843413));
#12419=CARTESIAN_POINT('Ctrl Pts',(3.78162170816747,1.50245031203677,7.52059140226085));
#12420=CARTESIAN_POINT('Ctrl Pts',(3.770676341725,1.49282015971812,7.52150743574005));
#12421=CARTESIAN_POINT('Ctrl Pts',(3.70966727997524,1.43794382381555,7.52662150516241));
#12422=CARTESIAN_POINT('Ctrl Pts',(3.66181414125883,1.39029551515154,7.53066467284083));
#12423=CARTESIAN_POINT('Ctrl Pts',(3.50176865881665,1.21388442307065,7.54470041148724));
#12424=CARTESIAN_POINT('Ctrl Pts',(3.40377855382796,1.07326733954188,7.55433997793486));
#12425=CARTESIAN_POINT('Ctrl Pts',(3.30451813096039,0.882804188253043,7.56732597241304));
#12426=CARTESIAN_POINT('Ctrl Pts',(3.28545151715098,0.843058201071235,7.5700277931325));
#12427=CARTESIAN_POINT('Ctrl Pts',(3.26203940070591,0.789797632278761,7.57365434516304));
#12428=CARTESIAN_POINT('Ctrl Pts',(3.25649834857213,0.776820132121396,7.57453841837982));
#12429=CARTESIAN_POINT('Ctrl Pts',(3.24772797026515,0.755660448273479,7.57598107488438));
#12430=CARTESIAN_POINT('Ctrl Pts',(3.24441419772565,0.747513626916368,7.57653680211545));
#12431=CARTESIAN_POINT('Ctrl Pts',(3.23814911312386,0.731814397028634,7.57760837056788));
#12432=CARTESIAN_POINT('Ctrl Pts',(3.23518975720093,0.724265370652425,7.57812392938153));
#12433=CARTESIAN_POINT('Ctrl Pts',(3.22845157753333,0.706763644744733,7.57931997970669));
#12434=CARTESIAN_POINT('Ctrl Pts',(3.22470626769621,0.696798389737538,7.580001571668));
#12435=CARTESIAN_POINT('Ctrl Pts',(3.21307895282669,0.665092864707059,7.58217221998937));
#12436=CARTESIAN_POINT('Ctrl Pts',(3.20549537075811,0.643245922617052,7.5836710482719));
#12437=CARTESIAN_POINT('Ctrl Pts',(3.16887203689989,0.531506348518307,7.5913557999887));
#12438=CARTESIAN_POINT('Ctrl Pts',(3.14586828773197,0.439776077536353,7.59773403576874));
#12439=CARTESIAN_POINT('Ctrl Pts',(3.10938169734766,0.233089039633766,7.61219694062287));
#12440=CARTESIAN_POINT('Ctrl Pts',(3.09922025961846,0.117882804479479,7.62032354062417));
#12441=CARTESIAN_POINT('Ctrl Pts',(3.09905898623916,-0.0135881838842559,
7.62938162180226));
#12442=CARTESIAN_POINT('Ctrl Pts',(3.09923266791226,-0.0296232678572957,
7.63048243732483));
#12443=CARTESIAN_POINT('Ctrl Pts',(3.10070229976475,-0.0938175958722112,
7.63486961836063));
#12444=CARTESIAN_POINT('Ctrl Pts',(3.10354943996742,-0.141929141577623,
7.63811334000337));
#12445=CARTESIAN_POINT('Ctrl Pts',(3.10898784104279,-0.198797508202418,
7.64186018613473));
#12446=CARTESIAN_POINT('Ctrl Pts',(3.10989914782426,-0.207695019061908,
7.64244385633825));
#12447=CARTESIAN_POINT('Ctrl Pts',(3.11148482923736,-0.222212732893909,
7.6433917091354));
#12448=CARTESIAN_POINT('Ctrl Pts',(3.11212332384377,-0.227836613952299,
7.64375778483184));
#12449=CARTESIAN_POINT('Ctrl Pts',(3.11331221260484,-0.237925109660984,
7.64441240161624));
#12450=CARTESIAN_POINT('Ctrl Pts',(3.11385377702376,-0.242390632215528,
7.64470142130376));
#12451=CARTESIAN_POINT('Ctrl Pts',(3.11507373683139,-0.252172951390316,
7.64533293744749));
#12452=CARTESIAN_POINT('Ctrl Pts',(3.1157584557532,-0.257488854138161,7.64567507781246));
#12453=CARTESIAN_POINT('Ctrl Pts',(3.11778073763001,-0.272704812716511,
7.64665159452664));
#12454=CARTESIAN_POINT('Ctrl Pts',(3.11917127810093,-0.282597834558267,
7.64728309280997));
#12455=CARTESIAN_POINT('Ctrl Pts',(3.12945229288826,-0.351957756811089,
7.65168921556053));
#12456=CARTESIAN_POINT('Ctrl Pts',(3.14095415393568,-0.4110126672403,7.65533092965514));
#12457=CARTESIAN_POINT('Ctrl Pts',(3.17683776130088,-0.559199402976622,
7.66439188835514));
#12458=CARTESIAN_POINT('Ctrl Pts',(3.20477253058801,-0.647322581658998,
7.66971147220542));
#12459=CARTESIAN_POINT('Ctrl Pts',(3.28637826284454,-0.853799134393472,
7.68261682854989));
#12460=CARTESIAN_POINT('Ctrl Pts',(3.34568332038866,-0.969448930436627,
7.69023426476554));
#12461=CARTESIAN_POINT('Ctrl Pts',(3.4245543767293,-1.09216253350547,7.69928041885801));
#12462=CARTESIAN_POINT('Ctrl Pts',(3.43348935738593,-1.10569841348626,7.70029202123762));
#12463=CARTESIAN_POINT('Ctrl Pts',(3.44832124857513,-1.12758250026291,7.70195095958232));
#12464=CARTESIAN_POINT('Ctrl Pts',(3.45411912372077,-1.13599716061122,7.70259459130304));
#12465=CARTESIAN_POINT('Ctrl Pts',(3.46460209568651,-1.15096400559889,7.70374992511146));
#12466=CARTESIAN_POINT('Ctrl Pts',(3.46926273877118,-1.15753310557866,7.70426069080376));
#12467=CARTESIAN_POINT('Ctrl Pts',(3.47922387408791,-1.17139450104773,7.70534637675932));
#12468=CARTESIAN_POINT('Ctrl Pts',(3.48453425931719,-1.17867943196744,7.70592166965179));
#12469=CARTESIAN_POINT('Ctrl Pts',(3.49887886925119,-1.19808010247063,7.70746654768593));
#12470=CARTESIAN_POINT('Ctrl Pts',(3.50800156811642,-1.2101293952983,7.70843954912044));
#12471=CARTESIAN_POINT('Ctrl Pts',(3.55440252110325,-1.26999012228401,7.71334273963552));
#12472=CARTESIAN_POINT('Ctrl Pts',(3.59370643402031,-1.31618374394274,7.71735248324679));
#12473=CARTESIAN_POINT('Ctrl Pts',(3.72219952978876,-1.45395748255061,7.73004589455525));
#12474=CARTESIAN_POINT('Ctrl Pts',(3.81811925593308,-1.53880385495083,7.7389786311471));
#12475=CARTESIAN_POINT('Ctrl Pts',(4.00009499929227,-1.67099354149216,7.75463566391836));
#12476=CARTESIAN_POINT('Ctrl Pts',(4.082788992514,-1.72228793169034,7.76134804747826));
#12477=CARTESIAN_POINT('Ctrl Pts',(4.17856517640783,-1.77241136158735,7.76845251611215));
#12478=CARTESIAN_POINT('Ctrl Pts',(4.18827038008275,-1.77738950833605,7.76916506839146));
#12479=CARTESIAN_POINT('Ctrl Pts',(4.20304024411531,-1.7848131159357,7.77023781296761));
#12480=CARTESIAN_POINT('Ctrl Pts',(4.20807503233778,-1.78731708392591,7.77060145780591));
#12481=CARTESIAN_POINT('Ctrl Pts',(4.2171549500782,-1.79178503889408,7.77125352291199));
#12482=CARTESIAN_POINT('Ctrl Pts',(4.22119617175201,-1.79375665817198,7.77154240470188));
#12483=CARTESIAN_POINT('Ctrl Pts',(4.23009697626533,-1.79806195658588,7.7721757367278));
#12484=CARTESIAN_POINT('Ctrl Pts',(4.23495935952318,-1.80038960586883,7.77251981619273));
#12485=CARTESIAN_POINT('Ctrl Pts',(4.24899141502858,-1.80703704311368,7.77350747950672));
#12486=CARTESIAN_POINT('Ctrl Pts',(4.25818481314968,-1.81130676293157,7.77414808181425));
#12487=CARTESIAN_POINT('Ctrl Pts',(4.32590243563476,-1.84213175348497,7.77882212642475));
#12488=CARTESIAN_POINT('Ctrl Pts',(4.38565345086151,-1.86591789088091,7.78270352559359));
#12489=CARTESIAN_POINT('Ctrl Pts',(4.57596206307224,-1.93121462403671,7.79462719138739));
#12490=CARTESIAN_POINT('Ctrl Pts',(4.70970219905284,-1.96219901981723,7.80240512551316));
#12491=CARTESIAN_POINT('Ctrl Pts',(4.9271840764416,-1.98947831170805,7.81533992358522));
#12492=CARTESIAN_POINT('Ctrl Pts',(5.00934827425976,-1.994656563911,7.82028474325504));
#12493=CARTESIAN_POINT('Ctrl Pts',(5.10699659190726,-1.99476601414574,7.82634703418628));
#12494=CARTESIAN_POINT('Ctrl Pts',(5.1224011998441,-1.99460482013604,7.82730871462794));
#12495=CARTESIAN_POINT('Ctrl Pts',(5.14777159253123,-1.99404538563801,7.82890199393496));
#12496=CARTESIAN_POINT('Ctrl Pts',(5.15773918133644,-1.99375079923028,7.8295303697587));
#12497=CARTESIAN_POINT('Ctrl Pts',(5.1757302081478,-1.99308403259137,7.8306690755864));
#12498=CARTESIAN_POINT('Ctrl Pts',(5.18375444993668,-1.99273810362685,7.83117857718081));
#12499=CARTESIAN_POINT('Ctrl Pts',(5.2009398908741,-1.99189321976894,7.83227334636384));
#12500=CARTESIAN_POINT('Ctrl Pts',(5.21010014677491,-1.99137950273603,7.83285906297571));
#12501=CARTESIAN_POINT('Ctrl Pts',(5.23506781679531,-1.98980643056041,7.83446162202954));
#12502=CARTESIAN_POINT('Ctrl Pts',(5.25086640514954,-1.9886219363252,7.83548233790329));
#12503=CARTESIAN_POINT('Ctrl Pts',(5.33775551433902,-1.98106560135035,7.84113413887891));
#12504=CARTESIAN_POINT('Ctrl Pts',(5.40847084081499,-1.97107058257865,7.84587716745047));
#12505=CARTESIAN_POINT('Ctrl Pts',(5.6726362358696,-1.91915486044602,7.86413779330567));
#12506=CARTESIAN_POINT('Ctrl Pts',(5.85999553274186,-1.85233605605529,7.87833316509535));
#12507=CARTESIAN_POINT('Ctrl Pts',(6.05345619596284,-1.74888660180752,7.89297430662287));
#12508=CARTESIAN_POINT('Ctrl Pts',(6.07230043743263,-1.73841375062501,7.89439864503102));
#12509=CARTESIAN_POINT('Ctrl Pts',(6.09748686678872,-1.72387683068597,7.89629622203952));
#12510=CARTESIAN_POINT('Ctrl Pts',(6.1039804474656,-1.72007978725546,7.89678489665242));
#12511=CARTESIAN_POINT('Ctrl Pts',(6.1141862787711,-1.71403432129829,7.89755186280676));
#12512=CARTESIAN_POINT('Ctrl Pts',(6.11791285585614,-1.71181040837794,7.8978316868636));
#12513=CARTESIAN_POINT('Ctrl Pts',(6.12548242906986,-1.70725954134041,7.89839956584807));
#12514=CARTESIAN_POINT('Ctrl Pts',(6.12932483702202,-1.70493175725099,7.89868755123272));
#12515=CARTESIAN_POINT('Ctrl Pts',(6.13842358379824,-1.69937750447354,7.89936890451943));
#12516=CARTESIAN_POINT('Ctrl Pts',(6.14367293749366,-1.69613956889572,7.89976153193726));
#12517=CARTESIAN_POINT('Ctrl Pts',(6.15484709329693,-1.68917531360146,7.90059649649099));
#12518=CARTESIAN_POINT('Ctrl Pts',(6.16076749060382,-1.68544204087414,7.90103839491648));
#12519=CARTESIAN_POINT('Ctrl Pts',(6.17697301819635,-1.67510358171146,7.90224697853333));
#12520=CARTESIAN_POINT('Ctrl Pts',(6.18721745786905,-1.66843478513719,7.90300988275566));
#12521=CARTESIAN_POINT('Ctrl Pts',(6.21995579059073,-1.64669214219128,7.90544652243883));
#12522=CARTESIAN_POINT('Ctrl Pts',(6.24220513610413,-1.63125377295922,7.90710037292865));
#12523=CARTESIAN_POINT('Ctrl Pts',(6.33917146107056,-1.56100322148526,7.91433121135577));
#12524=CARTESIAN_POINT('Ctrl Pts',(6.41033540763591,-1.50147332450867,7.9197038438506));
#12525=CARTESIAN_POINT('Ctrl Pts',(6.57773991937719,-1.34035023714681,7.93319125840135));
#12526=CARTESIAN_POINT('Ctrl Pts',(6.66790995192704,-1.23320451905554,7.94130122088101));
#12527=CARTESIAN_POINT('Ctrl Pts',(6.75990306235257,-1.09718800246761,7.95140475770934));
#12528=CARTESIAN_POINT('Ctrl Pts',(6.77328161495573,-1.07659791797566,7.95292844054435));
#12529=CARTESIAN_POINT('Ctrl Pts',(6.79161112533453,-1.04721475944494,7.9550973864577));
#12530=CARTESIAN_POINT('Ctrl Pts',(6.79688100405623,-1.0386225221909,7.95573098361736));
#12531=CARTESIAN_POINT('Ctrl Pts',(6.80596326563009,-1.02355942823479,7.95684080628152));
#12532=CARTESIAN_POINT('Ctrl Pts',(6.80980467580243,-1.01710624324983,7.95731596791938));
#12533=CARTESIAN_POINT('Ctrl Pts',(6.81778513585097,-1.00352596878321,7.95831537078586));
#12534=CARTESIAN_POINT('Ctrl Pts',(6.82191663075262,-0.996394625749096,
7.95883987254407));
#12535=CARTESIAN_POINT('Ctrl Pts',(6.83168232875221,-0.979294682021079,
7.9600969236779));
#12536=CARTESIAN_POINT('Ctrl Pts',(6.8372750721431,-0.969302857917051,7.96083093701832));
#12537=CARTESIAN_POINT('Ctrl Pts',(6.85614227444794,-0.934903686414441,
7.96335657219048));
#12538=CARTESIAN_POINT('Ctrl Pts',(6.86899217847674,-0.910268363729511,
7.9651630344857));
#12539=CARTESIAN_POINT('Ctrl Pts',(6.89875827024245,-0.850173104793242,
7.96956636078178));
#12540=CARTESIAN_POINT('Ctrl Pts',(6.91514902314378,-0.814467279397957,
7.97218000464471));
#12541=CARTESIAN_POINT('Ctrl Pts',(6.98422589300265,-0.651458957983918,
7.98409941527029));
#12542=CARTESIAN_POINT('Ctrl Pts',(7.02468777710179,-0.519398848269831,
7.99375656232509));
#12543=CARTESIAN_POINT('Ctrl Pts',(7.06467948136437,-0.315676379723536,
8.00818527300753));
#12544=CARTESIAN_POINT('Ctrl Pts',(7.07452871502381,-0.24644146029606,8.01300296490859));
#12545=CARTESIAN_POINT('Ctrl Pts',(7.08287314268722,-0.152680442555139,
8.01930439382029));
#12546=CARTESIAN_POINT('Ctrl Pts',(7.08458189267994,-0.128494977962203,
8.02090984207486));
#12547=CARTESIAN_POINT('Ctrl Pts',(7.08626098899028,-0.0964207821697378,
8.02300737035582));
#12548=CARTESIAN_POINT('Ctrl Pts',(7.08662604207885,-0.0885559184528152,
8.02351918939281));
#12549=CARTESIAN_POINT('Ctrl Pts',(7.0871425850431,-0.075796664057269,8.02434522295565));
#12550=CARTESIAN_POINT('Ctrl Pts',(7.08732263218961,-0.0709036078754027,
8.02466097505791));
#12551=CARTESIAN_POINT('Ctrl Pts',(7.08762640566968,-0.0617289157230825,
8.02525104179397));
#12552=CARTESIAN_POINT('Ctrl Pts',(7.08775435916531,-0.0574475049421949,
8.02552558446984));
#12553=CARTESIAN_POINT('Ctrl Pts',(7.08798983547183,-0.0486156896671062,
8.02609029333832));
#12554=CARTESIAN_POINT('Ctrl Pts',(7.08809557651759,-0.044065240109889,
8.02638036173127));
#12555=CARTESIAN_POINT('Ctrl Pts',(7.08831313844747,-0.0330845257221766,
8.02707826876798));
#12556=CARTESIAN_POINT('Ctrl Pts',(7.08840944041291,-0.0266539558067715,
8.02748527688118));
#12557=CARTESIAN_POINT('Ctrl Pts',(7.0885412802017,-0.0136502073555671,
8.0283050782654));
#12558=CARTESIAN_POINT('Ctrl Pts',(7.08857543142776,-0.00707710677330047,
8.0287177952261));
#12559=CARTESIAN_POINT('Ctrl Pts',(7.08857709181481,-0.000503870024376882,
8.02912895344979));
#12560=CARTESIAN_POINT('Origin',(5.09382715545311,0.,-6.77268258743872));
#12561=CARTESIAN_POINT('',(7.08857715545311,-2.42987105381791E-11,8.98643389536848));
#12562=CARTESIAN_POINT('',(7.08857715545311,2.37118846529926E-11,8.82627928344061));
#12563=CARTESIAN_POINT('',(7.08857715545311,8.3550772080578E-14,-6.77268258743872));
#12564=CARTESIAN_POINT('Ctrl Pts',(7.08857715545311,-2.42987105381791E-11,
8.98643389536847));
#12565=CARTESIAN_POINT('Ctrl Pts',(7.08857715545217,-0.0768861299635129,
8.98188427170841));
#12566=CARTESIAN_POINT('Ctrl Pts',(7.08413199158264,-0.153700434669362,
8.97725037645284));
#12567=CARTESIAN_POINT('Ctrl Pts',(7.07351340805477,-0.245154605042594,
8.97153280431997));
#12568=CARTESIAN_POINT('Ctrl Pts',(7.07158860162889,-0.260226980213967,
8.97058406073964));
#12569=CARTESIAN_POINT('Ctrl Pts',(7.06812460096116,-0.28508826224742,8.96900782365654));
#12570=CARTESIAN_POINT('Ctrl Pts',(7.06668430181189,-0.294890479652502,
8.96838343332432));
#12571=CARTESIAN_POINT('Ctrl Pts',(7.06394499586537,-0.312614284625093,
8.96724898751005));
#12572=CARTESIAN_POINT('Ctrl Pts',(7.06267107287381,-0.320539579195344,
8.96673973220162));
#12573=CARTESIAN_POINT('Ctrl Pts',(7.05983097379962,-0.337552339224633,
8.96564218571651));
#12574=CARTESIAN_POINT('Ctrl Pts',(7.05824955293433,-0.346637036464673,
8.96505342371758));
#12575=CARTESIAN_POINT('Ctrl Pts',(7.053741860145,-0.371510086450372,8.96343393333251));
#12576=CARTESIAN_POINT('Ctrl Pts',(7.05068790132971,-0.387274308890986,
8.96239919267632));
#12577=CARTESIAN_POINT('Ctrl Pts',(7.03228433285138,-0.476489098409318,
8.95649455301054));
#12578=CARTESIAN_POINT('Ctrl Pts',(7.01299192665855,-0.549055805456616,
8.95150037752538));
#12579=CARTESIAN_POINT('Ctrl Pts',(6.95814209236811,-0.716679030325624,
8.9395123392995));
#12580=CARTESIAN_POINT('Ctrl Pts',(6.91933047072042,-0.810452754549243,
8.93244409452282));
#12581=CARTESIAN_POINT('Ctrl Pts',(6.84845799928886,-0.950467878084056,
8.92150726084807));
#12582=CARTESIAN_POINT('Ctrl Pts',(6.82128563742958,-0.999002620037872,
8.91764134562758));
#12583=CARTESIAN_POINT('Ctrl Pts',(6.76423917224009,-1.09159354332584,8.91018762972556));
#12584=CARTESIAN_POINT('Ctrl Pts',(6.73455768588789,-1.13571879224412,8.90659804740044));
#12585=CARTESIAN_POINT('Ctrl Pts',(6.69771101177791,-1.18603067177925,8.90250575321088));
#12586=CARTESIAN_POINT('Ctrl Pts',(6.69222450047737,-1.19341447708133,8.90190519378536));
#12587=CARTESIAN_POINT('Ctrl Pts',(6.6832335745464,-1.20534132506341,8.90093552576006));
#12588=CARTESIAN_POINT('Ctrl Pts',(6.67976036659062,-1.20990756950831,8.90056438021396));
#12589=CARTESIAN_POINT('Ctrl Pts',(6.67352589512187,-1.21803108808302,8.89990436535768));
#12590=CARTESIAN_POINT('Ctrl Pts',(6.67077224487407,-1.22159405119846,8.89961498199324));
#12591=CARTESIAN_POINT('Ctrl Pts',(6.66475168736986,-1.22932980134138,8.89898691034954));
#12592=CARTESIAN_POINT('Ctrl Pts',(6.66148021211496,-1.23349890188389,8.89864854921027));
#12593=CARTESIAN_POINT('Ctrl Pts',(6.65216926067984,-1.24526771183702,8.89769361584132));
#12594=CARTESIAN_POINT('Ctrl Pts',(6.646090772534,-1.25283656682012,8.89707972620055));
#12595=CARTESIAN_POINT('Ctrl Pts',(6.60630112023768,-1.3016479610396,8.89312019398319));
#12596=CARTESIAN_POINT('Ctrl Pts',(6.5710015160374,-1.34157441475001,8.88987856237572));
#12597=CARTESIAN_POINT('Ctrl Pts',(6.41543092826237,-1.50393940045418,8.87644751630348));
#12598=CARTESIAN_POINT('Ctrl Pts',(6.28122789122965,-1.61200392653529,8.8668121835552));
#12599=CARTESIAN_POINT('Ctrl Pts',(6.08222164566746,-1.7337558050609,8.85288298244007));
#12600=CARTESIAN_POINT('Ctrl Pts',(6.0281408006372,-1.76348795104782,8.84913668845719));
#12601=CARTESIAN_POINT('Ctrl Pts',(5.95872411697379,-1.79756105232033,8.8443280146994));
#12602=CARTESIAN_POINT('Ctrl Pts',(5.94459477265088,-1.80429125435264,8.8433493291224));
#12603=CARTESIAN_POINT('Ctrl Pts',(5.92201562471875,-1.81472214911176,8.84178481800752));
#12604=CARTESIAN_POINT('Ctrl Pts',(5.91361663478611,-1.81853177703217,8.84120273539858));
#12605=CARTESIAN_POINT('Ctrl Pts',(5.89785871807872,-1.82554792883914,8.84011029408799));
#12606=CARTESIAN_POINT('Ctrl Pts',(5.89050624404744,-1.82876855312802,8.83960042894666));
#12607=CARTESIAN_POINT('Ctrl Pts',(5.87403734417291,-1.83586430539414,8.83845795776896));
#12608=CARTESIAN_POINT('Ctrl Pts',(5.86491113754304,-1.83971605774887,8.83782457530857));
#12609=CARTESIAN_POINT('Ctrl Pts',(5.83791797043586,-1.85087249779595,8.83595013619377));
#12610=CARTESIAN_POINT('Ctrl Pts',(5.81997365093233,-1.85798583629272,8.83470270957932));
#12611=CARTESIAN_POINT('Ctrl Pts',(5.67579446958418,-1.91273248849412,8.8246661210579));
#12612=CARTESIAN_POINT('Ctrl Pts',(5.54514922678451,-1.94769798420551,8.81545195342419));
#12613=CARTESIAN_POINT('Ctrl Pts',(5.27710185000606,-1.99100742935538,8.79656440894279));
#12614=CARTESIAN_POINT('Ctrl Pts',(5.14031192627656,-1.99888591023311,8.78694140782125));
#12615=CARTESIAN_POINT('Ctrl Pts',(4.98855948659348,-1.99202874351317,8.77688607469454));
#12616=CARTESIAN_POINT('Ctrl Pts',(4.97334360153486,-1.99116637774985,8.7758851352434));
#12617=CARTESIAN_POINT('Ctrl Pts',(4.95224861962275,-1.98972810537196,8.77450892526519));
#12618=CARTESIAN_POINT('Ctrl Pts',(4.94636040498974,-1.98930037318386,8.77412602747462));
#12619=CARTESIAN_POINT('Ctrl Pts',(4.93623658102202,-1.98851976016467,8.77346993339159));
#12620=CARTESIAN_POINT('Ctrl Pts',(4.9320000817217,-1.9881794749837,8.77319605286148));
#12621=CARTESIAN_POINT('Ctrl Pts',(4.92313063702136,-1.98743852359684,8.77262411986344));
#12622=CARTESIAN_POINT('Ctrl Pts',(4.91849796176131,-1.98703519367603,8.77232622689462));
#12623=CARTESIAN_POINT('Ctrl Pts',(4.90716917715524,-1.98600895933872,8.77159971891355));
#12624=CARTESIAN_POINT('Ctrl Pts',(4.90047464752232,-1.98536837846942,8.77117207988868));
#12625=CARTESIAN_POINT('Ctrl Pts',(4.87629143783103,-1.98293087377884,8.76963293400567));
#12626=CARTESIAN_POINT('Ctrl Pts',(4.85882287030421,-1.9809365649555,8.76853183143856));
#12627=CARTESIAN_POINT('Ctrl Pts',(4.8152676773671,-1.97537977394779,8.7658080336922));
#12628=CARTESIAN_POINT('Ctrl Pts',(4.78922033401845,-1.97153124558076,8.76419856240537));
#12629=CARTESIAN_POINT('Ctrl Pts',(4.67637425800728,-1.95256809490912,8.75728106926091));
#12630=CARTESIAN_POINT('Ctrl Pts',(4.59054866339174,-1.93222727146068,8.75215976658576));
#12631=CARTESIAN_POINT('Ctrl Pts',(4.36699907829934,-1.86333292842259,8.73857743293405));
#12632=CARTESIAN_POINT('Ctrl Pts',(4.23280010509147,-1.80524654918499,8.73013619328223));
#12633=CARTESIAN_POINT('Ctrl Pts',(4.08454018405959,-1.72075134202396,8.71963392253941));
#12634=CARTESIAN_POINT('Ctrl Pts',(4.06317795220974,-1.70804200961265,8.71809097209041));
#12635=CARTESIAN_POINT('Ctrl Pts',(4.03367942197034,-1.68973714296457,8.71591571796825));
#12636=CARTESIAN_POINT('Ctrl Pts',(4.02533816647287,-1.68447502325769,8.71529554036448));
#12637=CARTESIAN_POINT('Ctrl Pts',(4.0101303712653,-1.67472270789988,8.71415529517673));
#12638=CARTESIAN_POINT('Ctrl Pts',(4.00325182098143,-1.67025156937388,8.71363593817461));
#12639=CARTESIAN_POINT('Ctrl Pts',(3.98936166952506,-1.66110042311804,8.71257971012247));
#12640=CARTESIAN_POINT('Ctrl Pts',(3.98235176873429,-1.6564181496325,8.71204276171826));
#12641=CARTESIAN_POINT('Ctrl Pts',(3.96509700138599,-1.64473395526746,8.71071126044905));
#12642=CARTESIAN_POINT('Ctrl Pts',(3.95488750244197,-1.63768067693914,8.70991478427794));
#12643=CARTESIAN_POINT('Ctrl Pts',(3.9167818972426,-1.61082658013847,8.7069089165668));
#12644=CARTESIAN_POINT('Ctrl Pts',(3.88933221577727,-1.59040545544929,8.70467602557586));
#12645=CARTESIAN_POINT('Ctrl Pts',(3.82155136846083,-1.53721855601956,8.69898560827842));
#12646=CARTESIAN_POINT('Ctrl Pts',(3.78195187679679,-1.50356545217721,8.69549548243061));
#12647=CARTESIAN_POINT('Ctrl Pts',(3.66016408295872,-1.39158879677805,8.68422825200392));
#12648=CARTESIAN_POINT('Ctrl Pts',(3.58332816119793,-1.30778376583525,8.67627827189778));
#12649=CARTESIAN_POINT('Ctrl Pts',(3.4582825948367,-1.14558354156204,8.66203591021737));
#12650=CARTESIAN_POINT('Ctrl Pts',(3.40754976563659,-1.06950462436886,8.65574428287472));
#12651=CARTESIAN_POINT('Ctrl Pts',(3.35676839910661,-0.980700968856299,
8.64902054810288));
#12652=CARTESIAN_POINT('Ctrl Pts',(3.35140988989883,-0.971148597775236,
8.64830499837596));
#12653=CARTESIAN_POINT('Ctrl Pts',(3.34341501250365,-0.956617279343384,
8.64722865227209));
#12654=CARTESIAN_POINT('Ctrl Pts',(3.3407207127681,-0.95167068454312,8.64686436951905));
#12655=CARTESIAN_POINT('Ctrl Pts',(3.33591310556014,-0.942754463339986,
8.64621163728329));
#12656=CARTESIAN_POINT('Ctrl Pts',(3.3337922461384,-0.938789062641845,8.64592272179111));
#12657=CARTESIAN_POINT('Ctrl Pts',(3.32916233090399,-0.930061605541731,
8.64528987742471));
#12658=CARTESIAN_POINT('Ctrl Pts',(3.32665913490921,-0.925296558897963,
8.64494631541515));
#12659=CARTESIAN_POINT('Ctrl Pts',(3.3195157286768,-0.911563751548811,8.6439616314221));
#12660=CARTESIAN_POINT('Ctrl Pts',(3.31492420005311,-0.902570660774414,
8.64332346315416));
#12661=CARTESIAN_POINT('Ctrl Pts',(3.28212997691631,-0.837116527885047,
8.63872402239285));
#12662=CARTESIAN_POINT('Ctrl Pts',(3.25654963249738,-0.779373958277573,
8.63490932965599));
#12663=CARTESIAN_POINT('Ctrl Pts',(3.186615409539,-0.598830701309576,8.62342646125249));
#12664=CARTESIAN_POINT('Ctrl Pts',(3.15153442409377,-0.472817656618723,
8.61600044493617));
#12665=CARTESIAN_POINT('Ctrl Pts',(3.11358467568438,-0.256235374654983,
8.60306763301469));
#12666=CARTESIAN_POINT('Ctrl Pts',(3.10409457636425,-0.167266817828607,
8.59771304159364));
#12667=CARTESIAN_POINT('Ctrl Pts',(3.09998889508395,-0.0623073507497877,
8.59119430501158));
#12668=CARTESIAN_POINT('Ctrl Pts',(3.09956089217759,-0.0466397237229232,
8.59021617096358));
#12669=CARTESIAN_POINT('Ctrl Pts',(3.09916148559782,-0.0209165895202022,
8.5886012323589));
#12670=CARTESIAN_POINT('Ctrl Pts',(3.09908140183857,-0.0108632739091539,
8.58796780616427));
#12671=CARTESIAN_POINT('Ctrl Pts',(3.09907405603421,0.00722851253278823,
8.58682364938202));
#12672=CARTESIAN_POINT('Ctrl Pts',(3.09911938218848,0.0152668016787727,
8.5863137829533));
#12673=CARTESIAN_POINT('Ctrl Pts',(3.09931982486487,0.0324225310801107,
8.5852222792427));
#12674=CARTESIAN_POINT('Ctrl Pts',(3.09948887677084,0.0415395948063888,
8.58464021939651));
#12675=CARTESIAN_POINT('Ctrl Pts',(3.10011622867037,0.0662361746737126,
8.58305793787235));
#12676=CARTESIAN_POINT('Ctrl Pts',(3.10069461928511,0.0818117405072412,
8.58205400624125));
#12677=CARTESIAN_POINT('Ctrl Pts',(3.10474190317115,0.164619422998105,8.57668336069927));
#12678=CARTESIAN_POINT('Ctrl Pts',(3.11142980511974,0.231643460043858,8.57221758295055));
#12679=CARTESIAN_POINT('Ctrl Pts',(3.1457476111784,0.458629711051173,8.55668432209717));
#12680=CARTESIAN_POINT('Ctrl Pts',(3.18948883210554,0.61550027988165,8.54518914496262));
#12681=CARTESIAN_POINT('Ctrl Pts',(3.27333552229397,0.817318324660651,8.53018373929405));
#12682=CARTESIAN_POINT('Ctrl Pts',(3.29713673405649,0.868391508567531,8.52637356877625));
#12683=CARTESIAN_POINT('Ctrl Pts',(3.32736643097465,0.926677482888834,8.52206371308));
#12684=CARTESIAN_POINT('Ctrl Pts',(3.33172110512173,0.934931507565759,8.52145432300223));
#12685=CARTESIAN_POINT('Ctrl Pts',(3.33886508750732,0.948245261303438,8.52047326905627));
#12686=CARTESIAN_POINT('Ctrl Pts',(3.34161867305235,0.95332385459402,8.52009949127387));
#12687=CARTESIAN_POINT('Ctrl Pts',(3.34655930266378,0.962342411996359,8.51943663660777));
#12688=CARTESIAN_POINT('Ctrl Pts',(3.34873767033393,0.966286995471901,8.51914702733419));
#12689=CARTESIAN_POINT('Ctrl Pts',(3.35349274696385,0.974828950386027,8.51852057661019));
#12690=CARTESIAN_POINT('Ctrl Pts',(3.35607431228292,0.979423500574573,8.51818404807517));
#12691=CARTESIAN_POINT('Ctrl Pts',(3.36339547555441,0.992333295091624,8.51723951827058));
#12692=CARTESIAN_POINT('Ctrl Pts',(3.36817682949126,1.00062486901939,8.51663410764764));
#12693=CARTESIAN_POINT('Ctrl Pts',(3.39849981598762,1.05234556997332,8.51286339713194));
#12694=CARTESIAN_POINT('Ctrl Pts',(3.42562181081653,1.09483234154442,8.50979100724284));
#12695=CARTESIAN_POINT('Ctrl Pts',(3.53780172510662,1.25669731365442,8.49800098503722));
#12696=CARTESIAN_POINT('Ctrl Pts',(3.63429958858564,1.36758477823499,8.48970510928694));
#12697=CARTESIAN_POINT('Ctrl Pts',(3.80615413487898,1.52594797700006,8.47594607970505));
#12698=CARTESIAN_POINT('Ctrl Pts',(3.87401953223029,1.58072314280811,8.47072084120669));
#12699=CARTESIAN_POINT('Ctrl Pts',(3.95799793978512,1.63986675163689,8.46434575294678));
#12700=CARTESIAN_POINT('Ctrl Pts',(3.97085822391302,1.64870001139537,8.46337202370236));
#12701=CARTESIAN_POINT('Ctrl Pts',(3.99215566579857,1.66296365820533,8.46176288177512));
#12702=CARTESIAN_POINT('Ctrl Pts',(4.00053267708518,1.66848295685161,8.46113080555867));
#12703=CARTESIAN_POINT('Ctrl Pts',(4.01569490016964,1.67830956289343,8.4599881113902));
#12704=CARTESIAN_POINT('Ctrl Pts',(4.02246522780034,1.68263952339214,8.45947834804337));
#12705=CARTESIAN_POINT('Ctrl Pts',(4.03698534055985,1.69180269473325,8.45838599819257));
#12706=CARTESIAN_POINT('Ctrl Pts',(4.04474250253744,1.69662381395242,8.45780298217343));
#12707=CARTESIAN_POINT('Ctrl Pts',(4.06588352603216,1.70956265721521,8.45621540346887));
#12708=CARTESIAN_POINT('Ctrl Pts',(4.07933005009587,1.71757625284766,8.45520708841639));
#12709=CARTESIAN_POINT('Ctrl Pts',(4.15198944460403,1.75972747058815,8.4497650795519));
#12710=CARTESIAN_POINT('Ctrl Pts',(4.21282678695162,1.79095939887924,8.44522913517843));
#12711=CARTESIAN_POINT('Ctrl Pts',(4.42955991635475,1.88850522519052,8.42913725373259));
#12712=CARTESIAN_POINT('Ctrl Pts',(4.5921760263042,1.93805016089112,8.41711100793078));
#12713=CARTESIAN_POINT('Ctrl Pts',(4.80717533295674,1.97464891138987,8.40220409720123));
#12714=CARTESIAN_POINT('Ctrl Pts',(4.85555772929438,1.98106944190795,8.39891807992833));
#12715=CARTESIAN_POINT('Ctrl Pts',(4.91306497354076,1.98656314802436,8.39512892916408));
#12716=CARTESIAN_POINT('Ctrl Pts',(4.92200484459242,1.98735633648343,8.39454321059797));
#12717=CARTESIAN_POINT('Ctrl Pts',(4.93660031035549,1.98855209195383,8.3935927093419));
#12718=CARTESIAN_POINT('Ctrl Pts',(4.94225269171582,1.98899092182216,8.39322601633843));
#12719=CARTESIAN_POINT('Ctrl Pts',(4.95239363218515,1.98973474604223,8.3925707476869));
#12720=CARTESIAN_POINT('Ctrl Pts',(4.95688140627286,1.99004865873386,8.39228168911091));
#12721=CARTESIAN_POINT('Ctrl Pts',(4.96671060636588,1.99070278798841,8.39165061663439));
#12722=CARTESIAN_POINT('Ctrl Pts',(4.97205234791763,1.99103669102747,8.39130895518265));
#12723=CARTESIAN_POINT('Ctrl Pts',(4.98733236623254,1.99193009474744,8.3903351834966));
#12724=CARTESIAN_POINT('Ctrl Pts',(4.99727374154781,1.99243672181617,8.38970592611087));
#12725=CARTESIAN_POINT('Ctrl Pts',(5.06634066297629,1.99543831261368,8.38536142173749));
#12726=CARTESIAN_POINT('Ctrl Pts',(5.12555395675346,1.99537576008364,8.38177487576219));
#12727=CARTESIAN_POINT('Ctrl Pts',(5.27756827611796,1.98844473611097,8.37272555693766));
#12728=CARTESIAN_POINT('Ctrl Pts',(5.37004859284434,1.97772006300377,8.3673684069124));
#12729=CARTESIAN_POINT('Ctrl Pts',(5.58923872019216,1.93662072453541,8.35440606374597));
#12730=CARTESIAN_POINT('Ctrl Pts',(5.71436354305339,1.90022647387958,8.34677012645167));
#12731=CARTESIAN_POINT('Ctrl Pts',(5.85011753619847,1.84589160690041,8.33770241937153));
#12732=CARTESIAN_POINT('Ctrl Pts',(5.86511060504782,1.83967735776198,8.33669014581121));
#12733=CARTESIAN_POINT('Ctrl Pts',(5.88942040117033,1.82925215297393,8.33503032597712));
#12734=CARTESIAN_POINT('Ctrl Pts',(5.89878371076913,1.82515122376565,8.33438649062051));
#12735=CARTESIAN_POINT('Ctrl Pts',(5.91546811112118,1.81769045306529,8.33323093185639));
#12736=CARTESIAN_POINT('Ctrl Pts',(5.92280119963922,1.81435786827327,8.33272014628719));
#12737=CARTESIAN_POINT('Ctrl Pts',(5.93023342020656,1.81092576880909,8.33219945699855));
#12738=CARTESIAN_POINT('Ctrl Pts',(5.93035301864395,1.81087052548448,8.33219107733513));
#12739=CARTESIAN_POINT('Ctrl Pts',(5.93063569325418,1.81073992219651,8.33217126987011));
#12740=CARTESIAN_POINT('Ctrl Pts',(5.93079876470571,1.81066455205763,8.33215984171894));
#12741=CARTESIAN_POINT('Ctrl Pts',(5.93111204402587,1.8105197058461,8.33213788407547));
#12742=CARTESIAN_POINT('Ctrl Pts',(5.93126225344108,1.81045023310424,8.33212735469762));
#12743=CARTESIAN_POINT('Ctrl Pts',(5.93155085113882,1.81031671136304,8.33210712217725));
#12744=CARTESIAN_POINT('Ctrl Pts',(5.93168924073376,1.81025266518316,8.33209741913152));
#12745=CARTESIAN_POINT('Ctrl Pts',(5.931955155254,1.81012956392626,8.33207877276479));
#12746=CARTESIAN_POINT('Ctrl Pts',(5.93208268128827,1.81007051123897,8.33206982952602));
#12747=CARTESIAN_POINT('Ctrl Pts',(5.93232774588016,1.80995699925015,8.33205264172367));
#12748=CARTESIAN_POINT('Ctrl Pts',(5.93244528538545,1.80990254197012,8.33204439722926));
#12749=CARTESIAN_POINT('Ctrl Pts',(5.93267118129554,1.80979785530666,8.33202855089063));
#12750=CARTESIAN_POINT('Ctrl Pts',(5.9327795384945,1.80974762764129,8.33202094910573));
#12751=CARTESIAN_POINT('Ctrl Pts',(5.93298780729639,1.80965106443957,8.33200633678234));
#12752=CARTESIAN_POINT('Ctrl Pts',(5.93308771958151,1.80960473035638,8.33199932629357));
#12753=CARTESIAN_POINT('Ctrl Pts',(5.93327977483871,1.80951564586344,8.33198584939493));
#12754=CARTESIAN_POINT('Ctrl Pts',(5.93337191838284,1.80947289668986,8.33197938302775));
#12755=CARTESIAN_POINT('Ctrl Pts',(5.93354905636797,1.8093906986619,8.33196695108956));
#12756=CARTESIAN_POINT('Ctrl Pts',(5.93363405129377,1.80935125085726,8.33196098555485));
#12757=CARTESIAN_POINT('Ctrl Pts',(5.93379746092356,1.8092753952625,8.33194951555891));
#12758=CARTESIAN_POINT('Ctrl Pts',(5.93387587605352,1.80923898835726,8.33194401112752));
#12759=CARTESIAN_POINT('Ctrl Pts',(5.93402664810861,1.80916897536033,8.33193342686913));
#12760=CARTESIAN_POINT('Ctrl Pts',(5.93409900537906,1.80913537002816,8.33192834706865));
#12761=CARTESIAN_POINT('Ctrl Pts',(5.93423814080111,1.80907074036043,8.33191857858641));
#12762=CARTESIAN_POINT('Ctrl Pts',(5.93430491924985,1.80903971666878,8.33191388992694));
#12763=CARTESIAN_POINT('Ctrl Pts',(5.93443333686407,1.80898004822983,8.33190487297095));
#12764=CARTESIAN_POINT('Ctrl Pts',(5.93449497629299,1.80895140402506,8.33190054469265));
#12765=CARTESIAN_POINT('Ctrl Pts',(5.93461351986193,1.80889630876453,8.33189222023801));
#12766=CARTESIAN_POINT('Ctrl Pts',(5.93467042421093,1.80886985817731,8.33188822407822));
#12767=CARTESIAN_POINT('Ctrl Pts',(5.93481394540416,1.80880313764433,8.33187814471686));
#12768=CARTESIAN_POINT('Ctrl Pts',(5.93490056058505,1.80876286417095,8.33187206139461));
#12769=CARTESIAN_POINT('Ctrl Pts',(5.93507230327991,1.8086829939413,8.3318599984062));
#12770=CARTESIAN_POINT('Ctrl Pts',(5.93515743090216,1.80864339739138,8.33185401874661));
#12771=CARTESIAN_POINT('Ctrl Pts',(5.93532623282861,1.8085648657965,8.33184216071285));
#12772=CARTESIAN_POINT('Ctrl Pts',(5.9354099072215,1.80852593095683,8.33183628234607));
#12773=CARTESIAN_POINT('Ctrl Pts',(5.94418633816392,1.80444139660216,8.33121967189457));
#12774=CARTESIAN_POINT('Ctrl Pts',(5.95284968817242,1.80033324037226,8.33060679308141));
#12775=CARTESIAN_POINT('Ctrl Pts',(5.97771805022388,1.78832031026126,8.3288351479526));
#12776=CARTESIAN_POINT('Ctrl Pts',(5.99384560396007,1.78025824054228,8.32767096904429));
#12777=CARTESIAN_POINT('Ctrl Pts',(6.03011286853432,1.76150968173623,8.32501754142283));
#12778=CARTESIAN_POINT('Ctrl Pts',(6.05018282345811,1.75069445117057,8.32352394320666));
#12779=CARTESIAN_POINT('Ctrl Pts',(6.114781433277,1.71444147054619,8.31863284198301));
#12780=CARTESIAN_POINT('Ctrl Pts',(6.15851275476344,1.68763178540857,8.31518950509405));
#12781=CARTESIAN_POINT('Ctrl Pts',(6.29920847943317,1.59373117748438,8.30367584203508));
#12782=CARTESIAN_POINT('Ctrl Pts',(6.39125794563229,1.51973436816758,8.29541147782027));
#12783=CARTESIAN_POINT('Ctrl Pts',(6.53971008470285,1.37702734462932,8.28110151323893));
#12784=CARTESIAN_POINT('Ctrl Pts',(6.59908988729707,1.31185726720574,8.27504433863938));
#12785=CARTESIAN_POINT('Ctrl Pts',(6.66079155827713,1.23441073021474,8.26853612773482));
#12786=CARTESIAN_POINT('Ctrl Pts',(6.66753941210539,1.22579649076068,8.26782125243606));
#12787=CARTESIAN_POINT('Ctrl Pts',(6.67765174048795,1.212666049915,8.26674571656514));
#12788=CARTESIAN_POINT('Ctrl Pts',(6.68106841005942,1.20819057533575,8.26638157724237));
#12789=CARTESIAN_POINT('Ctrl Pts',(6.68717968426723,1.20011478743902,8.2657289951711));
#12790=CARTESIAN_POINT('Ctrl Pts',(6.68988109269775,1.19651979285541,8.26544008742162));
#12791=CARTESIAN_POINT('Ctrl Pts',(6.69579035901357,1.18860020505537,8.26480713413915));
#12792=CARTESIAN_POINT('Ctrl Pts',(6.69899286984829,1.18427175259263,8.26446345634563));
#12793=CARTESIAN_POINT('Ctrl Pts',(6.70815560169035,1.17178212849741,8.26347810598919));
#12794=CARTESIAN_POINT('Ctrl Pts',(6.71407148439505,1.16358842107007,8.26283939335486));
#12795=CARTESIAN_POINT('Ctrl Pts',(6.75662710421767,1.10369349163699,8.25822346757823));
#12796=CARTESIAN_POINT('Ctrl Pts',(6.79085100798916,1.05031174920634,8.25439403239074));
#12797=CARTESIAN_POINT('Ctrl Pts',(6.89077320284531,0.876780394944098,8.2425200051691));
#12798=CARTESIAN_POINT('Ctrl Pts',(6.9466819209477,0.751459313874922,8.23474557418199));
#12799=CARTESIAN_POINT('Ctrl Pts',(7.00605985454118,0.570334326301552,8.2235022825315));
#12800=CARTESIAN_POINT('Ctrl Pts',(7.02072836183434,0.518619576807721,8.22029487172644));
#12801=CARTESIAN_POINT('Ctrl Pts',(7.04192616888963,0.430467162853203,8.21478072001062));
#12802=CARTESIAN_POINT('Ctrl Pts',(7.04956212233093,0.394325014991496,8.21250715945146));
#12803=CARTESIAN_POINT('Ctrl Pts',(7.05855933338069,0.345006247997024,8.20937792601514));
#12804=CARTESIAN_POINT('Ctrl Pts',(7.06079954723259,0.331996142844514,8.20854996035052));
#12805=CARTESIAN_POINT('Ctrl Pts',(7.0641477185964,0.311326702201238,8.20723022730679));
#12806=CARTESIAN_POINT('Ctrl Pts',(7.06534055094648,0.303681355556016,8.20674114115148));
#12807=CARTESIAN_POINT('Ctrl Pts',(7.06764215524666,0.288344069974504,8.20575803004754));
#12808=CARTESIAN_POINT('Ctrl Pts',(7.068750518875,0.280652208109691,8.20526400152734));
#12809=CARTESIAN_POINT('Ctrl Pts',(7.07088754613947,0.265181707018643,8.20426831591472));
#12810=CARTESIAN_POINT('Ctrl Pts',(7.07191531690994,0.257403086162201,8.20376664015122));
#12811=CARTESIAN_POINT('Ctrl Pts',(7.07416351492177,0.23957853480187,8.20261459723933));
#12812=CARTESIAN_POINT('Ctrl Pts',(7.07535343194504,0.229529040219516,8.20196328603193));
#12813=CARTESIAN_POINT('Ctrl Pts',(7.0793888932144,0.193073824154529,8.1995939081006));
#12814=CARTESIAN_POINT('Ctrl Pts',(7.0817833742856,0.16662195568988,8.19786191458116));
#12815=CARTESIAN_POINT('Ctrl Pts',(7.08696839553794,0.0929961691002093,
8.19300382847231));
#12816=CARTESIAN_POINT('Ctrl Pts',(7.08861171175909,0.04576206065972,8.18984437323121));
#12817=CARTESIAN_POINT('Ctrl Pts',(7.08857660471244,-0.00148228863371718,
8.18664306094147));
#12818=CARTESIAN_POINT('Ctrl Pts',(7.0885770914503,-0.000505311004862244,
8.02912886331594));
#12819=CARTESIAN_POINT('Ctrl Pts',(7.08858251806087,0.0209166073635135,
8.03046881243805));
#12820=CARTESIAN_POINT('Ctrl Pts',(7.08824286466212,0.0423383398002704,
8.03179210744699));
#12821=CARTESIAN_POINT('Ctrl Pts',(7.08330683993958,0.196704910921732,8.0412343602088));
#12822=CARTESIAN_POINT('Ctrl Pts',(7.06576668731101,0.328914167340696,8.04883839769366));
#12823=CARTESIAN_POINT('Ctrl Pts',(7.01596266478146,0.539836700377552,8.06144819132248));
#12824=CARTESIAN_POINT('Ctrl Pts',(6.99163096249784,0.619973938727455,8.06635430442614));
#12825=CARTESIAN_POINT('Ctrl Pts',(6.94571488809877,0.74282900711577,8.07426859149292));
#12826=CARTESIAN_POINT('Ctrl Pts',(6.9275058841988,0.786705079275837,8.07717666730591));
#12827=CARTESIAN_POINT('Ctrl Pts',(6.9019385443612,0.842588789713423,8.08100819488785));
#12828=CARTESIAN_POINT('Ctrl Pts',(6.89599429150016,0.855228777198025,8.08188344848281));
#12829=CARTESIAN_POINT('Ctrl Pts',(6.88610530183051,0.875695958024054,8.08331527850948));
#12830=CARTESIAN_POINT('Ctrl Pts',(6.88224079348846,0.883561554285801,8.08386907968198));
#12831=CARTESIAN_POINT('Ctrl Pts',(6.87469654244288,0.89866440020061,8.08493941293801));
#12832=CARTESIAN_POINT('Ctrl Pts',(6.87102419258478,0.905905163761391,8.08545567944673));
#12833=CARTESIAN_POINT('Ctrl Pts',(6.86248507869253,0.922489949639226,8.08664545760591));
#12834=CARTESIAN_POINT('Ctrl Pts',(6.85758831892418,0.931818173161683,8.08732001118322));
#12835=CARTESIAN_POINT('Ctrl Pts',(6.84169684231514,0.961517009108036,8.08948507979792));
#12836=CARTESIAN_POINT('Ctrl Pts',(6.83042166863756,0.981734599214327,8.09098544697355));
#12837=CARTESIAN_POINT('Ctrl Pts',(6.73435337694826,1.14715994975751,8.10348761656134));
#12838=CARTESIAN_POINT('Ctrl Pts',(6.63187659969673,1.28128216831225,8.11516608799867));
#12839=CARTESIAN_POINT('Ctrl Pts',(6.44166860061383,1.47407863303438,8.13403576160537));
#12840=CARTESIAN_POINT('Ctrl Pts',(6.36395670642084,1.54154471052709,8.14115701217674));
#12841=CARTESIAN_POINT('Ctrl Pts',(6.27461501859275,1.60774331296646,8.14847679566218));
#12842=CARTESIAN_POINT('Ctrl Pts',(6.26781415209506,1.61271605548102,8.14902887121365));
#12843=CARTESIAN_POINT('Ctrl Pts',(6.25517826253906,1.62183303217412,8.15004488410969));
#12844=CARTESIAN_POINT('Ctrl Pts',(6.24935207736232,1.62598921791927,8.15050956960234));
#12845=CARTESIAN_POINT('Ctrl Pts',(6.23967638133744,1.63281323086345,8.15127488453989));
#12846=CARTESIAN_POINT('Ctrl Pts',(6.23583967614752,1.63549897554897,8.15157670467607));
#12847=CARTESIAN_POINT('Ctrl Pts',(6.22829969410445,1.64073759390073,8.15216656417929));
#12848=CARTESIAN_POINT('Ctrl Pts',(6.22459719063908,1.64329149002111,8.15245466978984));
#12849=CARTESIAN_POINT('Ctrl Pts',(6.21533551155887,1.64963384592458,8.1531715939762));
#12850=CARTESIAN_POINT('Ctrl Pts',(6.20976568609022,1.65340679126196,8.15359937726235));
#12851=CARTESIAN_POINT('Ctrl Pts',(6.19069794281657,1.66618284765166,8.15505280548452));
#12852=CARTESIAN_POINT('Ctrl Pts',(6.17710890987038,1.67504969654972,8.15606985649493));
#12853=CARTESIAN_POINT('Ctrl Pts',(6.07906264973981,1.73733261114568,8.16328620545652));
#12854=CARTESIAN_POINT('Ctrl Pts',(5.99079426573619,1.78450793293673,8.16914672343449));
#12855=CARTESIAN_POINT('Ctrl Pts',(5.81221707027307,1.86333445751262,8.18050455438396));
#12856=CARTESIAN_POINT('Ctrl Pts',(5.72244224080311,1.89550569494378,8.18599300302687));
#12857=CARTESIAN_POINT('Ctrl Pts',(5.57977520500691,1.93537579453606,8.19474985383873));
#12858=CARTESIAN_POINT('Ctrl Pts',(5.52829355516862,1.94757883349386,8.1979150992948));
#12859=CARTESIAN_POINT('Ctrl Pts',(5.44237684918372,1.96436803506055,8.20325307012839));
#12860=CARTESIAN_POINT('Ctrl Pts',(5.40819751425057,1.97012682866522,8.20539072435081));
#12861=CARTESIAN_POINT('Ctrl Pts',(5.36154047116294,1.97674293871183,8.20833555284953));
#12862=CARTESIAN_POINT('Ctrl Pts',(5.34917799885267,1.97837787106688,8.20911835234385));
#12863=CARTESIAN_POINT('Ctrl Pts',(5.32842157975269,1.98092511080476,8.21043723105269));
#12864=CARTESIAN_POINT('Ctrl Pts',(5.3200355931394,1.98190024413456,8.21097132986456));
#12865=CARTESIAN_POINT('Ctrl Pts',(5.30349844810045,1.98371687961533,8.21202713495702));
#12866=CARTESIAN_POINT('Ctrl Pts',(5.29534778931679,1.9845614478462,8.21254873406146));
#12867=CARTESIAN_POINT('Ctrl Pts',(5.27741423704017,1.98630809860511,8.21369917510282));
#12868=CARTESIAN_POINT('Ctrl Pts',(5.26762946308296,1.98718817208549,8.21432869239916));
#12869=CARTESIAN_POINT('Ctrl Pts',(5.23330664651686,1.99001983744563,8.21654350929019));
#12870=CARTESIAN_POINT('Ctrl Pts',(5.20874015941342,1.99158941396377,8.21814062510251));
#12871=CARTESIAN_POINT('Ctrl Pts',(5.03347179218353,1.99953392188722,8.22962441370651));
#12872=CARTESIAN_POINT('Ctrl Pts',(4.88252998948568,1.98925010129459,8.24003944089881));
#12873=CARTESIAN_POINT('Ctrl Pts',(4.65111298145257,1.94683600092371,8.25644212576776));
#12874=CARTESIAN_POINT('Ctrl Pts',(4.56905355768173,1.92633862831664,8.26233441767993));
#12875=CARTESIAN_POINT('Ctrl Pts',(4.4640415149418,1.89289685946804,8.26980782260311));
#12876=CARTESIAN_POINT('Ctrl Pts',(4.43969733495707,1.8846227155951,8.27153512329383));
#12877=CARTESIAN_POINT('Ctrl Pts',(4.39927672673215,1.87000683459093,8.27438690642788));
#12878=CARTESIAN_POINT('Ctrl Pts',(4.38311096679276,1.86392285433591,8.2755230362087));
#12879=CARTESIAN_POINT('Ctrl Pts',(4.36080654584855,1.85519620148584,8.27708248246566));
#12880=CARTESIAN_POINT('Ctrl Pts',(4.35459961242113,1.85273171366393,8.27751557028158));
#12881=CARTESIAN_POINT('Ctrl Pts',(4.34410031590908,1.84850176284116,8.27824652226261));
#12882=CARTESIAN_POINT('Ctrl Pts',(4.33980155653575,1.84675241950539,8.27854533085519));
#12883=CARTESIAN_POINT('Ctrl Pts',(4.33156848127149,1.84336849968653,8.27911666697057));
#12884=CARTESIAN_POINT('Ctrl Pts',(4.32763326095993,1.84173630818035,8.27938933969216));
#12885=CARTESIAN_POINT('Ctrl Pts',(4.31822181810818,1.83779738608704,8.28004054153849));
#12886=CARTESIAN_POINT('Ctrl Pts',(4.31275057601281,1.83547875248459,8.28041836232799));
#12887=CARTESIAN_POINT('Ctrl Pts',(4.29304373435961,1.82702320308407,8.28177681217749));
#12888=CARTESIAN_POINT('Ctrl Pts',(4.27886899855799,1.82074465787578,8.2827493437851));
#12889=CARTESIAN_POINT('Ctrl Pts',(4.14549696155639,1.75979929171473,8.2918697894921));
#12890=CARTESIAN_POINT('Ctrl Pts',(4.03187295569726,1.69366075541644,8.29942367317559));
#12891=CARTESIAN_POINT('Ctrl Pts',(3.8107025879474,1.53385013738658,8.31526532361536));
#12892=CARTESIAN_POINT('Ctrl Pts',(3.70503759851615,1.43887503210483,8.32353472504687));
#12893=CARTESIAN_POINT('Ctrl Pts',(3.59808696493624,1.31989553804707,8.33345220169072));
#12894=CARTESIAN_POINT('Ctrl Pts',(3.58603259641644,1.30610814325686,8.33459488664062));
#12895=CARTESIAN_POINT('Ctrl Pts',(3.56788516642986,1.28476563703569,8.33635491566129));
#12896=CARTESIAN_POINT('Ctrl Pts',(3.56165436066719,1.27732854722181,8.3369666209017));
#12897=CARTESIAN_POINT('Ctrl Pts',(3.55087125813924,1.26426541212841,8.33803844961714));
#12898=CARTESIAN_POINT('Ctrl Pts',(3.54629482636944,1.25865945416265,8.33849758696586));
#12899=CARTESIAN_POINT('Ctrl Pts',(3.53603263773524,1.24594807945994,8.33953687657863));
#12900=CARTESIAN_POINT('Ctrl Pts',(3.53036482625584,1.23882844527107,8.34011773177511));
#12901=CARTESIAN_POINT('Ctrl Pts',(3.51517434557535,1.21947659805728,8.34169334400111));
#12902=CARTESIAN_POINT('Ctrl Pts',(3.5057453833678,1.20717195547585,8.34269175787554));
#12903=CARTESIAN_POINT('Ctrl Pts',(3.46199922717546,1.14868431728759,8.34742258294061));
#12904=CARTESIAN_POINT('Ctrl Pts',(3.42955024247315,1.10114454163414,8.3512257396862));
#12905=CARTESIAN_POINT('Ctrl Pts',(3.29940960558362,0.891560654485373,8.36782518059771));
#12906=CARTESIAN_POINT('Ctrl Pts',(3.22300188684097,0.717502778069679,8.38131809175999));
#12907=CARTESIAN_POINT('Ctrl Pts',(3.16106719270336,0.495178833552528,8.39700661807852));
#12908=CARTESIAN_POINT('Ctrl Pts',(3.15114624964832,0.454702781591051,8.39979839589397));
#12909=CARTESIAN_POINT('Ctrl Pts',(3.14061470556361,0.405057025541294,8.40312145803544));
#12910=CARTESIAN_POINT('Ctrl Pts',(3.13879045134856,0.396158505502843,8.40371315699248));
#12911=CARTESIAN_POINT('Ctrl Pts',(3.13602449843945,0.38218187505547,8.40463603947316));
#12912=CARTESIAN_POINT('Ctrl Pts',(3.13504165414558,0.377112172649173,8.40496946038762));
#12913=CARTESIAN_POINT('Ctrl Pts',(3.13323508122034,0.367595879247602,8.40559274929203));
#12914=CARTESIAN_POINT('Ctrl Pts',(3.13240679281982,0.363150345583298,8.40588285860311));
#12915=CARTESIAN_POINT('Ctrl Pts',(3.13054357121205,0.352957826505537,8.40654562688854));
#12916=CARTESIAN_POINT('Ctrl Pts',(3.12951874948858,0.3472090836459,8.40691771409429));
#12917=CARTESIAN_POINT('Ctrl Pts',(3.12684963772621,0.331846550350842,8.40790765194156));
#12918=CARTESIAN_POINT('Ctrl Pts',(3.12525056381405,0.322224921536757,8.40852305987001));
#12919=CARTESIAN_POINT('Ctrl Pts',(3.11286504184186,0.244165338931582,8.41348145969738));
#12920=CARTESIAN_POINT('Ctrl Pts',(3.10557902584076,0.175211731448138,8.4176483792396));
#12921=CARTESIAN_POINT('Ctrl Pts',(3.09389006622732,-0.044420719629715,
8.43063610357305));
#12922=CARTESIAN_POINT('Ctrl Pts',(3.1029500579936,-0.195274428597169,8.43917042205476));
#12923=CARTESIAN_POINT('Ctrl Pts',(3.14017136784546,-0.408083455549092,
8.45204781741629));
#12924=CARTESIAN_POINT('Ctrl Pts',(3.15459595434313,-0.471894133822141,
8.45601468193832));
#12925=CARTESIAN_POINT('Ctrl Pts',(3.17627076682403,-0.549767178981537,
8.4610438783365));
#12926=CARTESIAN_POINT('Ctrl Pts',(3.18058803950855,-0.564608287914711,
8.46201086084256));
#12927=CARTESIAN_POINT('Ctrl Pts',(3.18771760357172,-0.588095715646715,
8.46355541786468));
#12928=CARTESIAN_POINT('Ctrl Pts',(3.19041734980186,-0.596775755101909,
8.46412933238892));
#12929=CARTESIAN_POINT('Ctrl Pts',(3.19561727315955,-0.613099897900092,
8.46521466776373));
#12930=CARTESIAN_POINT('Ctrl Pts',(3.19810454222504,-0.620747946146378,
8.4657256576209));
#12931=CARTESIAN_POINT('Ctrl Pts',(3.20381870828088,-0.637963621633583,
8.46688163301552));
#12932=CARTESIAN_POINT('Ctrl Pts',(3.20707211865166,-0.647522152393601,
8.46752747845391));
#12933=CARTESIAN_POINT('Ctrl Pts',(3.2156076472777,-0.671988983575927,8.46919117625997));
#12934=CARTESIAN_POINT('Ctrl Pts',(3.22099468293552,-0.686859680722899,
8.47021246033649));
#12935=CARTESIAN_POINT('Ctrl Pts',(3.25950708254536,-0.789348878406707,
8.47732290018869));
#12936=CARTESIAN_POINT('Ctrl Pts',(3.29858669607508,-0.874590745668232,
8.48361021640595));
#12937=CARTESIAN_POINT('Ctrl Pts',(3.42555110413713,-1.10686239746261,8.50178190473632));
#12938=CARTESIAN_POINT('Ctrl Pts',(3.52655988983565,-1.24577718849533,8.51397567667169));
#12939=CARTESIAN_POINT('Ctrl Pts',(3.65469063042048,-1.3813593433869,8.52644061005131));
#12940=CARTESIAN_POINT('Ctrl Pts',(3.66546272227107,-1.39249511725272,8.52746852702062));
#12941=CARTESIAN_POINT('Ctrl Pts',(3.68460581394031,-1.41182859874492,8.52925873141401));
#12942=CARTESIAN_POINT('Ctrl Pts',(3.69292121725599,-1.4200800504525,8.53002461864009));
#12943=CARTESIAN_POINT('Ctrl Pts',(3.70539967897826,-1.43224625829029,8.53115595780354));
#12944=CARTESIAN_POINT('Ctrl Pts',(3.709507471702,-1.43621698115368,8.53152553348375));
#12945=CARTESIAN_POINT('Ctrl Pts',(3.71688222903986,-1.44328462004672,8.5321838664326));
#12946=CARTESIAN_POINT('Ctrl Pts',(3.72014266241019,-1.44638817048052,8.53247312679796));
#12947=CARTESIAN_POINT('Ctrl Pts',(3.7272775953262,-1.45313390213895,8.53310221813287));
#12948=CARTESIAN_POINT('Ctrl Pts',(3.73115615851254,-1.45677163395887,8.53344171322459));
#12949=CARTESIAN_POINT('Ctrl Pts',(3.74202044743837,-1.46687997242698,8.53438593925357));
#12950=CARTESIAN_POINT('Ctrl Pts',(3.7490381352246,-1.47331623520628,8.53498814091406));
#12951=CARTESIAN_POINT('Ctrl Pts',(3.78828009745533,-1.50879294763232,8.53831480908532));
#12952=CARTESIAN_POINT('Ctrl Pts',(3.82140147678086,-1.53682881083467,8.54097140728786));
#12953=CARTESIAN_POINT('Ctrl Pts',(3.96971141029772,-1.65428196234825,8.55235858167986));
#12954=CARTESIAN_POINT('Ctrl Pts',(4.09359596654081,-1.73200151596034,8.56061703646805));
#12955=CARTESIAN_POINT('Ctrl Pts',(4.3030957794994,-1.8333922186254,8.57427776584483));
#12956=CARTESIAN_POINT('Ctrl Pts',(4.38372018901782,-1.86609985613317,8.57946462700225));
#12957=CARTESIAN_POINT('Ctrl Pts',(4.48726042658427,-1.90041994320643,8.58619684775099));
#12958=CARTESIAN_POINT('Ctrl Pts',(4.50842048798065,-1.90704434398851,8.58757592840611));
#12959=CARTESIAN_POINT('Ctrl Pts',(4.53972688898628,-1.91627504365491,8.58962298865096));
#12960=CARTESIAN_POINT('Ctrl Pts',(4.54979083388597,-1.9191564872006,8.59028205475521));
#12961=CARTESIAN_POINT('Ctrl Pts',(4.56766595928698,-1.92412247820514,8.59145464018497));
#12962=CARTESIAN_POINT('Ctrl Pts',(4.57546806454906,-1.92623902079519,8.5919671135139));
#12963=CARTESIAN_POINT('Ctrl Pts',(4.59186602792484,-1.93058059309345,8.5930456877877));
#12964=CARTESIAN_POINT('Ctrl Pts',(4.60046428951419,-1.93279576735484,8.59361209333547));
#12965=CARTESIAN_POINT('Ctrl Pts',(4.62313632437615,-1.93847563208265,8.59510799045172));
#12966=CARTESIAN_POINT('Ctrl Pts',(4.63723336170456,-1.94184441287745,8.5960405289032));
#12967=CARTESIAN_POINT('Ctrl Pts',(4.69761572769017,-1.95558017893758,8.60004600109448));
#12968=CARTESIAN_POINT('Ctrl Pts',(4.74422288914394,-1.9644473935644,8.60316595430959));
#12969=CARTESIAN_POINT('Ctrl Pts',(4.97595077612397,-2.00002714378665,8.61882681360413));
#12970=CARTESIAN_POINT('Ctrl Pts',(5.16386607788232,-2.00226797880707,8.63211021460256));
#12971=CARTESIAN_POINT('Ctrl Pts',(5.40345533786732,-1.97132972157052,8.6486738400749));
#12972=CARTESIAN_POINT('Ctrl Pts',(5.45731716406399,-1.96211280652047,8.65236285635033));
#12973=CARTESIAN_POINT('Ctrl Pts',(5.52028894483963,-1.94865422822784,8.65658499714032));
#12974=CARTESIAN_POINT('Ctrl Pts',(5.52982546226143,-1.94654269019723,8.65722190359077));
#12975=CARTESIAN_POINT('Ctrl Pts',(5.54452432165419,-1.94317468239781,8.65819931608898));
#12976=CARTESIAN_POINT('Ctrl Pts',(5.54969764123958,-1.94196752900474,8.65854250132478));
#12977=CARTESIAN_POINT('Ctrl Pts',(5.55924613021899,-1.93969920536832,8.6591743320978));
#12978=CARTESIAN_POINT('Ctrl Pts',(5.56362250992979,-1.9386438958638,8.65946329225351));
#12979=CARTESIAN_POINT('Ctrl Pts',(5.57355140504399,-1.93621406991845,8.66011747081952));
#12980=CARTESIAN_POINT('Ctrl Pts',(5.57910159957395,-1.93483048250477,8.66048216704427));
#12981=CARTESIAN_POINT('Ctrl Pts',(5.59350704671697,-1.93117351625073,8.66142634956856));
#12982=CARTESIAN_POINT('Ctrl Pts',(5.60235287334175,-1.92886307064639,8.66200379202124));
#12983=CARTESIAN_POINT('Ctrl Pts',(5.6615950072679,-1.91295371366528,8.66585720895393));
#12984=CARTESIAN_POINT('Ctrl Pts',(5.71146137050406,-1.89744070967401,8.66903366645225));
#12985=CARTESIAN_POINT('Ctrl Pts',(5.91719165158419,-1.82446738501356,8.68207493178618));
#12986=CARTESIAN_POINT('Ctrl Pts',(6.06617514596389,-1.74961603315116,8.69141659753913));
#12987=CARTESIAN_POINT('Ctrl Pts',(6.26056670204711,-1.61936892377206,8.70534274481421));
#12988=CARTESIAN_POINT('Ctrl Pts',(6.31499731187939,-1.57872697835795,8.70945640249277));
#12989=CARTESIAN_POINT('Ctrl Pts',(6.37927239960398,-1.52541869155086,8.71465064829089));
#12990=CARTESIAN_POINT('Ctrl Pts',(6.39118029638218,-1.51530408373663,8.71562794480809));
#12991=CARTESIAN_POINT('Ctrl Pts',(6.40985415136407,-1.49906097535857,8.71718518080149));
#12992=CARTESIAN_POINT('Ctrl Pts',(6.41669912642473,-1.49302398030502,8.71776135456346));
#12993=CARTESIAN_POINT('Ctrl Pts',(6.42949361859769,-1.4815826879341,8.7188486090298));
#12994=CARTESIAN_POINT('Ctrl Pts',(6.4354523883057,-1.47618897619571,8.71935924124324));
#12995=CARTESIAN_POINT('Ctrl Pts',(6.44878199469795,-1.46397601604263,8.72051125705207));
#12996=CARTESIAN_POINT('Ctrl Pts',(6.4561342209239,-1.45713686565038,8.72115347627051));
#12997=CARTESIAN_POINT('Ctrl Pts',(6.47480005068658,-1.43950888017823,8.72280163659338));
#12998=CARTESIAN_POINT('Ctrl Pts',(6.48603886253647,-1.42864218513244,8.72381090200112));
#12999=CARTESIAN_POINT('Ctrl Pts',(6.55983867822185,-1.35558801711397,8.73055314346655));
#13000=CARTESIAN_POINT('Ctrl Pts',(6.61833478770932,-1.28945001544624,8.73646092925677));
#13001=CARTESIAN_POINT('Ctrl Pts',(6.75268843812737,-1.11557645449979,8.75150759052761));
#13002=CARTESIAN_POINT('Ctrl Pts',(6.82262043869341,-1.00379381895217,8.76078608390787));
#13003=CARTESIAN_POINT('Ctrl Pts',(6.90915760239952,-0.829223211579989,
8.77420670870219));
#13004=CARTESIAN_POINT('Ctrl Pts',(6.93456292949947,-0.771186928061262,
8.77850413407092));
#13005=CARTESIAN_POINT('Ctrl Pts',(6.96077324167648,-0.702596584522218,
8.7833216827151));
#13006=CARTESIAN_POINT('Ctrl Pts',(6.96430817035543,-0.693130891392002,
8.78398086589617));
#13007=CARTESIAN_POINT('Ctrl Pts',(6.96961626501422,-0.678580698977294,
8.7849850454084));
#13008=CARTESIAN_POINT('Ctrl Pts',(6.97144096157011,-0.673515363819161,
8.78533295092669));
#13009=CARTESIAN_POINT('Ctrl Pts',(6.97475206710415,-0.664205737172418,
8.78596921390301));
#13010=CARTESIAN_POINT('Ctrl Pts',(6.9762446304581,-0.659963813517728,8.78625792051927));
#13011=CARTESIAN_POINT('Ctrl Pts',(6.97957390264843,-0.650398705194746,
8.78690623266583));
#13012=CARTESIAN_POINT('Ctrl Pts',(6.981402421407,-0.645072776902345,8.78726535634368));
#13013=CARTESIAN_POINT('Ctrl Pts',(6.98671835523619,-0.629372899194462,
8.78831871395971));
#13014=CARTESIAN_POINT('Ctrl Pts',(6.99014304260979,-0.618977713080454,
8.7890094034956));
#13015=CARTESIAN_POINT('Ctrl Pts',(7.02046019823809,-0.524340132543225,
8.79524070683956));
#13016=CARTESIAN_POINT('Ctrl Pts',(7.0418120707574,-0.438413372603167,8.80049373021013));
#13017=CARTESIAN_POINT('Ctrl Pts',(7.07805808635704,-0.235843900652832,
8.81253528393552));
#13018=CARTESIAN_POINT('Ctrl Pts',(7.08849340269679,-0.118748807800604,
8.81925117900009));
#13019=CARTESIAN_POINT('Ctrl Pts',(7.088576988111,-0.000943539479336892,
8.82622343083489));
#13020=CARTESIAN_POINT('Ctrl Pts',(7.08857715545312,-0.000471768392112177,
8.82625135561015));
#13021=CARTESIAN_POINT('Ctrl Pts',(7.08857715545311,2.37118846529926E-11,
8.82627928344061));
#13022=CARTESIAN_POINT('Origin',(5.09382715545311,0.,-6.77268258743872));
#13023=CARTESIAN_POINT('',(7.08857712371941,0.00025895104517608,9.78359198969069));
#13024=CARTESIAN_POINT('',(7.08857665886015,0.00140753592649714,9.62731741260996));
#13025=CARTESIAN_POINT('',(7.08857715545311,8.3550772080578E-14,-6.77268258743872));
#13026=CARTESIAN_POINT('Ctrl Pts',(7.08857709519816,0.000490292911708074,
9.78359207680131));
#13027=CARTESIAN_POINT('Ctrl Pts',(7.08858056938264,-0.0136443786806656,
9.78270707410814));
#13028=CARTESIAN_POINT('Ctrl Pts',(7.08843380748817,-0.0277791914842937,
9.78182936076363));
#13029=CARTESIAN_POINT('Ctrl Pts',(7.08471229123831,-0.204862142831645,
9.77091144180494));
#13030=CARTESIAN_POINT('Ctrl Pts',(7.0613293095822,-0.366799471128801,9.76171666375718));
#13031=CARTESIAN_POINT('Ctrl Pts',(6.9937958317104,-0.614803472615814,9.74667589271688));
#13032=CARTESIAN_POINT('Ctrl Pts',(6.96271955935319,-0.703635144582146,
9.74108856917276));
#13033=CARTESIAN_POINT('Ctrl Pts',(6.91636435148483,-0.811121371616562,
9.73387104510844));
#13034=CARTESIAN_POINT('Ctrl Pts',(6.90686263552512,-0.83214301059918,9.73243718144363));
#13035=CARTESIAN_POINT('Ctrl Pts',(6.89245087133043,-0.862608488093872,
9.73032414307598));
#13036=CARTESIAN_POINT('Ctrl Pts',(6.8878262041889,-0.872185806567827,9.72965474317748));
#13037=CARTESIAN_POINT('Ctrl Pts',(6.87954180212753,-0.888997460646529,
9.72847041339689));
#13038=CARTESIAN_POINT('Ctrl Pts',(6.87591410985923,-0.89624738112057,9.72795660335941));
#13039=CARTESIAN_POINT('Ctrl Pts',(6.86825676563868,-0.911320226460795,
9.72688184340351));
#13040=CARTESIAN_POINT('Ctrl Pts',(6.86421934744489,-0.919138987923251,
9.72632063030293));
#13041=CARTESIAN_POINT('Ctrl Pts',(6.85356339133805,-0.939444335542812,
9.72485334422801));
#13042=CARTESIAN_POINT('Ctrl Pts',(6.84686374989247,-0.951887577942564,
9.72394443242433));
#13043=CARTESIAN_POINT('Ctrl Pts',(6.81864035172033,-1.00299820907502,9.72016985308271));
#13044=CARTESIAN_POINT('Ctrl Pts',(6.79596639209372,-1.04101271731831,9.71726362896545));
#13045=CARTESIAN_POINT('Ctrl Pts',(6.67987439671137,-1.22170362279321,9.70295184442103));
#13046=CARTESIAN_POINT('Ctrl Pts',(6.56969235241088,-1.35274164048764,9.69093381550683));
#13047=CARTESIAN_POINT('Ctrl Pts',(6.40719131537045,-1.50220967333437,9.67565830083682));
#13048=CARTESIAN_POINT('Ctrl Pts',(6.36887988860476,-1.53486172735929,9.67220860034838));
#13049=CARTESIAN_POINT('Ctrl Pts',(6.3147282647795,-1.5775854892631,9.66757575729102));
#13050=CARTESIAN_POINT('Ctrl Pts',(6.29992235910093,-1.58893357584229,9.66633275627732));
#13051=CARTESIAN_POINT('Ctrl Pts',(6.27741574355493,-1.60568802923844,9.66448112299737));
#13052=CARTESIAN_POINT('Ctrl Pts',(6.26983281286004,-1.61125004104356,9.6638636019593));
#13053=CARTESIAN_POINT('Ctrl Pts',(6.25745694076085,-1.62019371834059,9.6628663645966));
#13054=CARTESIAN_POINT('Ctrl Pts',(6.25268801725202,-1.6236081630847,9.66248461512802));
#13055=CARTESIAN_POINT('Ctrl Pts',(6.24351892422364,-1.6301120524599,9.66175556997557));
#13056=CARTESIAN_POINT('Ctrl Pts',(6.239121195777,-1.63320483393593,9.66140805820121));
#13057=CARTESIAN_POINT('Ctrl Pts',(6.23469233951648,-1.63629282061832,9.66106029046108));
#13058=CARTESIAN_POINT('Ctrl Pts',(6.2346737238234,-1.63630579979805,9.66105882873723));
#13059=CARTESIAN_POINT('Ctrl Pts',(6.23463604278237,-1.63633207070898,9.66105587006107));
#13060=CARTESIAN_POINT('Ctrl Pts',(6.23461697748994,-1.63634536237841,9.66105437311503));
#13061=CARTESIAN_POINT('Ctrl Pts',(6.2345783808954,-1.63637226960089,9.66105134271614));
#13062=CARTESIAN_POINT('Ctrl Pts',(6.23455884948748,-1.63638588520322,9.66104980925702));
#13063=CARTESIAN_POINT('Ctrl Pts',(6.23451930333827,-1.63641345229388,9.66104670447797));
#13064=CARTESIAN_POINT('Ctrl Pts',(6.23449928864725,-1.63642740372116,9.66104513316414));
#13065=CARTESIAN_POINT('Ctrl Pts',(6.23445875778972,-1.63645565502901,9.66104195125792));
#13066=CARTESIAN_POINT('Ctrl Pts',(6.23443824156244,-1.63646995492429,9.66104034066303));
#13067=CARTESIAN_POINT('Ctrl Pts',(6.23439668851203,-1.63649891641127,9.66103707870061));
#13068=CARTESIAN_POINT('Ctrl Pts',(6.23437565169313,-1.6365135779706,9.66103542733583));
#13069=CARTESIAN_POINT('Ctrl Pts',(6.23433303731909,-1.63654327673325,9.66103208226002));
#13070=CARTESIAN_POINT('Ctrl Pts',(6.23431145975342,-1.63655831391257,9.66103038855074));
#13071=CARTESIAN_POINT('Ctrl Pts',(6.23426774271571,-1.63658877857337,9.66102695713206));
#13072=CARTESIAN_POINT('Ctrl Pts',(6.23424560317639,-1.63660420606834,9.66102521942013));
#13073=CARTESIAN_POINT('Ctrl Pts',(6.23420073976778,-1.63663546688454,9.66102169824452));
#13074=CARTESIAN_POINT('Ctrl Pts',(6.23417801593563,-1.63665130014424,9.6610199147867));
#13075=CARTESIAN_POINT('Ctrl Pts',(6.23413196034228,-1.63668338882488,9.66101630027611));
#13076=CARTESIAN_POINT('Ctrl Pts',(6.23410862854145,-1.63669964423535,9.66101446922338));
#13077=CARTESIAN_POINT('Ctrl Pts',(6.23406133206577,-1.63673259448129,9.66101075757486));
#13078=CARTESIAN_POINT('Ctrl Pts',(6.2340373673861,-1.63674928927944,9.66100887698207));
#13079=CARTESIAN_POINT('Ctrl Pts',(6.23398877878535,-1.63678313654587,9.66100506419453));
#13080=CARTESIAN_POINT('Ctrl Pts',(6.23396415482753,-1.6368002889962,9.66100313200049));
#13081=CARTESIAN_POINT('Ctrl Pts',(6.23391421977074,-1.6368350708691,9.66099921383216));
#13082=CARTESIAN_POINT('Ctrl Pts',(6.23388890863097,-1.63685270027345,9.66099722785852));
#13083=CARTESIAN_POINT('Ctrl Pts',(6.23383756964423,-1.63688845650577,9.66099319982288));
#13084=CARTESIAN_POINT('Ctrl Pts',(6.23381154175922,-1.63690658331021,9.66099115776204));
#13085=CARTESIAN_POINT('Ctrl Pts',(6.23375873790175,-1.63694335604527,9.66098701510257));
#13086=CARTESIAN_POINT('Ctrl Pts',(6.2337319619427,-1.63696200191286,9.66098491450945));
#13087=CARTESIAN_POINT('Ctrl Pts',(6.233677628672,-1.63699983577588,9.66098065218925));
#13088=CARTESIAN_POINT('Ctrl Pts',(6.23365007134942,-1.63701902372123,9.6609784904661));
#13089=CARTESIAN_POINT('Ctrl Pts',(6.23359414003372,-1.63705796615616,9.66097410312986));
#13090=CARTESIAN_POINT('Ctrl Pts',(6.23356576601462,-1.63707772060176,9.66097187751987));
#13091=CARTESIAN_POINT('Ctrl Pts',(6.23350816374731,-1.63711782199749,9.66096735947955));
#13092=CARTESIAN_POINT('Ctrl Pts',(6.23347893545422,-1.63713816891202,9.66096506705123));
#13093=CARTESIAN_POINT('Ctrl Pts',(6.23341958463795,-1.63717948288866,9.66096041225373));
#13094=CARTESIAN_POINT('Ctrl Pts',(6.23338946207873,-1.63720044990376,9.66095804988769));
#13095=CARTESIAN_POINT('Ctrl Pts',(6.23332828009777,-1.63724303353703,9.66095325188946));
#13096=CARTESIAN_POINT('Ctrl Pts',(6.23329722063836,-1.63726465010355,9.66095081626076));
#13097=CARTESIAN_POINT('Ctrl Pts',(6.22967705170315,-1.63978403952007,9.66066694157444));
#13098=CARTESIAN_POINT('Ctrl Pts',(6.22607979889914,-1.64226996411107,9.66038632171062));
#13099=CARTESIAN_POINT('Ctrl Pts',(6.21772880464628,-1.6480005368209,9.65973820104804));
#13100=CARTESIAN_POINT('Ctrl Pts',(6.21296917595704,-1.65123645379734,9.65937128751451));
#13101=CARTESIAN_POINT('Ctrl Pts',(6.20051530823203,-1.65962484966764,9.658417502493));
#13102=CARTESIAN_POINT('Ctrl Pts',(6.19279897735725,-1.66474450037611,9.65783274392952));
#13103=CARTESIAN_POINT('Ctrl Pts',(6.13936651480117,-1.69966257897415,9.65382400915616));
#13104=CARTESIAN_POINT('Ctrl Pts',(6.09247560886973,-1.72763070594891,9.65050885529362));
#13105=CARTESIAN_POINT('Ctrl Pts',(5.9004466135813,-1.83173130853402,9.63748319666908));
#13106=CARTESIAN_POINT('Ctrl Pts',(5.74732598455105,-1.89177683628475,9.62825747267546));
#13107=CARTESIAN_POINT('Ctrl Pts',(5.52312546357385,-1.9491781367545,9.6144809713942));
#13108=CARTESIAN_POINT('Ctrl Pts',(5.45686969536153,-1.96259805394567,9.61038651847628));
#13109=CARTESIAN_POINT('Ctrl Pts',(5.37463635595553,-1.97494738745605,9.60521385785075));
#13110=CARTESIAN_POINT('Ctrl Pts',(5.35918089712315,-1.9770832962727,9.60423788239153));
#13111=CARTESIAN_POINT('Ctrl Pts',(5.33465200774986,-1.98018033692472,9.60268227035092));
#13112=CARTESIAN_POINT('Ctrl Pts',(5.32559409753436,-1.98126092585779,9.60210638587147));
#13113=CARTESIAN_POINT('Ctrl Pts',(5.30854148282648,-1.9831767266888,9.60101937934311));
#13114=CARTESIAN_POINT('Ctrl Pts',(5.30054849794739,-1.98402582017711,9.60050870355426));
#13115=CARTESIAN_POINT('Ctrl Pts',(5.28255229761046,-1.98582762425466,9.59935619130425));
#13116=CARTESIAN_POINT('Ctrl Pts',(5.27254663413481,-1.98675309849769,9.598713516167));
#13117=CARTESIAN_POINT('Ctrl Pts',(5.24693463544017,-1.98892704059709,9.59706340432625));
#13118=CARTESIAN_POINT('Ctrl Pts',(5.23132004967282,-1.99006742453171,9.59605262991334));
#13119=CARTESIAN_POINT('Ctrl Pts',(5.12697557375343,-1.99645415556563,9.58926492181038));
#13120=CARTESIAN_POINT('Ctrl Pts',(5.03800585766431,-1.99594792476099,9.58331037962471));
#13121=CARTESIAN_POINT('Ctrl Pts',(4.81878094809907,-1.98003087160968,9.56825426549758));
#13122=CARTESIAN_POINT('Ctrl Pts',(4.68944631896635,-1.9577143797468,9.55901893538542));
#13123=CARTESIAN_POINT('Ctrl Pts',(4.50230976806325,-1.90607695918899,9.5456480602962));
#13124=CARTESIAN_POINT('Ctrl Pts',(4.44221021137005,-1.88637728108261,9.5413581719478));
#13125=CARTESIAN_POINT('Ctrl Pts',(4.37370461417087,-1.86025619220699,9.53654793882348));
#13126=CARTESIAN_POINT('Ctrl Pts',(4.36429448228101,-1.85658602389859,9.5358889991515));
#13127=CARTESIAN_POINT('Ctrl Pts',(4.3499122580467,-1.85085038984857,9.53488511188149));
#13128=CARTESIAN_POINT('Ctrl Pts',(4.34492013701131,-1.8488360715766,9.53453725765405));
#13129=CARTESIAN_POINT('Ctrl Pts',(4.33577275985302,-1.84510198044021,9.53390104379138));
#13130=CARTESIAN_POINT('Ctrl Pts',(4.33161517102542,-1.84338836833191,9.53361233537026));
#13131=CARTESIAN_POINT('Ctrl Pts',(4.32226362220931,-1.83949694067467,9.53296396369223));
#13132=CARTESIAN_POINT('Ctrl Pts',(4.31707307659657,-1.83731118306846,9.53260478270446));
#13133=CARTESIAN_POINT('Ctrl Pts',(4.30181944793839,-1.83081163019887,9.5315510989295));
#13134=CARTESIAN_POINT('Ctrl Pts',(4.29178235185806,-1.82643685349128,9.53086014382531));
#13135=CARTESIAN_POINT('Ctrl Pts',(4.20062818028855,-1.78580997186265,9.52460237576486));
#13136=CARTESIAN_POINT('Ctrl Pts',(4.12197095640795,-1.74425379498136,9.51932590898579));
#13137=CARTESIAN_POINT('Ctrl Pts',(3.94705508826657,-1.63632261763769,9.50730098817407));
#13138=CARTESIAN_POINT('Ctrl Pts',(3.85333917991286,-1.56646973547093,9.50062221577276));
#13139=CARTESIAN_POINT('Ctrl Pts',(3.72780610447813,-1.45453399966291,9.49066909945868));
#13140=CARTESIAN_POINT('Ctrl Pts',(3.69069277409877,-1.41876566282053,9.4875822401573));
#13141=CARTESIAN_POINT('Ctrl Pts',(3.63145465382288,-1.35707428007224,9.48236408210045));
#13142=CARTESIAN_POINT('Ctrl Pts',(3.60853402830026,-1.3319489670316,9.48026578004398));
#13143=CARTESIAN_POINT('Ctrl Pts',(3.578160135571,-1.29689411135084,9.47736679987743));
#13144=CARTESIAN_POINT('Ctrl Pts',(3.57013995786508,-1.28746190784513,9.47658950366655));
#13145=CARTESIAN_POINT('Ctrl Pts',(3.55681125577626,-1.27148757459588,9.47527729677973));
#13146=CARTESIAN_POINT('Ctrl Pts',(3.55145536234603,-1.26498528707381,9.47474432206891));
#13147=CARTESIAN_POINT('Ctrl Pts',(3.54096226265785,-1.25208049566206,9.47368870969787));
#13148=CARTESIAN_POINT('Ctrl Pts',(3.53582306915413,-1.24567981707606,9.47316616648768));
#13149=CARTESIAN_POINT('Ctrl Pts',(3.5245855286729,-1.23150554029621,9.47201116258807));
#13150=CARTESIAN_POINT('Ctrl Pts',(3.51850516557976,-1.22371802365883,9.47137800637246));
#13151=CARTESIAN_POINT('Ctrl Pts',(3.49726382693966,-1.1960921828152,9.46913665044792));
#13152=CARTESIAN_POINT('Ctrl Pts',(3.48241823441085,-1.17601537722967,9.46751625563855));
#13153=CARTESIAN_POINT('Ctrl Pts',(3.38512038145608,-1.0391298215808,9.45651984453848));
#13154=CARTESIAN_POINT('Ctrl Pts',(3.31507053328199,-0.914046248028136,
9.44667503502914));
#13155=CARTESIAN_POINT('Ctrl Pts',(3.22361127193429,-0.699611164795465,
9.43042647786043));
#13156=CARTESIAN_POINT('Ctrl Pts',(3.19389125817874,-0.614335779374709,
9.42412306870551));
#13157=CARTESIAN_POINT('Ctrl Pts',(3.16299192542781,-0.501611846912927,
9.41618806453014));
#13158=CARTESIAN_POINT('Ctrl Pts',(3.15645637525136,-0.475745449077102,
9.41439398017825));
#13159=CARTESIAN_POINT('Ctrl Pts',(3.14643835506666,-0.432457659654682,
9.4114441045883));
#13160=CARTESIAN_POINT('Ctrl Pts',(3.14266630746869,-0.415107413588062,
9.41027567582744));
#13161=CARTESIAN_POINT('Ctrl Pts',(3.13778028132236,-0.39109303702865,9.40867973581492));
#13162=CARTESIAN_POINT('Ctrl Pts',(3.1364678676022,-0.384470751620982,9.40824185674323));
#13163=CARTESIAN_POINT('Ctrl Pts',(3.13430729209359,-0.373270865109169,
9.40750519522455));
#13164=CARTESIAN_POINT('Ctrl Pts',(3.13344149647407,-0.368696763301027,
9.40720543445994));
#13165=CARTESIAN_POINT('Ctrl Pts',(3.13181689183311,-0.35994625292207,9.40663412232349));
#13166=CARTESIAN_POINT('Ctrl Pts',(3.13105539197332,-0.355770410303584,
9.40636241480066));
#13167=CARTESIAN_POINT('Ctrl Pts',(3.12927032448868,-0.345801428119675,
9.40571591472891));
#13168=CARTESIAN_POINT('Ctrl Pts',(3.12825903622795,-0.34000608898839,9.40534180751977));
#13169=CARTESIAN_POINT('Ctrl Pts',(3.12474215280575,-0.319311862415041,
9.40401181569426));
#13170=CARTESIAN_POINT('Ctrl Pts',(3.12238012467823,-0.304388649727275,
9.40306358849415));
#13171=CARTESIAN_POINT('Ctrl Pts',(3.10010148894006,-0.15247438414952,9.39350797008247));
#13172=CARTESIAN_POINT('Ctrl Pts',(3.09432419758453,-0.0137696955232201,
9.38556616124658));
#13173=CARTESIAN_POINT('Ctrl Pts',(3.11128240416563,0.25755680127145,9.36977508909929));
#13174=CARTESIAN_POINT('Ctrl Pts',(3.13293257237779,0.389493497569308,9.36196463275907));
#13175=CARTESIAN_POINT('Ctrl Pts',(3.1725849889209,0.536867604732247,9.35251446783645));
#13176=CARTESIAN_POINT('Ctrl Pts',(3.17785640447052,0.555386647847233,9.35131406042808));
#13177=CARTESIAN_POINT('Ctrl Pts',(3.18624168023227,0.583303649203234,9.34948360208502));
#13178=CARTESIAN_POINT('Ctrl Pts',(3.18915887780729,0.592759849276397,9.34885992394804));
#13179=CARTESIAN_POINT('Ctrl Pts',(3.19456932430477,0.609845615308215,9.34772623526088));
#13180=CARTESIAN_POINT('Ctrl Pts',(3.19703850463564,0.617482627085696,9.34721701983474));
#13181=CARTESIAN_POINT('Ctrl Pts',(3.2024461017685,0.63386943731624,9.34611895725713));
#13182=CARTESIAN_POINT('Ctrl Pts',(3.20539928343338,0.642614130931088,9.34552963529677));
#13183=CARTESIAN_POINT('Ctrl Pts',(3.2135336148364,0.666160409487546,9.34393358603061));
#13184=CARTESIAN_POINT('Ctrl Pts',(3.21882871333236,0.680921661336426,9.34292312734048));
#13185=CARTESIAN_POINT('Ctrl Pts',(3.24596467076561,0.753851691292376,9.33788043124632));
#13186=CARTESIAN_POINT('Ctrl Pts',(3.27033891862018,0.811034773642312,9.33376487718167));
#13187=CARTESIAN_POINT('Ctrl Pts',(3.37172755740359,1.02112369187189,9.31802145785408));
#13188=CARTESIAN_POINT('Ctrl Pts',(3.46564442619002,1.16504468483995,9.30587383360492));
#13189=CARTESIAN_POINT('Ctrl Pts',(3.61130597810591,1.33566129315734,9.29050491391615));
#13190=CARTESIAN_POINT('Ctrl Pts',(3.64747237274151,1.3747432732696,9.28691300176108));
#13191=CARTESIAN_POINT('Ctrl Pts',(3.69203359655889,1.41918870126688,9.28278686651145));
#13192=CARTESIAN_POINT('Ctrl Pts',(3.69895515817053,1.42599224117467,9.28215406137601));
#13193=CARTESIAN_POINT('Ctrl Pts',(3.70973224106526,1.43643200632066,9.28118158470513));
#13194=CARTESIAN_POINT('Ctrl Pts',(3.71355294595723,1.44010372855299,9.28083927543976));
#13195=CARTESIAN_POINT('Ctrl Pts',(3.72064754867731,1.44686751570607,9.28020824778634));
#13196=CARTESIAN_POINT('Ctrl Pts',(3.72391726872113,1.44996370415353,9.27991922124559));
#13197=CARTESIAN_POINT('Ctrl Pts',(3.73137697020129,1.45697974397677,9.2792638670414));
#13198=CARTESIAN_POINT('Ctrl Pts',(3.73557339323591,1.4608926042123,9.27889806950475));
#13199=CARTESIAN_POINT('Ctrl Pts',(3.74654294434242,1.47103278996635,9.27794912108883));
#13200=CARTESIAN_POINT('Ctrl Pts',(3.75334246628194,1.47723153918274,9.27736804820794));
#13201=CARTESIAN_POINT('Ctrl Pts',(3.79974471839693,1.51894969481013,9.2734487175258));
#13202=CARTESIAN_POINT('Ctrl Pts',(3.84071547388534,1.55292296076116,9.27021382853565));
#13203=CARTESIAN_POINT('Ctrl Pts',(4.01422392448764,1.6854527125434,9.25718033031886));
#13204=CARTESIAN_POINT('Ctrl Pts',(4.15738888706473,1.76900637772122,9.24788829119936));
#13205=CARTESIAN_POINT('Ctrl Pts',(4.37151336828064,1.86061301819059,9.23402615948148));
#13206=CARTESIAN_POINT('Ctrl Pts',(4.43511645045457,1.88406920465866,9.22992064547232));
#13207=CARTESIAN_POINT('Ctrl Pts',(4.51469103213906,1.90889306332427,9.22473555252779));
#13208=CARTESIAN_POINT('Ctrl Pts',(4.5296508464989,1.91336782851897,9.22375881523377));
#13209=CARTESIAN_POINT('Ctrl Pts',(4.55343357211658,1.9201785335369,9.22220226671657));
#13210=CARTESIAN_POINT('Ctrl Pts',(4.56222283199847,1.9226304024417,9.22162621544305));
#13211=CARTESIAN_POINT('Ctrl Pts',(4.57878515899622,1.92712840981505,9.22053906609375));
#13212=CARTESIAN_POINT('Ctrl Pts',(4.58655439600613,1.92918804435095,9.220028415565));
#13213=CARTESIAN_POINT('Ctrl Pts',(4.60406012394034,1.93371577698622,9.21887619012968));
#13214=CARTESIAN_POINT('Ctrl Pts',(4.61380317943314,1.9361573871178,9.21823377831003));
#13215=CARTESIAN_POINT('Ctrl Pts',(4.63876593118917,1.94221305206307,9.21658479353995));
#13216=CARTESIAN_POINT('Ctrl Pts',(4.65401022985351,1.94572179572118,9.21557489062507));
#13217=CARTESIAN_POINT('Ctrl Pts',(4.75576409181738,1.96788535423448,9.208813282744));
#13218=CARTESIAN_POINT('Ctrl Pts',(4.84337972908982,1.98094211418654,9.20288557826055));
#13219=CARTESIAN_POINT('Ctrl Pts',(5.07638100322952,1.99995881899078,9.18687517736236));
#13220=CARTESIAN_POINT('Ctrl Pts',(5.22204591425514,1.99591982084095,9.17659012793101));
#13221=CARTESIAN_POINT('Ctrl Pts',(5.41571784836937,1.96924738150639,9.16322156967735));
#13222=CARTESIAN_POINT('Ctrl Pts',(5.46518936716049,1.96052031732577,9.15983880124491));
#13223=CARTESIAN_POINT('Ctrl Pts',(5.52363081081484,1.94791884449774,9.15592044176644));
#13224=CARTESIAN_POINT('Ctrl Pts',(5.53296423654172,1.94583597450386,9.15529705678845));
#13225=CARTESIAN_POINT('Ctrl Pts',(5.54741591761246,1.94250162204944,9.154335925822));
#13226=CARTESIAN_POINT('Ctrl Pts',(5.55254465176657,1.94129688016715,9.15399563628537));
#13227=CARTESIAN_POINT('Ctrl Pts',(5.56205145050944,1.93902395013897,9.15336643493351));
#13228=CARTESIAN_POINT('Ctrl Pts',(5.56643064118469,1.93796125234192,9.15307722994925));
#13229=CARTESIAN_POINT('Ctrl Pts',(5.57641814168836,1.93550171913232,9.15241905093835));
#13230=CARTESIAN_POINT('Ctrl Pts',(5.58202400396105,1.93409534508421,9.15205062595321));
#13231=CARTESIAN_POINT('Ctrl Pts',(5.59667348040336,1.93035239781506,9.15109027859986));
#13232=CARTESIAN_POINT('Ctrl Pts',(5.60570705591467,1.92797660299644,9.1505005169776));
#13233=CARTESIAN_POINT('Ctrl Pts',(5.66928952027276,1.91077626534526,9.14636454296859));
#13234=CARTESIAN_POINT('Ctrl Pts',(5.72320870401148,1.89370087524915,9.14293517080237));
#13235=CARTESIAN_POINT('Ctrl Pts',(5.92859991479799,1.81891198074968,9.12991935822585));
#13236=CARTESIAN_POINT('Ctrl Pts',(6.0735445964106,1.74512042158038,9.12078764113241));
#13237=CARTESIAN_POINT('Ctrl Pts',(6.26378708595887,1.61701864263524,9.10713270216937));
#13238=CARTESIAN_POINT('Ctrl Pts',(6.31766017312476,1.57663783125968,9.10305428042643));
#13239=CARTESIAN_POINT('Ctrl Pts',(6.38136796813201,1.52364992181965,9.09789963969131));
#13240=CARTESIAN_POINT('Ctrl Pts',(6.39323200251213,1.5135446641578,9.09692477334345));
#13241=CARTESIAN_POINT('Ctrl Pts',(6.41184791224716,1.4973082478483,9.09537052467234));
#13242=CARTESIAN_POINT('Ctrl Pts',(6.41867839791675,1.49126787845384,9.09479488303838));
#13243=CARTESIAN_POINT('Ctrl Pts',(6.43145216248658,1.47981469127294,9.09370808407573));
#13244=CARTESIAN_POINT('Ctrl Pts',(6.43740461995159,1.47441234861633,9.09319737113171));
#13245=CARTESIAN_POINT('Ctrl Pts',(6.45072837455823,1.46217226511459,9.09204443948996));
#13246=CARTESIAN_POINT('Ctrl Pts',(6.45808091142421,1.45531451394619,9.09140137953981));
#13247=CARTESIAN_POINT('Ctrl Pts',(6.47676322007462,1.43762342874743,9.08974962024798));
#13248=CARTESIAN_POINT('Ctrl Pts',(6.48801753812336,1.42671175624055,9.08873757186156));
#13249=CARTESIAN_POINT('Ctrl Pts',(6.5626221999405,1.35265275062906,9.08191189022883));
#13250=CARTESIAN_POINT('Ctrl Pts',(6.62178324286563,1.28544723489754,9.07591829454578));
#13251=CARTESIAN_POINT('Ctrl Pts',(6.75564465433856,1.11103694458457,9.06085433178684));
#13252=CARTESIAN_POINT('Ctrl Pts',(6.82471376230149,1.00003446359356,9.05165506144627));
#13253=CARTESIAN_POINT('Ctrl Pts',(6.91039312417284,0.826498006955609,9.03832574008705));
#13254=CARTESIAN_POINT('Ctrl Pts',(6.93563543445955,0.768605767662508,9.03404214709338));
#13255=CARTESIAN_POINT('Ctrl Pts',(6.96168395794934,0.700171749112511,9.02923802531838));
#13256=CARTESIAN_POINT('Ctrl Pts',(6.9652042514705,0.690707816397884,9.02857928952517));
#13257=CARTESIAN_POINT('Ctrl Pts',(6.97049074950568,0.676158478411955,9.02757564690223));
#13258=CARTESIAN_POINT('Ctrl Pts',(6.97230842386432,0.671092139014209,9.02722783558428));
#13259=CARTESIAN_POINT('Ctrl Pts',(6.97560706783441,0.66177953018706,9.02659166274013));
#13260=CARTESIAN_POINT('Ctrl Pts',(6.97709418342905,0.657535616790079,9.02630295273997));
#13261=CARTESIAN_POINT('Ctrl Pts',(6.98041169206445,0.647964563429164,9.02565453099698));
#13262=CARTESIAN_POINT('Ctrl Pts',(6.98223387850055,0.642634685849197,9.02529530187292));
#13263=CARTESIAN_POINT('Ctrl Pts',(6.98753257020638,0.626918906040165,9.02424134427596));
#13264=CARTESIAN_POINT('Ctrl Pts',(6.99094621120514,0.616511811453599,9.02355016624073));
#13265=CARTESIAN_POINT('Ctrl Pts',(7.02195676509225,0.519273465365948,9.01715038345162));
#13266=CARTESIAN_POINT('Ctrl Pts',(7.04366360600454,0.430663346349435,9.01174733098971));
#13267=CARTESIAN_POINT('Ctrl Pts',(7.07867991309622,0.228763564477506,8.99976859373272));
#13268=CARTESIAN_POINT('Ctrl Pts',(7.08849541674042,0.115202496718061,8.99324927811289));
#13269=CARTESIAN_POINT('Ctrl Pts',(7.0885769860218,0.000949408244314996,
8.98649007198198));
#13270=CARTESIAN_POINT('Ctrl Pts',(7.08857715545312,0.000474702745457553,
8.98646198520671));
#13271=CARTESIAN_POINT('Ctrl Pts',(7.08857715545311,-2.42987105381791E-11,
8.98643389536847));
#13272=CARTESIAN_POINT('Ctrl Pts',(7.08857715545311,2.37118846529926E-11,
8.82627928344061));
#13273=CARTESIAN_POINT('Ctrl Pts',(7.08857715545221,0.0760979497660257,
8.83078414338272));
#13274=CARTESIAN_POINT('Ctrl Pts',(7.08422265935748,0.152126168627862,8.835372281333));
#13275=CARTESIAN_POINT('Ctrl Pts',(7.07380624533671,0.242776038297638,8.84103906841134));
#13276=CARTESIAN_POINT('Ctrl Pts',(7.07190396794442,0.257816805620438,8.84198571175015));
#13277=CARTESIAN_POINT('Ctrl Pts',(7.0684768006953,0.282638092816422,8.84355918120427));
#13278=CARTESIAN_POINT('Ctrl Pts',(7.06705020351653,0.292431718342481,8.8441829234237));
#13279=CARTESIAN_POINT('Ctrl Pts',(7.06433477441333,0.310147881550535,8.84531668026858));
#13280=CARTESIAN_POINT('Ctrl Pts',(7.06307088492161,0.31807407265161,8.84582589931603));
#13281=CARTESIAN_POINT('Ctrl Pts',(7.06025093466268,0.335097388987296,8.84692391548401));
#13282=CARTESIAN_POINT('Ctrl Pts',(7.05867951050679,0.344191745515105,8.84751318705433));
#13283=CARTESIAN_POINT('Ctrl Pts',(7.05419493632479,0.369113414579321,8.84913551434706));
#13284=CARTESIAN_POINT('Ctrl Pts',(7.05115332234949,0.384916614859681,8.85017260581042));
#13285=CARTESIAN_POINT('Ctrl Pts',(7.03271965249735,0.47481637841628,8.85612140679021));
#13286=CARTESIAN_POINT('Ctrl Pts',(7.01331377466768,0.548017677217242,8.86115962069973));
#13287=CARTESIAN_POINT('Ctrl Pts',(6.95485744178155,0.726797709814179,8.87394924089058));
#13288=CARTESIAN_POINT('Ctrl Pts',(6.91094503843883,0.830510371622907,8.88181566906143));
#13289=CARTESIAN_POINT('Ctrl Pts',(6.81398859389791,1.01449628934127,8.89628916999919));
#13290=CARTESIAN_POINT('Ctrl Pts',(6.76341882492772,1.09573082704069,8.90288524759426));
#13291=CARTESIAN_POINT('Ctrl Pts',(6.70077471736184,1.18189128282182,8.90988690350465));
#13292=CARTESIAN_POINT('Ctrl Pts',(6.69426228995225,1.19069511812867,8.91060232555328));
#13293=CARTESIAN_POINT('Ctrl Pts',(6.68429084625799,1.20394540279637,8.91167851831354));
#13294=CARTESIAN_POINT('Ctrl Pts',(6.68088507665168,1.20843139702795,8.9120427739568));
#13295=CARTESIAN_POINT('Ctrl Pts',(6.67472595970842,1.21647308046997,8.91269547785338));
#13296=CARTESIAN_POINT('Ctrl Pts',(6.67197956142243,1.22003392146302,8.91298439192521));
#13297=CARTESIAN_POINT('Ctrl Pts',(6.66591923884948,1.22783672294277,8.91361725701998));
#13298=CARTESIAN_POINT('Ctrl Pts',(6.66260018139192,1.23207456414338,8.91396084101251));
#13299=CARTESIAN_POINT('Ctrl Pts',(6.6530050411444,1.24422420269283,8.91494565132783));
#13300=CARTESIAN_POINT('Ctrl Pts',(6.64668587034087,1.25210197966945,8.91558392275841));
#13301=CARTESIAN_POINT('Ctrl Pts',(6.60041323684749,1.30889847037254,8.92018647651089));
#13302=CARTESIAN_POINT('Ctrl Pts',(6.55821184370865,1.35594838761058,8.92400395321448));
#13303=CARTESIAN_POINT('Ctrl Pts',(6.42201128856213,1.49400554635726,8.93550538715055));
#13304=CARTESIAN_POINT('Ctrl Pts',(6.32124600335177,1.57783756365826,8.94294624494332));
#13305=CARTESIAN_POINT('Ctrl Pts',(6.13925826234273,1.7011868816636,8.95587898018585));
#13306=CARTESIAN_POINT('Ctrl Pts',(6.06226250357025,1.74616525125904,8.96121628034075));
#13307=CARTESIAN_POINT('Ctrl Pts',(5.96850265769208,1.79282337478631,8.96771574529454));
#13308=CARTESIAN_POINT('Ctrl Pts',(5.95439875500756,1.799635904198,8.96869323865727));
#13309=CARTESIAN_POINT('Ctrl Pts',(5.93111551755111,1.81054598757118,8.9703073342681));
#13310=CARTESIAN_POINT('Ctrl Pts',(5.9219826771311,1.81474157950974,8.97094056426278));
#13311=CARTESIAN_POINT('Ctrl Pts',(5.90548923246542,1.82216817207927,8.97208450831558));
#13312=CARTESIAN_POINT('Ctrl Pts',(5.89814001994176,1.82542405690789,8.97259435960373));
#13313=CARTESIAN_POINT('Ctrl Pts',(5.88241018807183,1.83227933229988,8.97368598538797));
#13314=CARTESIAN_POINT('Ctrl Pts',(5.87402418296078,1.83586582969306,8.97426818345401));
#13315=CARTESIAN_POINT('Ctrl Pts',(5.85123279958213,1.84542880722114,8.97585123020299));
#13316=CARTESIAN_POINT('Ctrl Pts',(5.83678168750217,1.85129396173417,8.97685579495235));
#13317=CARTESIAN_POINT('Ctrl Pts',(5.75945496379858,1.8816267248029,8.98223666026397));
#13318=CARTESIAN_POINT('Ctrl Pts',(5.69544365968772,1.90305946659127,8.98671247759826));
#13319=CARTESIAN_POINT('Ctrl Pts',(5.473269407412,1.96511912721978,9.00232246334067));
#13320=CARTESIAN_POINT('Ctrl Pts',(5.31127170631543,1.98956711685327,9.0138902050785));
#13321=CARTESIAN_POINT('Ctrl Pts',(5.09289195806131,1.99551528072559,9.02888123939717));
#13322=CARTESIAN_POINT('Ctrl Pts',(5.03760015232606,1.99472349654567,9.03261826235321));
#13323=CARTESIAN_POINT('Ctrl Pts',(4.97313342366823,1.9911169897593,9.03685610531516));
#13324=CARTESIAN_POINT('Ctrl Pts',(4.96386267486578,1.99053336709388,9.03746263177369));
#13325=CARTESIAN_POINT('Ctrl Pts',(4.94884619986041,1.98948267360683,9.0384399950554));
#13326=CARTESIAN_POINT('Ctrl Pts',(4.94309795245298,1.98905542794523,9.0388129207009));
#13327=CARTESIAN_POINT('Ctrl Pts',(4.9328603819417,1.98824987258025,9.03947485346613));
#13328=CARTESIAN_POINT('Ctrl Pts',(4.92837041459726,1.9878812656327,9.03976438704435));
#13329=CARTESIAN_POINT('Ctrl Pts',(4.91862140371193,1.98704765391972,9.04039135086999));
#13330=CARTESIAN_POINT('Ctrl Pts',(4.91336294831854,1.98657698211864,9.04072846365312));
#13331=CARTESIAN_POINT('Ctrl Pts',(4.89853375228362,1.9851902893926,9.04167630579501));
#13332=CARTESIAN_POINT('Ctrl Pts',(4.88896752370563,1.98422592928882,9.04228441539479));
#13333=CARTESIAN_POINT('Ctrl Pts',(4.82843013702353,1.97768074990426,9.04611364248889));
#13334=CARTESIAN_POINT('Ctrl Pts',(4.77767841846249,1.97020498653982,9.04923848047464));
#13335=CARTESIAN_POINT('Ctrl Pts',(4.57638209666626,1.93257341706803,9.06148933290478));
#13336=CARTESIAN_POINT('Ctrl Pts',(4.42925148129793,1.88704385505036,9.07015789140508));
#13337=CARTESIAN_POINT('Ctrl Pts',(4.21577461234178,1.79288035495328,9.08394381316185));
#13338=CARTESIAN_POINT('Ctrl Pts',(4.14476461206291,1.75632409323216,9.08874687082529));
#13339=CARTESIAN_POINT('Ctrl Pts',(4.06298031694305,1.70781043019178,9.0946512422459));
#13340=CARTESIAN_POINT('Ctrl Pts',(4.04991136331929,1.69985336678142,9.09560649252288));
#13341=CARTESIAN_POINT('Ctrl Pts',(4.02850546524009,1.686480376724,9.09719130245843));
#13342=CARTESIAN_POINT('Ctrl Pts',(4.02011502125607,1.68115097830449,9.0978176989037));
#13343=CARTESIAN_POINT('Ctrl Pts',(4.00501956260879,1.67140361923066,9.09895428425956));
#13344=CARTESIAN_POINT('Ctrl Pts',(3.9983006873012,1.66700743463307,9.09946365878022));
#13345=CARTESIAN_POINT('Ctrl Pts',(3.98394269266574,1.65748865363546,9.10055978438395));
#13346=CARTESIAN_POINT('Ctrl Pts',(3.9763121190566,1.65235356278161,9.1011469952109));
#13347=CARTESIAN_POINT('Ctrl Pts',(3.95554848108372,1.63817079579533,9.10275785618563));
#13348=CARTESIAN_POINT('Ctrl Pts',(3.94248820141562,1.62901825809904,9.10378544757433));
#13349=CARTESIAN_POINT('Ctrl Pts',(3.8701535440139,1.57702231991211,9.10955899788924));
#13350=CARTESIAN_POINT('Ctrl Pts',(3.81316732380429,1.53110570448652,9.11442274949977));
#13351=CARTESIAN_POINT('Ctrl Pts',(3.61247074237118,1.35033805252826,9.13276218955385));
#13352=CARTESIAN_POINT('Ctrl Pts',(3.48645868926604,1.19757455498695,9.14689395726083));
#13353=CARTESIAN_POINT('Ctrl Pts',(3.37418982158714,1.01109060527131,9.16140627367036));
#13354=CARTESIAN_POINT('Ctrl Pts',(3.36378099166898,0.993175273625215,9.16277416484257));
#13355=CARTESIAN_POINT('Ctrl Pts',(3.35003282845752,0.968640151642241,9.16460882973998));
#13356=CARTESIAN_POINT('Ctrl Pts',(3.346448893022,0.962159867370846,9.16508979893298));
#13357=CARTESIAN_POINT('Ctrl Pts',(3.34083303921776,0.951870697021146,9.16584759161114));
#13358=CARTESIAN_POINT('Ctrl Pts',(3.3387772980346,0.948074993995554,9.1661258864888));
#13359=CARTESIAN_POINT('Ctrl Pts',(3.33455709681111,0.940222084572862,9.16669901085324));
#13360=CARTESIAN_POINT('Ctrl Pts',(3.33239433332008,0.93616404601662,9.16699372195623));
#13361=CARTESIAN_POINT('Ctrl Pts',(3.32723235133456,0.926397292947214,9.16769961272918));
#13362=CARTESIAN_POINT('Ctrl Pts',(3.32424671266118,0.920681381132768,9.16810994574711));
#13363=CARTESIAN_POINT('Ctrl Pts',(3.3140354567574,0.900899072733677,9.16952083754897));
#13364=CARTESIAN_POINT('Ctrl Pts',(3.30694920314536,0.886760875499597,9.17051313686825));
#13365=CARTESIAN_POINT('Ctrl Pts',(3.26519662890606,0.800924540663502,9.17645029898195));
#13366=CARTESIAN_POINT('Ctrl Pts',(3.23467754965281,0.727279392004382,9.1811808851516));
#13367=CARTESIAN_POINT('Ctrl Pts',(3.1934935346287,0.608200205706659,9.18855867868733));
#13368=CARTESIAN_POINT('Ctrl Pts',(3.17987627503896,0.56388609139749,9.19124720347536));
#13369=CARTESIAN_POINT('Ctrl Pts',(3.13236526242235,0.387619044713416,9.20184428856065));
#13370=CARTESIAN_POINT('Ctrl Pts',(3.11048366598882,0.25283234994045,9.2097667027817));
#13371=CARTESIAN_POINT('Ctrl Pts',(3.10106095662865,0.0922878943931453,
9.2196612316521));
#13372=CARTESIAN_POINT('Ctrl Pts',(3.10007342597037,0.0676768962468813,
9.22118954601111));
#13373=CARTESIAN_POINT('Ctrl Pts',(3.09932401521739,0.03296436106125,9.22336401478594));
#13374=CARTESIAN_POINT('Ctrl Pts',(3.0991827605493,0.0228726348444884,9.22399842265227));
#13375=CARTESIAN_POINT('Ctrl Pts',(3.09906996070037,0.00526734985763139,
9.22510925584522));
#13376=CARTESIAN_POINT('Ctrl Pts',(3.09906427112982,-0.00224584441580045,
9.2255846122532));
#13377=CARTESIAN_POINT('Ctrl Pts',(3.09914133289803,-0.0179974714150017,
9.22658401629271));
#13378=CARTESIAN_POINT('Ctrl Pts',(3.09923267930035,-0.0262357017633881,
9.22710832219145));
#13379=CARTESIAN_POINT('Ctrl Pts',(3.09957266627717,-0.0459057957901291,
9.22836413746277));
#13380=CARTESIAN_POINT('Ctrl Pts',(3.09986857207116,-0.0573364496693194,
9.22909710336108));
#13381=CARTESIAN_POINT('Ctrl Pts',(3.10121707771109,-0.096431662920323,
9.2316152549893));
#13382=CARTESIAN_POINT('Ctrl Pts',(3.10274726524423,-0.124075505898767,
9.23341516284926));
#13383=CARTESIAN_POINT('Ctrl Pts',(3.10782508414471,-0.190661902722997,
9.23779946483038));
#13384=CARTESIAN_POINT('Ctrl Pts',(3.1119433354543,-0.229548196846885,9.24040044888724));
#13385=CARTESIAN_POINT('Ctrl Pts',(3.13280924536336,-0.383279842485552,
9.25084352172333));
#13386=CARTESIAN_POINT('Ctrl Pts',(3.15842089913588,-0.496680837974895,
9.25892172714264));
#13387=CARTESIAN_POINT('Ctrl Pts',(3.22486205567496,-0.70459293903088,9.27413646645248));
#13388=CARTESIAN_POINT('Ctrl Pts',(3.26343090228397,-0.799459477458545,
9.28124378889092));
#13389=CARTESIAN_POINT('Ctrl Pts',(3.31640767013586,-0.905579715879931,
9.28910683041745));
#13390=CARTESIAN_POINT('Ctrl Pts',(3.32388689301532,-0.920112035050285,
9.29018141595129));
#13391=CARTESIAN_POINT('Ctrl Pts',(3.33469378866268,-0.940490592871772,
9.29168348457136));
#13392=CARTESIAN_POINT('Ctrl Pts',(3.33787347857867,-0.94641399252528,9.29211950691601));
#13393=CARTESIAN_POINT('Ctrl Pts',(3.34328088132122,-0.956366298440255,
9.29285097176382));
#13394=CARTESIAN_POINT('Ctrl Pts',(3.34549268662557,-0.960403738683668,
9.29314739700613));
#13395=CARTESIAN_POINT('Ctrl Pts',(3.35004932808787,-0.968653546099105,
9.29375239096686));
#13396=CARTESIAN_POINT('Ctrl Pts',(3.35239548619422,-0.972865122244218,
9.29406087335462));
#13397=CARTESIAN_POINT('Ctrl Pts',(3.35844608601426,-0.983634501491481,
9.29484884699529));
#13398=CARTESIAN_POINT('Ctrl Pts',(3.36217248194113,-0.990179975922129,
9.29532696091645));
#13399=CARTESIAN_POINT('Ctrl Pts',(3.37776430662929,-1.01721003561123,9.29729869049969));
#13400=CARTESIAN_POINT('Ctrl Pts',(3.38995738761668,-1.03750464481498,9.29877268952594));
#13401=CARTESIAN_POINT('Ctrl Pts',(3.42353875935214,-1.09120918983404,9.30266924859209));
#13402=CARTESIAN_POINT('Ctrl Pts',(3.44556777915511,-1.1242073823748,9.30505926463014));
#13403=CARTESIAN_POINT('Ctrl Pts',(3.52259727882864,-1.23245627405984,9.31296181766228));
#13404=CARTESIAN_POINT('Ctrl Pts',(3.58188390471015,-1.30450798586023,9.3183309009443));
#13405=CARTESIAN_POINT('Ctrl Pts',(3.73555534470127,-1.46665510003005,9.33131554380514));
#13406=CARTESIAN_POINT('Ctrl Pts',(3.83414113913017,-1.55214826217755,9.33896163386031));
#13407=CARTESIAN_POINT('Ctrl Pts',(3.95356478482326,-1.63679316161392,9.34803926752736));
#13408=CARTESIAN_POINT('Ctrl Pts',(3.9668981282197,-1.64600154049722,9.3490499587622));
#13409=CARTESIAN_POINT('Ctrl Pts',(3.9888166389429,-1.66074791930276,9.350707700327));
#13410=CARTESIAN_POINT('Ctrl Pts',(3.99733493892073,-1.66638432119765,9.35135105546176));
#13411=CARTESIAN_POINT('Ctrl Pts',(4.01264673484449,-1.67634761549912,9.35250608373521));
#13412=CARTESIAN_POINT('Ctrl Pts',(4.01942390282066,-1.68069928230313,9.35301682243748));
#13413=CARTESIAN_POINT('Ctrl Pts',(4.03384459688311,-1.68983604430843,9.35410265339705));
#13414=CARTESIAN_POINT('Ctrl Pts',(4.04149456995901,-1.694610576574,9.35467811958011));
#13415=CARTESIAN_POINT('Ctrl Pts',(4.06206172425826,-1.70725406082268,9.35622395387176));
#13416=CARTESIAN_POINT('Ctrl Pts',(4.07503626793683,-1.71502811635564,9.35719774565479));
#13417=CARTESIAN_POINT('Ctrl Pts',(4.14059247829747,-1.75330151593455,9.36211216540894));
#13418=CARTESIAN_POINT('Ctrl Pts',(4.19445555233717,-1.78153079575272,9.36613278910501));
#13419=CARTESIAN_POINT('Ctrl Pts',(4.36590098780595,-1.86162619808905,9.37888405024058));
#13420=CARTESIAN_POINT('Ctrl Pts',(4.48725283064651,-1.90462315719648,9.38786672760109));
#13421=CARTESIAN_POINT('Ctrl Pts',(4.70526344586078,-1.95890462597907,9.40350397943443));
#13422=CARTESIAN_POINT('Ctrl Pts',(4.80022096742692,-1.9753705601034,9.41014932078351));
#13423=CARTESIAN_POINT('Ctrl Pts',(4.90690254671284,-1.98600268619209,9.41719590674751));
#13424=CARTESIAN_POINT('Ctrl Pts',(4.91780825444627,-1.98699895277892,9.41791135234793));
#13425=CARTESIAN_POINT('Ctrl Pts',(4.93433489835356,-1.98837157127777,9.41898757340141));
#13426=CARTESIAN_POINT('Ctrl Pts',(4.93994992586598,-1.98881398970185,9.41935183405247));
#13427=CARTESIAN_POINT('Ctrl Pts',(4.95005132119147,-1.98956686098157,9.42000454319236));
#13428=CARTESIAN_POINT('Ctrl Pts',(4.9545369111246,-1.98988592985929,9.42029345753496));
#13429=CARTESIAN_POINT('Ctrl Pts',(4.96439410300606,-1.99055359664685,9.42092631882941));
#13430=CARTESIAN_POINT('Ctrl Pts',(4.96976604529517,-1.99089562226996,9.42126989878135));
#13431=CARTESIAN_POINT('Ctrl Pts',(4.98521986352393,-1.9918167575792,9.42225468584763));
#13432=CARTESIAN_POINT('Ctrl Pts',(4.99530501221645,-1.9923410694518,9.42289293828642));
#13433=CARTESIAN_POINT('Ctrl Pts',(5.06848361258688,-1.99558848725332,9.42749491824918));
#13434=CARTESIAN_POINT('Ctrl Pts',(5.131677675699,-1.99539087944476,9.43131188180093));
#13435=CARTESIAN_POINT('Ctrl Pts',(5.32725024375857,-1.98548215522978,9.44292544165388));
#13436=CARTESIAN_POINT('Ctrl Pts',(5.45874131759604,-1.96557019456372,9.45047012875908));
#13437=CARTESIAN_POINT('Ctrl Pts',(5.67181894277521,-1.91116838431199,9.46341675945952));
#13438=CARTESIAN_POINT('Ctrl Pts',(5.75483485760147,-1.88406612541645,9.46864839780292));
#13439=CARTESIAN_POINT('Ctrl Pts',(5.85031925129852,-1.84580383195983,9.47503251129424));
#13440=CARTESIAN_POINT('Ctrl Pts',(5.86476498519205,-1.83981708823951,9.47600841563369));
#13441=CARTESIAN_POINT('Ctrl Pts',(5.88837011826137,-1.82970759861217,9.47762042018723));
#13442=CARTESIAN_POINT('Ctrl Pts',(5.89757158047095,-1.82568434005061,9.47825316327613));
#13443=CARTESIAN_POINT('Ctrl Pts',(5.91408191052871,-1.81831633672508,9.47939657954902));
#13444=CARTESIAN_POINT('Ctrl Pts',(5.92140173058969,-1.81499655182456,9.47990639340876));
#13445=CARTESIAN_POINT('Ctrl Pts',(5.92884967517527,-1.81156423589755,9.48042812604344));
#13446=CARTESIAN_POINT('Ctrl Pts',(5.92899814071914,-1.81149579480493,9.4804385273545));
#13447=CARTESIAN_POINT('Ctrl Pts',(5.92928339003147,-1.81136425527705,9.48045851390645));
#13448=CARTESIAN_POINT('Ctrl Pts',(5.9294201750788,-1.8113011595933,9.48046809905304));
#13449=CARTESIAN_POINT('Ctrl Pts',(5.92968300903404,-1.81117988444209,9.48048651900443));
#13450=CARTESIAN_POINT('Ctrl Pts',(5.92980905902013,-1.81112170730783,9.48049535372895));
#13451=CARTESIAN_POINT('Ctrl Pts',(5.93005128995293,-1.81100987732168,9.48051233315567));
#13452=CARTESIAN_POINT('Ctrl Pts',(5.93016747181586,-1.81095622644582,9.48052047778998));
#13453=CARTESIAN_POINT('Ctrl Pts',(5.9303907614827,-1.81085308887491,9.48053613238079));
#13454=CARTESIAN_POINT('Ctrl Pts',(5.93049787005777,-1.81080360385768,9.48054364227931));
#13455=CARTESIAN_POINT('Ctrl Pts',(5.93070374196281,-1.81070846722772,9.48055807817218));
#13456=CARTESIAN_POINT('Ctrl Pts',(5.93080250595016,-1.81066281703651,9.48056500411757));
#13457=CARTESIAN_POINT('Ctrl Pts',(5.93099235691375,-1.81057504623099,9.48057831868741));
#13458=CARTESIAN_POINT('Ctrl Pts',(5.93108344444756,-1.81053292682299,9.48058470727029));
#13459=CARTESIAN_POINT('Ctrl Pts',(5.93125855526064,-1.81045193851897,9.48059698985632));
#13460=CARTESIAN_POINT('Ctrl Pts',(5.93134257902751,-1.81041307064042,9.48060288382517));
#13461=CARTESIAN_POINT('Ctrl Pts',(5.93150412438894,-1.81033832901781,9.48061421641117));
#13462=CARTESIAN_POINT('Ctrl Pts',(5.93158164638699,-1.81030245614279,9.48061965499843));
#13463=CARTESIAN_POINT('Ctrl Pts',(5.93173070388572,-1.81023346898623,9.48063011282872));
#13464=CARTESIAN_POINT('Ctrl Pts',(5.9318022397345,-1.81020035544066,9.48063513204671));
#13465=CARTESIAN_POINT('Ctrl Pts',(5.93193979827163,-1.81013667045927,9.48064478420504));
#13466=CARTESIAN_POINT('Ctrl Pts',(5.93200582123244,-1.8101060996599,9.48064941712247));
#13467=CARTESIAN_POINT('Ctrl Pts',(5.93213278846033,-1.81004730122706,9.48065832704396));
#13468=CARTESIAN_POINT('Ctrl Pts',(5.93219373299605,-1.81001907411771,9.48066260403112));
#13469=CARTESIAN_POINT('Ctrl Pts',(5.93231094247213,-1.80996478011355,9.48067082999567));
#13470=CARTESIAN_POINT('Ctrl Pts',(5.93236720762715,-1.80993871367104,9.4806747789577));
#13471=CARTESIAN_POINT('Ctrl Pts',(5.93250999999545,-1.80987255293429,9.48068480126619));
#13472=CARTESIAN_POINT('Ctrl Pts',(5.93259652554851,-1.80983245505883,9.48069087473609));
#13473=CARTESIAN_POINT('Ctrl Pts',(5.93276809181106,-1.80975293247147,9.48070291827513));
#13474=CARTESIAN_POINT('Ctrl Pts',(5.93285313261335,-1.80971350797206,9.48070888833669));
#13475=CARTESIAN_POINT('Ctrl Pts',(5.93302176367064,-1.80963531699865,9.48072072742483));
#13476=CARTESIAN_POINT('Ctrl Pts',(5.93310535401702,-1.80959655072767,9.4807265964443));
#13477=CARTESIAN_POINT('Ctrl Pts',(5.94188974115152,-1.80552192047103,9.48134340392352));
#13478=CARTESIAN_POINT('Ctrl Pts',(5.95056119154166,-1.80142342070975,9.48195649054254));
#13479=CARTESIAN_POINT('Ctrl Pts',(5.97546048355993,-1.78943450129263,9.48372926714405));
#13480=CARTESIAN_POINT('Ctrl Pts',(5.99161091641285,-1.78138638224235,9.48489438020845));
#13481=CARTESIAN_POINT('Ctrl Pts',(6.02793467326662,-1.76266601802192,9.4875502764903));
#13482=CARTESIAN_POINT('Ctrl Pts',(6.04803821000352,-1.75186458917444,9.48904542108051));
#13483=CARTESIAN_POINT('Ctrl Pts',(6.11276662779995,-1.71564194454389,9.4939431761243));
#13484=CARTESIAN_POINT('Ctrl Pts',(6.15659329920891,-1.68884348774038,9.49739175985414));
#13485=CARTESIAN_POINT('Ctrl Pts',(6.29726581779495,-1.59518183063793,9.50889579464913));
#13486=CARTESIAN_POINT('Ctrl Pts',(6.38923092549112,-1.52144496764536,9.5171439812789));
#13487=CARTESIAN_POINT('Ctrl Pts',(6.53779882822161,-1.37903795842688,9.53144564528473));
#13488=CARTESIAN_POINT('Ctrl Pts',(6.59733706958975,-1.31387269477853,9.53751019681739));
#13489=CARTESIAN_POINT('Ctrl Pts',(6.6592029196654,-1.23642469282774,9.54402521966077));
#13490=CARTESIAN_POINT('Ctrl Pts',(6.66596222848696,-1.22781864673421,9.54474013625047));
#13491=CARTESIAN_POINT('Ctrl Pts',(6.67609188756291,-1.21470061488759,9.54581572176763));
#13492=CARTESIAN_POINT('Ctrl Pts',(6.67951438762365,-1.21022942861895,9.54617986991202));
#13493=CARTESIAN_POINT('Ctrl Pts',(6.68563611988732,-1.20216138888012,9.54683246126748));
#13494=CARTESIAN_POINT('Ctrl Pts',(6.68834214992285,-1.19856986352876,9.54712136954119));
#13495=CARTESIAN_POINT('Ctrl Pts',(6.69426152553844,-1.19065796048385,9.5477543162887));
#13496=CARTESIAN_POINT('Ctrl Pts',(6.69746952979353,-1.18633371724526,9.54809798707632));
#13497=CARTESIAN_POINT('Ctrl Pts',(6.7066479246318,-1.17385639869053,9.54908329692072));
#13498=CARTESIAN_POINT('Ctrl Pts',(6.71257402455141,-1.16567073487496,9.54972197642747));
#13499=CARTESIAN_POINT('Ctrl Pts',(6.75519727277702,-1.10584372710711,9.55433689328225));
#13500=CARTESIAN_POINT('Ctrl Pts',(6.78948196929028,-1.05251959611752,9.55816542616727));
#13501=CARTESIAN_POINT('Ctrl Pts',(6.88917882007176,-0.879902704455365,
9.56998592505028));
#13502=CARTESIAN_POINT('Ctrl Pts',(6.94496842010109,-0.755509949121724,
9.57771181580295));
#13503=CARTESIAN_POINT('Ctrl Pts',(7.00455075706617,-0.575371357012546,
9.58889908402287));
#13504=CARTESIAN_POINT('Ctrl Pts',(7.01935974925831,-0.523679768541553,
9.59210576573021));
#13505=CARTESIAN_POINT('Ctrl Pts',(7.04095496221828,-0.434898150257322,
9.59765952352239));
#13506=CARTESIAN_POINT('Ctrl Pts',(7.04881069084071,-0.398098219727024,
9.59997453170923));
#13507=CARTESIAN_POINT('Ctrl Pts',(7.0580277373281,-0.348023590749774,9.60315218491388));
#13508=CARTESIAN_POINT('Ctrl Pts',(7.06030379627913,-0.334923801939445,
9.60398598233022));
#13509=CARTESIAN_POINT('Ctrl Pts',(7.06383891523775,-0.313297768495138,
9.60536701102355));
#13510=CARTESIAN_POINT('Ctrl Pts',(7.06517400136076,-0.304784243023742,
9.60591183502028));
#13511=CARTESIAN_POINT('Ctrl Pts',(7.06759305366699,-0.288677283330814,
9.60694489277299));
#13512=CARTESIAN_POINT('Ctrl Pts',(7.06868847149326,-0.281085706829267,
9.60743275570657));
#13513=CARTESIAN_POINT('Ctrl Pts',(7.07083142104456,-0.265603198143267,
9.60842974767316));
#13514=CARTESIAN_POINT('Ctrl Pts',(7.07187555637616,-0.257711943088819,
9.60893897416393));
#13515=CARTESIAN_POINT('Ctrl Pts',(7.07418210140739,-0.239439374524609,
9.61012067163815));
#13516=CARTESIAN_POINT('Ctrl Pts',(7.07541015104722,-0.229054034506356,
9.61079420626002));
#13517=CARTESIAN_POINT('Ctrl Pts',(7.07947028174991,-0.192238192817203,
9.61318886685787));
#13518=CARTESIAN_POINT('Ctrl Pts',(7.08185555676161,-0.165762213074701,
9.61492377101967));
#13519=CARTESIAN_POINT('Ctrl Pts',(7.08698906719848,-0.0924029772202507,
9.61976789925707));
#13520=CARTESIAN_POINT('Ctrl Pts',(7.08861168291996,-0.0454612198587802,
9.62290974847365));
#13521=CARTESIAN_POINT('Ctrl Pts',(7.08857659854753,0.00149056180381668,
9.62609269279555));
#13522=CARTESIAN_POINT('Origin',(5.09382715545311,0.,-6.77268258743872));
#13523=CARTESIAN_POINT('',(7.08857715545311,-1.10669651073376E-10,10.5860251696757));
#13524=CARTESIAN_POINT('',(7.08881171743497,0.000532106016453122,10.4273173692856));
#13525=CARTESIAN_POINT('',(7.08857715545311,8.3550772080578E-14,-6.77268258743872));
#13526=CARTESIAN_POINT('Ctrl Pts',(7.08857715545311,-1.10669651073376E-10,
10.5860251696757));
#13527=CARTESIAN_POINT('Ctrl Pts',(7.08857715545308,-0.000599462547748238,
10.5859836762134));
#13528=CARTESIAN_POINT('Ctrl Pts',(7.0885768852439,-0.00119893046783767,
10.5859421786901));
#13529=CARTESIAN_POINT('Ctrl Pts',(7.08855819975973,-0.0219244591617089,
10.5845073491028));
#13530=CARTESIAN_POINT('Ctrl Pts',(7.08823546281962,-0.0420488502924382,
10.5831099857508));
#13531=CARTESIAN_POINT('Ctrl Pts',(7.08334007563174,-0.199056514380295,
10.5721835474355));
#13532=CARTESIAN_POINT('Ctrl Pts',(7.06498482681452,-0.335153859351847,
10.5625376395421));
#13533=CARTESIAN_POINT('Ctrl Pts',(7.02925382487065,-0.483097059662853,
10.5524634367512));
#13534=CARTESIAN_POINT('Ctrl Pts',(7.02551172804868,-0.497849281578507,
10.5514638891355));
#13535=CARTESIAN_POINT('Ctrl Pts',(7.02008491108987,-0.518260007798101,
10.5500892621842));
#13536=CARTESIAN_POINT('Ctrl Pts',(7.01854347556669,-0.523955595490136,
10.5497065780188));
#13537=CARTESIAN_POINT('Ctrl Pts',(7.01584851510462,-0.533741052855737,
10.5490507530661));
#13538=CARTESIAN_POINT('Ctrl Pts',(7.01470716270303,-0.537834191021118,
10.5487769292742));
#13539=CARTESIAN_POINT('Ctrl Pts',(7.01228918015534,-0.546399719620556,
10.5482050037561));
#13540=CARTESIAN_POINT('Ctrl Pts',(7.0110099759631,-0.550871334485474,10.5479070620912));
#13541=CARTESIAN_POINT('Ctrl Pts',(7.00784179232394,-0.561801398355937,
10.5471802526425));
#13542=CARTESIAN_POINT('Ctrl Pts',(7.00593572802216,-0.568254917424667,
10.5467523627501));
#13543=CARTESIAN_POINT('Ctrl Pts',(6.99892427357803,-0.591559419580452,
10.5452112931866));
#13544=CARTESIAN_POINT('Ctrl Pts',(6.9936283156223,-0.608352840223046,10.5441085519588));
#13545=CARTESIAN_POINT('Ctrl Pts',(6.97984412034227,-0.650125727974056,
10.5413798891469));
#13546=CARTESIAN_POINT('Ctrl Pts',(6.97108123491948,-0.675011636705886,
10.5397672521843));
#13547=CARTESIAN_POINT('Ctrl Pts',(6.93081162175451,-0.782517335977318,
10.5328278033662));
#13548=CARTESIAN_POINT('Ctrl Pts',(6.8943230200319,-0.863169943455942,10.5276889224015));
#13549=CARTESIAN_POINT('Ctrl Pts',(6.78401041632274,-1.06931865939343,10.514113730496));
#13550=CARTESIAN_POINT('Ctrl Pts',(6.70162343553738,-1.18959951639321,10.5056959185175));
#13551=CARTESIAN_POINT('Ctrl Pts',(6.59069502250191,-1.31872395567599,10.4952195192943));
#13552=CARTESIAN_POINT('Ctrl Pts',(6.57413520152104,-1.33728616469576,10.4936754518274));
#13553=CARTESIAN_POINT('Ctrl Pts',(6.5505292075649,-1.36277071357071,10.4914988814599));
#13554=CARTESIAN_POINT('Ctrl Pts',(6.54377174707401,-1.3699582336865,10.4908785244618));
#13555=CARTESIAN_POINT('Ctrl Pts',(6.53129710083977,-1.38303110480649,10.4897380531767));
#13556=CARTESIAN_POINT('Ctrl Pts',(6.52559635816397,-1.38893190173582,10.4892186505209));
#13557=CARTESIAN_POINT('Ctrl Pts',(6.51396563492926,-1.40082308260004,10.4881624373525));
#13558=CARTESIAN_POINT('Ctrl Pts',(6.5080337692579,-1.40681138022494,10.4876255501408));
#13559=CARTESIAN_POINT('Ctrl Pts',(6.49327891701845,-1.42151897575238,10.4862944045453));
#13560=CARTESIAN_POINT('Ctrl Pts',(6.48441230680191,-1.4301938178947,10.4854982251227));
#13561=CARTESIAN_POINT('Ctrl Pts',(6.45081511868682,-1.46245656496623,10.4824948176625));
#13562=CARTESIAN_POINT('Ctrl Pts',(6.42556180116407,-1.48548918950875,10.4802641400281));
#13563=CARTESIAN_POINT('Ctrl Pts',(6.36051180438649,-1.54182663092727,10.4745806688895));
#13564=CARTESIAN_POINT('Ctrl Pts',(6.31998581935925,-1.57424697616775,10.4710953775931));
#13565=CARTESIAN_POINT('Ctrl Pts',(6.18634617389968,-1.67286402788076,10.4597848540869));
#13566=CARTESIAN_POINT('Ctrl Pts',(6.088797928418,-1.73265731439188,10.4517835429541));
#13567=CARTESIAN_POINT('Ctrl Pts',(5.90555252806303,-1.82437940646711,10.4375350110504));
#13568=CARTESIAN_POINT('Ctrl Pts',(5.82173872983681,-1.85941036416094,10.4312865435898));
#13569=CARTESIAN_POINT('Ctrl Pts',(5.72545309321104,-1.89214063457353,10.424602328379));
#13570=CARTESIAN_POINT('Ctrl Pts',(5.71505478882372,-1.89558005548044,10.4238868000604));
#13571=CARTESIAN_POINT('Ctrl Pts',(5.69926636998255,-1.90065847698566,10.4228104791935));
#13572=CARTESIAN_POINT('Ctrl Pts',(5.69389697131518,-1.90236050910386,10.4224462005224));
#13573=CARTESIAN_POINT('Ctrl Pts',(5.68422791060329,-1.90538046943463,10.4217934722072));
#13574=CARTESIAN_POINT('Ctrl Pts',(5.67993095717825,-1.90670661607181,10.4215045565843));
#13575=CARTESIAN_POINT('Ctrl Pts',(5.6704809477854,-1.90958815915744,10.4208717079793));
#13576=CARTESIAN_POINT('Ctrl Pts',(5.66532607316748,-1.91113723277385,10.4205281418899));
#13577=CARTESIAN_POINT('Ctrl Pts',(5.65048310137547,-1.91553221751809,10.4195434346326));
#13578=CARTESIAN_POINT('Ctrl Pts',(5.64077941639249,-1.91832550752721,10.4189052473956));
#13579=CARTESIAN_POINT('Ctrl Pts',(5.57026570396313,-1.93804493492006,10.414305236726));
#13580=CARTESIAN_POINT('Ctrl Pts',(5.50869727104413,-1.95215172651041,10.4104900343397));
#13581=CARTESIAN_POINT('Ctrl Pts',(5.31807612803448,-1.98639880059593,10.3990037688106));
#13582=CARTESIAN_POINT('Ctrl Pts',(5.18763636419986,-1.99681505598292,10.3915750368805));
#13583=CARTESIAN_POINT('Ctrl Pts',(4.96779737679195,-1.99276778877225,10.3786422444231));
#13584=CARTESIAN_POINT('Ctrl Pts',(4.87870666721918,-1.98512650068646,10.3732908215123));
#13585=CARTESIAN_POINT('Ctrl Pts',(4.77494550999999,-1.96915912272347,10.3667756169436));
#13586=CARTESIAN_POINT('Ctrl Pts',(4.75948544460175,-1.966593184419,10.3657976005076));
#13587=CARTESIAN_POINT('Ctrl Pts',(4.73416024706406,-1.96208265408815,10.364182816774));
#13588=CARTESIAN_POINT('Ctrl Pts',(4.72427655714809,-1.96024513156493,10.3635494267183));
#13589=CARTESIAN_POINT('Ctrl Pts',(4.70651568697519,-1.95680402814337,10.3624053092976));
#13590=CARTESIAN_POINT('Ctrl Pts',(4.69863346171493,-1.95522738307424,10.3618954458368));
#13591=CARTESIAN_POINT('Ctrl Pts',(4.68183014341675,-1.95176053381556,10.3608039202311));
#13592=CARTESIAN_POINT('Ctrl Pts',(4.67291207741406,-1.9498567157173,10.3602218353381));
#13593=CARTESIAN_POINT('Ctrl Pts',(4.64878576231143,-1.94453302974595,10.3586394145476));
#13594=CARTESIAN_POINT('Ctrl Pts',(4.63360428940466,-1.94099599076064,10.3576353675814));
#13595=CARTESIAN_POINT('Ctrl Pts',(4.55305855206054,-1.92123205814174,10.3522628593987));
#13596=CARTESIAN_POINT('Ctrl Pts',(4.48851282294736,-1.90188225513687,10.3477952518183));
#13597=CARTESIAN_POINT('Ctrl Pts',(4.27204264495189,-1.82485126251408,10.3322480883833));
#13598=CARTESIAN_POINT('Ctrl Pts',(4.12624001382956,-1.75190665899648,10.3207397776508));
#13599=CARTESIAN_POINT('Ctrl Pts',(3.94415329151834,-1.6310817529194,10.3057369744724));
#13600=CARTESIAN_POINT('Ctrl Pts',(3.89871244618756,-1.59808627780061,10.3019400651605));
#13601=CARTESIAN_POINT('Ctrl Pts',(3.84741278736068,-1.55742278396653,10.2976432502069));
#13602=CARTESIAN_POINT('Ctrl Pts',(3.84014619881516,-1.55157937985299,10.2970343695622));
#13603=CARTESIAN_POINT('Ctrl Pts',(3.82844605819217,-1.54203488533367,10.2960539722246));
#13604=CARTESIAN_POINT('Ctrl Pts',(3.82398723351944,-1.53836519837608,10.2956803460877));
#13605=CARTESIAN_POINT('Ctrl Pts',(3.81607769436862,-1.53179769561979,10.2950176558302));
#13606=CARTESIAN_POINT('Ctrl Pts',(3.81262080356292,-1.52890750238688,10.2947280603738));
#13607=CARTESIAN_POINT('Ctrl Pts',(3.80514072526564,-1.52261046820306,10.2941015196967));
#13608=CARTESIAN_POINT('Ctrl Pts',(3.80112124224428,-1.5191993867589,10.2937648881957));
#13609=CARTESIAN_POINT('Ctrl Pts',(3.78983661918175,-1.50954562530997,10.2928197744973));
#13610=CARTESIAN_POINT('Ctrl Pts',(3.78260273786755,-1.50326639321613,10.2922138880703));
#13611=CARTESIAN_POINT('Ctrl Pts',(3.73748817822398,-1.46353212683689,10.2884329604784));
#13612=CARTESIAN_POINT('Ctrl Pts',(3.70084168171641,-1.42869665312083,10.2853514131281));
#13613=CARTESIAN_POINT('Ctrl Pts',(3.59549091598594,-1.32063978636248,10.2763178372346));
#13614=CARTESIAN_POINT('Ctrl Pts',(3.53094625167718,-1.24358622921299,10.27053801495));
#13615=CARTESIAN_POINT('Ctrl Pts',(3.395575430884,-1.05470108000084,10.2570342308051));
#13616=CARTESIAN_POINT('Ctrl Pts',(3.3295289033972,-0.940052350042298,10.249288977798));
#13617=CARTESIAN_POINT('Ctrl Pts',(3.26863874556675,-0.804970149263604,
10.2400999944944));
#13618=CARTESIAN_POINT('Ctrl Pts',(3.26216573500036,-0.790130425711512,
10.2390901648597));
#13619=CARTESIAN_POINT('Ctrl Pts',(3.25190633737254,-0.765806441943793,
10.237433555207));
#13620=CARTESIAN_POINT('Ctrl Pts',(3.24801080081811,-0.756368815693512,
10.2367904618385));
#13621=CARTESIAN_POINT('Ctrl Pts',(3.24117241336094,-0.739434127717005,
10.23563572281));
#13622=CARTESIAN_POINT('Ctrl Pts',(3.23820217058637,-0.731948314481599,
10.235125009734));
#13623=CARTESIAN_POINT('Ctrl Pts',(3.23200146009965,-0.716040506210221,
10.2340390415917));
#13624=CARTESIAN_POINT('Ctrl Pts',(3.22878263297337,-0.707614196571379,
10.2334634113715));
#13625=CARTESIAN_POINT('Ctrl Pts',(3.22031567293655,-0.684990076442046,
10.2319166710647));
#13626=CARTESIAN_POINT('Ctrl Pts',(3.21517189284533,-0.670754100506691,
10.2309421303004));
#13627=CARTESIAN_POINT('Ctrl Pts',(3.19013613469209,-0.598917014140809,
10.2260170331588));
#13628=CARTESIAN_POINT('Ctrl Pts',(3.17273093725686,-0.540489689512963,
10.2219860602655));
#13629=CARTESIAN_POINT('Ctrl Pts',(3.12687280475239,-0.356071155971735,
10.2091794492502));
#13630=CARTESIAN_POINT('Ctrl Pts',(3.10795787543648,-0.2280622679266,10.2001489053877));
#13631=CARTESIAN_POINT('Ctrl Pts',(3.09680021821498,-0.00384584750200338,
10.1845257738886));
#13632=CARTESIAN_POINT('Ctrl Pts',(3.09890095585723,0.0916794254478449,
10.1779397834552));
#13633=CARTESIAN_POINT('Ctrl Pts',(3.10885811519948,0.197599038056236,10.1709473268837));
#13634=CARTESIAN_POINT('Ctrl Pts',(3.10997277717449,0.208492899953273,10.1702319064362));
#13635=CARTESIAN_POINT('Ctrl Pts',(3.11179654097423,0.224975393944017,10.1691557156769));
#13636=CARTESIAN_POINT('Ctrl Pts',(3.11243967559041,0.230570902617754,10.1687914604506));
#13637=CARTESIAN_POINT('Ctrl Pts',(3.11363891310289,0.240628987555381,10.1681387570443));
#13638=CARTESIAN_POINT('Ctrl Pts',(3.11418641146809,0.245092453436738,10.1678498430485));
#13639=CARTESIAN_POINT('Ctrl Pts',(3.11542243387575,0.254894673469399,10.1672169778063));
#13640=CARTESIAN_POINT('Ctrl Pts',(3.11611747397427,0.26023250055568,10.1668733935923));
#13641=CARTESIAN_POINT('Ctrl Pts',(3.11817859434596,0.275576321791976,10.1658885819915));
#13642=CARTESIAN_POINT('Ctrl Pts',(3.11959908656849,0.285575013376463,10.1652503095084));
#13643=CARTESIAN_POINT('Ctrl Pts',(3.13045408936712,0.358026663959927,10.1606477238445));
#13644=CARTESIAN_POINT('Ctrl Pts',(3.14277522590672,0.420017827779554,10.1568302185709));
#13645=CARTESIAN_POINT('Ctrl Pts',(3.18957155994404,0.608224480438732,10.1453285939656));
#13646=CARTESIAN_POINT('Ctrl Pts',(3.23352594698046,0.731716165531569,10.1378875836846));
#13647=CARTESIAN_POINT('Ctrl Pts',(3.3272109076008,0.930607053516934,10.1249548485714));
#13648=CARTESIAN_POINT('Ctrl Pts',(3.3705204314355,1.00855019360554,10.1196177254241));
#13649=CARTESIAN_POINT('Ctrl Pts',(3.42739547724703,1.09648453976341,10.1131184577155));
#13650=CARTESIAN_POINT('Ctrl Pts',(3.43605619823787,1.10953518002995,10.1121409708667));
#13651=CARTESIAN_POINT('Ctrl Pts',(3.4505250831585,1.13079037534133,10.1105268838046));
#13652=CARTESIAN_POINT('Ctrl Pts',(3.45624327171693,1.13905557001066,10.1098936557819));
#13653=CARTESIAN_POINT('Ctrl Pts',(3.46664672929416,1.15385269219551,10.1087497138347));
#13654=CARTESIAN_POINT('Ctrl Pts',(3.47130951288325,1.16040022019669,10.1082398626659));
#13655=CARTESIAN_POINT('Ctrl Pts',(3.48134730724134,1.1743166057018,10.1071482355477));
#13656=CARTESIAN_POINT('Ctrl Pts',(3.48673352435178,1.18167711649526,10.1065660360181));
#13657=CARTESIAN_POINT('Ctrl Pts',(3.50146614169614,1.20152286590383,10.1049829812778));
#13658=CARTESIAN_POINT('Ctrl Pts',(3.51090864008498,1.21393564339,10.1039784099382));
#13659=CARTESIAN_POINT('Ctrl Pts',(3.56197123760016,1.27945189959197,10.0985974386307));
#13660=CARTESIAN_POINT('Ctrl Pts',(3.60611560835696,1.33052332176757,10.0941215172144));
#13661=CARTESIAN_POINT('Ctrl Pts',(3.76562505819221,1.49718138558852,10.0785107287734));
#13662=CARTESIAN_POINT('Ctrl Pts',(3.89253845144535,1.60080236122784,10.066942226672));
#13663=CARTESIAN_POINT('Ctrl Pts',(4.07738078135029,1.71724129427331,10.0519513458941));
#13664=CARTESIAN_POINT('Ctrl Pts',(4.12534295215322,1.74474079303491,10.0482150906697));
#13665=CARTESIAN_POINT('Ctrl Pts',(4.1826324038277,1.77449653701363,10.0439780042499));
#13666=CARTESIAN_POINT('Ctrl Pts',(4.19090519114034,1.77872026174765,10.0433715082488));
#13667=CARTESIAN_POINT('Ctrl Pts',(4.20435903567263,1.78547115585104,10.0423941842037));
#13668=CARTESIAN_POINT('Ctrl Pts',(4.2095219622558,1.7880338676253,10.0420212676046));
#13669=CARTESIAN_POINT('Ctrl Pts',(4.21873992210693,1.79255967597386,10.0413593446132));
#13670=CARTESIAN_POINT('Ctrl Pts',(4.2227905638387,1.79453144729192,10.0410698118255));
#13671=CARTESIAN_POINT('Ctrl Pts',(4.23160272861058,1.79878416526217,10.040442842516));
#13672=CARTESIAN_POINT('Ctrl Pts',(4.23636663497285,1.80105993592911,10.0401057235068));
#13673=CARTESIAN_POINT('Ctrl Pts',(4.24983169074333,1.80742680706651,10.0391578458821));
#13674=CARTESIAN_POINT('Ctrl Pts',(4.25855360321885,1.81147401556139,10.0385497073387));
#13675=CARTESIAN_POINT('Ctrl Pts',(4.3139801319694,1.83670801783921,10.0347198434615));
#13676=CARTESIAN_POINT('Ctrl Pts',(4.36146226365271,1.85615203459918,10.0315944346581));
#13677=CARTESIAN_POINT('Ctrl Pts',(4.55390681186152,1.9264214722359,10.0193383691277));
#13678=CARTESIAN_POINT('Ctrl Pts',(4.70377437515435,1.96226359983741,10.0106655790503));
#13679=CARTESIAN_POINT('Ctrl Pts',(4.93543258137789,1.99004880409893,9.99687928098526));
#13680=CARTESIAN_POINT('Ctrl Pts',(5.0150763202738,1.99478800668835,9.99208099290881));
#13681=CARTESIAN_POINT('Ctrl Pts',(5.11008104609107,1.99474243243903,9.98618193123487));
#13682=CARTESIAN_POINT('Ctrl Pts',(5.12537711085488,1.99455913443252,9.98522690014019));
#13683=CARTESIAN_POINT('Ctrl Pts',(5.15060532600748,1.99396654493551,9.98364237902414));
#13684=CARTESIAN_POINT('Ctrl Pts',(5.16053939128895,1.99365890132386,9.98301605018612));
#13685=CARTESIAN_POINT('Ctrl Pts',(5.17849391892104,1.99296853223438,9.98187953720926));
#13686=CARTESIAN_POINT('Ctrl Pts',(5.18651520419292,1.99261159132031,9.9813701669821));
#13687=CARTESIAN_POINT('Ctrl Pts',(5.20372064211897,1.99174184917191,9.98027399464174));
#13688=CARTESIAN_POINT('Ctrl Pts',(5.21290381156008,1.99121393061263,9.97968673241593));
#13689=CARTESIAN_POINT('Ctrl Pts',(5.23800135396251,1.98959689706702,9.97807558527741));
#13690=CARTESIAN_POINT('Ctrl Pts',(5.25390656007519,1.98838038919043,9.9770477567756));
#13691=CARTESIAN_POINT('Ctrl Pts',(5.34270810250086,1.98051605385441,9.97126993128384));
#13692=CARTESIAN_POINT('Ctrl Pts',(5.41520180019137,1.97005118601866,9.96640193318113));
#13693=CARTESIAN_POINT('Ctrl Pts',(5.58301898027906,1.9363163957845,9.95477916896341));
#13694=CARTESIAN_POINT('Ctrl Pts',(5.67752771218157,1.90995304332527,9.94795560492661));
#13695=CARTESIAN_POINT('Ctrl Pts',(5.86810284474545,1.84132065702192,9.93383479326349));
#13696=CARTESIAN_POINT('Ctrl Pts',(5.96356794133179,1.79819906362994,9.92655841622439));
#13697=CARTESIAN_POINT('Ctrl Pts',(6.06945905914812,1.73995232816911,9.91854710021814));
#13698=CARTESIAN_POINT('Ctrl Pts',(6.08360392465455,1.73194506360236,9.9174784622305));
#13699=CARTESIAN_POINT('Ctrl Pts',(6.10346737371326,1.72037772381891,9.91598160774956));
#13700=CARTESIAN_POINT('Ctrl Pts',(6.10926779321026,1.7169604530348,9.91554497127354));
#13701=CARTESIAN_POINT('Ctrl Pts',(6.11890370288825,1.71121762234335,9.91482053516186));
#13702=CARTESIAN_POINT('Ctrl Pts',(6.1227488084779,1.70890839787518,9.91453170365837));
#13703=CARTESIAN_POINT('Ctrl Pts',(6.13059989898833,1.70415722594928,9.91394251344165));
#13704=CARTESIAN_POINT('Ctrl Pts',(6.13460511205222,1.70171408252216,9.91364223526679));
#13705=CARTESIAN_POINT('Ctrl Pts',(6.14468430313437,1.69551697184758,9.91288722902877));
#13706=CARTESIAN_POINT('Ctrl Pts',(6.1507468738196,1.69174444266313,9.91243369503725));
#13707=CARTESIAN_POINT('Ctrl Pts',(6.16390250842044,1.68345982057725,9.91145054395757));
#13708=CARTESIAN_POINT('Ctrl Pts',(6.17098760457852,1.67893525812927,9.91092170137893));
#13709=CARTESIAN_POINT('Ctrl Pts',(6.19139445401717,1.66572103191961,9.90939972331708));
#13710=CARTESIAN_POINT('Ctrl Pts',(6.204641459335,1.6569164575297,9.90841325528953));
#13711=CARTESIAN_POINT('Ctrl Pts',(6.25053041079244,1.6256187911397,9.9049961044636));
#13712=CARTESIAN_POINT('Ctrl Pts',(6.2826076690896,1.60231087895737,9.90260751065806));
#13713=CARTESIAN_POINT('Ctrl Pts',(6.38771528200104,1.52104254941276,9.89470458506133));
#13714=CARTESIAN_POINT('Ctrl Pts',(6.45737568526177,1.45892221067634,9.88933392394672));
#13715=CARTESIAN_POINT('Ctrl Pts',(6.6133136861744,1.29890064862328,9.87634709284605));
#13716=CARTESIAN_POINT('Ctrl Pts',(6.69482688753028,1.19698607437713,9.86870042755989));
#13717=CARTESIAN_POINT('Ctrl Pts',(6.77466216495409,1.07428291859378,9.85962216126105));
#13718=CARTESIAN_POINT('Ctrl Pts',(6.78333298281527,1.06059424551384,9.85861148788484));
#13719=CARTESIAN_POINT('Ctrl Pts',(6.79719604296018,1.03810708711837,9.85695376984846));
#13720=CARTESIAN_POINT('Ctrl Pts',(6.80248926312967,1.02937150088087,9.85631042020696));
#13721=CARTESIAN_POINT('Ctrl Pts',(6.8118358479494,1.01367576780172,9.85515539809639));
#13722=CARTESIAN_POINT('Ctrl Pts',(6.81591461553315,1.00673095038384,9.85464466002542));
#13723=CARTESIAN_POINT('Ctrl Pts',(6.82447082143923,0.991958357690129,9.85355882648744));
#13724=CARTESIAN_POINT('Ctrl Pts',(6.82893744815606,0.984124560092876,9.85298335706967));
#13725=CARTESIAN_POINT('Ctrl Pts',(6.84075334344385,0.963070731518586,9.85143750457792));
#13726=CARTESIAN_POINT('Ctrl Pts',(6.8480055059105,0.949797154214314,9.85046369768773));
#13727=CARTESIAN_POINT('Ctrl Pts',(6.88364373198603,0.882768120150708,9.845549061164));
#13728=CARTESIAN_POINT('Ctrl Pts',(6.90971033082473,0.827822400030444,9.84152822726493));
#13729=CARTESIAN_POINT('Ctrl Pts',(7.00196410874102,0.607951264074163,9.82546103938766));
#13730=CARTESIAN_POINT('Ctrl Pts',(7.04849753441028,0.435707167263862,9.81283344067696));
#13731=CARTESIAN_POINT('Ctrl Pts',(7.07540183278938,0.230731212823433,9.79870074335504));
#13732=CARTESIAN_POINT('Ctrl Pts',(7.07855834208674,0.201785468863893,9.79672771518192));
#13733=CARTESIAN_POINT('Ctrl Pts',(7.0831453897689,0.149026805318393,9.79318415203214));
#13734=CARTESIAN_POINT('Ctrl Pts',(7.08478464020475,0.125237536219724,9.79160570920069));
#13735=CARTESIAN_POINT('Ctrl Pts',(7.08639479774754,0.0936106327978812,
9.7895378267005));
#13736=CARTESIAN_POINT('Ctrl Pts',(7.08674659782671,0.0857954589777864,
9.78902932055115));
#13737=CARTESIAN_POINT('Ctrl Pts',(7.08724338865359,0.07309684294638,9.78820730907328));
#13738=CARTESIAN_POINT('Ctrl Pts',(7.08741642780105,0.0682146733619648,
9.78789229300434));
#13739=CARTESIAN_POINT('Ctrl Pts',(7.0877073502051,0.0590561714255483,9.78730332351803));
#13740=CARTESIAN_POINT('Ctrl Pts',(7.08782941431966,0.054780054595996,9.78702914421586));
#13741=CARTESIAN_POINT('Ctrl Pts',(7.08805314356808,0.0459462026499021,
9.78646434933058));
#13742=CARTESIAN_POINT('Ctrl Pts',(7.08815294246162,0.0413884219076879,
9.78617383625334));
#13743=CARTESIAN_POINT('Ctrl Pts',(7.0883496707764,0.0307353165076802,9.78549680352272));
#13744=CARTESIAN_POINT('Ctrl Pts',(7.08843428662043,0.0246397717790206,
9.78511094297792));
#13745=CARTESIAN_POINT('Ctrl Pts',(7.08854690723099,0.0125257642969657,
9.78434696682734));
#13746=CARTESIAN_POINT('Ctrl Pts',(7.08857562044335,0.00650738875274101,
9.7839688201241));
#13747=CARTESIAN_POINT('Ctrl Pts',(7.08857709553963,0.000488901638750699,
9.78359198969069));
#13748=CARTESIAN_POINT('Ctrl Pts',(7.08857665886015,0.00140753592649714,
9.62731741260996));
#13749=CARTESIAN_POINT('Ctrl Pts',(7.08852025530264,0.0813422404025034,
9.63240191524386));
#13750=CARTESIAN_POINT('Ctrl Pts',(7.08365504861875,0.161085982574378,9.63748641787775));
#13751=CARTESIAN_POINT('Ctrl Pts',(7.07407361416448,0.240107320298838,9.64257092051165));
#13752=CARTESIAN_POINT('Ctrl Pts',(7.0644056661666,0.319842164542561,9.64770133259078));
#13753=CARTESIAN_POINT('Ctrl Pts',(7.04993604781898,0.398841308736947,9.6528317446699));
#13754=CARTESIAN_POINT('Ctrl Pts',(7.03080957818391,0.476578069713561,9.65796215674903));
#13755=CARTESIAN_POINT('Ctrl Pts',(7.0133888038839,0.547382279461962,9.66263503954453));
#13756=CARTESIAN_POINT('Ctrl Pts',(6.99210541276568,0.617139371892782,9.66730792234004));
#13757=CARTESIAN_POINT('Ctrl Pts',(6.96710304201831,0.685467005269678,9.67198080513555));
#13758=CARTESIAN_POINT('Ctrl Pts',(6.94326378476616,0.75061602837474,9.67643630482383));
#13759=CARTESIAN_POINT('Ctrl Pts',(6.91597500802296,0.814647922360064,9.68089180451211));
#13760=CARTESIAN_POINT('Ctrl Pts',(6.8853617690878,0.877172326654685,9.68534730420039));
#13761=CARTESIAN_POINT('Ctrl Pts',(6.85479430590389,0.939603238666971,9.68979614161273));
#13762=CARTESIAN_POINT('Ctrl Pts',(6.82091246049086,1.00053069921662,9.69424497902506));
#13763=CARTESIAN_POINT('Ctrl Pts',(6.78389005025252,1.05958245272478,9.69869381643739));
#13764=CARTESIAN_POINT('Ctrl Pts',(6.7469109726107,1.11856508956029,9.70313744674205));
#13765=CARTESIAN_POINT('Ctrl Pts',(6.70679888962395,1.17567596732585,9.7075810770467));
#13766=CARTESIAN_POINT('Ctrl Pts',(6.66377357393471,1.2305672698381,9.71202470735136));
#13767=CARTESIAN_POINT('Ctrl Pts',(6.62077516153372,1.28542424938235,9.7164655590996));
#13768=CARTESIAN_POINT('Ctrl Pts',(6.57486743131534,1.33806402288491,9.72090641084784));
#13769=CARTESIAN_POINT('Ctrl Pts',(6.52631264525958,1.38816889606198,9.72534726259608));
#13770=CARTESIAN_POINT('Ctrl Pts',(6.47777175274261,1.43825943215601,9.72978684363239));
#13771=CARTESIAN_POINT('Ctrl Pts',(6.42658564834507,1.48581615680537,9.73422642466869));
#13772=CARTESIAN_POINT('Ctrl Pts',(6.37305474201621,1.53055687391092,9.738666005705));
#13773=CARTESIAN_POINT('Ctrl Pts',(6.31952099876136,1.57529996209724,9.74310582202152));
#13774=CARTESIAN_POINT('Ctrl Pts',(6.26364258375581,1.61722643461298,9.74754563833803));
#13775=CARTESIAN_POINT('Ctrl Pts',(6.20575302226661,1.65609432980463,9.75198545465455));
#13776=CARTESIAN_POINT('Ctrl Pts',(6.14780235396479,1.69500325300077,9.75642995753315));
#13777=CARTESIAN_POINT('Ctrl Pts',(6.08783670902331,1.7308468818767,9.76087446041174));
#13778=CARTESIAN_POINT('Ctrl Pts',(6.02621782555706,1.76342711808657,9.76531896329034));
#13779=CARTESIAN_POINT('Ctrl Pts',(5.9645627950711,1.79602646659407,9.76976607341405));
#13780=CARTESIAN_POINT('Ctrl Pts',(5.90125303967262,1.82535840636816,9.77421318353777));
#13781=CARTESIAN_POINT('Ctrl Pts',(5.83667154955317,1.85127247282892,9.77866029366148));
#13782=CARTESIAN_POINT('Ctrl Pts',(5.77197855925583,1.8772312800198,9.78311508173702));
#13783=CARTESIAN_POINT('Ctrl Pts',(5.70600991434269,1.89976027706512,9.78756986981256));
#13784=CARTESIAN_POINT('Ctrl Pts',(5.63916428794348,1.91875870667137,9.79202465788809));
#13785=CARTESIAN_POINT('Ctrl Pts',(5.60523510120037,1.92840183967287,9.79428579814001));
#13786=CARTESIAN_POINT('Ctrl Pts',(5.57108014905197,1.93713619981271,9.79654693839193));
#13787=CARTESIAN_POINT('Ctrl Pts',(5.53675230609608,1.9449536944174,9.79880807864385));
#13788=CARTESIAN_POINT('Ctrl Pts',(5.46911046323752,1.96035780070738,9.80326357833248));
#13789=CARTESIAN_POINT('Ctrl Pts',(5.40053119820327,1.97225927914909,9.80771907802112));
#13790=CARTESIAN_POINT('Ctrl Pts',(5.33141014156992,1.98055090497766,9.81217457770975));
#13791=CARTESIAN_POINT('Ctrl Pts',(5.26239244114616,1.98883013239887,9.81662341512234));
#13792=CARTESIAN_POINT('Ctrl Pts',(5.19283503888196,1.9935101629964,9.82107225253493));
#13793=CARTESIAN_POINT('Ctrl Pts',(5.1231448738556,1.99453454066047,9.82552108994752));
#13794=CARTESIAN_POINT('Ctrl Pts',(5.05353627715152,1.99555771934951,9.82996472025228));
#13795=CARTESIAN_POINT('Ctrl Pts',(4.98379571311575,1.99293373624857,9.83440835055704));
#13796=CARTESIAN_POINT('Ctrl Pts',(4.91433458783194,1.98665799287868,9.8388519808618));
#13797=CARTESIAN_POINT('Ctrl Pts',(4.84491689587822,1.98038617366684,9.84329283261005));
#13798=CARTESIAN_POINT('Ctrl Pts',(4.7757787821183,1.97046716802976,9.8477336843583));
#13799=CARTESIAN_POINT('Ctrl Pts',(4.70732946599528,1.95694841489084,9.85217453610656));
#13800=CARTESIAN_POINT('Ctrl Pts',(4.63889973606288,1.94343353002834,9.85661411714279));
#13801=CARTESIAN_POINT('Ctrl Pts',(4.57115889214703,1.92632103729661,9.86105369817902));
#13802=CARTESIAN_POINT('Ctrl Pts',(4.50450709454416,1.90570969150872,9.86549327921525));
#13803=CARTESIAN_POINT('Ctrl Pts',(4.43785176466142,1.88509725340158,9.8699330955316));
#13804=CARTESIAN_POINT('Ctrl Pts',(4.3722860622907,1.86098574094044,9.87437291184795));
#13805=CARTESIAN_POINT('Ctrl Pts',(4.30819437751614,1.83352357517732,9.8788127281643));
#13806=CARTESIAN_POINT('Ctrl Pts',(4.24403503912045,1.80603242102103,9.88325723104259));
#13807=CARTESIAN_POINT('Ctrl Pts',(4.18135327427906,1.7751837474656,9.88770173392088));
#13808=CARTESIAN_POINT('Ctrl Pts',(4.1205119920654,1.74117349945936,9.89214623679917));
#13809=CARTESIAN_POINT('Ctrl Pts',(4.05963501899147,1.7071433002791,9.8965933469225));
#13810=CARTESIAN_POINT('Ctrl Pts',(4.00060109148739,1.6699480959816,9.90104045704583));
#13811=CARTESIAN_POINT('Ctrl Pts',(3.94374468911479,1.62982756238848,9.90548756716917));
#13812=CARTESIAN_POINT('Ctrl Pts',(3.8867901239578,1.58963776054896,9.90994235524422));
#13813=CARTESIAN_POINT('Ctrl Pts',(3.83202097241562,1.54651285059152,9.91439714331927));
#13814=CARTESIAN_POINT('Ctrl Pts',(3.77973851683813,1.50073269184189,9.91885193139432));
#13815=CARTESIAN_POINT('Ctrl Pts',(3.75320123541932,1.47749581548026,9.92111307164687));
#13816=CARTESIAN_POINT('Ctrl Pts',(3.72730401706465,1.45357544997633,9.92337421189943));
#13817=CARTESIAN_POINT('Ctrl Pts',(3.70208239602652,1.42901157696802,9.92563535215199));
#13818=CARTESIAN_POINT('Ctrl Pts',(3.6523840522613,1.38060930325504,9.93009085187593));
#13819=CARTESIAN_POINT('Ctrl Pts',(3.60511609883124,1.32951623683033,9.93454635159989));
#13820=CARTESIAN_POINT('Ctrl Pts',(3.56058359273093,1.27600616764614,9.93900185132384));
#13821=CARTESIAN_POINT('Ctrl Pts',(3.51611767575858,1.22257611167379,9.9434506887719));
#13822=CARTESIAN_POINT('Ctrl Pts',(3.47437939805803,1.16673659927669,9.94789952621997));
#13823=CARTESIAN_POINT('Ctrl Pts',(3.43563735068529,1.10879850913684,9.95234836366803));
#13824=CARTESIAN_POINT('Ctrl Pts',(3.39694064864549,1.05092823219131,9.95679199400835));
#13825=CARTESIAN_POINT('Ctrl Pts',(3.36123348221421,0.990964660774739,9.96123562434866));
#13826=CARTESIAN_POINT('Ctrl Pts',(3.32874334356431,0.929250611787858,9.96567925468898));
#13827=CARTESIAN_POINT('Ctrl Pts',(3.29627352066493,0.867575151962949,9.97012010647281));
#13828=CARTESIAN_POINT('Ctrl Pts',(3.26701696225748,0.804151817862348,9.97456095825664));
#13829=CARTESIAN_POINT('Ctrl Pts',(3.24115629394578,0.73934987754221,9.97900181004047));
#13830=CARTESIAN_POINT('Ctrl Pts',(3.21530302544484,0.674566479747334,9.98344139111225));
#13831=CARTESIAN_POINT('Ctrl Pts',(3.19284389916565,0.608405712978014,9.98788097218403));
#13832=CARTESIAN_POINT('Ctrl Pts',(3.17391354398806,0.541257135760092,9.99232055325581));
#13833=CARTESIAN_POINT('Ctrl Pts',(3.15498218557738,0.474104999936243,9.99676036960763));
#13834=CARTESIAN_POINT('Ctrl Pts',(3.13958009994461,0.405965421204017,10.0012001859594));
#13835=CARTESIAN_POINT('Ctrl Pts',(3.12779165588568,0.337241718861464,10.0056400023113));
#13836=CARTESIAN_POINT('Ctrl Pts',(3.11599076823344,0.268445473459133,10.0100845052247));
#13837=CARTESIAN_POINT('Ctrl Pts',(3.10781121821081,0.199064356886703,10.0145290081381));
#13838=CARTESIAN_POINT('Ctrl Pts',(3.10328580844011,0.12950949128021,10.0189735110514));
#13839=CARTESIAN_POINT('Ctrl Pts',(3.09875774396275,0.0599138232328149,
10.0234206212097));
#13840=CARTESIAN_POINT('Ctrl Pts',(3.09788809245653,-0.00985530746950176,
10.027867731368));
#13841=CARTESIAN_POINT('Ctrl Pts',(3.1006574969992,-0.0793868699390318,
10.0323148415263));
#13842=CARTESIAN_POINT('Ctrl Pts',(3.10343168292841,-0.149038478892176,
10.0367696296357));
#13843=CARTESIAN_POINT('Ctrl Pts',(3.10985742085494,-0.218451213938643,
10.041224417745));
#13844=CARTESIAN_POINT('Ctrl Pts',(3.11986358019106,-0.287220065522337,
10.0456792058544));
#13845=CARTESIAN_POINT('Ctrl Pts',(3.12494245844923,-0.32212542865076,10.0479403457897));
#13846=CARTESIAN_POINT('Ctrl Pts',(3.13094295371157,-0.356865081974095,
10.050201485725));
#13847=CARTESIAN_POINT('Ctrl Pts',(3.13785082285443,-0.391387466347351,
10.0524626256602));
#13848=CARTESIAN_POINT('Ctrl Pts',(3.15146254500617,-0.459412655358127,
10.0569181253098));
#13849=CARTESIAN_POINT('Ctrl Pts',(3.16865391578513,-0.52686054247854,10.0613736249593));
#13850=CARTESIAN_POINT('Ctrl Pts',(3.18936095080603,-0.593326249088268,
10.0658291246088));
#13851=CARTESIAN_POINT('Ctrl Pts',(3.21003702274976,-0.659692570015737,
10.0702779619825));
#13852=CARTESIAN_POINT('Ctrl Pts',(3.23421818055781,-0.725079162137858,
10.0747267993562));
#13853=CARTESIAN_POINT('Ctrl Pts',(3.26178948698271,-0.789091594053275,
10.0791756367299));
#13854=CARTESIAN_POINT('Ctrl Pts',(3.28932852278481,-0.853029103111823,
10.0836192669962));
#13855=CARTESIAN_POINT('Ctrl Pts',(3.32024963353363,-0.915595199337671,
10.0880628972625));
#13856=CARTESIAN_POINT('Ctrl Pts',(3.35438873385719,-0.97641258696102,10.0925065275288));
#13857=CARTESIAN_POINT('Ctrl Pts',(3.3885064873532,-1.03719194609873,10.0969473792389));
#13858=CARTESIAN_POINT('Ctrl Pts',(3.42583799967954,-1.09622434027595,10.101388230949));
#13859=CARTESIAN_POINT('Ctrl Pts',(3.46617259490296,-1.15315575444963,10.1058290826591));
#13860=CARTESIAN_POINT('Ctrl Pts',(3.50649564872761,-1.21007087818703,10.1102686636576));
#13861=CARTESIAN_POINT('Ctrl Pts',(3.54981979684907,-1.26488581646807,10.114708244656));
#13862=CARTESIAN_POINT('Ctrl Pts',(3.59589124229518,-1.31727581112374,10.1191478256545));
#13863=CARTESIAN_POINT('Ctrl Pts',(3.64196512934875,-1.36966858224542,10.1235876419335));
#13864=CARTESIAN_POINT('Ctrl Pts',(3.69078627793172,-1.41963578886794,10.1280274582124));
#13865=CARTESIAN_POINT('Ctrl Pts',(3.74206202046107,-1.46688737888086,10.1324672744914));
#13866=CARTESIAN_POINT('Ctrl Pts',(3.79339188842568,-1.51418884653085,10.1369117773332));
#13867=CARTESIAN_POINT('Ctrl Pts',(3.84718116123485,-1.5587686441913,10.141356280175));
#13868=CARTESIAN_POINT('Ctrl Pts',(3.90310259156291,-1.60037576070387,10.1458007830168));
#13869=CARTESIAN_POINT('Ctrl Pts',(3.95905682666169,-1.64200728488823,10.1502478931041));
#13870=CARTESIAN_POINT('Ctrl Pts',(4.0171453014733,-1.68066238591739,10.1546950031914));
#13871=CARTESIAN_POINT('Ctrl Pts',(4.07701249234068,-1.71613388270833,10.1591421132787));
#13872=CARTESIAN_POINT('Ctrl Pts',(4.13698304414484,-1.75166662117578,10.1635969013187));
#13873=CARTESIAN_POINT('Ctrl Pts',(4.19873800863606,-1.78400455710301,10.1680516893588));
#13874=CARTESIAN_POINT('Ctrl Pts',(4.26189877303869,-1.81298723907074,10.1725064773989));
#13875=CARTESIAN_POINT('Ctrl Pts',(4.29395762001292,-1.82769813395768,10.1747676179888));
#13876=CARTESIAN_POINT('Ctrl Pts',(4.32637835074632,-1.84154538609442,10.1770287585786));
#13877=CARTESIAN_POINT('Ctrl Pts',(4.35910994638157,-1.85451292397603,10.1792898991685));
#13878=CARTESIAN_POINT('Ctrl Pts',(4.42360642854782,-1.88006501086606,10.183745398844));
#13879=CARTESIAN_POINT('Ctrl Pts',(4.48956417630287,-1.90229868475508,10.1882008985195));
#13880=CARTESIAN_POINT('Ctrl Pts',(4.5566085713,-1.9210475671728,10.192656398195));
#13881=CARTESIAN_POINT('Ctrl Pts',(4.62355271529725,-1.93976841452197,10.197105235594));
#13882=CARTESIAN_POINT('Ctrl Pts',(4.69157981419015,-1.95501468213493,10.2015540729929));
#13883=CARTESIAN_POINT('Ctrl Pts',(4.76029632158471,-1.96666843808484,10.2060029103919));
#13884=CARTESIAN_POINT('Ctrl Pts',(4.82893240025759,-1.97830855398333,10.2104465406825));
#13885=CARTESIAN_POINT('Ctrl Pts',(4.89825580476789,-1.98636442833082,10.214890170973));
#13886=CARTESIAN_POINT('Ctrl Pts',(4.96786065566025,-1.99076869661695,10.2193338012636));
#13887=CARTESIAN_POINT('Ctrl Pts',(5.03742198334651,-1.99517021095886,10.2237746529972));
#13888=CARTESIAN_POINT('Ctrl Pts',(5.1072639212017,-1.99592461815519,10.2282155047309));
#13889=CARTESIAN_POINT('Ctrl Pts',(5.17697480487905,-1.99301631475885,10.2326563564646));
#13890=CARTESIAN_POINT('Ctrl Pts',(5.24666574137353,-1.99010884354906,10.2370959374859));
#13891=CARTESIAN_POINT('Ctrl Pts',(5.31622520963413,-1.98354076279362,10.2415355185072));
#13892=CARTESIAN_POINT('Ctrl Pts',(5.38524266250854,-1.97334856645947,10.2459750995285));
#13893=CARTESIAN_POINT('Ctrl Pts',(5.45426377302825,-1.96315582998021,10.2504149158296));
#13894=CARTESIAN_POINT('Ctrl Pts',(5.5227423275696,-1.94933867047341,10.2548547321308));
#13895=CARTESIAN_POINT('Ctrl Pts',(5.590275780436,-1.93198507376548,10.2592945484319));
#13896=CARTESIAN_POINT('Ctrl Pts',(5.65788051996472,-1.91461315902499,10.2637390512946));
#13897=CARTESIAN_POINT('Ctrl Pts',(5.72453769198412,-1.89369747852418,10.2681835541573));
#13898=CARTESIAN_POINT('Ctrl Pts',(5.78985872320934,-1.86937626474362,10.27262805702));
#13899=CARTESIAN_POINT('Ctrl Pts',(5.85521807321282,-1.84504078359494,10.2770751671275));
#13900=CARTESIAN_POINT('Ctrl Pts',(5.91923927338325,-1.81729598738069,10.281522277235));
#13901=CARTESIAN_POINT('Ctrl Pts',(5.98155516904373,-1.78632766769886,10.2859693873425));
#13902=CARTESIAN_POINT('Ctrl Pts',(6.04397865332126,-1.75530588110218,10.2904241754015));
#13903=CARTESIAN_POINT('Ctrl Pts',(6.10469053029643,-1.72104970235199,10.2948789634605));
#13904=CARTESIAN_POINT('Ctrl Pts',(6.16335031735875,-1.68378970440117,10.2993337515196));
#13905=CARTESIAN_POINT('Ctrl Pts',(6.19312457637739,-1.66487744976166,10.3015948919053));
#13906=CARTESIAN_POINT('Ctrl Pts',(6.22237064400853,-1.64519198609486,10.303856032291));
#13907=CARTESIAN_POINT('Ctrl Pts',(6.25104729766808,-1.62476740026133,10.3061171726767));
#13908=CARTESIAN_POINT('Ctrl Pts',(6.30716481321017,-1.58479840574191,10.3105420118592));
#13909=CARTESIAN_POINT('Ctrl Pts',(6.36132690120277,-1.54183465873047,10.3149668510417));
#13910=CARTESIAN_POINT('Ctrl Pts',(6.41319290414351,-1.49609544604702,10.3193916902243));
#13911=CARTESIAN_POINT('Ctrl Pts',(6.46590360890188,-1.44961131388067,10.3238885933695));
#13912=CARTESIAN_POINT('Ctrl Pts',(6.51624229576162,-1.40026072416253,10.3283854965147));
#13913=CARTESIAN_POINT('Ctrl Pts',(6.56388183109682,-1.34831999655796,10.33288239966));
#13914=CARTESIAN_POINT('Ctrl Pts',(6.61063286537051,-1.297347989393,10.3372954333218));
#13915=CARTESIAN_POINT('Ctrl Pts',(6.65478420930858,-1.2438820088483,10.3417084669836));
#13916=CARTESIAN_POINT('Ctrl Pts',(6.69606156793214,-1.18822239078717,10.3461215006454));
#13917=CARTESIAN_POINT('Ctrl Pts',(6.73731423946764,-1.13259606152983,10.3505318949681));
#13918=CARTESIAN_POINT('Ctrl Pts',(6.77569603923256,-1.07477909471519,10.3549422892907));
#13919=CARTESIAN_POINT('Ctrl Pts',(6.8109729785983,-1.01510481456597,10.3593526836133));
#13920=CARTESIAN_POINT('Ctrl Pts',(6.84624120760493,-0.955445268813201,
10.3637619889492));
#13921=CARTESIAN_POINT('Ctrl Pts',(6.87840584553228,-0.893929747592757,
10.3681712942851));
#13922=CARTESIAN_POINT('Ctrl Pts',(6.90727729444706,-0.830918862394405,
10.372580599621));
#13923=CARTESIAN_POINT('Ctrl Pts',(6.93714461717892,-0.765734518879353,
10.3771419967951));
#13924=CARTESIAN_POINT('Ctrl Pts',(6.96348712604202,-0.698950254759972,
10.3817033939691));
#13925=CARTESIAN_POINT('Ctrl Pts',(6.98614865883704,-0.630988819497452,
10.3862647911432));
#13926=CARTESIAN_POINT('Ctrl Pts',(7.00808028594709,-0.565216355228417,
10.3906792702002));
#13927=CARTESIAN_POINT('Ctrl Pts',(7.02656439386085,-0.498341915087311,
10.3950937492571));
#13928=CARTESIAN_POINT('Ctrl Pts',(7.04151065576395,-0.430762748060807,
10.3995082283141));
#13929=CARTESIAN_POINT('Ctrl Pts',(7.05720305666604,-0.35980993133084,10.4041430845467));
#13930=CARTESIAN_POINT('Ctrl Pts',(7.06899502657416,-0.288080797450994,
10.4087779407793));
#13931=CARTESIAN_POINT('Ctrl Pts',(7.0768433357553,-0.216042567934474,10.4134127970119));
#13932=CARTESIAN_POINT('Ctrl Pts',(7.08469164493643,-0.144004338417935,
10.4180476532445));
#13933=CARTESIAN_POINT('Ctrl Pts',(7.08859633704874,-0.0716576417186778,
10.4226825094771));
#13934=CARTESIAN_POINT('Ctrl Pts',(7.08857708451418,0.000531987659116302,
10.4273173657097));
#13935=CARTESIAN_POINT('Origin',(5.09382715545311,0.,-6.77268258743872));
#13936=CARTESIAN_POINT('',(7.08573554628195,0.000892988623384845,11.3854254802821));
#13937=CARTESIAN_POINT('',(7.08797502715347,-0.00179838111111824,11.2273170635307));
#13938=CARTESIAN_POINT('',(7.08857715545311,8.3550772080578E-14,-6.77268258743872));
#13939=CARTESIAN_POINT('Ctrl Pts',(7.08857700164749,0.000783331027041838,
11.3870615703915));
#13940=CARTESIAN_POINT('Ctrl Pts',(7.08859050212995,-0.0335956025044396,
11.3849657369292));
#13941=CARTESIAN_POINT('Ctrl Pts',(7.08771523812136,-0.067967775722241,
11.3828458996653));
#13942=CARTESIAN_POINT('Ctrl Pts',(7.0854599564119,-0.111886118516987,11.3800989790134));
#13943=CARTESIAN_POINT('Ctrl Pts',(7.08489844898603,-0.121469404999907,
11.3794972526833));
#13944=CARTESIAN_POINT('Ctrl Pts',(7.08376269282117,-0.138719976608432,
11.3784097358079));
#13945=CARTESIAN_POINT('Ctrl Pts',(7.08321324344236,-0.146388746298036,
11.3779247219182));
#13946=CARTESIAN_POINT('Ctrl Pts',(7.08200019851094,-0.162048797123054,
11.3769310261121));
#13947=CARTESIAN_POINT('Ctrl Pts',(7.08133272365181,-0.170039628061656,
11.3764222321024));
#13948=CARTESIAN_POINT('Ctrl Pts',(7.07978810543651,-0.187277727010127,
11.3753207857812));
#13949=CARTESIAN_POINT('Ctrl Pts',(7.07889451733559,-0.196523296030458,
11.3747276303283));
#13950=CARTESIAN_POINT('Ctrl Pts',(7.07629189812463,-0.221619654077708,
11.3731108712311));
#13951=CARTESIAN_POINT('Ctrl Pts',(7.07445739048664,-0.237456469029167,
11.3720833697502));
#13952=CARTESIAN_POINT('Ctrl Pts',(7.06493459325003,-0.311851079412598,
11.3672213034655));
#13953=CARTESIAN_POINT('Ctrl Pts',(7.05483863455043,-0.370065422645639,
11.3633122878388));
#13954=CARTESIAN_POINT('Ctrl Pts',(7.00214150058168,-0.610099164649372,
11.346751212321));
#13955=CARTESIAN_POINT('Ctrl Pts',(6.93671349231064,-0.785899920915602,
11.3334378185118));
#13956=CARTESIAN_POINT('Ctrl Pts',(6.82806189668402,-0.986497642712622,
11.3179319640882));
#13957=CARTESIAN_POINT('Ctrl Pts',(6.80717455467169,-1.0223448489466,11.3151529315244));
#13958=CARTESIAN_POINT('Ctrl Pts',(6.78037417045649,-1.06520843276605,11.3118429187444));
#13959=CARTESIAN_POINT('Ctrl Pts',(6.77551285210947,-1.07286675044914,11.3112520534972));
#13960=CARTESIAN_POINT('Ctrl Pts',(6.76780391671225,-1.0848299401623,11.3103302080942));
#13961=CARTESIAN_POINT('Ctrl Pts',(6.76499161690613,-1.08915726162217,11.3099969979051));
#13962=CARTESIAN_POINT('Ctrl Pts',(6.75968340657217,-1.09725610768888,11.3093738980191));
#13963=CARTESIAN_POINT('Ctrl Pts',(6.75719148820311,-1.10103002331704,11.3090837685017));
#13964=CARTESIAN_POINT('Ctrl Pts',(6.75145030982186,-1.1096608427009,11.3084207193772));
#13965=CARTESIAN_POINT('Ctrl Pts',(6.74819252600374,-1.11451196966086,11.3080483734133));
#13966=CARTESIAN_POINT('Ctrl Pts',(6.7394326235441,-1.12743319212184,11.3070573058941));
#13967=CARTESIAN_POINT('Ctrl Pts',(6.73389239170094,-1.13547742786139,11.3064410356748));
#13968=CARTESIAN_POINT('Ctrl Pts',(6.68833390002943,-1.20059772016784,11.3014552649411));
#13969=CARTESIAN_POINT('Ctrl Pts',(6.64540341735061,-1.25558749182682,11.2972640011223));
#13970=CARTESIAN_POINT('Ctrl Pts',(6.50112251675087,-1.42166434451098,11.2842763383867));
#13971=CARTESIAN_POINT('Ctrl Pts',(6.39006625285841,-1.5236062553347,11.2757615618428));
#13972=CARTESIAN_POINT('Ctrl Pts',(6.23375663532229,-1.63751289683915,11.2642325375425));
#13973=CARTESIAN_POINT('Ctrl Pts',(6.19808769398939,-1.66177495709315,11.261631546079));
#13974=CARTESIAN_POINT('Ctrl Pts',(6.14458229319352,-1.69568573173536,11.2577518704288));
#13975=CARTESIAN_POINT('Ctrl Pts',(6.12733935837669,-1.70624996479905,11.2565048652517));
#13976=CARTESIAN_POINT('Ctrl Pts',(6.09969239175197,-1.72261559235524,11.254508801344));
#13977=CARTESIAN_POINT('Ctrl Pts',(6.08939159825758,-1.72858924654958,11.2537658320926));
#13978=CARTESIAN_POINT('Ctrl Pts',(6.0697367374453,-1.73975356863666,11.2523491851439));
#13979=CARTESIAN_POINT('Ctrl Pts',(6.06039316513557,-1.74496192898744,11.2516761624429));
#13980=CARTESIAN_POINT('Ctrl Pts',(6.04398366350237,-1.75393679448646,11.2504947016232));
#13981=CARTESIAN_POINT('Ctrl Pts',(6.03693604773138,-1.75773640888276,11.2499874510321));
#13982=CARTESIAN_POINT('Ctrl Pts',(6.02315108676149,-1.7650615889023,11.248995518425));
#13983=CARTESIAN_POINT('Ctrl Pts',(6.01641607331925,-1.76859126649599,11.2485109923619));
#13984=CARTESIAN_POINT('Ctrl Pts',(6.00037496040749,-1.77688151121632,11.2473571495161));
#13985=CARTESIAN_POINT('Ctrl Pts',(5.99105137126729,-1.78160756825438,11.2466866400883));
#13986=CARTESIAN_POINT('Ctrl Pts',(5.96281189524195,-1.79564405509356,11.2446559779213));
#13987=CARTESIAN_POINT('Ctrl Pts',(5.94378561982559,-1.80472784738692,11.2432880633953));
#13988=CARTESIAN_POINT('Ctrl Pts',(5.77400919200274,-1.88250470529182,11.2310801496649));
#13989=CARTESIAN_POINT('Ctrl Pts',(5.6154170001361,-1.93245812405543,11.2195839429194));
#13990=CARTESIAN_POINT('Ctrl Pts',(5.37918533188267,-1.97564056366196,11.2028492990731));
#13991=CARTESIAN_POINT('Ctrl Pts',(5.30515417568186,-1.98492498818679,11.1976716347176));
#13992=CARTESIAN_POINT('Ctrl Pts',(5.20693799968771,-1.9916837846586,11.1910106874793));
#13993=CARTESIAN_POINT('Ctrl Pts',(5.18307430131863,-1.99289573582765,11.1894086136156));
#13994=CARTESIAN_POINT('Ctrl Pts',(5.14285593274497,-1.99421436796962,11.1867421270537));
#13995=CARTESIAN_POINT('Ctrl Pts',(5.1265117323196,-1.99454920372412,11.1856678247984));
#13996=CARTESIAN_POINT('Ctrl Pts',(5.10363021598478,-1.99473661523291,11.1841785561112));
#13997=CARTESIAN_POINT('Ctrl Pts',(5.09709545075546,-1.99475802675018,11.1837549153987));
#13998=CARTESIAN_POINT('Ctrl Pts',(5.08594642630417,-1.99473976928282,11.1830351410441));
#13999=CARTESIAN_POINT('Ctrl Pts',(5.08133222486416,-1.99471620323393,11.1827381295447));
#14000=CARTESIAN_POINT('Ctrl Pts',(5.07242381926647,-1.99463979239863,11.1821664483625));
#14001=CARTESIAN_POINT('Ctrl Pts',(5.06812967580166,-1.99458909166899,11.1818916559751));
#14002=CARTESIAN_POINT('Ctrl Pts',(5.05654490179536,-1.99441489252716,11.1811523340471));
#14003=CARTESIAN_POINT('Ctrl Pts',(5.04925464417529,-1.99426528454597,11.1806892347172));
#14004=CARTESIAN_POINT('Ctrl Pts',(5.02203622625401,-1.99355738795772,11.1789677348685));
#14005=CARTESIAN_POINT('Ctrl Pts',(5.00211521229091,-1.99274032101949,11.1777227857297));
#14006=CARTESIAN_POINT('Ctrl Pts',(4.8428969442853,-1.98381712282033,11.1678688644336));
#14007=CARTESIAN_POINT('Ctrl Pts',(4.70476982860234,-1.96141304161784,11.1598908889779));
#14008=CARTESIAN_POINT('Ctrl Pts',(4.48668418079415,-1.90207204543683,11.1467494400709));
#14009=CARTESIAN_POINT('Ctrl Pts',(4.40483854025718,-1.87397803108736,11.1416888867652));
#14010=CARTESIAN_POINT('Ctrl Pts',(4.28033488005824,-1.82197942609904,11.1335531348843));
#14011=CARTESIAN_POINT('Ctrl Pts',(4.23629105254116,-1.80166866114592,11.1305856577438));
#14012=CARTESIAN_POINT('Ctrl Pts',(4.1804828045708,-1.77342254597474,11.1266864497802));
#14013=CARTESIAN_POINT('Ctrl Pts',(4.16800003325703,-1.76693790317709,11.1258051089959));
#14014=CARTESIAN_POINT('Ctrl Pts',(4.14783432556259,-1.75618971339038,11.1243658083576));
#14015=CARTESIAN_POINT('Ctrl Pts',(4.14010900043112,-1.75200639850894,11.1238106794371));
#14016=CARTESIAN_POINT('Ctrl Pts',(4.12530447387874,-1.7438627165738,11.1227395026326));
#14017=CARTESIAN_POINT('Ctrl Pts',(4.11822128787983,-1.73990992495575,11.1222237319706));
#14018=CARTESIAN_POINT('Ctrl Pts',(4.10203592977094,-1.73074773220773,11.1210375544509));
#14019=CARTESIAN_POINT('Ctrl Pts',(4.09295039931226,-1.72550956530975,11.1203661264057));
#14020=CARTESIAN_POINT('Ctrl Pts',(4.06417187168313,-1.70861384312165,11.1182212904702));
#14021=CARTESIAN_POINT('Ctrl Pts',(4.04463856380536,-1.69668927486082,11.1167382876586));
#14022=CARTESIAN_POINT('Ctrl Pts',(3.88138193346995,-1.59312815524446,11.1041065818927));
#14023=CARTESIAN_POINT('Ctrl Pts',(3.74977047466984,-1.48376862296477,11.0922596469863));
#14024=CARTESIAN_POINT('Ctrl Pts',(3.56491759556801,-1.28516583036661,11.0733597123531));
#14025=CARTESIAN_POINT('Ctrl Pts',(3.50184737784965,-1.20615948013205,11.0663698761083));
#14026=CARTESIAN_POINT('Ctrl Pts',(3.43830522429634,-1.11284195408442,11.0589385943018));
#14027=CARTESIAN_POINT('Ctrl Pts',(3.43167463031966,-1.10291390378076,11.0581578424654));
#14028=CARTESIAN_POINT('Ctrl Pts',(3.42197913589062,-1.08811070413213,11.0570089357811));
#14029=CARTESIAN_POINT('Ctrl Pts',(3.41884571003396,-1.08328106438982,11.0566364730371));
#14030=CARTESIAN_POINT('Ctrl Pts',(3.41329793205102,-1.07464849208454,11.0559750457173));
#14031=CARTESIAN_POINT('Ctrl Pts',(3.41087551244865,-1.07085088640116,11.05568555786));
#14032=CARTESIAN_POINT('Ctrl Pts',(3.40563919110418,-1.06258029498531,11.0550583300518));
#14033=CARTESIAN_POINT('Ctrl Pts',(3.40283019423773,-1.05810432613117,11.054720910004));
#14034=CARTESIAN_POINT('Ctrl Pts',(3.39508664303426,-1.04565584326884,11.0537879472045));
#14035=CARTESIAN_POINT('Ctrl Pts',(3.39019038589964,-1.03765949938148,11.0531948382425));
#14036=CARTESIAN_POINT('Ctrl Pts',(3.36406701926906,-0.994312652124109,
11.0500112566252));
#14037=CARTESIAN_POINT('Ctrl Pts',(3.34388188387452,-0.958342249428195,
11.0474819839229));
#14038=CARTESIAN_POINT('Ctrl Pts',(3.31179863076767,-0.896770059389174,
11.0432946766284));
#14039=CARTESIAN_POINT('Ctrl Pts',(3.29930331114055,-0.871496693820793,
11.0416147334492));
#14040=CARTESIAN_POINT('Ctrl Pts',(3.24229803838006,-0.749767388698813,
11.0336679963512));
#14041=CARTESIAN_POINT('Ctrl Pts',(3.20500345326026,-0.650121359538879,
11.027580877731));
#14042=CARTESIAN_POINT('Ctrl Pts',(3.14876826736442,-0.453289119408947,
11.0156221138267));
#14043=CARTESIAN_POINT('Ctrl Pts',(3.12876766603665,-0.356739327193686,
11.0097835050644));
#14044=CARTESIAN_POINT('Ctrl Pts',(3.11291087850071,-0.235702744641075,
11.0022611009819));
#14045=CARTESIAN_POINT('Ctrl Pts',(3.11025977963813,-0.212239187226894,
11.0007940487766));
#14046=CARTESIAN_POINT('Ctrl Pts',(3.1070102052518,-0.178048314735636,10.9986411443714));
#14047=CARTESIAN_POINT('Ctrl Pts',(3.10608083106555,-0.167353932346221,
10.9979656079912));
#14048=CARTESIAN_POINT('Ctrl Pts',(3.10460005185348,-0.148556547509568,
10.9967742492367));
#14049=CARTESIAN_POINT('Ctrl Pts',(3.10401172521529,-0.140456640715687,
10.9962595908666));
#14050=CARTESIAN_POINT('Ctrl Pts',(3.10296280396824,-0.124682781596197,
10.9952547276015));
#14051=CARTESIAN_POINT('Ctrl Pts',(3.10249707686687,-0.117009304941435,
10.9947646923633));
#14052=CARTESIAN_POINT('Ctrl Pts',(3.10136640753617,-0.0964116472297227,
10.993445989413));
#14053=CARTESIAN_POINT('Ctrl Pts',(3.10078287021135,-0.0834835417316138,
10.9926148017454));
#14054=CARTESIAN_POINT('Ctrl Pts',(3.09908385627865,-0.0354758387549812,
10.9895147212196));
#14055=CARTESIAN_POINT('Ctrl Pts',(3.09876851823717,-0.000376080368230205,
10.9872212428741));
#14056=CARTESIAN_POINT('Ctrl Pts',(3.1028860610232,0.236205784078398,10.9715719864317));
#14057=CARTESIAN_POINT('Ctrl Pts',(3.13691051066298,0.435988478456032,10.957256317076));
#14058=CARTESIAN_POINT('Ctrl Pts',(3.21774239621701,0.680020182160489,10.9396203170828));
#14059=CARTESIAN_POINT('Ctrl Pts',(3.23743488298876,0.732072693490488,10.9358610974789));
#14060=CARTESIAN_POINT('Ctrl Pts',(3.26313156028253,0.792260968475792,10.9315697331184));
#14061=CARTESIAN_POINT('Ctrl Pts',(3.26705017335975,0.801255060180023,10.9309299703773));
#14062=CARTESIAN_POINT('Ctrl Pts',(3.27319649702166,0.815082747470845,10.9299491253994));
#14063=CARTESIAN_POINT('Ctrl Pts',(3.27537739754418,0.819936801955177,10.9296053348741));
#14064=CARTESIAN_POINT('Ctrl Pts',(3.27943880886156,0.828880419470953,10.9289729469639));
#14065=CARTESIAN_POINT('Ctrl Pts',(3.28131372840238,0.832972328161857,10.9286840304972));
#14066=CARTESIAN_POINT('Ctrl Pts',(3.28559775454483,0.842239025692224,10.9280306546167));
#14067=CARTESIAN_POINT('Ctrl Pts',(3.28801522939811,0.847409837306923,10.9276667119581));
#14068=CARTESIAN_POINT('Ctrl Pts',(3.2943453019036,0.86079932251171,10.9267257898313));
#14069=CARTESIAN_POINT('Ctrl Pts',(3.29829206810475,0.86900182529183,10.9261508309693));
#14070=CARTESIAN_POINT('Ctrl Pts',(3.32490261567474,0.923350767754326,10.9223490455802));
#14071=CARTESIAN_POINT('Ctrl Pts',(3.34928908238131,0.9686374783957,10.9192187352752));
#14072=CARTESIAN_POINT('Ctrl Pts',(3.40398899219318,1.0614349121035,10.9127791978383));
#14073=CARTESIAN_POINT('Ctrl Pts',(3.43461928442492,1.10870507240111,10.9094839109244));
#14074=CARTESIAN_POINT('Ctrl Pts',(3.526683245807,1.23840411003592,10.9002256783233));
#14075=CARTESIAN_POINT('Ctrl Pts',(3.59253938965534,1.31746690734485,10.894311569077));
#14076=CARTESIAN_POINT('Ctrl Pts',(3.71640414327561,1.44476254392003,10.8837833589001));
#14077=CARTESIAN_POINT('Ctrl Pts',(3.77159080436036,1.49543375269944,10.8792626418684));
#14078=CARTESIAN_POINT('Ctrl Pts',(3.84190273511683,1.55305194431792,10.8736113018938));
#14079=CARTESIAN_POINT('Ctrl Pts',(3.85443727387511,1.56307318890195,10.8726078900301));
#14080=CARTESIAN_POINT('Ctrl Pts',(3.87436093855319,1.57861163853467,10.8710185557582));
#14081=CARTESIAN_POINT('Ctrl Pts',(3.88166991595748,1.58423084858865,10.8704366724332));
#14082=CARTESIAN_POINT('Ctrl Pts',(3.89541520311462,1.5946475450852,10.8693444031634));
#14083=CARTESIAN_POINT('Ctrl Pts',(3.90184205029887,1.59945725374903,10.8688345092295));
#14084=CARTESIAN_POINT('Ctrl Pts',(3.91626784426315,1.61011796043722,10.8676917104519));
#14085=CARTESIAN_POINT('Ctrl Pts',(3.92428167302932,1.61594837064765,10.8670580272072));
#14086=CARTESIAN_POINT('Ctrl Pts',(3.94469914662214,1.63057153769293,10.865446299987));
#14087=CARTESIAN_POINT('Ctrl Pts',(3.9571603116017,1.6392825214536,10.864465177593));
#14088=CARTESIAN_POINT('Ctrl Pts',(4.03379632819752,1.69156102246822,10.8584454991326));
#14089=CARTESIAN_POINT('Ctrl Pts',(4.10036009073022,1.73149201988066,10.8532732244031));
#14090=CARTESIAN_POINT('Ctrl Pts',(4.28027821191365,1.82562808503646,10.8394432889076));
#14091=CARTESIAN_POINT('Ctrl Pts',(4.39672232160349,1.87318451079591,10.8306231485748));
#14092=CARTESIAN_POINT('Ctrl Pts',(4.58678666636478,1.93061530956486,10.8168572315459));
#14093=CARTESIAN_POINT('Ctrl Pts',(4.65784073161889,1.94789207557644,10.8118482390382));
#14094=CARTESIAN_POINT('Ctrl Pts',(4.74459659578435,1.96399986611261,10.806010913221));
#14095=CARTESIAN_POINT('Ctrl Pts',(4.75953574276866,1.9665977581881,10.8050156409445));
#14096=CARTESIAN_POINT('Ctrl Pts',(4.78076281291103,1.97004022502322,10.8036168358518));
#14097=CARTESIAN_POINT('Ctrl Pts',(4.78702694579063,1.97102547035342,10.8032059399985));
#14098=CARTESIAN_POINT('Ctrl Pts',(4.79782329513392,1.97267084221676,10.8025011350625));
#14099=CARTESIAN_POINT('Ctrl Pts',(4.80235325152159,1.97334525669059,10.8022064367495));
#14100=CARTESIAN_POINT('Ctrl Pts',(4.81118770882578,1.97462943482469,10.8016337463239));
#14101=CARTESIAN_POINT('Ctrl Pts',(4.81549189529821,1.97524073102381,10.8013556639534));
#14102=CARTESIAN_POINT('Ctrl Pts',(4.82728710209811,1.97687660881291,10.8005960811779));
#14103=CARTESIAN_POINT('Ctrl Pts',(4.83478209645489,1.9778726926405,10.8001161533745));
#14104=CARTESIAN_POINT('Ctrl Pts',(4.86394534797918,1.98157986708738,10.7982587205718));
#14105=CARTESIAN_POINT('Ctrl Pts',(4.88565278766873,1.98397780721929,10.7968975487706));
#14106=CARTESIAN_POINT('Ctrl Pts',(5.10214214581195,2.00430002365368,10.7834962197265));
#14107=CARTESIAN_POINT('Ctrl Pts',(5.29854105444291,1.99384114128001,10.7726434854575));
#14108=CARTESIAN_POINT('Ctrl Pts',(5.56187053028585,1.94043716977198,10.7567002408052));
#14109=CARTESIAN_POINT('Ctrl Pts',(5.63258568713428,1.92200376887631,10.7522865357292));
#14110=CARTESIAN_POINT('Ctrl Pts',(5.71730841999873,1.89487540820673,10.7467553042911));
#14111=CARTESIAN_POINT('Ctrl Pts',(5.73243159710898,1.88983227929282,10.7457584269983));
#14112=CARTESIAN_POINT('Ctrl Pts',(5.75618080472414,1.88159500852578,10.7441771263741));
#14113=CARTESIAN_POINT('Ctrl Pts',(5.76484817845943,1.87852147044783,10.7435966730059));
#14114=CARTESIAN_POINT('Ctrl Pts',(5.78104285711955,1.87265229392335,10.7425056855572));
#14115=CARTESIAN_POINT('Ctrl Pts',(5.78857516059319,1.86987091555283,10.7419956327077));
#14116=CARTESIAN_POINT('Ctrl Pts',(5.80539565774374,1.8635441147646,10.7408506432768));
#14117=CARTESIAN_POINT('Ctrl Pts',(5.81467450011127,1.85997459685158,10.7402149145381));
#14118=CARTESIAN_POINT('Ctrl Pts',(5.8381706128949,1.85073354958053,10.7385944649756));
#14119=CARTESIAN_POINT('Ctrl Pts',(5.85234979485469,1.84496754391589,10.737606607556));
#14120=CARTESIAN_POINT('Ctrl Pts',(5.94016140901111,1.80807533354587,10.7314252850219));
#14121=CARTESIAN_POINT('Ctrl Pts',(6.01192456389537,1.77271327841365,10.7260894304148));
#14122=CARTESIAN_POINT('Ctrl Pts',(6.20215408152322,1.66432137021369,10.7111586952375));
#14123=CARTESIAN_POINT('Ctrl Pts',(6.3154133706686,1.58305916377974,10.7013471941833));
#14124=CARTESIAN_POINT('Ctrl Pts',(6.46761859198697,1.44772465904652,10.6873094853261));
#14125=CARTESIAN_POINT('Ctrl Pts',(6.51383332505937,1.40242428366876,10.6829165666868));
#14126=CARTESIAN_POINT('Ctrl Pts',(6.56466367532966,1.34750528935272,10.6780064589811));
#14127=CARTESIAN_POINT('Ctrl Pts',(6.57150099053989,1.3400039628807,10.6773442576048));
#14128=CARTESIAN_POINT('Ctrl Pts',(6.58188366204331,1.32843685791351,10.6763364580841));
#14129=CARTESIAN_POINT('Ctrl Pts',(6.58547015875157,1.32440847348426,10.6759879189442));
#14130=CARTESIAN_POINT('Ctrl Pts',(6.59201658600006,1.31699514439885,10.6753510496281));
#14131=CARTESIAN_POINT('Ctrl Pts',(6.59498140787082,1.31361474239271,10.675062365685));
#14132=CARTESIAN_POINT('Ctrl Pts',(6.6016260710158,1.30598681975566,10.6744147890303));
#14133=CARTESIAN_POINT('Ctrl Pts',(6.6052994028311,1.30173376325867,10.6740563730353));
#14134=CARTESIAN_POINT('Ctrl Pts',(6.61603914817315,1.28919232093253,10.6730070337502));
#14135=CARTESIAN_POINT('Ctrl Pts',(6.6230558424132,1.28086136121408,10.6723196145986));
#14136=CARTESIAN_POINT('Ctrl Pts',(6.6933905249563,1.19595071159921,10.6654052068969));
#14137=CARTESIAN_POINT('Ctrl Pts',(6.75097975288173,1.11478778209156,10.6595428744423));
#14138=CARTESIAN_POINT('Ctrl Pts',(6.86735588215672,0.921691312295174,10.6463971792345));
#14139=CARTESIAN_POINT('Ctrl Pts',(6.92204271454937,0.807802950007679,10.6391713742038));
#14140=CARTESIAN_POINT('Ctrl Pts',(6.98643114614844,0.633011710764672,10.6280315007438));
#14141=CARTESIAN_POINT('Ctrl Pts',(7.00467516930955,0.575597519728701,10.6243687102326));
#14142=CARTESIAN_POINT('Ctrl Pts',(7.024206003035,0.502884216341028,10.6196819660917));
#14143=CARTESIAN_POINT('Ctrl Pts',(7.02795296433797,0.488274887758236,10.6187380274384));
#14144=CARTESIAN_POINT('Ctrl Pts',(7.03367269191741,0.464874181844254,10.6172218024364));
#14145=CARTESIAN_POINT('Ctrl Pts',(7.03575223197809,0.456109310534919,10.6166529444937));
#14146=CARTESIAN_POINT('Ctrl Pts',(7.03957883339206,0.439480221324501,10.6155717607668));
#14147=CARTESIAN_POINT('Ctrl Pts',(7.04133776661476,0.431618898382836,10.6150598261905));
#14148=CARTESIAN_POINT('Ctrl Pts',(7.0452222297898,0.413750508949665,10.6138942895309));
#14149=CARTESIAN_POINT('Ctrl Pts',(7.04731847756764,0.403737374789287,10.6132397694319));
#14150=CARTESIAN_POINT('Ctrl Pts',(7.05254626365009,0.377771502294452,10.6115387322755));
#14151=CARTESIAN_POINT('Ctrl Pts',(7.05555991799737,0.36179606860488,10.6104885189985));
#14152=CARTESIAN_POINT('Ctrl Pts',(7.07847589052951,0.231601106159984,10.6018980869804));
#14153=CARTESIAN_POINT('Ctrl Pts',(7.08857715545954,0.115902333697236,10.5940476725223));
#14154=CARTESIAN_POINT('Ctrl Pts',(7.08857715545311,-1.10669147457276E-10,
10.5860251696756));
#14155=CARTESIAN_POINT('Ctrl Pts',(7.09165123813443,0.000533538373458679,
10.4273174125613));
#14156=CARTESIAN_POINT('Ctrl Pts',(7.09175584924485,0.0297929794135023,
10.4291930904358));
#14157=CARTESIAN_POINT('Ctrl Pts',(7.07793077862856,0.718427657987238,10.4733445261464));
#14158=CARTESIAN_POINT('Ctrl Pts',(6.28614855086912,2.03262338503281,10.5597717196931));
#14159=CARTESIAN_POINT('Ctrl Pts',(4.03585361648675,2.10567798773344,10.6865989932013));
#14160=CARTESIAN_POINT('Ctrl Pts',(2.75131770239386,0.256588624035499,10.8134262667095));
#14161=CARTESIAN_POINT('Ctrl Pts',(3.60511495718796,-1.82672508052752,10.9402535402178));
#14162=CARTESIAN_POINT('Ctrl Pts',(5.81786594038741,-2.24253297202115,11.067080813726));
#14163=CARTESIAN_POINT('Ctrl Pts',(6.98867395944926,-1.01178906555039,11.1627686548303));
#14164=CARTESIAN_POINT('Ctrl Pts',(7.08951450949766,-0.176350808701007,
11.2161807380985));
#14165=CARTESIAN_POINT('Ctrl Pts',(7.08797502715347,-0.00179838111111824,
11.2273170635307));
#14166=CARTESIAN_POINT('Origin',(5.09382715545311,0.,-6.77268258743872));
#14167=CARTESIAN_POINT('',(7.08857671409759,0.0013269467482341,12.1854076497708));
#14168=CARTESIAN_POINT('',(7.08857715545311,1.48164940157807E-8,12.0255409243712));
#14169=CARTESIAN_POINT('',(7.08857715545311,8.3550772080578E-14,-6.77268258743872));
#14170=CARTESIAN_POINT('Ctrl Pts',(7.08570589435167,0.000894132952252917,
11.3854084069082));
#14171=CARTESIAN_POINT('Ctrl Pts',(7.08680590574586,0.276931583514048,11.4029688699668));
#14172=CARTESIAN_POINT('Ctrl Pts',(6.90460270567564,1.21611910765721,11.4628050908614));
#14173=CARTESIAN_POINT('Ctrl Pts',(5.4714363682364,2.32605240372542,11.5649170695921));
#14174=CARTESIAN_POINT('Ctrl Pts',(3.34667780576886,1.5813865206481,11.6917443431003));
#14175=CARTESIAN_POINT('Ctrl Pts',(2.81680521163759,-0.606947692680927,
11.8185716166085));
#14176=CARTESIAN_POINT('Ctrl Pts',(4.3654468926145,-2.24101245944887,11.9453988901168));
#14177=CARTESIAN_POINT('Ctrl Pts',(6.49966051365026,-1.84456996298104,12.0676771988713));
#14178=CARTESIAN_POINT('Ctrl Pts',(7.08670906604921,-0.587748414857904,
12.1476797497898));
#14179=CARTESIAN_POINT('Ctrl Pts',(7.09088662258869,0.00131120050381758,
12.1854065428722));
#14180=CARTESIAN_POINT('Ctrl Pts',(7.08857715545311,1.48164940157807E-8,
12.0255409243712));
#14181=CARTESIAN_POINT('Ctrl Pts',(7.08857715560486,-0.0204294858188712,
12.0241991575096));
#14182=CARTESIAN_POINT('Ctrl Pts',(7.08826330894787,-0.0408607784063718,
12.0228667225922));
#14183=CARTESIAN_POINT('Ctrl Pts',(7.08717163368709,-0.076375701020997,
12.0205665158892));
#14184=CARTESIAN_POINT('Ctrl Pts',(7.08653653486394,-0.0914593163802701,
12.0195945812698));
#14185=CARTESIAN_POINT('Ctrl Pts',(7.08524929289252,-0.115527185493051,
12.0180513772495));
#14186=CARTESIAN_POINT('Ctrl Pts',(7.0847074389005,-0.124516510658469,12.017476695354));
#14187=CARTESIAN_POINT('Ctrl Pts',(7.08356622597029,-0.141529969751081,
12.0163921571722));
#14188=CARTESIAN_POINT('Ctrl Pts',(7.08297915809114,-0.149554720992709,
12.0158819286443));
#14189=CARTESIAN_POINT('Ctrl Pts',(7.0815371704763,-0.167751779511177,12.014727810809));
#14190=CARTESIAN_POINT('Ctrl Pts',(7.08065268490258,-0.177921570061504,
12.0140848569458));
#14191=CARTESIAN_POINT('Ctrl Pts',(7.07816258338,-0.204212978209397,12.0124276916232));
#14192=CARTESIAN_POINT('Ctrl Pts',(7.07643854125095,-0.220322826678904,
12.0114171805031));
#14193=CARTESIAN_POINT('Ctrl Pts',(7.06146836141441,-0.345745910053498,
12.0035842620008));
#14194=CARTESIAN_POINT('Ctrl Pts',(7.03938725592229,-0.45382016427159,11.9970536774645));
#14195=CARTESIAN_POINT('Ctrl Pts',(7.00416595533655,-0.574344306882903,
11.9897252512486));
#14196=CARTESIAN_POINT('Ctrl Pts',(6.99966543581773,-0.589106245051875,
11.9888265709252));
#14197=CARTESIAN_POINT('Ctrl Pts',(6.96112767873423,-0.710445995464346,
11.9814224742288));
#14198=CARTESIAN_POINT('Ctrl Pts',(6.9183529365093,-0.814031239082437,11.975002622826));
#14199=CARTESIAN_POINT('Ctrl Pts',(6.84639343525565,-0.953723564535285,
11.9655610833747));
#14200=CARTESIAN_POINT('Ctrl Pts',(6.82429869269057,-0.993249597015682,
11.9627929142148));
#14201=CARTESIAN_POINT('Ctrl Pts',(6.79633730320581,-1.03950174723979,11.9593950391903));
#14202=CARTESIAN_POINT('Ctrl Pts',(6.79174445096947,-1.04698688466185,11.958840043649));
#14203=CARTESIAN_POINT('Ctrl Pts',(6.78413825013445,-1.05920130749264,11.95792557125));
#14204=CARTESIAN_POINT('Ctrl Pts',(6.78115406260131,-1.06394873615532,11.9575679363026));
#14205=CARTESIAN_POINT('Ctrl Pts',(6.77574238880087,-1.07247792737476,11.9569213133934));
#14206=CARTESIAN_POINT('Ctrl Pts',(6.77332209942813,-1.07626413540411,11.956632797633));
#14207=CARTESIAN_POINT('Ctrl Pts',(6.76796557779976,-1.08458160514534,11.9559957279569));
#14208=CARTESIAN_POINT('Ctrl Pts',(6.76502376783589,-1.08910908383634,11.95564681605));
#14209=CARTESIAN_POINT('Ctrl Pts',(6.7564853416555,-1.10213376847607,11.954637022104));
#14210=CARTESIAN_POINT('Ctrl Pts',(6.7508421440695,-1.11060002016434,11.9539731822478));
#14211=CARTESIAN_POINT('Ctrl Pts',(6.70844060907201,-1.17317067295451,11.9490135126114));
#14212=CARTESIAN_POINT('Ctrl Pts',(6.66910923265989,-1.22547564890171,11.9445694547647));
#14213=CARTESIAN_POINT('Ctrl Pts',(6.53604804838631,-1.38541604178657,11.9302250166383));
#14214=CARTESIAN_POINT('Ctrl Pts',(6.4332983087131,-1.48499215679976,11.9201537398576));
#14215=CARTESIAN_POINT('Ctrl Pts',(6.26097273160203,-1.61943116664853,11.905281212892));
#14216=CARTESIAN_POINT('Ctrl Pts',(6.19852110929785,-1.66266046802766,11.9002234551428));
#14217=CARTESIAN_POINT('Ctrl Pts',(6.12083401567374,-1.71012092248311,11.8943167379608));
#14218=CARTESIAN_POINT('Ctrl Pts',(6.10782797010078,-1.71786467139318,11.8933400229155));
#14219=CARTESIAN_POINT('Ctrl Pts',(6.08617834223766,-1.73042322337279,11.8917338566114));
#14220=CARTESIAN_POINT('Ctrl Pts',(6.07758501817901,-1.73532299103841,11.8911013670765));
#14221=CARTESIAN_POINT('Ctrl Pts',(6.06195102701605,-1.7440837709808,11.8899596352602));
#14222=CARTESIAN_POINT('Ctrl Pts',(6.05492286426732,-1.74796655358801,11.8894496241813));
#14223=CARTESIAN_POINT('Ctrl Pts',(6.03975647963111,-1.75622625499351,11.8883559158525));
#14224=CARTESIAN_POINT('Ctrl Pts',(6.03161087738241,-1.7605892878742,11.8877727187404));
#14225=CARTESIAN_POINT('Ctrl Pts',(6.00916134239369,-1.77241393445275,11.8861767316648));
#14226=CARTESIAN_POINT('Ctrl Pts',(5.99479654652679,-1.7797589750001,11.8851680337521));
#14227=CARTESIAN_POINT('Ctrl Pts',(5.91197720593532,-1.82084663236703,11.8794210778035));
#14228=CARTESIAN_POINT('Ctrl Pts',(5.84171581341721,-1.85081509069313,11.874815299007));
#14229=CARTESIAN_POINT('Ctrl Pts',(5.66045126731508,-1.91611561703539,11.8634032207174));
#14230=CARTESIAN_POINT('Ctrl Pts',(5.5477619045618,-1.94589449072751,11.8567394609109));
#14231=CARTESIAN_POINT('Ctrl Pts',(5.34366366450904,-1.98112340814124,11.8446292804051));
#14232=CARTESIAN_POINT('Ctrl Pts',(5.25326984666581,-1.99043762429821,11.8392457949777));
#14233=CARTESIAN_POINT('Ctrl Pts',(5.15162914606547,-1.99394240756791,11.8328685748772));
#14234=CARTESIAN_POINT('Ctrl Pts',(5.14068622328987,-1.9942295780237,11.8321777614457));
#14235=CARTESIAN_POINT('Ctrl Pts',(5.1241088498934,-1.99452809499195,11.8311241086831));
#14236=CARTESIAN_POINT('Ctrl Pts',(5.11847559462421,-1.99460566411278,11.8307648115901));
#14237=CARTESIAN_POINT('Ctrl Pts',(5.10834325609253,-1.99470225532085,11.8301161890694));
#14238=CARTESIAN_POINT('Ctrl Pts',(5.10384435611217,-1.99472992143752,11.829827345741));
#14239=CARTESIAN_POINT('Ctrl Pts',(5.09395892011331,-1.99475726816465,11.82919078955));
#14240=CARTESIAN_POINT('Ctrl Pts',(5.08857253677882,-1.99475035119417,11.8288427275511));
#14241=CARTESIAN_POINT('Ctrl Pts',(5.07307350750902,-1.99466767171319,11.8278378292703));
#14242=CARTESIAN_POINT('Ctrl Pts',(5.06296149916303,-1.9945368222858,11.8271780785227));
#14243=CARTESIAN_POINT('Ctrl Pts',(4.9893244100172,-1.99302385658667,11.8223457257424));
#14244=CARTESIAN_POINT('Ctrl Pts',(4.92590270814704,-1.98868413302647,11.8180331513315));
#14245=CARTESIAN_POINT('Ctrl Pts',(4.73095675971474,-1.9659533434419,11.8045132303469));
#14246=CARTESIAN_POINT('Ctrl Pts',(4.60097098022095,-1.93745808772483,11.795148782149));
#14247=CARTESIAN_POINT('Ctrl Pts',(4.39227811762146,-1.86932797264268,11.7801258880887));
#14248=CARTESIAN_POINT('Ctrl Pts',(4.31162072448025,-1.8370396955942,11.7743157675162));
#14249=CARTESIAN_POINT('Ctrl Pts',(4.21923743572319,-1.79286469300563,11.7676673568594));
#14250=CARTESIAN_POINT('Ctrl Pts',(4.20524096419635,-1.78596908955846,11.7666600742175));
#14251=CARTESIAN_POINT('Ctrl Pts',(4.18238002017592,-1.77437096537491,11.7650144701619));
#14252=CARTESIAN_POINT('Ctrl Pts',(4.17346777565167,-1.76976462311721,11.7643728422437));
#14253=CARTESIAN_POINT('Ctrl Pts',(4.15747921910262,-1.76134740781965,11.7632214583307));
#14254=CARTESIAN_POINT('Ctrl Pts',(4.15039051967552,-1.75756065792886,11.7627108707643));
#14255=CARTESIAN_POINT('Ctrl Pts',(4.13529524742915,-1.74937919189992,11.7616232558951));
#14256=CARTESIAN_POINT('Ctrl Pts',(4.12729555935203,-1.74497210692932,11.7610466800849));
#14257=CARTESIAN_POINT('Ctrl Pts',(4.10566921693358,-1.73286365205934,11.7594872295732));
#14258=CARTESIAN_POINT('Ctrl Pts',(4.09210229885574,-1.72505648651231,11.7585081390555));
#14259=CARTESIAN_POINT('Ctrl Pts',(4.01981514766311,-1.68231800636631,11.7532847599309));
#14260=CARTESIAN_POINT('Ctrl Pts',(3.96282341474003,-1.64454482738862,11.7491452045988));
#14261=CARTESIAN_POINT('Ctrl Pts',(3.77184146997626,-1.50333127156703,11.7350129599237));
#14262=CARTESIAN_POINT('Ctrl Pts',(3.64916789920824,-1.38585822686345,11.7255116645967));
#14263=CARTESIAN_POINT('Ctrl Pts',(3.51198603411108,-1.21622654812987,11.7124442578769));
#14264=CARTESIAN_POINT('Ctrl Pts',(3.48259247892641,-1.17700904896186,11.709456273408));
#14265=CARTESIAN_POINT('Ctrl Pts',(3.44955478681268,-1.12937003125684,11.7058130992666));
#14266=CARTESIAN_POINT('Ctrl Pts',(3.44448463001982,-1.12195254644654,11.7052454708539));
#14267=CARTESIAN_POINT('Ctrl Pts',(3.43629575591612,-1.10979700621703,11.7043141980256));
#14268=CARTESIAN_POINT('Ctrl Pts',(3.43314677012879,-1.10507935975399,11.7039525066836));
#14269=CARTESIAN_POINT('Ctrl Pts',(3.42753652478423,-1.09659624890082,11.7033015409498));
#14270=CARTESIAN_POINT('Ctrl Pts',(3.42506783427205,-1.09283581849832,11.7030127672697));
#14271=CARTESIAN_POINT('Ctrl Pts',(3.41969161091006,-1.08458579657519,11.7023787411732));
#14272=CARTESIAN_POINT('Ctrl Pts',(3.41678944820669,-1.08009291197126,11.7020331562719));
#14273=CARTESIAN_POINT('Ctrl Pts',(3.40854556981275,-1.06721710422248,11.7010420389919));
#14274=CARTESIAN_POINT('Ctrl Pts',(3.4032484887669,-1.05880599374926,11.7003937100007));
#14275=CARTESIAN_POINT('Ctrl Pts',(3.36702756727262,-1.00032686767989,11.6958819526625));
#14276=CARTESIAN_POINT('Ctrl Pts',(3.33827261477922,-0.948956004926795,
11.6918982132154));
#14277=CARTESIAN_POINT('Ctrl Pts',(3.26994381664234,-0.81312137884562,11.6814484010711));
#14278=CARTESIAN_POINT('Ctrl Pts',(3.23394406004819,-0.727015299442956,
11.6749088485831));
#14279=CARTESIAN_POINT('Ctrl Pts',(3.16241652549728,-0.515388887929364,
11.659390173647));
#14280=CARTESIAN_POINT('Ctrl Pts',(3.13290038855704,-0.38826583577615,11.6505252877003));
#14281=CARTESIAN_POINT('Ctrl Pts',(3.11387783629447,-0.243086001126109,
11.6410111930238));
#14282=CARTESIAN_POINT('Ctrl Pts',(3.11196853217163,-0.226994566722795,
11.6399644523661));
#14283=CARTESIAN_POINT('Ctrl Pts',(3.10917573533098,-0.200725219938103,
11.6382679406204));
#14284=CARTESIAN_POINT('Ctrl Pts',(3.10817400701529,-0.190560892639338,
11.6376145046309));
#14285=CARTESIAN_POINT('Ctrl Pts',(3.1065221425037,-0.172369358011783,11.6364502311264));
#14286=CARTESIAN_POINT('Ctrl Pts',(3.10584247403451,-0.164345123525658,
11.6359384823668));
#14287=CARTESIAN_POINT('Ctrl Pts',(3.10450489849324,-0.147328896534347,
11.6348570056964));
#14288=CARTESIAN_POINT('Ctrl Pts',(3.10385932275352,-0.138336094042632,
11.6342876733457));
#14289=CARTESIAN_POINT('Ctrl Pts',(3.10229433713584,-0.114250679488671,
11.6327685604097));
#14290=CARTESIAN_POINT('Ctrl Pts',(3.10148551122797,-0.099151281702897,
11.6318222328006));
#14291=CARTESIAN_POINT('Ctrl Pts',(3.09828939981654,-0.0233600746593698,
11.6271004173928));
#14292=CARTESIAN_POINT('Ctrl Pts',(3.09850312078127,0.0374126224863856,
11.6234064619461));
#14293=CARTESIAN_POINT('Ctrl Pts',(3.10779791010855,0.226210296203055,11.6121060131336));
#14294=CARTESIAN_POINT('Ctrl Pts',(3.12644962887386,0.353426146694047,11.6047609273293));
#14295=CARTESIAN_POINT('Ctrl Pts',(3.1803072298058,0.571644957561606,11.5916448303444));
#14296=CARTESIAN_POINT('Ctrl Pts',(3.21018867241104,0.66350393532436,11.5859441217902));
#14297=CARTESIAN_POINT('Ctrl Pts',(3.25072467712301,0.762968373975857,11.5792092606406));
#14298=CARTESIAN_POINT('Ctrl Pts',(3.25494093482936,0.773074990007728,11.5785181984935));
#14299=CARTESIAN_POINT('Ctrl Pts',(3.26145121226026,0.788325874490059,11.5774644116682));
#14300=CARTESIAN_POINT('Ctrl Pts',(3.26368423840555,0.793496176989743,11.5771052367517));
#14301=CARTESIAN_POINT('Ctrl Pts',(3.26773950774613,0.802777482404624,11.5764568884718));
#14302=CARTESIAN_POINT('Ctrl Pts',(3.26955378822361,0.806891854079918,11.5761681974725));
#14303=CARTESIAN_POINT('Ctrl Pts',(3.2735704485401,0.815917923389075,11.5755320324392));
#14304=CARTESIAN_POINT('Ctrl Pts',(3.27577877481209,0.820826790967474,11.5751842096672));
#14305=CARTESIAN_POINT('Ctrl Pts',(3.28218695193392,0.8349187408802,11.5741805311362));
#14306=CARTESIAN_POINT('Ctrl Pts',(3.28643662822085,0.844078789394303,11.5735217707392));
#14307=CARTESIAN_POINT('Ctrl Pts',(3.31775848364197,0.910270953411155,11.5687173289571));
#14308=CARTESIAN_POINT('Ctrl Pts',(3.34745253536849,0.966016114350126,11.5644334249775));
#14309=CARTESIAN_POINT('Ctrl Pts',(3.44645538127054,1.13234727732085,11.5511020071269));
#14310=CARTESIAN_POINT('Ctrl Pts',(3.52401071206225,1.23762820550267,11.5419009114411));
#14311=CARTESIAN_POINT('Ctrl Pts',(3.67110811152646,1.40103195543772,11.5268370571725));
#14312=CARTESIAN_POINT('Ctrl Pts',(3.73532700286554,1.46338692694807,11.5208451720603));
#14313=CARTESIAN_POINT('Ctrl Pts',(3.81547589695396,1.5313690984305,11.5140210918967));
#14314=CARTESIAN_POINT('Ctrl Pts',(3.82754898014606,1.54136720532858,11.5130090495106));
#14315=CARTESIAN_POINT('Ctrl Pts',(3.84755773514497,1.55754331700233,11.5113572728041));
#14316=CARTESIAN_POINT('Ctrl Pts',(3.85542431510439,1.56380531507149,11.51071418991));
#14317=CARTESIAN_POINT('Ctrl Pts',(3.86966517140209,1.57496654650411,11.5095611996311));
#14318=CARTESIAN_POINT('Ctrl Pts',(3.87602231055481,1.57988719490776,11.5090504511024));
#14319=CARTESIAN_POINT('Ctrl Pts',(3.88965379784387,1.59030727904153,11.5079635573533));
#14320=CARTESIAN_POINT('Ctrl Pts',(3.89693648090182,1.59579554911348,11.5073878566739));
#14321=CARTESIAN_POINT('Ctrl Pts',(3.91676776666068,1.61052838411179,11.5058333997876));
#14322=CARTESIAN_POINT('Ctrl Pts',(3.92938766422097,1.61967625581621,11.5048583852831));
#14323=CARTESIAN_POINT('Ctrl Pts',(3.99706719964905,1.66753565296911,11.4997020045978));
#14324=CARTESIAN_POINT('Ctrl Pts',(4.05395571379944,1.70359219421477,11.4956220633021));
#14325=CARTESIAN_POINT('Ctrl Pts',(4.25381655472482,1.81651639960299,11.4819550380108));
#14326=CARTESIAN_POINT('Ctrl Pts',(4.4042662964113,1.87878955856959,11.4728138322018));
#14327=CARTESIAN_POINT('Ctrl Pts',(4.61485900524822,1.93721170622776,11.4597980825417));
#14328=CARTESIAN_POINT('Ctrl Pts',(4.66973898160766,1.94996093511623,11.4563813201229));
#14329=CARTESIAN_POINT('Ctrl Pts',(4.73425083427601,1.96209569912148,11.4522593735123));
#14330=CARTESIAN_POINT('Ctrl Pts',(4.74343454934524,1.96375652180609,11.4516701133919));
#14331=CARTESIAN_POINT('Ctrl Pts',(4.75832176221106,1.96634103693494,11.4507104041076));
#14332=CARTESIAN_POINT('Ctrl Pts',(4.76401833455827,1.96730452194909,11.4503421104856));
#14333=CARTESIAN_POINT('Ctrl Pts',(4.774165577162,1.96897545609932,11.4496840547051));
#14334=CARTESIAN_POINT('Ctrl Pts',(4.77861455609376,1.96969258716985,11.4493948404896));
#14335=CARTESIAN_POINT('Ctrl Pts',(4.78827213971658,1.97121573475031,11.4487654923335));
#14336=CARTESIAN_POINT('Ctrl Pts',(4.79348144022065,1.97201617396001,11.4484250643612));
#14337=CARTESIAN_POINT('Ctrl Pts',(4.80816098012414,1.97421225621957,11.4474631773094));
#14338=CARTESIAN_POINT('Ctrl Pts',(4.81763802915656,1.97556036457421,11.4468391685647));
#14339=CARTESIAN_POINT('Ctrl Pts',(4.8770824348877,1.9835802337602,11.4429077395189));
#14340=CARTESIAN_POINT('Ctrl Pts',(4.92727376450225,1.98842345519148,11.4395118678819));
#14341=CARTESIAN_POINT('Ctrl Pts',(5.12402973110369,1.99990828585557,11.426032931973));
#14342=CARTESIAN_POINT('Ctrl Pts',(5.27096758985521,1.99227774766367,11.4156466494535));
#14343=CARTESIAN_POINT('Ctrl Pts',(5.5015524753863,1.95457079073536,11.3996565449744));
#14344=CARTESIAN_POINT('Ctrl Pts',(5.58635709749293,1.93494310283634,11.3938349806183));
#14345=CARTESIAN_POINT('Ctrl Pts',(5.68455797807565,1.90533673127471,11.3871758661661));
#14346=CARTESIAN_POINT('Ctrl Pts',(5.69944221329449,1.90065814625408,11.3861686296699));
#14347=CARTESIAN_POINT('Ctrl Pts',(5.72380443770009,1.89268508218576,11.3845230947587));
#14348=CARTESIAN_POINT('Ctrl Pts',(5.73331495794085,1.88949293541946,11.3838814900212));
#14349=CARTESIAN_POINT('Ctrl Pts',(5.75040028972526,1.88361457439304,11.382730144248));
#14350=CARTESIAN_POINT('Ctrl Pts',(5.75798366125667,1.88095408885977,11.3822195716927));
#14351=CARTESIAN_POINT('Ctrl Pts',(5.77415033922349,1.87517234888367,11.3811319850696));
#14352=CARTESIAN_POINT('Ctrl Pts',(5.78272872921884,1.87203781973731,11.3805554225017));
#14353=CARTESIAN_POINT('Ctrl Pts',(5.80524392747031,1.86363508144071,11.3790433712668));
#14354=CARTESIAN_POINT('Ctrl Pts',(5.81914393464503,1.85826939086074,11.3781111287979));
#14355=CARTESIAN_POINT('Ctrl Pts',(5.88756817124212,1.8309714784427,11.3735264018142));
#14356=CARTESIAN_POINT('Ctrl Pts',(5.94116779089437,1.80679168336258,11.3699498741989));
#14357=CARTESIAN_POINT('Ctrl Pts',(6.10256747418618,1.72521613558311,11.3591277120932));
#14358=CARTESIAN_POINT('Ctrl Pts',(6.20622532553586,1.66027093979745,11.3521167650349));
#14359=CARTESIAN_POINT('Ctrl Pts',(6.34356960318351,1.5555500211298,11.3420594671607));
#14360=CARTESIAN_POINT('Ctrl Pts',(6.38265443822109,1.52332395142324,11.339094760132));
#14361=CARTESIAN_POINT('Ctrl Pts',(6.46156619235591,1.45304715459529,11.3327955795476));
#14362=CARTESIAN_POINT('Ctrl Pts',(6.50112723761924,1.41476549442104,11.3294540449623));
#14363=CARTESIAN_POINT('Ctrl Pts',(6.54544682484455,1.36817907937161,11.3254159573132));
#14364=CARTESIAN_POINT('Ctrl Pts',(6.5517951725238,1.36141210190463,11.3248300556563));
#14365=CARTESIAN_POINT('Ctrl Pts',(6.56200810911264,1.35037233329508,11.3238747749475));
#14366=CARTESIAN_POINT('Ctrl Pts',(6.56590188664579,1.34612656723289,11.3235075197805));
#14367=CARTESIAN_POINT('Ctrl Pts',(6.5728075525418,1.3385308517446,11.3228506074677));
#14368=CARTESIAN_POINT('Ctrl Pts',(6.57582655010998,1.33518749606565,11.322561490991));
#14369=CARTESIAN_POINT('Ctrl Pts',(6.58236063324838,1.32790193300165,11.3219315113848));
#14370=CARTESIAN_POINT('Ctrl Pts',(6.58587134202905,1.32395604229581,11.3215903485464));
#14371=CARTESIAN_POINT('Ctrl Pts',(6.59308779257652,1.31577989505242,11.3208835978736));
#14372=CARTESIAN_POINT('Ctrl Pts',(6.59679139508719,1.31154781949649,11.3205178632326));
#14373=CARTESIAN_POINT('Ctrl Pts',(6.61545622083189,1.29003680253104,11.3186595855437));
#14374=CARTESIAN_POINT('Ctrl Pts',(6.63013687293991,1.27251809778387,11.3171484720793));
#14375=CARTESIAN_POINT('Ctrl Pts',(6.69740922142852,1.18937955789207,11.3100029078068));
#14376=CARTESIAN_POINT('Ctrl Pts',(6.74611468525271,1.12073307907979,11.3041797932713));
#14377=CARTESIAN_POINT('Ctrl Pts',(6.83249001194355,0.981071210953838,11.2927431948972));
#14378=CARTESIAN_POINT('Ctrl Pts',(6.87049712651189,0.91043614565442,11.2871429091292));
#14379=CARTESIAN_POINT('Ctrl Pts',(6.94615230437225,0.746941129047247,11.2747424973385));
#14380=CARTESIAN_POINT('Ctrl Pts',(6.98127167658435,0.653137132023966,11.2680106557683));
#14381=CARTESIAN_POINT('Ctrl Pts',(7.01368105693964,0.541705590254264,11.2604719982906));
#14382=CARTESIAN_POINT('Ctrl Pts',(7.01796762451514,0.526276951425439,11.2594378099577));
#14383=CARTESIAN_POINT('Ctrl Pts',(7.02466876595964,0.500980424685786,11.2577574519961));
#14384=CARTESIAN_POINT('Ctrl Pts',(7.0271944967768,0.491142994014301,11.2571077336037));
#14385=CARTESIAN_POINT('Ctrl Pts',(7.0315867617794,0.473476543393289,11.255947512305));
#14386=CARTESIAN_POINT('Ctrl Pts',(7.03348124097738,0.465654765531611,11.2554361234979));
#14387=CARTESIAN_POINT('Ctrl Pts',(7.03740594312717,0.449011135717347,11.2543527405092));
#14388=CARTESIAN_POINT('Ctrl Pts',(7.03942356160959,0.440186474804402,11.2537811591504));
#14389=CARTESIAN_POINT('Ctrl Pts',(7.04341203632877,0.4221783589964,11.2526203949873));
#14390=CARTESIAN_POINT('Ctrl Pts',(7.04537824427773,0.412994100472801,11.2520313717092));
#14391=CARTESIAN_POINT('Ctrl Pts',(7.0501324881265,0.389994405001584,11.250563512928));
#14392=CARTESIAN_POINT('Ctrl Pts',(7.0528391407603,0.376162528202848,11.2496872309534));
#14393=CARTESIAN_POINT('Ctrl Pts',(7.07757825008149,0.242220603678845,11.2412608649073));
#14394=CARTESIAN_POINT('Ctrl Pts',(7.08868493723875,0.120353679506743,11.2340749555492));
#14395=CARTESIAN_POINT('Ctrl Pts',(7.08857636721997,-0.00177331764829418,
11.2269712774823));
#14396=CARTESIAN_POINT('Origin',(5.09382715545311,0.,-5.29363746883395));
#14397=CARTESIAN_POINT('',(7.54432661329192,-0.00163007106614652,-5.03580997262189));
#14398=CARTESIAN_POINT('',(4.01701575109769,-2.20564845811992,-5.29358888258478));
#14399=CARTESIAN_POINT('Ctrl Pts',(7.54716444752953,-0.00163195879212374,
-5.03580997262189));
#14400=CARTESIAN_POINT('Ctrl Pts',(7.54778240942886,-0.0888794390604748,
-5.04035856840935));
#14401=CARTESIAN_POINT('Ctrl Pts',(7.50402127856605,-0.986360486250927,
-5.08718292203284));
#14402=CARTESIAN_POINT('Ctrl Pts',(6.43805680969878,-2.52634576703256,-5.17310922535387));
#14403=CARTESIAN_POINT('Ctrl Pts',(4.69254185664738,-2.5308373754473,-5.25448693288734));
#14404=CARTESIAN_POINT('Ctrl Pts',(4.01701575109769,-2.20564845811992,-5.29358888258478));
#14405=CARTESIAN_POINT('',(6.1689156158044,-2.20207516956608,-5.29363746883395));
#14406=CARTESIAN_POINT('Origin',(5.09382715545311,0.,-5.29363746883395));
#14407=CARTESIAN_POINT('',(7.54449186889422,-0.00262135351006776,-5.15146496504602));
#14408=CARTESIAN_POINT('Ctrl Pts',(6.1689156158044,-2.20207516956608,-5.29363746883395));
#14409=CARTESIAN_POINT('Ctrl Pts',(6.90007729696917,-1.84511029528062,-5.25136171099787));
#14410=CARTESIAN_POINT('Ctrl Pts',(7.497763573434,-1.00822696320923,-5.20397087640191));
#14411=CARTESIAN_POINT('Ctrl Pts',(7.54733002393177,-0.100698414309727,
-5.15658004180592));
#14412=CARTESIAN_POINT('Ctrl Pts',(7.54656647390473,-0.00262357261131683,
-5.15146496504602));
#14413=CARTESIAN_POINT('',(7.54432697499699,-0.000940433632949707,-4.35146496508883));
#14414=CARTESIAN_POINT('Ctrl Pts',(7.54432575358315,-0.0026211758248253,
-5.15146496504602));
#14415=CARTESIAN_POINT('Ctrl Pts',(7.54441040290628,0.0765162272050172,
-5.14733375399662));
#14416=CARTESIAN_POINT('Ctrl Pts',(7.54065738891893,0.155829528594839,-5.14320254294721));
#14417=CARTESIAN_POINT('Ctrl Pts',(7.53304225424233,0.234904133294203,-5.13907133189781));
#14418=CARTESIAN_POINT('Ctrl Pts',(7.52543177817542,0.313930363573951,-5.13494264814446));
#14419=CARTESIAN_POINT('Ctrl Pts',(7.51396386810591,0.392717702539037,-5.13081396439111));
#14420=CARTESIAN_POINT('Ctrl Pts',(7.49866616683113,0.470849847992309,-5.12668528063777));
#14421=CARTESIAN_POINT('Ctrl Pts',(7.48339424086519,0.548850347511155,-5.12256355336088));
#14422=CARTESIAN_POINT('Ctrl Pts',(7.4643054647924,0.626197374386007,-5.118441826084));
#14423=CARTESIAN_POINT('Ctrl Pts',(7.44147915557445,0.702481555861974,-5.11432009880711));
#14424=CARTESIAN_POINT('Ctrl Pts',(7.41866391570903,0.778728744213543,-5.11020037031382));
#14425=CARTESIAN_POINT('Ctrl Pts',(7.39211487585167,0.853913642941191,-5.10608064182052));
#14426=CARTESIAN_POINT('Ctrl Pts',(7.36196189456157,0.92763950716289,-5.10196091332722));
#14427=CARTESIAN_POINT('Ctrl Pts',(7.33181340312425,1.00135439342277,-5.09784179827159));
#14428=CARTESIAN_POINT('Ctrl Pts',(7.29806222060958,1.07361022558622,-5.09372268321596));
#14429=CARTESIAN_POINT('Ctrl Pts',(7.26088665635795,1.14402944434926,-5.08960356816033));
#14430=CARTESIAN_POINT('Ctrl Pts',(7.22356724224814,1.21472114840839,-5.08546851429842));
#14431=CARTESIAN_POINT('Ctrl Pts',(7.18279711056472,1.28356155334622,-5.08133346043652));
#14432=CARTESIAN_POINT('Ctrl Pts',(7.13880262173743,1.35019464978026,-5.07719840657462));
#14433=CARTESIAN_POINT('Ctrl Pts',(7.09492122864415,1.41665645387401,-5.07307398261124));
#14434=CARTESIAN_POINT('Ctrl Pts',(7.04783235903743,1.48092191342971,-5.06894955864786));
#14435=CARTESIAN_POINT('Ctrl Pts',(6.99780214333237,1.54266960024827,-5.06482513468448));
#14436=CARTESIAN_POINT('Ctrl Pts',(6.94757851293935,1.6046560010002,-5.06068476587332));
#14437=CARTESIAN_POINT('Ctrl Pts',(6.89439108978141,1.66410476551921,-5.05654439706216));
#14438=CARTESIAN_POINT('Ctrl Pts',(6.83854606016657,1.720728390402,-5.052404028251));
#14439=CARTESIAN_POINT('Ctrl Pts',(6.78270103055173,1.77735201528479,-5.04826365943984));
#14440=CARTESIAN_POINT('Ctrl Pts',(6.724198804172,1.83115022519108,-5.04412329062867));
#14441=CARTESIAN_POINT('Ctrl Pts',(6.66337677971777,1.88187784592164,-5.03998292181751));
#14442=CARTESIAN_POINT('Ctrl Pts',(6.60111142291994,1.93380925452955,-5.03574430030475));
#14443=CARTESIAN_POINT('Ctrl Pts',(6.53615191711457,1.98274220618099,-5.03150567879198));
#14444=CARTESIAN_POINT('Ctrl Pts',(6.46881852374267,2.02838580825473,-5.02726705727922));
#14445=CARTESIAN_POINT('Ctrl Pts',(6.40158107006867,2.07396437523705,-5.02303447514821));
#14446=CARTESIAN_POINT('Ctrl Pts',(6.33197682745093,2.11626264435325,-5.0188018930172));
#14447=CARTESIAN_POINT('Ctrl Pts',(6.2603593791009,2.15502965668488,-5.01456931088619));
#14448=CARTESIAN_POINT('Ctrl Pts',(6.18882484308392,2.1937517880062,-5.01034162886357));
#14449=CARTESIAN_POINT('Ctrl Pts',(6.11528213913476,2.22895056917049,-5.00611394684095));
#14450=CARTESIAN_POINT('Ctrl Pts',(6.04011287722191,2.26041889542105,-5.00188626481833));
#14451=CARTESIAN_POINT('Ctrl Pts',(5.96499148420126,2.29186718217835,-4.99766127504583));
#14452=CARTESIAN_POINT('Ctrl Pts',(5.88824601557778,2.31958955200984,-4.99343628527334));
#14453=CARTESIAN_POINT('Ctrl Pts',(5.8102806585679,2.34342583152839,-4.98921129550084));
#14454=CARTESIAN_POINT('Ctrl Pts',(5.73234130671429,2.36725416051357,-4.98498771496347));
#14455=CARTESIAN_POINT('Ctrl Pts',(5.65318331704386,2.38719883833571,-4.9807641344261));
#14456=CARTESIAN_POINT('Ctrl Pts',(5.57322740388629,2.40314911143737,-4.97654055388872));
#14457=CARTESIAN_POINT('Ctrl Pts',(5.49327391264045,2.41909890139586,-4.97231710128609));
#14458=CARTESIAN_POINT('Ctrl Pts',(5.41252300024027,2.43105443771684,-4.96809364868346));
#14459=CARTESIAN_POINT('Ctrl Pts',(5.33140558690961,2.43895607564111,-4.96387019608083));
#14460=CARTESIAN_POINT('Ctrl Pts',(5.2502104169818,2.44686528782658,-4.95964269500958));
#14461=CARTESIAN_POINT('Ctrl Pts',(5.16864850614162,2.45071279281044,-4.95541519393833));
#14462=CARTESIAN_POINT('Ctrl Pts',(5.08715538903955,2.45049091765975,-4.95118769286707));
#14463=CARTESIAN_POINT('Ctrl Pts',(5.00562544874515,2.45026894225334,-4.9469582815721));
#14464=CARTESIAN_POINT('Ctrl Pts',(4.92416482723625,2.44597394660128,-4.94272887027713));
#14465=CARTESIAN_POINT('Ctrl Pts',(4.84320606541023,2.43765036853641,-4.93849945898217));
#14466=CARTESIAN_POINT('Ctrl Pts',(4.76210292966866,2.42931194701879,-4.93426250536991));
#14467=CARTESIAN_POINT('Ctrl Pts',(4.68150390129521,2.41693065545801,-4.93002555175765));
#14468=CARTESIAN_POINT('Ctrl Pts',(4.60183332778805,2.40060249177982,-4.92578859814539));
#14469=CARTESIAN_POINT('Ctrl Pts',(4.52265109367718,2.38437441129724,-4.92157761486669));
#14470=CARTESIAN_POINT('Ctrl Pts',(4.44438637243818,2.36424791318695,-4.91736663158799));
#14471=CARTESIAN_POINT('Ctrl Pts',(4.36743896401488,2.340365451236,-4.9131556483093));
#14472=CARTESIAN_POINT('Ctrl Pts',(4.28997216954912,2.3163217854492,-4.90891624138405));
#14473=CARTESIAN_POINT('Ctrl Pts',(4.21356166607285,2.28838467134188,-4.9046768344588));
#14474=CARTESIAN_POINT('Ctrl Pts',(4.13862570813318,2.25666578053506,-4.90043742753356));
#14475=CARTESIAN_POINT('Ctrl Pts',(4.06379399234112,2.22499101334243,-4.8962039179758));
#14476=CARTESIAN_POINT('Ctrl Pts',(3.99043317048696,2.18954509819096,-4.89197040841805));
#14477=CARTESIAN_POINT('Ctrl Pts',(3.91894595991049,2.15048934579094,-4.8877368988603));
#14478=CARTESIAN_POINT('Ctrl Pts',(3.84753791118406,2.11147684204463,-4.88350807730822));
#14479=CARTESIAN_POINT('Ctrl Pts',(3.77799975419623,2.06886266693087,-4.87927925575614));
#14480=CARTESIAN_POINT('Ctrl Pts',(3.71071252885978,2.02285545200432,-4.87505043420406));
#14481=CARTESIAN_POINT('Ctrl Pts',(3.6434660984384,1.97687613034303,-4.87082417650292));
#14482=CARTESIAN_POINT('Ctrl Pts',(3.57846827138453,1.92750811351861,-4.86659791880178));
#14483=CARTESIAN_POINT('Ctrl Pts',(3.51607285230926,1.87500442903772,-4.86237166110065));
#14484=CARTESIAN_POINT('Ctrl Pts',(3.45369636419676,1.82251667433678,-4.85814668565914));
#14485=CARTESIAN_POINT('Ctrl Pts',(3.39392106969408,1.76689543933148,-4.85392171021764));
#14486=CARTESIAN_POINT('Ctrl Pts',(3.33706817332974,1.70843440867036,-4.84969673477613));
#14487=CARTESIAN_POINT('Ctrl Pts',(3.28021530742337,1.64997340932875,-4.84547176159809));
#14488=CARTESIAN_POINT('Ctrl Pts',(3.22628515825109,1.58867295004995,-4.84124678842004));
#14489=CARTESIAN_POINT('Ctrl Pts',(3.17556149055324,1.52486297380003,-4.83702181524199));
#14490=CARTESIAN_POINT('Ctrl Pts',(3.12478693488892,1.46098898088728,-4.83279260340568));
#14491=CARTESIAN_POINT('Ctrl Pts',(3.0772255758737,1.39460080451466,-4.82856339156937));
#14492=CARTESIAN_POINT('Ctrl Pts',(3.03311999921932,1.32606043084275,-4.82433417973306));
#14493=CARTESIAN_POINT('Ctrl Pts',(2.98899339547624,1.25748738092836,-4.82010295164349));
#14494=CARTESIAN_POINT('Ctrl Pts',(2.94832608785976,1.18676049106336,-4.81587172355392));
#14495=CARTESIAN_POINT('Ctrl Pts',(2.91131523202827,1.11426745178544,-4.81164049546435));
#14496=CARTESIAN_POINT('Ctrl Pts',(2.8742369808903,1.04164240554658,-4.80740156247558));
#14497=CARTESIAN_POINT('Ctrl Pts',(2.8408286781381,0.967245205970693,-4.8031626294868));
#14498=CARTESIAN_POINT('Ctrl Pts',(2.81123970595368,0.891484596270571,-4.79892369649802));
#14499=CARTESIAN_POINT('Ctrl Pts',(2.78193338253604,0.816447690076199,-4.79472525593237));
#14500=CARTESIAN_POINT('Ctrl Pts',(2.75637377629209,0.74007375723796,-4.79052681536673));
#14501=CARTESIAN_POINT('Ctrl Pts',(2.7346569978228,0.662771768670451,-4.78632837480108));
#14502=CARTESIAN_POINT('Ctrl Pts',(2.71279595531059,0.584956264831261,-4.7821020440946));
#14503=CARTESIAN_POINT('Ctrl Pts',(2.69474723143283,0.505908991203818,-4.77787571338812));
#14504=CARTESIAN_POINT('Ctrl Pts',(2.68064637115932,0.426038439950232,-4.77364938268164));
#14505=CARTESIAN_POINT('Ctrl Pts',(2.66656596150763,0.346283725773699,-4.7694291814658));
#14506=CARTESIAN_POINT('Ctrl Pts',(2.65642212514089,0.265708560236698,-4.76520898024995));
#14507=CARTESIAN_POINT('Ctrl Pts',(2.65030041091275,0.184735753756496,-4.7609887790341));
#14508=CARTESIAN_POINT('Ctrl Pts',(2.64416643639912,0.103600778692895,-4.75676012579489));
#14509=CARTESIAN_POINT('Ctrl Pts',(2.64207082859058,0.0220670254031271,
-4.75253147255567));
#14510=CARTESIAN_POINT('Ctrl Pts',(2.64404793261838,-0.0594307106405606,
-4.74830281931645));
#14511=CARTESIAN_POINT('Ctrl Pts',(2.6460174770955,-0.14061683623954,-4.7440903345327));
#14512=CARTESIAN_POINT('Ctrl Pts',(2.65202864769558,-0.22176675096376,-4.73987784974896));
#14513=CARTESIAN_POINT('Ctrl Pts',(2.66206332567863,-0.302448220693316,
-4.73566536496521));
#14514=CARTESIAN_POINT('Ctrl Pts',(2.67209460104101,-0.383102332451107,
-4.73145430857686));
#14515=CARTESIAN_POINT('Ctrl Pts',(2.68614661716576,-0.463287852423471,
-4.72724325218851));
#14516=CARTESIAN_POINT('Ctrl Pts',(2.70414938777136,-0.542577567401701,
-4.72303219580016));
#14517=CARTESIAN_POINT('Ctrl Pts',(2.72215160421661,-0.621864841688081,
-4.71882126903633));
#14518=CARTESIAN_POINT('Ctrl Pts',(2.74410422910218,-0.700255911458633,
-4.7146103422725));
#14519=CARTESIAN_POINT('Ctrl Pts',(2.76988644792786,-0.77733508727384,-4.71039941550866));
#14520=CARTESIAN_POINT('Ctrl Pts',(2.79585601766407,-0.854974372126607,
-4.70615788932401));
#14521=CARTESIAN_POINT('Ctrl Pts',(2.82571092881134,-0.931282159326933,
-4.70191636313936));
#14522=CARTESIAN_POINT('Ctrl Pts',(2.8592776600035,-1.00585227662211,-4.69767483695472));
#14523=CARTESIAN_POINT('Ctrl Pts',(2.89265037987298,-1.07999138837773,-4.6934578262375));
#14524=CARTESIAN_POINT('Ctrl Pts',(2.92969185937331,-1.15241247193342,-4.68924081552028));
#14525=CARTESIAN_POINT('Ctrl Pts',(2.97018535081307,-1.22274107462912,-4.68502380480306));
#14526=CARTESIAN_POINT('Ctrl Pts',(3.0110319538301,-1.29368295721111,-4.68077002088469));
#14527=CARTESIAN_POINT('Ctrl Pts',(3.05539080386526,-1.36249528115039,-4.67651623696633));
#14528=CARTESIAN_POINT('Ctrl Pts',(3.10299593847398,-1.42882515217972,-4.67226245304796));
#14529=CARTESIAN_POINT('Ctrl Pts',(3.1506010730827,-1.49515502320905,-4.6680086691296));
#14530=CARTESIAN_POINT('Ctrl Pts',(3.20145214292242,-1.55900210626518,-4.66375488521123));
#14531=CARTESIAN_POINT('Ctrl Pts',(3.25524435580459,-1.62005047416326,-4.65950110129287));
#14532=CARTESIAN_POINT('Ctrl Pts',(3.30877840952224,-1.68080585921481,-4.65526773210079));
#14533=CARTESIAN_POINT('Ctrl Pts',(3.3654266037922,-1.73901772985628,-4.65103436290872));
#14534=CARTESIAN_POINT('Ctrl Pts',(3.42491790165664,-1.79435006411583,-4.64680099371664));
#14535=CARTESIAN_POINT('Ctrl Pts',(3.48432428573454,-1.84960342080744,-4.64257366694456));
#14536=CARTESIAN_POINT('Ctrl Pts',(3.54656537632463,-1.90198509065237,-4.63834634017248));
#14537=CARTESIAN_POINT('Ctrl Pts',(3.61133105720728,-1.9511933703982,-4.6341190134004));
#14538=CARTESIAN_POINT('Ctrl Pts',(3.67608993510763,-2.00039648130999,-4.62989213066641));
#14539=CARTESIAN_POINT('Ctrl Pts',(3.74337254318219,-2.04642653984645,-4.62566524793242));
#14540=CARTESIAN_POINT('Ctrl Pts',(3.81283321839339,-2.08902005333032,-4.62143836519843));
#14541=CARTESIAN_POINT('Ctrl Pts',(3.88217701172922,-2.13154189446551,-4.61721859506419));
#14542=CARTESIAN_POINT('Ctrl Pts',(3.95369116722407,-2.17063848015603,-4.61299882492994));
#14543=CARTESIAN_POINT('Ctrl Pts',(4.02700158347371,-2.20609008178968,-4.6087790547957));
#14544=CARTESIAN_POINT('Ctrl Pts',(4.10028795109302,-2.2415300539373,-4.60456066890802));
#14545=CARTESIAN_POINT('Ctrl Pts',(4.17536899153297,-2.27332721461545,-4.60034228302035));
#14546=CARTESIAN_POINT('Ctrl Pts',(4.25184670815908,-2.30130814459397,-4.59612389713267));
#14547=CARTESIAN_POINT('Ctrl Pts',(4.32832269787782,-2.32928844274826,-4.59190560649838));
#14548=CARTESIAN_POINT('Ctrl Pts',(4.4061948645903,-2.3534525230627,-4.58768731586409));
#14549=CARTESIAN_POINT('Ctrl Pts',(4.48504732199531,-2.37367591814365,-4.58346902522981));
#14550=CARTESIAN_POINT('Ctrl Pts',(4.56417349122223,-2.39396951246119,-4.57923609210938));
#14551=CARTESIAN_POINT('Ctrl Pts',(4.64428631532835,-2.41029489064329,-4.57500315898895));
#14552=CARTESIAN_POINT('Ctrl Pts',(4.72495420216572,-2.42257775816031,-4.57077022586852));
#14553=CARTESIAN_POINT('Ctrl Pts',(4.80545917820924,-2.4348358201224,-4.56654584126128));
#14554=CARTESIAN_POINT('Ctrl Pts',(4.88651650907397,-2.44306767202367,-4.56232145665404));
#14555=CARTESIAN_POINT('Ctrl Pts',(4.96769285381683,-2.44725159882484,-4.55809707204681));
#14556=CARTESIAN_POINT('Ctrl Pts',(5.04911560263457,-2.45144822558948,-4.55385986466978));
#14557=CARTESIAN_POINT('Ctrl Pts',(5.13065761996133,-2.45157232879408,-4.54962265729275));
#14558=CARTESIAN_POINT('Ctrl Pts',(5.21188426209025,-2.44765454457374,-4.54538544991573));
#14559=CARTESIAN_POINT('Ctrl Pts',(5.29311090421916,-2.44373676035339,-4.5411482425387));
#14560=CARTESIAN_POINT('Ctrl Pts',(5.37402171465691,-2.43577719546714,-4.53691103516168));
#14561=CARTESIAN_POINT('Ctrl Pts',(5.45419165970096,-2.42385801442209,-4.53267382778465));
#14562=CARTESIAN_POINT('Ctrl Pts',(5.53428105576291,-2.41195080891102,-4.52844087764818));
#14563=CARTESIAN_POINT('Ctrl Pts',(5.61392832466803,-2.39604775380258,-4.5242079275117));
#14564=CARTESIAN_POINT('Ctrl Pts',(5.69270415841357,-2.37619371797105,-4.51997497737523));
#14565=CARTESIAN_POINT('Ctrl Pts',(5.77136778124399,-2.35636796288787,-4.51574805679358));
#14566=CARTESIAN_POINT('Ctrl Pts',(5.84916198766149,-2.33260251745521,-4.51152113621193));
#14567=CARTESIAN_POINT('Ctrl Pts',(5.92566503819675,-2.30499370646268,-4.50729421563028));
#14568=CARTESIAN_POINT('Ctrl Pts',(6.00216927074345,-2.27738446889985,-4.50306722974054));
#14569=CARTESIAN_POINT('Ctrl Pts',(6.07738185167261,-2.24593184421965,-4.4988402438508));
#14570=CARTESIAN_POINT('Ctrl Pts',(6.15089365509811,-2.21078281731342,-4.49461325796105));
#14571=CARTESIAN_POINT('Ctrl Pts',(6.22427350784327,-2.1756968814728,-4.49039385933809));
#14572=CARTESIAN_POINT('Ctrl Pts',(6.29595825306512,-2.13692797762798,-4.48617446071512));
#14573=CARTESIAN_POINT('Ctrl Pts',(6.36556019118147,-2.09467069866295,-4.48195506209215));
#14574=CARTESIAN_POINT('Ctrl Pts',(6.43513952610997,-2.05242714272403,-4.47773703371637));
#14575=CARTESIAN_POINT('Ctrl Pts',(6.50263700048167,-2.00669770229264,-4.47351900534059));
#14576=CARTESIAN_POINT('Ctrl Pts',(6.56769080516089,-1.95772219481469,-4.4693009769648));
#14577=CARTESIAN_POINT('Ctrl Pts',(6.63274336537986,-1.90874762422387,-4.46508302927867));
#14578=CARTESIAN_POINT('Ctrl Pts',(6.69535197849001,-1.85652739034329,-4.46086508159254));
#14579=CARTESIAN_POINT('Ctrl Pts',(6.75518620855875,-1.80134292866848,-4.4566471339064));
#14580=CARTESIAN_POINT('Ctrl Pts',(6.81523937887182,-1.74595654078005,-4.45241375227057));
#14581=CARTESIAN_POINT('Ctrl Pts',(6.87249747229355,-1.68758450384207,-4.44818037063474));
#14582=CARTESIAN_POINT('Ctrl Pts',(6.92666347913855,-1.62654888047646,-4.44394698899891));
#14583=CARTESIAN_POINT('Ctrl Pts',(6.98071048701252,-1.5656473481543,-4.43972290780976));
#14584=CARTESIAN_POINT('Ctrl Pts',(7.03167871727176,-1.50209430841,-4.43549882662062));
#14585=CARTESIAN_POINT('Ctrl Pts',(7.0793145170224,-1.43624168824353,-4.43127474543147));
#14586=CARTESIAN_POINT('Ctrl Pts',(7.12710764124051,-1.37017157979193,-4.4270367135723));
#14587=CARTESIAN_POINT('Ctrl Pts',(7.17154604090554,-1.30178707661587,-4.42279868171313));
#14588=CARTESIAN_POINT('Ctrl Pts',(7.21241914666087,-1.23146994473692,-4.41856064985395));
#14589=CARTESIAN_POINT('Ctrl Pts',(7.25329225241619,-1.16115281285797,-4.41432261799478));
#14590=CARTESIAN_POINT('Ctrl Pts',(7.29059990576516,-1.08890349424344,-4.41008458613561));
#14591=CARTESIAN_POINT('Ctrl Pts',(7.32418007214676,-1.01512369541655,-4.40584655427644));
#14592=CARTESIAN_POINT('Ctrl Pts',(7.36071056800757,-0.934861656061826,
-4.40123617195938));
#14593=CARTESIAN_POINT('Ctrl Pts',(7.3929488423299,-0.852528880741258,-4.39662578964233));
#14594=CARTESIAN_POINT('Ctrl Pts',(7.42067706440021,-0.76858295013151,-4.39201540732527));
#14595=CARTESIAN_POINT('Ctrl Pts',(7.44833404735281,-0.684852692709086,
-4.38741686996415));
#14596=CARTESIAN_POINT('Ctrl Pts',(7.47150395187169,-0.599517840836609,
-4.38281833260303));
#14597=CARTESIAN_POINT('Ctrl Pts',(7.49001655380418,-0.513056154070835,
-4.37821979524192));
#14598=CARTESIAN_POINT('Ctrl Pts',(7.5084493995364,-0.426966962518323,-4.37364106935128));
#14599=CARTESIAN_POINT('Ctrl Pts',(7.5222648532601,-0.339760926393879,-4.36906234346064));
#14600=CARTESIAN_POINT('Ctrl Pts',(7.53134271997225,-0.251928804877392,
-4.36448361757));
#14601=CARTESIAN_POINT('Ctrl Pts',(7.53994639377573,-0.168684696216461,
-4.36014406674294));
#14602=CARTESIAN_POINT('Ctrl Pts',(7.54429476187688,-0.0848785683972825,
-4.35580451591589));
#14603=CARTESIAN_POINT('Ctrl Pts',(7.54432697499699,-0.000940433632964154,
-4.35146496508883));
#14604=CARTESIAN_POINT('',(7.54432616501525,0.00220321015066406,-3.55146496500219));
#14605=CARTESIAN_POINT('Ctrl Pts',(7.54432697499731,-0.000940432804910453,
-4.35146496504602));
#14606=CARTESIAN_POINT('Ctrl Pts',(7.54435894273178,0.0823583708330137,
-4.34715846725177));
#14607=CARTESIAN_POINT('Ctrl Pts',(7.54013925399136,0.165631372021684,-4.34285196945752));
#14608=CARTESIAN_POINT('Ctrl Pts',(7.53170205545692,0.248427498339918,-4.33854547166327));
#14609=CARTESIAN_POINT('Ctrl Pts',(7.52325973533066,0.331273883990137,-4.3342363597165));
#14610=CARTESIAN_POINT('Ctrl Pts',(7.51059485692861,0.413642384925573,-4.32992724776972));
#14611=CARTESIAN_POINT('Ctrl Pts',(7.49379316422016,0.495089291706826,-4.32561813582295));
#14612=CARTESIAN_POINT('Ctrl Pts',(7.47696332659815,0.576672632131393,-4.32130180558066));
#14613=CARTESIAN_POINT('Ctrl Pts',(7.45598292601234,0.657330867510103,-4.31698547533837));
#14614=CARTESIAN_POINT('Ctrl Pts',(7.43098837314364,0.736632671365669,-4.31266914509608));
#14615=CARTESIAN_POINT('Ctrl Pts',(7.40597114511374,0.81600641814397,-4.30834889906123));
#14616=CARTESIAN_POINT('Ctrl Pts',(7.37693266243305,0.894020873270854,-4.30402865302639));
#14617=CARTESIAN_POINT('Ctrl Pts',(7.34405767683324,0.97026431999188,-4.29970840699154));
#14618=CARTESIAN_POINT('Ctrl Pts',(7.31111461608832,1.04666564613413,-4.29537921490333));
#14619=CARTESIAN_POINT('Ctrl Pts',(7.27431937545136,1.12128824639635,-4.29105002281511));
#14620=CARTESIAN_POINT('Ctrl Pts',(7.23390291427382,1.19374452732064,-4.28672083072689));
#14621=CARTESIAN_POINT('Ctrl Pts',(7.20993621035855,1.23671064016474,-4.28415364740734));
#14622=CARTESIAN_POINT('Ctrl Pts',(7.1846969767331,1.27891552146937,-4.28158646408778));
#14623=CARTESIAN_POINT('Ctrl Pts',(7.15824028834326,1.32028355543447,-4.27901928076822));
#14624=CARTESIAN_POINT('Ctrl Pts',(7.11462301567452,1.38848410988927,-4.27478694703129));
#14625=CARTESIAN_POINT('Ctrl Pts',(7.06754118317403,1.45464801911065,-4.27055461329436));
#14626=CARTESIAN_POINT('Ctrl Pts',(7.01721112668303,1.51840190635281,-4.26632227955743));
#14627=CARTESIAN_POINT('Ctrl Pts',(6.96695297675965,1.58206470839609,-4.26209599255704));
#14628=CARTESIAN_POINT('Ctrl Pts',(6.91345610538469,1.64332396541314,-4.25786970555666));
#14629=CARTESIAN_POINT('Ctrl Pts',(6.85698071948308,1.70183423389248,-4.25364341855628));
#14630=CARTESIAN_POINT('Ctrl Pts',(6.80049390648484,1.76035634120181,-4.24941627641893));
#14631=CARTESIAN_POINT('Ctrl Pts',(6.74102764743151,1.81612796965853,-4.24518913428159));
#14632=CARTESIAN_POINT('Ctrl Pts',(6.67888340738122,1.86883571461581,-4.24096199214424));
#14633=CARTESIAN_POINT('Ctrl Pts',(6.61686286860303,1.92143854212467,-4.23674326434843));
#14634=CARTESIAN_POINT('Ctrl Pts',(6.55217533763354,1.97098935202897,-4.23252453655261));
#14635=CARTESIAN_POINT('Ctrl Pts',(6.48515680212753,2.01721393617158,-4.22830580875679));
#14636=CARTESIAN_POINT('Ctrl Pts',(6.41816023415074,2.06342336868643,-4.22408846378776));
#14637=CARTESIAN_POINT('Ctrl Pts',(6.34883456118247,2.10630847704602,-4.21987111881873));
#14638=CARTESIAN_POINT('Ctrl Pts',(6.27754646223391,2.14563716707983,-4.21565377384969));
#14639=CARTESIAN_POINT('Ctrl Pts',(6.20625992476307,2.18496499566729,-4.21143652125639));
#14640=CARTESIAN_POINT('Ctrl Pts',(6.13301145415542,2.22073633738107,-4.20721926866309));
#14641=CARTESIAN_POINT('Ctrl Pts',(6.05819288644913,2.25276474290604,-4.20300201606979));
#14642=CARTESIAN_POINT('Ctrl Pts',(5.98307423198179,2.28492160986472,-4.19876784866897));
#14643=CARTESIAN_POINT('Ctrl Pts',(5.90637328831448,2.3133052574162,-4.19453368126816));
#14644=CARTESIAN_POINT('Ctrl Pts',(5.82850574459439,2.33777621269816,-4.19029951386734));
#14645=CARTESIAN_POINT('Ctrl Pts',(5.75083687156058,2.36218473296231,-4.18607614949052));
#14646=CARTESIAN_POINT('Ctrl Pts',(5.67200780663635,2.3827004234283,-4.1818527851137));
#14647=CARTESIAN_POINT('Ctrl Pts',(5.59244332756941,2.39923574558735,-4.17762942073688));
#14648=CARTESIAN_POINT('Ctrl Pts',(5.51257356926303,2.41583451176855,-4.17338985182407));
#14649=CARTESIAN_POINT('Ctrl Pts',(5.4319632089515,2.42842224104266,-4.16915028291125));
#14650=CARTESIAN_POINT('Ctrl Pts',(5.35104733214227,2.43696287019396,-4.16491071399844));
#14651=CARTESIAN_POINT('Ctrl Pts',(5.27013145533303,2.44550349934527,-4.16067114508563));
#14652=CARTESIAN_POINT('Ctrl Pts',(5.18891053157333,2.44999706458279,-4.15643157617281));
#14653=CARTESIAN_POINT('Ctrl Pts',(5.10781798867477,2.45046006018987,-4.15219200726));
#14654=CARTESIAN_POINT('Ctrl Pts',(5.02686672608006,2.45092224916102,-4.14795982456992));
#14655=CARTESIAN_POINT('Ctrl Pts',(4.94574161710686,2.44736963799979,-4.14372764187984));
#14656=CARTESIAN_POINT('Ctrl Pts',(4.8648736273461,2.4397808368719,-4.13949545918977));
#14657=CARTESIAN_POINT('Ctrl Pts',(4.78412116947314,2.43220287746919,-4.13526932279882));
#14658=CARTESIAN_POINT('Ctrl Pts',(4.70362556001836,2.42060022365766,-4.13104318640786));
#14659=CARTESIAN_POINT('Ctrl Pts',(4.62381816784454,2.40500349304677,-4.12681705001691));
#14660=CARTESIAN_POINT('Ctrl Pts',(4.54399107084123,2.38940291152798,-4.12258987017253));
#14661=CARTESIAN_POINT('Ctrl Pts',(4.46485299712538,2.36980630484773,-4.11836269032815));
#14662=CARTESIAN_POINT('Ctrl Pts',(4.38683090851581,2.34629634889043,-4.11413551048377));
#14663=CARTESIAN_POINT('Ctrl Pts',(4.30896756011833,2.32283422522603,-4.10991693106828));
#14664=CARTESIAN_POINT('Ctrl Pts',(4.23221611240439,2.29547477038324,-4.10569835165279));
#14665=CARTESIAN_POINT('Ctrl Pts',(4.15698933680047,2.26435093383119,-4.1014797722373));
#14666=CARTESIAN_POINT('Ctrl Pts',(4.08178719900443,2.23323729076542,-4.09726257446483));
#14667=CARTESIAN_POINT('Ctrl Pts',(4.00810917068676,2.19836189190233,-4.09304537669236));
#14668=CARTESIAN_POINT('Ctrl Pts',(3.93634935778715,2.15990634007828,-4.08882817891988));
#14669=CARTESIAN_POINT('Ctrl Pts',(3.8645910930412,2.12145161789831,-4.08461107212968));
#14670=CARTESIAN_POINT('Ctrl Pts',(3.79475137044941,2.07941711682518,-4.08039396533947));
#14671=CARTESIAN_POINT('Ctrl Pts',(3.72719965800537,2.03403036683815,-4.07617685854926));
#14672=CARTESIAN_POINT('Ctrl Pts',(3.65937183564308,1.98845810368831,-4.07194251481613));
#14673=CARTESIAN_POINT('Ctrl Pts',(3.59385116518287,1.93950638283866,-4.06770817108301));
#14674=CARTESIAN_POINT('Ctrl Pts',(3.53098072628333,1.88744835395071,-4.06347382734989));
#14675=CARTESIAN_POINT('Ctrl Pts',(3.46827539746185,1.83552703963584,-4.05925060383219));
#14676=CARTESIAN_POINT('Ctrl Pts',(3.4082067148203,1.78051605822941,-4.05502738031449));
#14677=CARTESIAN_POINT('Ctrl Pts',(3.35107902672125,1.72272435688406,-4.05080415679679));
#14678=CARTESIAN_POINT('Ctrl Pts',(3.29372570332407,1.66470439760992,-4.04656425295595));
#14679=CARTESIAN_POINT('Ctrl Pts',(3.23933696170591,1.60388206453133,-4.04232434911512));
#14680=CARTESIAN_POINT('Ctrl Pts',(3.18817963229373,1.54060305318291,-4.03808444527428));
#14681=CARTESIAN_POINT('Ctrl Pts',(3.13702230288155,1.47732404183449,-4.03384454143345));
#14682=CARTESIAN_POINT('Ctrl Pts',(3.08909661061961,1.41158876630477,-4.02960463759262));
#14683=CARTESIAN_POINT('Ctrl Pts',(3.04462434790387,1.34377010814064,-4.02536473375178));
#14684=CARTESIAN_POINT('Ctrl Pts',(3.00023531020732,1.2760783652442,-4.02113276443141));
#14685=CARTESIAN_POINT('Ctrl Pts',(2.95912113831476,1.20605844695567,-4.01690079511104));
#14686=CARTESIAN_POINT('Ctrl Pts',(2.92153406644567,1.13406039762022,-4.01266882579066));
#14687=CARTESIAN_POINT('Ctrl Pts',(2.88400073372037,1.0621652856335,-4.00844290701896));
#14688=CARTESIAN_POINT('Ctrl Pts',(2.84998469879711,0.988298068178758,-4.00421698824726));
#14689=CARTESIAN_POINT('Ctrl Pts',(2.81969476619186,0.912837403984379,-3.99999106947556));
#14690=CARTESIAN_POINT('Ctrl Pts',(2.78939540850371,0.837353259281616,-3.99576383575756));
#14691=CARTESIAN_POINT('Ctrl Pts',(2.76282470604432,0.760275080275662,-3.99153660203956));
#14692=CARTESIAN_POINT('Ctrl Pts',(2.74014540541728,0.682006209317958,-3.98730936832156));
#14693=CARTESIAN_POINT('Ctrl Pts',(2.71751375000239,0.60390176745901,-3.98309101527633));
#14694=CARTESIAN_POINT('Ctrl Pts',(2.69875731585562,0.524612070978461,-3.97887266223109));
#14695=CARTESIAN_POINT('Ctrl Pts',(2.68398890655482,0.444555805435994,-3.97465430918585));
#14696=CARTESIAN_POINT('Ctrl Pts',(2.66922534417337,0.364525813966359,-3.97043734058335));
#14697=CARTESIAN_POINT('Ctrl Pts',(2.65844729162773,0.283730209711626,-3.96622037198085));
#14698=CARTESIAN_POINT('Ctrl Pts',(2.65171656970815,0.202598462463126,-3.96200340337834));
#14699=CARTESIAN_POINT('Ctrl Pts',(2.6449859969881,0.121468513657372,-3.95778652825314));
#14700=CARTESIAN_POINT('Ctrl Pts',(2.6423026137912,0.0400028998962365,-3.95356965312794));
#14701=CARTESIAN_POINT('Ctrl Pts',(2.64367629924461,-0.0413646203990808,
-3.94935277800273));
#14702=CARTESIAN_POINT('Ctrl Pts',(2.64505576193407,-0.123074343758934,
-3.94511816818947));
#14703=CARTESIAN_POINT('Ctrl Pts',(2.65052649774286,-0.204684674653923,
-3.9408835583762));
#14704=CARTESIAN_POINT('Ctrl Pts',(2.6600457322559,-0.285759049025847,-3.93664894856294));
#14705=CARTESIAN_POINT('Ctrl Pts',(2.66953884154435,-0.366610917456189,
-3.93242596049639));
#14706=CARTESIAN_POINT('Ctrl Pts',(2.68305813794157,-0.446929313110711,
-3.92820297242984));
#14707=CARTESIAN_POINT('Ctrl Pts',(2.70050975822739,-0.526290875977058,
-3.92397998436328));
#14708=CARTESIAN_POINT('Ctrl Pts',(2.71803341931967,-0.605980045730181,
-3.91973956367667));
#14709=CARTESIAN_POINT('Ctrl Pts',(2.73952180815708,-0.684704012986985,
-3.91549914299005));
#14710=CARTESIAN_POINT('Ctrl Pts',(2.7648297406262,-0.762050714670325,-3.91125872230343));
#14711=CARTESIAN_POINT('Ctrl Pts',(2.79013767309531,-0.839397416353665,
-3.90701830161681));
#14712=CARTESIAN_POINT('Ctrl Pts',(2.81926492367267,-0.915366438150804,
-3.90277788093019));
#14713=CARTESIAN_POINT('Ctrl Pts',(2.85201897448302,-0.989568759478377,
-3.89853746024357));
#14714=CARTESIAN_POINT('Ctrl Pts',(2.88470900689497,-1.06362605099587,-3.89430532753765));
#14715=CARTESIAN_POINT('Ctrl Pts',(2.92113363261499,-1.1361998701706,-3.89007319483172));
#14716=CARTESIAN_POINT('Ctrl Pts',(2.96113610813775,-1.2068882080379,-3.8858410621258));
#14717=CARTESIAN_POINT('Ctrl Pts',(3.00108141513979,-1.27747552346457,-3.88161497766472));
#14718=CARTESIAN_POINT('Ctrl Pts',(3.04459418963606,-1.34618230829652,-3.87738889320364));
#14719=CARTESIAN_POINT('Ctrl Pts',(3.09147006458376,-1.41262745642482,-3.87316280874256));
#14720=CARTESIAN_POINT('Ctrl Pts',(3.13835823086516,-1.47909002715032,-3.86893561615893));
#14721=CARTESIAN_POINT('Ctrl Pts',(3.1886110488955,-1.5432893594117,-3.8647084235753));
#14722=CARTESIAN_POINT('Ctrl Pts',(3.24197843702879,-1.60486964394938,-3.86048123099166));
#14723=CARTESIAN_POINT('Ctrl Pts',(3.29523637498116,-1.66632363463009,-3.85626270787845));
#14724=CARTESIAN_POINT('Ctrl Pts',(3.3515958351206,-1.72516894203193,-3.85204418476524));
#14725=CARTESIAN_POINT('Ctrl Pts',(3.41076667511244,-1.78108328539556,-3.84782566165203));
#14726=CARTESIAN_POINT('Ctrl Pts',(3.4699181141398,-1.83697929553644,-3.84360852171028));
#14727=CARTESIAN_POINT('Ctrl Pts',(3.53187876493583,-1.88994593120588,-3.83939138176853));
#14728=CARTESIAN_POINT('Ctrl Pts',(3.59632172180472,-1.93969784404519,-3.83517424182678));
#14729=CARTESIAN_POINT('Ctrl Pts',(3.66076326611745,-1.98944866634839,-3.83095719432255));
#14730=CARTESIAN_POINT('Ctrl Pts',(3.72768663980081,-2.03598462286909,-3.82674014681832));
#14731=CARTESIAN_POINT('Ctrl Pts',(3.7967331044691,-2.07906163278097,-3.82252309931408));
#14732=CARTESIAN_POINT('Ctrl Pts',(3.86606383822575,-2.12231599373314,-3.81828868993252));
#14733=CARTESIAN_POINT('Ctrl Pts',(3.93753478830691,-2.16208260581578,-3.81405428055096));
#14734=CARTESIAN_POINT('Ctrl Pts',(4.01075634507282,-2.19816011011532,-3.8098198711694));
#14735=CARTESIAN_POINT('Ctrl Pts',(4.08378339864932,-2.23414177939082,-3.80559670992522));
#14736=CARTESIAN_POINT('Ctrl Pts',(4.15855132473493,-2.26645376745094,-3.80137354868105));
#14737=CARTESIAN_POINT('Ctrl Pts',(4.23465372403717,-2.29494471932309,-3.79715038743687));
#14738=CARTESIAN_POINT('Ctrl Pts',(4.31106016462263,-2.32354949711463,-3.79291035398661));
#14739=CARTESIAN_POINT('Ctrl Pts',(4.38881131177301,-2.34830250896049,-3.78867032053636));
#14740=CARTESIAN_POINT('Ctrl Pts',(4.46748251991742,-2.3691016541161,-3.78443028708611));
#14741=CARTESIAN_POINT('Ctrl Pts',(4.54615372806182,-2.38990079927172,-3.78019025363585));
#14742=CARTESIAN_POINT('Ctrl Pts',(4.62574452720736,-2.40674604182972,-3.7759502201856));
#14743=CARTESIAN_POINT('Ctrl Pts',(4.70582388447254,-2.41958750858661,-3.77171018673535));
#14744=CARTESIAN_POINT('Ctrl Pts',(4.78575337376834,-2.43240494262631,-3.76747808847869));
#14745=CARTESIAN_POINT('Ctrl Pts',(4.86646775907577,-2.44128140272402,-3.76324599022204));
#14746=CARTESIAN_POINT('Ctrl Pts',(4.94754441563542,-2.44612992501041,-3.75901389196539));
#14747=CARTESIAN_POINT('Ctrl Pts',(5.0285051998481,-2.4509715179329,-3.75478784209773));
#14748=CARTESIAN_POINT('Ctrl Pts',(5.10982676702841,-2.45179657878863,-3.75056179223008));
#14749=CARTESIAN_POINT('Ctrl Pts',(5.19107814952758,-2.44856947913502,-3.74633574236243));
#14750=CARTESIAN_POINT('Ctrl Pts',(5.27235166817822,-2.44534150028939,-3.74210854114845));
#14751=CARTESIAN_POINT('Ctrl Pts',(5.35355449950888,-2.43805910516314,-3.73788133993448));
#14752=CARTESIAN_POINT('Ctrl Pts',(5.43425204553073,-2.42673878780054,-3.73365413872051));
#14753=CARTESIAN_POINT('Ctrl Pts',(5.51478326397327,-2.415441803006,-3.72943565028878));
#14754=CARTESIAN_POINT('Ctrl Pts',(5.59481081425696,-2.40012356446573,-3.72521716185704));
#14755=CARTESIAN_POINT('Ctrl Pts',(5.67390647757363,-2.38085241668781,-3.7209986734253));
#14756=CARTESIAN_POINT('Ctrl Pts',(5.75297620761036,-2.36158758738614,-3.71678156811922));
#14757=CARTESIAN_POINT('Ctrl Pts',(5.83111420632424,-2.33837253259868,-3.71256446281314));
#14758=CARTESIAN_POINT('Ctrl Pts',(5.90790327031475,-2.31132653020117,-3.70834735750706));
#14759=CARTESIAN_POINT('Ctrl Pts',(5.98469065282652,-2.28428112004005,-3.70413034454451));
#14760=CARTESIAN_POINT('Ctrl Pts',(6.06012872143133,-2.25340508451674,-3.69991333158195));
#14761=CARTESIAN_POINT('Ctrl Pts',(6.13381760719522,-2.21886685276184,-3.6956963186194));
#14762=CARTESIAN_POINT('Ctrl Pts',(6.2078111989167,-2.18418580428673,-3.69146186817004));
#14763=CARTESIAN_POINT('Ctrl Pts',(6.28004067851953,-2.14581239714357,-3.68722741772069));
#14764=CARTESIAN_POINT('Ctrl Pts',(6.35012523492125,-2.10396420728221,-3.68299296727133));
#14765=CARTESIAN_POINT('Ctrl Pts',(6.42002238126497,-2.06222792184162,-3.67876983998139));
#14766=CARTESIAN_POINT('Ctrl Pts',(6.48778569490334,-2.01703570717693,-3.67454671269144));
#14767=CARTESIAN_POINT('Ctrl Pts',(6.55306723010677,-1.96864640159801,-3.67032358540149));
#14768=CARTESIAN_POINT('Ctrl Pts',(6.61861131715112,-1.92006248201038,-3.66608347337243));
#14769=CARTESIAN_POINT('Ctrl Pts',(6.68165326235673,-1.86825600696615,-3.66184336134337));
#14770=CARTESIAN_POINT('Ctrl Pts',(6.7418765192365,-1.81352792769595,-3.65760324931431));
#14771=CARTESIAN_POINT('Ctrl Pts',(6.80209977611626,-1.75879984842576,-3.65336313728525));
#14772=CARTESIAN_POINT('Ctrl Pts',(6.85950405901539,-1.70115053996431,-3.64912302525619));
#14773=CARTESIAN_POINT('Ctrl Pts',(6.91381319174004,-1.64091470763126,-3.64488291322713));
#14774=CARTESIAN_POINT('Ctrl Pts',(6.96744889663614,-1.58142579361072,-3.64069537816429));
#14775=CARTESIAN_POINT('Ctrl Pts',(7.01827548563093,-1.51918136726743,-3.63650784310144));
#14776=CARTESIAN_POINT('Ctrl Pts',(7.06599272976734,-1.45448038745451,-3.6323203080386));
#14777=CARTESIAN_POINT('Ctrl Pts',(7.11364716653421,-1.38986456969197,-3.62813828477903));
#14778=CARTESIAN_POINT('Ctrl Pts',(7.15820009761142,-1.32279899075967,-3.62395626151945));
#14779=CARTESIAN_POINT('Ctrl Pts',(7.19938935174628,-1.25361799904958,-3.61977423825987));
#14780=CARTESIAN_POINT('Ctrl Pts',(7.24053763994745,-1.18450581324478,-3.61559637434941));
#14781=CARTESIAN_POINT('Ctrl Pts',(7.27832864812245,-1.11328279551133,-3.61141851043894));
#14782=CARTESIAN_POINT('Ctrl Pts',(7.31254254993978,-1.04031353363678,-3.60724064652848));
#14783=CARTESIAN_POINT('Ctrl Pts',(7.34673342380052,-0.967393384342382,
-3.60306559456472));
#14784=CARTESIAN_POINT('Ctrl Pts',(7.37735177037304,-0.892729753487568,
-3.59889054260097));
#14785=CARTESIAN_POINT('Ctrl Pts',(7.40422367905159,-0.816711793562492,
-3.59471549063722));
#14786=CARTESIAN_POINT('Ctrl Pts',(7.43109295563704,-0.740701279567287,
-3.5905408476182));
#14787=CARTESIAN_POINT('Ctrl Pts',(7.45421635246627,-0.663337143335558,
-3.58636620459918));
#14788=CARTESIAN_POINT('Ctrl Pts',(7.47346857573817,-0.585027316339761,
-3.58219156158016));
#14789=CARTESIAN_POINT('Ctrl Pts',(7.49271959413475,-0.506722390262485,
-3.57801717982573));
#14790=CARTESIAN_POINT('Ctrl Pts',(7.50809981464966,-0.427472354483196,
-3.57384279807131));
#14791=CARTESIAN_POINT('Ctrl Pts',(7.51953466705069,-0.347697164467993,
-3.56966841631688));
#14792=CARTESIAN_POINT('Ctrl Pts',(7.53097725174323,-0.267868030160116,
-3.56549121182934));
#14793=CARTESIAN_POINT('Ctrl Pts',(7.53846908510302,-0.187513504758057,
-3.56131400734179));
#14794=CARTESIAN_POINT('Ctrl Pts',(7.54198738670963,-0.107059479234764,
-3.55713680285424));
#14795=CARTESIAN_POINT('Ctrl Pts',(7.54357977831448,-0.0706457975370414,
-3.5552461902515));
#14796=CARTESIAN_POINT('Ctrl Pts',(7.54435890520333,-0.0342117587869815,
-3.55335557764875));
#14797=CARTESIAN_POINT('Ctrl Pts',(7.54432616501601,0.00220320930666846,
-3.55146496504601));
#14798=CARTESIAN_POINT('',(7.54432706806737,-0.00065442915052629,-2.75146496500916));
#14799=CARTESIAN_POINT('Ctrl Pts',(7.54432616501525,0.00220321015066411,
-3.55146496500219));
#14800=CARTESIAN_POINT('Ctrl Pts',(7.54422973877529,0.109452355430954,-3.54589674412165));
#14801=CARTESIAN_POINT('Ctrl Pts',(7.53708802522586,0.216389416064109,-3.54032852324111));
#14802=CARTESIAN_POINT('Ctrl Pts',(7.52304979359998,0.322222941943559,-3.53476030236056));
#14803=CARTESIAN_POINT('Ctrl Pts',(7.5090115619741,0.428056467823009,-3.52919208148001));
#14804=CARTESIAN_POINT('Ctrl Pts',(7.48807700934417,0.532786801311883,-3.52362386059947));
#14805=CARTESIAN_POINT('Ctrl Pts',(7.46044938516695,0.635648858902682,-3.51805563971892));
#14806=CARTESIAN_POINT('Ctrl Pts',(7.43945115538403,0.71382862229388,-3.51382354285884));
#14807=CARTESIAN_POINT('Ctrl Pts',(7.41453567224234,0.79111260584736,-3.50959144599877));
#14808=CARTESIAN_POINT('Ctrl Pts',(7.38579644879979,0.867079585941174,-3.50535934913869));
#14809=CARTESIAN_POINT('Ctrl Pts',(7.35709829995641,0.942937992702671,-3.50113330086523));
#14810=CARTESIAN_POINT('Ctrl Pts',(7.32458742785988,1.01748270343279,-3.49690725259176));
#14811=CARTESIAN_POINT('Ctrl Pts',(7.28840760261012,1.09030587953846,-3.4926812043183));
#14812=CARTESIAN_POINT('Ctrl Pts',(7.25221790366536,1.16314892953311,-3.48845400273048));
#14813=CARTESIAN_POINT('Ctrl Pts',(7.21235739531423,1.23426906193182,-3.48422680114266));
#14814=CARTESIAN_POINT('Ctrl Pts',(7.16901889560869,1.30327644480749,-3.47999959955485));
#14815=CARTESIAN_POINT('Ctrl Pts',(7.12576974689923,1.37214155514399,-3.47578111318964));
#14816=CARTESIAN_POINT('Ctrl Pts',(7.07905715964822,1.43890221213298,-3.47156262682443));
#14817=CARTESIAN_POINT('Ctrl Pts',(7.02911865676118,1.50319561433792,-3.46734414045922));
#14818=CARTESIAN_POINT('Ctrl Pts',(6.97919652939898,1.56746793384827,-3.46312703739396));
#14819=CARTESIAN_POINT('Ctrl Pts',(6.92605087196958,1.62927423856367,-3.4589099343287));
#14820=CARTESIAN_POINT('Ctrl Pts',(6.86996117927447,1.68828261242724,-3.45469283126344));
#14821=CARTESIAN_POINT('Ctrl Pts',(6.81387271708422,1.74728969175544,-3.45047582071367));
#14822=CARTESIAN_POINT('Ctrl Pts',(6.75484066902482,1.80349862625898,-3.44625881016391));
#14823=CARTESIAN_POINT('Ctrl Pts',(6.69318229085379,1.8566134225701,-3.44204179961414));
#14824=CARTESIAN_POINT('Ctrl Pts',(6.63126888371411,1.90994791022124,-3.43780734683052));
#14825=CARTESIAN_POINT('Ctrl Pts',(6.56670772344626,1.96016229184336,-3.4335728940469));
#14826=CARTESIAN_POINT('Ctrl Pts',(6.49985311903929,2.00699806669602,-3.42933844126328));
#14827=CARTESIAN_POINT('Ctrl Pts',(6.43317736878537,2.0537085431804,-3.42511531678641));
#14828=CARTESIAN_POINT('Ctrl Pts',(6.36422084765703,2.09705825319777,-3.42089219230954));
#14829=CARTESIAN_POINT('Ctrl Pts',(6.29336207288622,2.13683556500231,-3.41666906783266));
#14830=CARTESIAN_POINT('Ctrl Pts',(6.22221818577473,2.17677292759111,-3.41242895089567));
#14831=CARTESIAN_POINT('Ctrl Pts',(6.14915713063745,2.21310888088526,-3.40818883395868));
#14832=CARTESIAN_POINT('Ctrl Pts',(6.07458301229684,2.2456776703852,-3.40394871702168));
#14833=CARTESIAN_POINT('Ctrl Pts',(6.00000889395624,2.27824645988515,-3.39970860008469));
#14834=CARTESIAN_POINT('Ctrl Pts',(5.92392217148605,2.30704797832714,-3.39546848314769));
#14835=CARTESIAN_POINT('Ctrl Pts',(5.84674123808758,2.33196711687165,-3.3912283662107));
#14836=CARTESIAN_POINT('Ctrl Pts',(5.7697064122947,2.35683908216358,-3.38699627604023));
#14837=CARTESIAN_POINT('Ctrl Pts',(5.69129412276694,2.37793615913287,-3.38276418586977));
#14838=CARTESIAN_POINT('Ctrl Pts',(5.61190875684904,2.39510786903117,-3.37853209569931));
#14839=CARTESIAN_POINT('Ctrl Pts',(5.53263685100436,2.41225503657913,-3.37430605416583));
#14840=CARTESIAN_POINT('Ctrl Pts',(5.45239508134243,2.42548788221613,-3.37008001263236));
#14841=CARTESIAN_POINT('Ctrl Pts',(5.37160391928243,2.43470538658716,-3.36585397109888));
#14842=CARTESIAN_POINT('Ctrl Pts',(5.29079054784242,2.44392542483754,-3.36162676783237));
#14843=CARTESIAN_POINT('Ctrl Pts',(5.20942793359722,2.44912779598835,-3.35739956456585));
#14844=CARTESIAN_POINT('Ctrl Pts',(5.12794809818051,2.45026243722329,-3.35317236129933));
#14845=CARTESIAN_POINT('Ctrl Pts',(5.04663641335074,2.45139473689005,-3.34895388174595));
#14846=CARTESIAN_POINT('Ctrl Pts',(4.96520845501238,2.44847604761854,-3.34473540219257));
#14847=CARTESIAN_POINT('Ctrl Pts',(4.88409785476334,2.44150852352233,-3.34051692263919));
#14848=CARTESIAN_POINT('Ctrl Pts',(4.80301385206782,2.43454328419647,-3.33629982639742));
#14849=CARTESIAN_POINT('Ctrl Pts',(4.72224746341948,2.42353188644212,-3.33208273015566));
#14850=CARTESIAN_POINT('Ctrl Pts',(4.64222921173274,2.40852850247356,-3.32786563391389));
#14851=CARTESIAN_POINT('Ctrl Pts',(4.56221271554549,2.39352544766032,-3.3236486301899));
#14852=CARTESIAN_POINT('Ctrl Pts',(4.48294478020379,2.37453066752952,-3.31943162646591));
#14853=CARTESIAN_POINT('Ctrl Pts',(4.40484630282877,2.35164955610249,-3.31521462274192));
#14854=CARTESIAN_POINT('Ctrl Pts',(4.32642452151457,2.32867372383447,-3.3109801619053));
#14855=CARTESIAN_POINT('Ctrl Pts',(4.24918235758169,2.30177943557109,-3.30674570106868));
#14856=CARTESIAN_POINT('Ctrl Pts',(4.17352938416566,2.27112356822859,-3.30251124023206));
#14857=CARTESIAN_POINT('Ctrl Pts',(4.09807906720647,2.24054982071795,-3.29828812251642));
#14858=CARTESIAN_POINT('Ctrl Pts',(4.02420984421193,2.20623485548807,-3.29406500480078));
#14859=CARTESIAN_POINT('Ctrl Pts',(3.95230510327355,2.16838134431833,-3.28984188708514));
#14860=CARTESIAN_POINT('Ctrl Pts',(3.88011066255758,2.13037532368087,-3.28560175468803));
#14861=CARTESIAN_POINT('Ctrl Pts',(3.80989696814085,2.08880243136719,-3.28136162229092));
#14862=CARTESIAN_POINT('Ctrl Pts',(3.74202281514706,2.04391175825419,-3.27712148989381));
#14863=CARTESIAN_POINT('Ctrl Pts',(3.67414866215327,1.99902108514119,-3.27288135749671));
#14864=CARTESIAN_POINT('Ctrl Pts',(3.60861439016784,1.95081295825972,-3.2686412250996));
#14865=CARTESIAN_POINT('Ctrl Pts',(3.54574405059633,1.89957599228275,-3.26440109270249));
#14866=CARTESIAN_POINT('Ctrl Pts',(3.48299299805349,1.84843624075493,-3.2601690053199));
#14867=CARTESIAN_POINT('Ctrl Pts',(3.42266165547484,1.79408835235942,-3.25593691793732));
#14868=CARTESIAN_POINT('Ctrl Pts',(3.36509614538569,1.73678995414854,-3.25170483055473));
#14869=CARTESIAN_POINT('Ctrl Pts',(3.30761291073701,1.67957344960877,-3.24747879187827));
#14870=CARTESIAN_POINT('Ctrl Pts',(3.25288798396186,1.61941513577923,-3.24325275320181));
#14871=CARTESIAN_POINT('Ctrl Pts',(3.20123471657503,1.55661302522545,-3.23902671452535));
#14872=CARTESIAN_POINT('Ctrl Pts',(3.14956720622137,1.49379359750235,-3.23479951055322));
#14873=CARTESIAN_POINT('Ctrl Pts',(3.10097339396209,1.42832922987503,-3.23057230658109));
#14874=CARTESIAN_POINT('Ctrl Pts',(3.05573013982453,1.36055532959373,-3.22634510260896));
#14875=CARTESIAN_POINT('Ctrl Pts',(3.01058029424646,1.29292135431376,-3.22212662606021));
#14876=CARTESIAN_POINT('Ctrl Pts',(2.96876746439428,1.2229877459403,-3.21790814951145));
#14877=CARTESIAN_POINT('Ctrl Pts',(2.93052555611176,1.15111964638223,-3.2136896729627));
#14878=CARTESIAN_POINT('Ctrl Pts',(2.89229618845911,1.07927511445655,-3.20947257977465));
#14879=CARTESIAN_POINT('Ctrl Pts',(2.85763563497825,1.00549776106932,-3.20525548658659));
#14880=CARTESIAN_POINT('Ctrl Pts',(2.82673244997499,0.930178394929204,-3.20103839339854));
#14881=CARTESIAN_POINT('Ctrl Pts',(2.79582994327943,0.854860682007235,-3.19682139277333));
#14882=CARTESIAN_POINT('Ctrl Pts',(2.76868481641195,0.778001453974088,-3.19260439214812));
#14883=CARTESIAN_POINT('Ctrl Pts',(2.74543739792786,0.700011283302266,-3.18838739152292));
#14884=CARTESIAN_POINT('Ctrl Pts',(2.72209370562171,0.621698134325635,-3.1841529271622));
#14885=CARTESIAN_POINT('Ctrl Pts',(2.70268022053618,0.542245104139516,-3.17991846280147));
#14886=CARTESIAN_POINT('Ctrl Pts',(2.68728790360722,0.462081247536648,-3.17568399844075));
#14887=CARTESIAN_POINT('Ctrl Pts',(2.67193684339092,0.382132257689247,-3.17146088390347));
#14888=CARTESIAN_POINT('Ctrl Pts',(2.66058544702283,0.301476715829103,-3.16723776936618));
#14889=CARTESIAN_POINT('Ctrl Pts',(2.65327200305062,0.220546589367562,-3.1630146548289));
#14890=CARTESIAN_POINT('Ctrl Pts',(2.64592907622978,0.139290207495064,-3.15877451555646));
#14891=CARTESIAN_POINT('Ctrl Pts',(2.6426567374437,0.0577574938856207,-3.15453437628402));
#14892=CARTESIAN_POINT('Ctrl Pts',(2.64344094462522,-0.0236149906744461,
-3.15029423701158));
#14893=CARTESIAN_POINT('Ctrl Pts',(2.64422515180675,-0.104987475234516,
-3.14605409773914));
#14894=CARTESIAN_POINT('Ctrl Pts',(2.64906581505127,-0.186199267937962,
-3.1418139584667));
#14895=CARTESIAN_POINT('Ctrl Pts',(2.65789683120988,-0.26682148607686,-3.13757381919427));
#14896=CARTESIAN_POINT('Ctrl Pts',(2.66671108470243,-0.347290670488414,
-3.13334172837711));
#14897=CARTESIAN_POINT('Ctrl Pts',(2.67953342467174,-0.427472732653372,
-3.12910963755995));
#14898=CARTESIAN_POINT('Ctrl Pts',(2.69633575485173,-0.506937110539796,
-3.12487754674279));
#14899=CARTESIAN_POINT('Ctrl Pts',(2.71311407055149,-0.586287915147322,
-3.12065150457842));
#14900=CARTESIAN_POINT('Ctrl Pts',(2.73386098347016,-0.664922621869127,
-3.11642546241405));
#14901=CARTESIAN_POINT('Ctrl Pts',(2.75849668580173,-0.742416222558389,
-3.11219942024968));
#14902=CARTESIAN_POINT('Ctrl Pts',(2.78313915584441,-0.819931111632119,
-3.10797221714286));
#14903=CARTESIAN_POINT('Ctrl Pts',(2.8116724750154,-0.896303807236035,-3.10374501403604));
#14904=CARTESIAN_POINT('Ctrl Pts',(2.8439656124048,-0.971119604946917,-3.09951781092922));
#14905=CARTESIAN_POINT('Ctrl Pts',(2.87619211189295,-1.04578101791411,-3.09529933078852));
#14906=CARTESIAN_POINT('Ctrl Pts',(2.91216276687888,-1.11889151541012,-3.09108085064782));
#14907=CARTESIAN_POINT('Ctrl Pts',(2.95169823903647,-1.19005628247225,-3.08686237050711));
#14908=CARTESIAN_POINT('Ctrl Pts',(2.99122074667082,-1.26119771309179,-3.08264527369588));
#14909=CARTESIAN_POINT('Ctrl Pts',(3.03430552449402,-1.33039427448151,-3.07842817688464));
#14910=CARTESIAN_POINT('Ctrl Pts',(3.08072703837876,-1.39727526587828,-3.07421108007341));
#14911=CARTESIAN_POINT('Ctrl Pts',(3.12714753362806,-1.46415478969372,-3.06999407579867));
#14912=CARTESIAN_POINT('Ctrl Pts',(3.17690435345151,-1.52871846345289,-3.06577707152393));
#14913=CARTESIAN_POINT('Ctrl Pts',(3.22972916030775,-1.59062532184517,-3.06156006724919));
#14914=CARTESIAN_POINT('Ctrl Pts',(3.28277263001954,-1.65278843731135,-3.05732560711893));
#14915=CARTESIAN_POINT('Ctrl Pts',(3.3389092436395,-1.7122723280798,-3.05309114698867));
#14916=CARTESIAN_POINT('Ctrl Pts',(3.39782831686894,-1.76876742098026,-3.04885668685841));
#14917=CARTESIAN_POINT('Ctrl Pts',(3.45658957655231,-1.82511119291694,-3.04463356864397));
#14918=CARTESIAN_POINT('Ctrl Pts',(3.5181180291659,-1.87848188213243,-3.04041045042953));
#14919=CARTESIAN_POINT('Ctrl Pts',(3.58207191229654,-1.92861254138529,-3.03618733221509));
#14920=CARTESIAN_POINT('Ctrl Pts',(3.64628343428149,-1.97894515249756,-3.03194720112691));
#14921=CARTESIAN_POINT('Ctrl Pts',(3.71293957967675,-2.02601130868253,-3.02770707003874));
#14922=CARTESIAN_POINT('Ctrl Pts',(3.78166628784708,-2.06958549171649,-3.02346693895057));
#14923=CARTESIAN_POINT('Ctrl Pts',(3.85039299601742,-2.11315967475046,-3.0192268078624));
#14924=CARTESIAN_POINT('Ctrl Pts',(3.92118982963898,-2.15324170852491,-3.01498667677422));
#14925=CARTESIAN_POINT('Ctrl Pts',(3.9936608735395,-2.18965394575042,-3.01074654568605));
#14926=CARTESIAN_POINT('Ctrl Pts',(4.06599447517755,-2.22599712670191,-3.00651445606076));
#14927=CARTESIAN_POINT('Ctrl Pts',(4.14026579677167,-2.25882002095934,-3.00228236643548));
#14928=CARTESIAN_POINT('Ctrl Pts',(4.21609817080659,-2.28791216603946,-2.99805027681019));
#14929=CARTESIAN_POINT('Ctrl Pts',(4.29182216231548,-2.31696273151442,-2.99382423584908));
#14930=CARTESIAN_POINT('Ctrl Pts',(4.36910234479523,-2.34229297294667,-2.98959819488797));
#14931=CARTESIAN_POINT('Ctrl Pts',(4.44753860300326,-2.36373885126346,-2.98537215392685));
#14932=CARTESIAN_POINT('Ctrl Pts',(4.52599643645029,-2.38519062863714,-2.98114495052065));
#14933=CARTESIAN_POINT('Ctrl Pts',(4.60561055332215,-2.40275572018323,-2.97691774711444));
#14934=CARTESIAN_POINT('Ctrl Pts',(4.6859616425133,-2.416318682077,-2.97269054370823));
#14935=CARTESIAN_POINT('Ctrl Pts',(4.76614689580707,-2.42985365149451,-2.96847206478948));
#14936=CARTESIAN_POINT('Ctrl Pts',(4.84706562832133,-2.43940289268036,-2.96425358587074));
#14937=CARTESIAN_POINT('Ctrl Pts',(4.92828896475836,-2.44490232062991,-2.96003510695199));
#14938=CARTESIAN_POINT('Ctrl Pts',(5.00948566624327,-2.45039994519379,-2.95581801136701));
#14939=CARTESIAN_POINT('Ctrl Pts',(5.09098631001662,-2.45185036249032,-2.95160091578203));
#14940=CARTESIAN_POINT('Ctrl Pts',(5.17235715004185,-2.44924137029201,-2.94738382019705));
#14941=CARTESIAN_POINT('Ctrl Pts',(5.25372620448142,-2.44663243534491,-2.94316681715119));
#14942=CARTESIAN_POINT('Ctrl Pts',(5.33496499642303,-2.43996428405567,-2.93894981410532));
#14943=CARTESIAN_POINT('Ctrl Pts',(5.41564147136897,-2.42927680515655,-2.93473281105946));
#14944=CARTESIAN_POINT('Ctrl Pts',(5.49665194950378,-2.41854507975266,-2.93049834948599));
#14945=CARTESIAN_POINT('Ctrl Pts',(5.57709497529563,-2.40376072474925,-2.92626388791252));
#14946=CARTESIAN_POINT('Ctrl Pts',(5.65654182376503,-2.38501623727525,-2.92202942633905));
#14947=CARTESIAN_POINT('Ctrl Pts',(5.73577582551224,-2.36632196831583,-2.91780630934732));
#14948=CARTESIAN_POINT('Ctrl Pts',(5.81401854313474,-2.34368892851612,-2.91358319235559));
#14949=CARTESIAN_POINT('Ctrl Pts',(5.89086013737419,-2.31725887110827,-2.90936007536386));
#14950=CARTESIAN_POINT('Ctrl Pts',(5.96801136159131,-2.29072231489381,-2.90511994149952));
#14951=CARTESIAN_POINT('Ctrl Pts',(6.04374971267005,-2.26035826006372,-2.90087980763518));
#14952=CARTESIAN_POINT('Ctrl Pts',(6.11768256730445,-2.22635809016041,-2.89663967377085));
#14953=CARTESIAN_POINT('Ctrl Pts',(6.19161542193886,-2.1923579202571,-2.89239953990651));
#14954=CARTESIAN_POINT('Ctrl Pts',(6.26374239458831,-2.15472190662379,-2.88815940604217));
#14955=CARTESIAN_POINT('Ctrl Pts',(6.33369916316487,-2.11368579843193,-2.88391927217784));
#14956=CARTESIAN_POINT('Ctrl Pts',(6.40352320772482,-2.0727275451384,-2.87968718281883));
#14957=CARTESIAN_POINT('Ctrl Pts',(6.47144578304493,-2.0282292937021,-2.87545509345982));
#14958=CARTESIAN_POINT('Ctrl Pts',(6.53708548680471,-1.9803927991649,-2.87122300410081));
#14959=CARTESIAN_POINT('Ctrl Pts',(6.60263137565911,-1.93262467447022,-2.86699696341417));
#14960=CARTESIAN_POINT('Ctrl Pts',(6.66590050076822,-1.88152805409757,-2.86277092272754));
#14961=CARTESIAN_POINT('Ctrl Pts',(6.7265376798801,-1.82734960897616,-2.8585448820409));
#14962=CARTESIAN_POINT('Ctrl Pts',(6.78719154319808,-1.7731562567572,-2.8543176785671));
#14963=CARTESIAN_POINT('Ctrl Pts',(6.84521162340756,-1.71587964237687,-2.8500904750933));
#14964=CARTESIAN_POINT('Ctrl Pts',(6.90027309242564,-1.65580896446282,-2.84586327161949));
#14965=CARTESIAN_POINT('Ctrl Pts',(6.95522091587987,-1.59586227100076,-2.84164479299322));
#14966=CARTESIAN_POINT('Ctrl Pts',(7.00722199651026,-1.53313336193388,-2.83742631436695));
#14967=CARTESIAN_POINT('Ctrl Pts',(7.05598941578056,-1.46794738125952,-2.83320783574069));
#14968=CARTESIAN_POINT('Ctrl Pts',(7.10474084304905,-1.40278277662549,-2.82899074045434));
#14969=CARTESIAN_POINT('Ctrl Pts',(7.15026043665294,-1.33516307229296,-2.82477364516799));
#14970=CARTESIAN_POINT('Ctrl Pts',(7.19230217857887,-1.2654457030301,-2.82055654988164));
#14971=CARTESIAN_POINT('Ctrl Pts',(7.23434299789154,-1.19572986372689,-2.81633954714017));
#14972=CARTESIAN_POINT('Ctrl Pts',(7.2729058782921,-1.12391684954804,-2.8121225443987));
#14973=CARTESIAN_POINT('Ctrl Pts',(7.30778944415839,-1.05039099110325,-2.80790554165724));
#14974=CARTESIAN_POINT('Ctrl Pts',(7.34281743446293,-0.97656072195563,-2.8036710797416));
#14975=CARTESIAN_POINT('Ctrl Pts',(7.37413536537025,-0.9010038160837,-2.79943661782597));
#14976=CARTESIAN_POINT('Ctrl Pts',(7.40158782827053,-0.824130406548198,
-2.79520215591033));
#14977=CARTESIAN_POINT('Ctrl Pts',(7.42896673878781,-0.747462961136234,
-2.79097903923413));
#14978=CARTESIAN_POINT('Ctrl Pts',(7.45250077237866,-0.669486517101287,
-2.78675592255792));
#14979=CARTESIAN_POINT('Ctrl Pts',(7.47208612987216,-0.590622130126553,
-2.78253280588172));
#14980=CARTESIAN_POINT('Ctrl Pts',(7.49175041032252,-0.511439943968847,
-2.77829267134637));
#14981=CARTESIAN_POINT('Ctrl Pts',(7.50743404143823,-0.431363107805052,
-2.77405253681102));
#14982=CARTESIAN_POINT('Ctrl Pts',(7.51908423982023,-0.350825205375978,
-2.76981240227567));
#14983=CARTESIAN_POINT('Ctrl Pts',(7.53073443820223,-0.270287302946905,
-2.76557226774032));
#14984=CARTESIAN_POINT('Ctrl Pts',(7.53835122203186,-0.189288805356301,
-2.76133213320497));
#14985=CARTESIAN_POINT('Ctrl Pts',(7.5419344305525,-0.10826365782412,-2.75709199866962));
#14986=CARTESIAN_POINT('Ctrl Pts',(7.54351950878196,-0.072421144988782,
-2.75521632079508));
#14987=CARTESIAN_POINT('Ctrl Pts',(7.54431748352352,-0.0365435678230778,
-2.75334064292055));
#14988=CARTESIAN_POINT('Ctrl Pts',(7.54432706806718,-0.000654429855887372,
-2.75146496504602));
#14989=CARTESIAN_POINT('',(7.54432654498802,-0.00172970779088622,-1.95146499540829));
#14990=CARTESIAN_POINT('Ctrl Pts',(7.54432706806737,-0.000654429150524658,
-2.75146496500915));
#14991=CARTESIAN_POINT('Ctrl Pts',(7.54434854189861,0.0797540024314393,
-2.74726257050805));
#14992=CARTESIAN_POINT('Ctrl Pts',(7.54040807903265,0.160320975657735,-2.74306017600695));
#14993=CARTESIAN_POINT('Ctrl Pts',(7.53248499309161,0.24062044992958,-2.73885778150585));
#14994=CARTESIAN_POINT('Ctrl Pts',(7.5245730202728,0.320807294112681,-2.73466128139036));
#14995=CARTESIAN_POINT('Ctrl Pts',(7.51268956108371,0.400726918697619,-2.73046478127487));
#14996=CARTESIAN_POINT('Ctrl Pts',(7.49686594348856,0.479952948940973,-2.72626828115938));
#14997=CARTESIAN_POINT('Ctrl Pts',(7.48105969025352,0.559092038931199,-2.72207638615639));
#14998=CARTESIAN_POINT('Ctrl Pts',(7.46132196055022,0.637538586300265,-2.7178844911534));
#14999=CARTESIAN_POINT('Ctrl Pts',(7.43773574774814,0.714872548756429,-2.71369259615041));
#15000=CARTESIAN_POINT('Ctrl Pts',(7.41416339531342,0.792161066141067,-2.70950316450196));
#15001=CARTESIAN_POINT('Ctrl Pts',(7.38674718490084,0.868337845776393,-2.70531373285352));
#15002=CARTESIAN_POINT('Ctrl Pts',(7.35562063744385,0.942995490351987,-2.70112430120508));
#15003=CARTESIAN_POINT('Ctrl Pts',(7.32450251971678,1.01763291605235,-2.69693600414368));
#15004=CARTESIAN_POINT('Ctrl Pts',(7.28967624164218,1.09075158831796,-2.69274770708227));
#15005=CARTESIAN_POINT('Ctrl Pts',(7.25132384901173,1.16196310926106,-2.68855941002087));
#15006=CARTESIAN_POINT('Ctrl Pts',(7.21296969206233,1.23317790613631,-2.68437092028591));
#15007=CARTESIAN_POINT('Ctrl Pts',(7.1710893240234,1.30248496302861,-2.68018243055095));
#15008=CARTESIAN_POINT('Ctrl Pts',(7.12591049593355,1.36952091891357,-2.67599394081599));
#15009=CARTESIAN_POINT('Ctrl Pts',(7.08068583935419,1.43662487471642,-2.67180120236175));
#15010=CARTESIAN_POINT('Ctrl Pts',(7.03215630756797,1.50145273850618,-2.66760846390752));
#15011=CARTESIAN_POINT('Ctrl Pts',(6.98059231043497,1.56367116106497,-2.66341572545328));
#15012=CARTESIAN_POINT('Ctrl Pts',(6.92900025385767,1.62592344085863,-2.65922070544762));
#15013=CARTESIAN_POINT('Ctrl Pts',(6.87437076450931,1.68556310558168,-2.65502568544195));
#15014=CARTESIAN_POINT('Ctrl Pts',(6.81701204744791,1.74229276472149,-2.65083066543629));
#15015=CARTESIAN_POINT('Ctrl Pts',(6.75955608568052,1.79911860207635,-2.64662853328608));
#15016=CARTESIAN_POINT('Ctrl Pts',(6.69936201011216,1.85302426976348,-2.64242640113586));
#15017=CARTESIAN_POINT('Ctrl Pts',(6.63677172151105,1.90375216771309,-2.63822426898564));
#15018=CARTESIAN_POINT('Ctrl Pts',(6.59725288303542,1.93578121966481,-2.6355710877109));
#15019=CARTESIAN_POINT('Ctrl Pts',(6.5567794139668,1.96654429048435,-2.63291790643615));
#15020=CARTESIAN_POINT('Ctrl Pts',(6.51544287596956,1.99598571968351,-2.6302647251614));
#15021=CARTESIAN_POINT('Ctrl Pts',(6.44950696129238,2.04294774547725,-2.62603263552277));
#15022=CARTESIAN_POINT('Ctrl Pts',(6.38111851702674,2.08672664771273,-2.62180054588414));
#15023=CARTESIAN_POINT('Ctrl Pts',(6.31061765686899,2.12705691641387,-2.61756845624552));
#15024=CARTESIAN_POINT('Ctrl Pts',(6.2402175592768,2.16732954352972,-2.61334241527365));
#15025=CARTESIAN_POINT('Ctrl Pts',(6.16771144212945,2.20416309767123,-2.60911637430179));
#15026=CARTESIAN_POINT('Ctrl Pts',(6.09346968054336,2.23733436750772,-2.60489033332993));
#15027=CARTESIAN_POINT('Ctrl Pts',(6.01920749772839,2.27051476156325,-2.60066312992673));
#15028=CARTESIAN_POINT('Ctrl Pts',(5.94320911055678,2.30003060757775,-2.59643592652353));
#15029=CARTESIAN_POINT('Ctrl Pts',(5.86587128518856,2.32570378847802,-2.59220872312033));
#15030=CARTESIAN_POINT('Ctrl Pts',(5.78869307653494,2.3513239827735,-2.58799024419725));
#15031=CARTESIAN_POINT('Ctrl Pts',(5.7101813862433,2.37311718764522,-2.58377176527416));
#15032=CARTESIAN_POINT('Ctrl Pts',(5.63075027478648,2.39095458215444,-2.57955328635107));
#15033=CARTESIAN_POINT('Ctrl Pts',(5.55134521061696,2.40878612737198,-2.57533619076419));
#15034=CARTESIAN_POINT('Ctrl Pts',(5.4710217770792,2.42266433661221,-2.57111909517731));
#15035=CARTESIAN_POINT('Ctrl Pts',(5.39020677054793,2.4325109195554,-2.56690199959043));
#15036=CARTESIAN_POINT('Ctrl Pts',(5.30939353745222,2.44235728642139,-2.56268499654511));
#15037=CARTESIAN_POINT('Ctrl Pts',(5.22808921422736,2.44817214783349,-2.5584679934998));
#15038=CARTESIAN_POINT('Ctrl Pts',(5.1467268796151,2.44992895186444,-2.55425099045448));
#15039=CARTESIAN_POINT('Ctrl Pts',(5.0650277024515,2.45169302911775,-2.55001652888771));
#15040=CARTESIAN_POINT('Ctrl Pts',(4.98327050395485,2.44936535339045,-2.54578206732093));
#15041=CARTESIAN_POINT('Ctrl Pts',(4.90189310547216,2.4429718726293,-2.54154760575416));
#15042=CARTESIAN_POINT('Ctrl Pts',(4.8207337258634,2.43659552069632,-2.53732448876905));
#15043=CARTESIAN_POINT('Ctrl Pts',(4.73995257228229,2.42617522202766,-2.53310137178393));
#15044=CARTESIAN_POINT('Ctrl Pts',(4.65997632302281,2.41178848682871,-2.52887825479882));
#15045=CARTESIAN_POINT('Ctrl Pts',(4.57967781282647,2.39734378088462,-2.52463812094121));
#15046=CARTESIAN_POINT('Ctrl Pts',(4.50019116460046,2.37890072070823,-2.52039798708361));
#15047=CARTESIAN_POINT('Ctrl Pts',(4.4219336209134,2.35658849361609,-2.516157853226));
#15048=CARTESIAN_POINT('Ctrl Pts',(4.34367607722634,2.33427626652394,-2.5119177193684));
#15049=CARTESIAN_POINT('Ctrl Pts',(4.2666480605307,2.30809508180683,-2.50767758551079));
#15050=CARTESIAN_POINT('Ctrl Pts',(4.19124561850368,2.27822229362238,-2.50343745165319));
#15051=CARTESIAN_POINT('Ctrl Pts',(4.11598622740783,2.2484061790688,-2.49920536203235));
#15052=CARTESIAN_POINT('Ctrl Pts',(4.04206546527402,2.21480123235921,-2.49497327241151));
#15053=CARTESIAN_POINT('Ctrl Pts',(3.96989106897527,2.17754860416774,-2.49074118279068));
#15054=CARTESIAN_POINT('Ctrl Pts',(3.89781982714067,2.14034921888645,-2.48651514183751));
#15055=CARTESIAN_POINT('Ctrl Pts',(3.82749040334373,2.09951271787029,-2.48228910088433));
#15056=CARTESIAN_POINT('Ctrl Pts',(3.75929148032207,2.05522864465308,-2.47806305993116));
#15057=CARTESIAN_POINT('Ctrl Pts',(3.69107379786298,2.01093239024204,-2.4738358565234));
#15058=CARTESIAN_POINT('Ctrl Pts',(3.62498821192454,1.96318686309778,-2.46960865311564));
#15059=CARTESIAN_POINT('Ctrl Pts',(3.56139990073682,1.91222827063159,-2.46538144970789));
#15060=CARTESIAN_POINT('Ctrl Pts',(3.49794282916828,1.86137485136696,-2.46116297080555));
#15061=CARTESIAN_POINT('Ctrl Pts',(3.43697311269183,1.80732188750033,-2.45694449190321));
#15062=CARTESIAN_POINT('Ctrl Pts',(3.37882395333543,1.75034689896777,-2.45272601300086));
#15063=CARTESIAN_POINT('Ctrl Pts',(3.32069386243527,1.69339059385365,-2.44850891743547));
#15064=CARTESIAN_POINT('Ctrl Pts',(3.26538282349842,1.63351449193571,-2.44429182187007));
#15065=CARTESIAN_POINT('Ctrl Pts',(3.21318854831966,1.5710342705871,-2.44007472630467));
#15066=CARTESIAN_POINT('Ctrl Pts',(3.16099541852096,1.50855542033906,-2.43585772328155));
#15067=CARTESIAN_POINT('Ctrl Pts',(3.11191921352454,1.44347292164478,-2.43164072025844));
#15068=CARTESIAN_POINT('Ctrl Pts',(3.06621763312194,1.37613584901781,-2.42742371723532));
#15069=CARTESIAN_POINT('Ctrl Pts',(3.02032684627744,1.30851999811211,-2.42318925564445));
#15070=CARTESIAN_POINT('Ctrl Pts',(2.97783896132905,1.23863124859839,-2.41895479405359));
#15071=CARTESIAN_POINT('Ctrl Pts',(2.93897018993233,1.16685119366035,-2.41472033246273));
#15072=CARTESIAN_POINT('Ctrl Pts',(2.9002055526267,1.09526344608142,-2.41049721550133));
#15073=CARTESIAN_POINT('Ctrl Pts',(2.86504082628886,1.02179495373373,-2.40627409853992));
#15074=CARTESIAN_POINT('Ctrl Pts',(2.83364288628048,0.946845985039064,-2.40205098157852));
#15075=CARTESIAN_POINT('Ctrl Pts',(2.80211842905802,0.871595011349318,-2.39781084767292));
#15076=CARTESIAN_POINT('Ctrl Pts',(2.77439133068076,0.794852051365718,-2.39357071376733));
#15077=CARTESIAN_POINT('Ctrl Pts',(2.75057996189763,0.717037544271118,-2.38933057986174));
#15078=CARTESIAN_POINT('Ctrl Pts',(2.7267685931145,0.639223037176518,-2.38509044595615));
#15079=CARTESIAN_POINT('Ctrl Pts',(2.70687300789286,0.560337451325784,-2.38085031205056));
#15080=CARTESIAN_POINT('Ctrl Pts',(2.69095962667335,0.480809618389507,-2.37661017814497));
#15081=CARTESIAN_POINT('Ctrl Pts',(2.67507643570977,0.401432662604738,-2.37237808845864));
#15082=CARTESIAN_POINT('Ctrl Pts',(2.6631010802132,0.321119758273199,-2.36814599877231));
#15083=CARTESIAN_POINT('Ctrl Pts',(2.65513672227431,0.240289868954506,-2.36391390908598));
#15084=CARTESIAN_POINT('Ctrl Pts',(2.64718374730434,0.159575504845203,-2.3596878680662));
#15085=CARTESIAN_POINT('Ctrl Pts',(2.64323042936626,0.0783460818593184,
-2.35546182704641));
#15086=CARTESIAN_POINT('Ctrl Pts',(2.64332895420887,-0.00296912424105906,
-2.35123578602663));
#15087=CARTESIAN_POINT('Ctrl Pts',(2.64342750615072,-0.0843066960672667,
-2.34700858263538));
#15088=CARTESIAN_POINT('Ctrl Pts',(2.64758019548345,-0.165729635981154,
-2.34278137924414));
#15089=CARTESIAN_POINT('Ctrl Pts',(2.65578726371151,-0.24680303133594,-2.33855417585289));
#15090=CARTESIAN_POINT('Ctrl Pts',(2.66397739357534,-0.327709101324162,
-2.33433569688171));
#15091=CARTESIAN_POINT('Ctrl Pts',(2.67620516165348,-0.408266603271003,
-2.33011721791053));
#15092=CARTESIAN_POINT('Ctrl Pts',(2.69241875185148,-0.488045007260048,
-2.32589873893934));
#15093=CARTESIAN_POINT('Ctrl Pts',(2.70862702524044,-0.567797250076017,
-2.32168164330441));
#15094=CARTESIAN_POINT('Ctrl Pts',(2.72881843260493,-0.646770447274864,
-2.31746454766949));
#15095=CARTESIAN_POINT('Ctrl Pts',(2.75288983833641,-0.7245431162674,-2.31324745203456));
#15096=CARTESIAN_POINT('Ctrl Pts',(2.77696071583506,-0.802314078584467,
-2.30903044894131));
#15097=CARTESIAN_POINT('Ctrl Pts',(2.80491128391827,-0.878884121503322,
-2.30481344584807));
#15098=CARTESIAN_POINT('Ctrl Pts',(2.83658862510449,-0.953847192746091,
-2.30059644275482));
#15099=CARTESIAN_POINT('Ctrl Pts',(2.86839711066191,-1.02912061152666,-2.29636198124498));
#15100=CARTESIAN_POINT('Ctrl Pts',(2.90396312099272,-1.10277328493736,-2.29212751973514));
#15101=CARTESIAN_POINT('Ctrl Pts',(2.94308389171767,-1.17441630757438,-2.2878930582253));
#15102=CARTESIAN_POINT('Ctrl Pts',(2.98209985461661,-1.24586739254472,-2.28366994119301));
#15103=CARTESIAN_POINT('Ctrl Pts',(3.02465127585166,-1.31531920385023,-2.27944682416072));
#15104=CARTESIAN_POINT('Ctrl Pts',(3.0704928975755,-1.38241409530533,-2.27522370712843));
#15105=CARTESIAN_POINT('Ctrl Pts',(3.11651923449117,-1.44977934032297,-2.27098357337982));
#15106=CARTESIAN_POINT('Ctrl Pts',(3.16586205112207,-1.51476826107824,-2.26674343963121));
#15107=CARTESIAN_POINT('Ctrl Pts',(3.21823279302944,-1.57705295968289,-2.26250330588259));
#15108=CARTESIAN_POINT('Ctrl Pts',(3.27060353493681,-1.63933765828753,-2.25826317213398));
#15109=CARTESIAN_POINT('Ctrl Pts',(3.32600183833949,-1.69891783485511,-2.25402303838536));
#15110=CARTESIAN_POINT('Ctrl Pts',(3.38410386532837,-1.75550463434451,-2.24978290463675));
#15111=CARTESIAN_POINT('Ctrl Pts',(3.44209566508421,-1.81198408118791,-2.2455508149829));
#15112=CARTESIAN_POINT('Ctrl Pts',(3.50299728362785,-1.86569222295865,-2.24131872532904));
#15113=CARTESIAN_POINT('Ctrl Pts',(3.5665131379305,-1.91631472933831,-2.23708663567519));
#15114=CARTESIAN_POINT('Ctrl Pts',(3.62993821290689,-1.9668648840654,-2.23286059468827));
#15115=CARTESIAN_POINT('Ctrl Pts',(3.69596974245664,-2.01433787515399,-2.22863455370135));
#15116=CARTESIAN_POINT('Ctrl Pts',(3.76427577817638,-2.05845655411562,-2.22440851271442));
#15117=CARTESIAN_POINT('Ctrl Pts',(3.83260060211639,-2.1025873683366,-2.22018130931501));
#15118=CARTESIAN_POINT('Ctrl Pts',(3.9032008312208,-2.14336171876791,-2.2159541059156));
#15119=CARTESIAN_POINT('Ctrl Pts',(3.97571154982797,-2.18054299257261,-2.21172690251619));
#15120=CARTESIAN_POINT('Ctrl Pts',(4.04807261464879,-2.21764752850307,-2.20750842357857));
#15121=CARTESIAN_POINT('Ctrl Pts',(4.12233588867037,-2.25117357010027,-2.20328994464096));
#15122=CARTESIAN_POINT('Ctrl Pts',(4.19811183741015,-2.28093058180717,-2.19907146570334));
#15123=CARTESIAN_POINT('Ctrl Pts',(4.27386293747027,-2.31067783550425,-2.19485437010218));
#15124=CARTESIAN_POINT('Ctrl Pts',(4.35112529495758,-2.33665834407526,-2.19063727450101));
#15125=CARTESIAN_POINT('Ctrl Pts',(4.42948907302834,-2.35872956530421,-2.18642017889984));
#15126=CARTESIAN_POINT('Ctrl Pts',(4.50785113144961,-2.38080030219249,-2.18220317584049));
#15127=CARTESIAN_POINT('Ctrl Pts',(4.58731411480005,-2.3989617974339,-2.17798617278114));
#15128=CARTESIAN_POINT('Ctrl Pts',(4.66745407730865,-2.4131216811909,-2.17376916972179));
#15129=CARTESIAN_POINT('Ctrl Pts',(4.74792582111344,-2.42734018719379,-2.16953470817235));
#15130=CARTESIAN_POINT('Ctrl Pts',(4.82907969906962,-2.43752378283115,-2.16530024662292));
#15131=CARTESIAN_POINT('Ctrl Pts',(4.91047906191892,-2.44363125831157,-2.16106578507348));
#15132=CARTESIAN_POINT('Ctrl Pts',(4.9916603476364,-2.44972237124701,-2.15684266807512));
#15133=CARTESIAN_POINT('Ctrl Pts',(5.07308533611021,-2.45175920627896,-2.15261955107676));
#15134=CARTESIAN_POINT('Ctrl Pts',(5.15432051711643,-2.44975321271239,-2.1483964340784));
#15135=CARTESIAN_POINT('Ctrl Pts',(5.2358830309886,-2.44773913610082,-2.14415630025342));
#15136=CARTESIAN_POINT('Ctrl Pts',(5.31725373503625,-2.44164962516456,-2.13991616642844));
#15137=CARTESIAN_POINT('Ctrl Pts',(5.39800055324951,-2.43154864110776,-2.13567603260347));
#15138=CARTESIAN_POINT('Ctrl Pts',(5.47874737146277,-2.42144765705095,-2.13143589877849));
#15139=CARTESIAN_POINT('Ctrl Pts',(5.55886985438538,-2.40733534220338,-2.12719576495352));
#15140=CARTESIAN_POINT('Ctrl Pts',(5.6379495174793,-2.38932649613715,-2.12295563112854));
#15141=CARTESIAN_POINT('Ctrl Pts',(5.71687915457629,-2.37135181555644,-2.1187235414742));
#15142=CARTESIAN_POINT('Ctrl Pts',(5.79506439894685,-2.34942833051731,-2.11449145181987));
#15143=CARTESIAN_POINT('Ctrl Pts',(5.8720807420363,-2.32363327678238,-2.11025936216553));
#15144=CARTESIAN_POINT('Ctrl Pts',(5.94898701037529,-2.29787509034065,-2.1060333211782));
#15145=CARTESIAN_POINT('Ctrl Pts',(6.02472725855494,-2.26825647147638,-2.10180728019086));
#15146=CARTESIAN_POINT('Ctrl Pts',(6.09888841933066,-2.23490539080581,-2.09758123920352));
#15147=CARTESIAN_POINT('Ctrl Pts',(6.17306997882485,-2.20154513660966,-2.09335403580422));
#15148=CARTESIAN_POINT('Ctrl Pts',(6.24567113357853,-2.16445049642864,-2.08912683240492));
#15149=CARTESIAN_POINT('Ctrl Pts',(6.31629491986107,-2.12379914657281,-2.08489962900562));
#15150=CARTESIAN_POINT('Ctrl Pts',(6.38677294677355,-2.0832316964264,-2.08068115006782));
#15151=CARTESIAN_POINT('Ctrl Pts',(6.45528134395092,-2.03912241338662,-2.07646267113002));
#15152=CARTESIAN_POINT('Ctrl Pts',(6.52144844062969,-1.99169468446114,-2.07224419219222));
#15153=CARTESIAN_POINT('Ctrl Pts',(6.58759383959166,-1.94428250818165,-2.06802709659095));
#15154=CARTESIAN_POINT('Ctrl Pts',(6.65139908537569,-1.89355431758331,-2.06381000098967));
#15155=CARTESIAN_POINT('Ctrl Pts',(6.712521754789,-1.83977662885493,-2.05959290538839));
#15156=CARTESIAN_POINT('Ctrl Pts',(6.77364308289814,-1.78600012024906,-2.05537590232902));
#15157=CARTESIAN_POINT('Ctrl Pts',(6.8320816035631,-1.72917455438314,-2.05115889926964));
#15158=CARTESIAN_POINT('Ctrl Pts',(6.88752933678303,-1.66960556260821,-2.04694189621026));
#15159=CARTESIAN_POINT('Ctrl Pts',(6.94320662489548,-1.60978995383543,-2.0427074346611));
#15160=CARTESIAN_POINT('Ctrl Pts',(6.9958679780722,-1.54720849164571,-2.03847297311194));
#15161=CARTESIAN_POINT('Ctrl Pts',(7.04524145247997,-1.48220527976363,-2.03423851156278));
#15162=CARTESIAN_POINT('Ctrl Pts',(7.09448265035379,-1.41737621806373,-2.03001539456458));
#15163=CARTESIAN_POINT('Ctrl Pts',(7.1404533341697,-1.35013877554761,-2.02579227756639));
#15164=CARTESIAN_POINT('Ctrl Pts',(7.18292746618936,-1.28086304563826,-2.02156916056819));
#15165=CARTESIAN_POINT('Ctrl Pts',(7.2255727454762,-1.2113081728414,-2.01732902674354));
#15166=CARTESIAN_POINT('Ctrl Pts',(7.2646930166829,-1.13969896950011,-2.0130888929189));
#15167=CARTESIAN_POINT('Ctrl Pts',(7.30010709790759,-1.0664328696749,-2.00884875909425));
#15168=CARTESIAN_POINT('Ctrl Pts',(7.33552117913229,-0.993166769849684,
-2.00460862526961));
#15169=CARTESIAN_POINT('Ctrl Pts',(7.3672289455247,-0.918244228162472,-2.00036849144496));
#15170=CARTESIAN_POINT('Ctrl Pts',(7.39509927478015,-0.842078905333729,
-1.99612835762031));
#15171=CARTESIAN_POINT('Ctrl Pts',(7.42717646114053,-0.754416889137817,
-1.99124820132078));
#15172=CARTESIAN_POINT('Ctrl Pts',(7.45427036000956,-0.664839421422339,
-1.98636804502124));
#15173=CARTESIAN_POINT('Ctrl Pts',(7.47618097156536,-0.573881995583924,
-1.9814878887217));
#15174=CARTESIAN_POINT('Ctrl Pts',(7.49864678047242,-0.480619781411635,
-1.97648407316947));
#15175=CARTESIAN_POINT('Ctrl Pts',(7.51566290806625,-0.385906846851153,
-1.97148025761723));
#15176=CARTESIAN_POINT('Ctrl Pts',(7.52706584652748,-0.290344144522799,
-1.96647644206499));
#15177=CARTESIAN_POINT('Ctrl Pts',(7.53846878498872,-0.194781442194444,
-1.96147262651276));
#15178=CARTESIAN_POINT('Ctrl Pts',(7.54425833113807,-0.0983691509038746,
-1.95646881096052));
#15179=CARTESIAN_POINT('Ctrl Pts',(7.54432654498802,-0.00172970779088622,
-1.95146499540829));
#15180=CARTESIAN_POINT('',(7.54193252997112,0.00182552697798459,-1.15146496504602));
#15181=CARTESIAN_POINT('Ctrl Pts',(7.54171139332785,-0.00172727609620038,
-1.95146496504602));
#15182=CARTESIAN_POINT('Ctrl Pts',(7.53826048626319,0.526658739318973,-1.92407700473471));
#15183=CARTESIAN_POINT('Ctrl Pts',(7.11114846716908,1.87574080279579,-1.85441328658734));
#15184=CARTESIAN_POINT('Ctrl Pts',(4.88956789803041,2.88771064714606,-1.74247381060388));
#15185=CARTESIAN_POINT('Ctrl Pts',(2.55897587967682,1.39825735648593,-1.61564653709567));
#15186=CARTESIAN_POINT('Ctrl Pts',(2.54229394979133,-1.3675792209613,-1.48881926358746));
#15187=CARTESIAN_POINT('Ctrl Pts',(4.8547500177879,-2.88503669780044,-1.36199199007923));
#15188=CARTESIAN_POINT('Ctrl Pts',(7.09859127194373,-1.89543272355351,-1.24954055723209));
#15189=CARTESIAN_POINT('Ctrl Pts',(7.53819513999477,-0.536315133329038,
-1.17936488222102));
#15190=CARTESIAN_POINT('Ctrl Pts',(7.54193252997112,0.00182552697798459,
-1.15146496504602));
#15191=CARTESIAN_POINT('',(7.54820283579053,0.000480549568469427,-0.351464965046016));
#15192=CARTESIAN_POINT('Ctrl Pts',(7.54193252997112,0.00182552697798459,
-1.15146496504602));
#15193=CARTESIAN_POINT('Ctrl Pts',(7.54385827485599,0.279110378301824,-1.13708912438495));
#15194=CARTESIAN_POINT('Ctrl Pts',(7.3724979850303,1.36951155024719,-1.08043752588781));
#15195=CARTESIAN_POINT('Ctrl Pts',(5.77063349163689,2.81469852890825,-0.981510169554581));
#15196=CARTESIAN_POINT('Ctrl Pts',(3.09918935794445,2.09809787237654,-0.854682896046374));
#15197=CARTESIAN_POINT('Ctrl Pts',(2.24852759774879,-0.533727507488469,
-0.727855622538154));
#15198=CARTESIAN_POINT('Ctrl Pts',(3.99516510083363,-2.67834581692979,-0.601028349029938));
#15199=CARTESIAN_POINT('Ctrl Pts',(6.715139087859,-2.3812954588471,-0.475564796532559));
#15200=CARTESIAN_POINT('Ctrl Pts',(7.54609087854429,-0.78345086191955,-0.39237700187125));
#15201=CARTESIAN_POINT('Ctrl Pts',(7.54820283579053,0.000480549568469427,
-0.351464965046016));
#15202=CARTESIAN_POINT('',(7.54432619069004,-0.00217446611864238,0.448535034953988));
#15203=CARTESIAN_POINT('Ctrl Pts',(7.54820283579053,0.000480549568469427,
-0.351464965046016));
#15204=CARTESIAN_POINT('Ctrl Pts',(7.54827323366592,0.0266113369811877,
-0.350101244035178));
#15205=CARTESIAN_POINT('Ctrl Pts',(7.53607092417593,0.862736984340334,-0.306461765188222));
#15206=CARTESIAN_POINT('Ctrl Pts',(6.58857745365878,2.47917651072543,-0.220546528505332));
#15207=CARTESIAN_POINT('Ctrl Pts',(3.82543063400702,2.60226149525943,-0.0937192549970498));
#15208=CARTESIAN_POINT('Ctrl Pts',(2.22012511854379,0.349901741046586,0.0331080185111337));
#15209=CARTESIAN_POINT('Ctrl Pts',(3.23804574570049,-2.22186182840879,0.159935292019368));
#15210=CARTESIAN_POINT('Ctrl Pts',(5.94999527582803,-2.76542415824012,0.286762565527575));
#15211=CARTESIAN_POINT('Ctrl Pts',(7.41422764622619,-1.26294971488547,0.382962317259512));
#15212=CARTESIAN_POINT('Ctrl Pts',(7.54523656020964,-0.22653931857562,0.436886311155375));
#15213=CARTESIAN_POINT('Ctrl Pts',(7.54330296331732,-0.00218295240421028,
0.448534547215166));
#15214=CARTESIAN_POINT('',(7.54432692296551,0.00106743696237302,1.24853503500156));
#15215=CARTESIAN_POINT('Ctrl Pts',(7.54432619069003,-0.00217446611864238,
0.448535034953988));
#15216=CARTESIAN_POINT('Ctrl Pts',(7.54439769743544,0.0784095490257859,
0.452717120495905));
#15217=CARTESIAN_POINT('Ctrl Pts',(7.54048996103696,0.159079511651245,0.456899206037822));
#15218=CARTESIAN_POINT('Ctrl Pts',(7.53260427432528,0.23940846782338,0.461081291579739));
#15219=CARTESIAN_POINT('Ctrl Pts',(7.52472246292544,0.319697947439349,0.465261321893471));
#15220=CARTESIAN_POINT('Ctrl Pts',(7.51286662670644,0.399646282378622,0.469441352207201));
#15221=CARTESIAN_POINT('Ctrl Pts',(7.4970900754961,0.478829392525623,0.473621382520934));
#15222=CARTESIAN_POINT('Ctrl Pts',(7.48131623537897,0.557998895592729,0.477800694524835));
#15223=CARTESIAN_POINT('Ctrl Pts',(7.46162311120078,0.636402970472835,0.481980006528739));
#15224=CARTESIAN_POINT('Ctrl Pts',(7.43811525099534,0.713627056030673,0.48615931853264));
#15225=CARTESIAN_POINT('Ctrl Pts',(7.41460391741901,0.790862551724844,0.490339248044919));
#15226=CARTESIAN_POINT('Ctrl Pts',(7.38727686924614,0.866917259459341,0.494519177557197));
#15227=CARTESIAN_POINT('Ctrl Pts',(7.35628824494104,0.941392621892211,0.498699107069475));
#15228=CARTESIAN_POINT('Ctrl Pts',(7.32526596372127,1.01594887242432,0.502883576426102));
#15229=CARTESIAN_POINT('Ctrl Pts',(7.29057435498377,1.08892191757199,0.507068045782728));
#15230=CARTESIAN_POINT('Ctrl Pts',(7.25241504782299,1.15993472269526,0.511252515139354));
#15231=CARTESIAN_POINT('Ctrl Pts',(7.21423132633598,1.23099296181407,0.515439661719641));
#15232=CARTESIAN_POINT('Ctrl Pts',(7.17257573845089,1.30008806150189,0.519626808299931));
#15233=CARTESIAN_POINT('Ctrl Pts',(7.12769372869992,1.36687124932426,0.523813954880218));
#15234=CARTESIAN_POINT('Ctrl Pts',(7.08273896064374,1.43376269949027,0.528007889251217));
#15235=CARTESIAN_POINT('Ctrl Pts',(7.03454762087561,1.49833438387621,0.532201823622214));
#15236=CARTESIAN_POINT('Ctrl Pts',(6.98340547657611,1.56027049524818,0.536395757993212));
#15237=CARTESIAN_POINT('Ctrl Pts',(6.96705959253474,1.58006631156223,0.537736209510145));
#15238=CARTESIAN_POINT('Ctrl Pts',(6.95041254789911,1.599593177255,0.539076661027078));
#15239=CARTESIAN_POINT('Ctrl Pts',(6.9334744274315,1.61884161198756,0.54041711254401));
#15240=CARTESIAN_POINT('Ctrl Pts',(6.8799971896741,1.67961300174232,0.544649202202974));
#15241=CARTESIAN_POINT('Ctrl Pts',(6.82340565434219,1.73784503569686,0.548881291861938));
#15242=CARTESIAN_POINT('Ctrl Pts',(6.76397035957675,1.79320158591264,0.553113381520903));
#15243=CARTESIAN_POINT('Ctrl Pts',(6.70462001204309,1.84847901839677,0.557339422512949));
#15244=CARTESIAN_POINT('Ctrl Pts',(6.64243431464192,1.90088881549488,0.561565463504997));
#15245=CARTESIAN_POINT('Ctrl Pts',(6.57772292224304,1.95012912477685,0.565791504497043));
#15246=CARTESIAN_POINT('Ctrl Pts',(6.51299373046252,1.99938297799636,0.570018707895176));
#15247=CARTESIAN_POINT('Ctrl Pts',(6.44573778191154,2.04546526724322,0.574245911293307));
#15248=CARTESIAN_POINT('Ctrl Pts',(6.3763007180164,2.08811202078007,0.57847311469144));
#15249=CARTESIAN_POINT('Ctrl Pts',(6.30700696413278,2.13067075638531,0.582691593634165));
#15250=CARTESIAN_POINT('Ctrl Pts',(6.23554147196038,2.16980785869403,0.586910072576891));
#15251=CARTESIAN_POINT('Ctrl Pts',(6.16227797187666,2.20530340381632,0.591128551519615));
#15252=CARTESIAN_POINT('Ctrl Pts',(6.08903849658293,2.24078730913139,0.595345647125882));
#15253=CARTESIAN_POINT('Ctrl Pts',(6.01400260215497,2.27263182628028,0.599562742732148));
#15254=CARTESIAN_POINT('Ctrl Pts',(5.93756795157103,2.30066332151541,0.603779838338415));
#15255=CARTESIAN_POINT('Ctrl Pts',(5.86113497830359,2.32869420161474,0.607996841402831));
#15256=CARTESIAN_POINT('Ctrl Pts',(5.78330374658067,2.35291206724796,0.612213844467248));
#15257=CARTESIAN_POINT('Ctrl Pts',(5.70448984443651,2.37319222362698,0.616430847531664));
#15258=CARTESIAN_POINT('Ctrl Pts',(5.62534965112499,2.39355634026833,0.620665309075044));
#15259=CARTESIAN_POINT('Ctrl Pts',(5.54521908721839,2.40994994376372,0.624899770618424));
#15260=CARTESIAN_POINT('Ctrl Pts',(5.46453034046925,2.42229837109694,0.629134232161804));
#15261=CARTESIAN_POINT('Ctrl Pts',(5.38405776682966,2.43461371577561,0.633357349165134));
#15262=CARTESIAN_POINT('Ctrl Pts',(5.30303046671959,2.44290552482371,0.637580466168465));
#15263=CARTESIAN_POINT('Ctrl Pts',(5.22188154726539,2.44715187978548,0.641803583171796));
#15264=CARTESIAN_POINT('Ctrl Pts',(5.14040564284983,2.45141534519335,0.646043716985201));
#15265=CARTESIAN_POINT('Ctrl Pts',(5.05880760837054,2.45160069338741,0.650283850798605));
#15266=CARTESIAN_POINT('Ctrl Pts',(4.97752315877383,2.44773847262252,0.65452398461201));
#15267=CARTESIAN_POINT('Ctrl Pts',(4.89623870917711,2.44387625185763,0.658764118425415));
#15268=CARTESIAN_POINT('Ctrl Pts',(4.81526830353269,2.4359665694822,0.663004252238823));
#15269=CARTESIAN_POINT('Ctrl Pts',(4.73503801466486,2.4240917066919,0.667244386052229));
#15270=CARTESIAN_POINT('Ctrl Pts',(4.65495993439779,2.41223937225435,0.67147647571119));
#15271=CARTESIAN_POINT('Ctrl Pts',(4.57532040791205,2.39639268582385,0.675708565370152));
#15272=CARTESIAN_POINT('Ctrl Pts',(4.49654862582763,2.37659601279823,0.679940655029114));
#15273=CARTESIAN_POINT('Ctrl Pts',(4.41788942743378,2.35682763394663,0.684166696021154));
#15274=CARTESIAN_POINT('Ctrl Pts',(4.34009595714993,2.33312059334035,0.688392737013193));
#15275=CARTESIAN_POINT('Ctrl Pts',(4.26358989931003,2.3055707207787,0.692618778005233));
#15276=CARTESIAN_POINT('Ctrl Pts',(4.1870627978721,2.27801327040609,0.696845981403367));
#15277=CARTESIAN_POINT('Ctrl Pts',(4.11182427435526,2.24661096831319,0.701073184801499));
#15278=CARTESIAN_POINT('Ctrl Pts',(4.03828377926988,2.2115104410777,0.705300388199633));
#15279=CARTESIAN_POINT('Ctrl Pts',(3.96489506320004,2.17648235724177,0.709518867142355));
#15280=CARTESIAN_POINT('Ctrl Pts',(3.89319780366117,2.13777147604315,0.713737346085078));
#15281=CARTESIAN_POINT('Ctrl Pts',(3.82357974791018,2.09557194427452,0.717955825027801));
#15282=CARTESIAN_POINT('Ctrl Pts',(3.75398452152405,2.05338625070485,0.722172920634062));
#15283=CARTESIAN_POINT('Ctrl Pts',(3.68646754197223,2.00771441915376,0.726390016240323));
#15284=CARTESIAN_POINT('Ctrl Pts',(3.62139071186076,1.95879584683578,0.730607111846584));
#15285=CARTESIAN_POINT('Ctrl Pts',(3.55631530982468,1.90987834800907,0.734824114910991));
#15286=CARTESIAN_POINT('Ctrl Pts',(3.49368032151808,1.85771453021222,0.739041117975399));
#15287=CARTESIAN_POINT('Ctrl Pts',(3.43381631600767,1.80258543845324,0.743258121039807));
#15288=CARTESIAN_POINT('Ctrl Pts',(3.37370447228947,1.74722811112628,0.747492582583193));
#15289=CARTESIAN_POINT('Ctrl Pts',(3.31638695987479,1.68888121508059,0.75172704412658));
#15290=CARTESIAN_POINT('Ctrl Pts',(3.26216137660341,1.62786692471803,0.755961505669966));
#15291=CARTESIAN_POINT('Ctrl Pts',(3.20808106901703,1.56701609765623,0.760184622673298));
#15292=CARTESIAN_POINT('Ctrl Pts',(3.15707640526136,1.50351254078266,0.76440773967663));
#15293=CARTESIAN_POINT('Ctrl Pts',(3.10940121141869,1.43770787110703,0.768630856679963));
#15294=CARTESIAN_POINT('Ctrl Pts',(3.06153391309053,1.37163804525283,0.772870990493376));
#15295=CARTESIAN_POINT('Ctrl Pts',(3.01702322307984,1.30324892287484,0.777111124306789));
#15296=CARTESIAN_POINT('Ctrl Pts',(2.97608034673345,1.23292282976579,0.781351258120202));
#15297=CARTESIAN_POINT('Ctrl Pts',(2.93513747038705,1.16259673665673,0.785591391933614));
#15298=CARTESIAN_POINT('Ctrl Pts',(2.89776256714275,1.09033411649246,0.789831525747029));
#15299=CARTESIAN_POINT('Ctrl Pts',(2.86411817867463,1.01653732291217,0.794071659560442));
#15300=CARTESIAN_POINT('Ctrl Pts',(2.83053761853575,0.942880532650499,0.798303749219408));
#15301=CARTESIAN_POINT('Ctrl Pts',(2.80054813471453,0.867420592882111,0.802535838878374));
#15302=CARTESIAN_POINT('Ctrl Pts',(2.77434578854549,0.790541863893586,0.80676792853734));
#15303=CARTESIAN_POINT('Ctrl Pts',(2.74818089178728,0.713773012970487,0.810993969529392));
#15304=CARTESIAN_POINT('Ctrl Pts',(2.72579253108114,0.635589836403893,0.815220010521445));
#15305=CARTESIAN_POINT('Ctrl Pts',(2.70732949048839,0.556398369082758,0.819446051513497));
#15306=CARTESIAN_POINT('Ctrl Pts',(2.68886137148995,0.477185119520685,0.823673254911629));
#15307=CARTESIAN_POINT('Ctrl Pts',(2.67432090143937,0.396963459550137,0.827900458309758));
#15308=CARTESIAN_POINT('Ctrl Pts',(2.66380757770066,0.316156767664058,0.83212766170789));
#15309=CARTESIAN_POINT('Ctrl Pts',(2.6533159522375,0.23551685137731,0.836346140650612));
#15310=CARTESIAN_POINT('Ctrl Pts',(2.64683495131427,0.154294773248336,0.840564619593335));
#15311=CARTESIAN_POINT('Ctrl Pts',(2.64441238840442,0.0729215260660757,
0.844783098536056));
#15312=CARTESIAN_POINT('Ctrl Pts',(2.64199061990878,-0.00842503695328016,
0.849000194142323));
#15313=CARTESIAN_POINT('Ctrl Pts',(2.64362466028645,-0.0899222064568432,
0.853217289748588));
#15314=CARTESIAN_POINT('Ctrl Pts',(2.64931029310321,-0.171136085285999,
0.857434385354854));
#15315=CARTESIAN_POINT('Ctrl Pts',(2.65499580115189,-0.252348181921224,
0.861651388419275));
#15316=CARTESIAN_POINT('Ctrl Pts',(2.66473269126414,-0.333276536768552,
0.865868391483699));
#15317=CARTESIAN_POINT('Ctrl Pts',(2.67846475733523,-0.413490913755362,
0.87008539454812));
#15318=CARTESIAN_POINT('Ctrl Pts',(2.69225367444079,-0.494037379903908,
0.874319856091498));
#15319=CARTESIAN_POINT('Ctrl Pts',(2.71007085127495,-0.573863476621761,
0.878554317634875));
#15320=CARTESIAN_POINT('Ctrl Pts',(2.73180763696944,-0.652544285318772,
0.882788779178253));
#15321=CARTESIAN_POINT('Ctrl Pts',(2.75348618767155,-0.731014300370378,
0.887011896181586));
#15322=CARTESIAN_POINT('Ctrl Pts',(2.77906318609869,-0.808344725248847,
0.891235013184922));
#15323=CARTESIAN_POINT('Ctrl Pts',(2.80838147504369,-0.88413137705768,0.895458130188255));
#15324=CARTESIAN_POINT('Ctrl Pts',(2.83781790036854,-0.960223406874867,
0.899698264001657));
#15325=CARTESIAN_POINT('Ctrl Pts',(2.87102563075662,-1.03475876913531,0.903938397815057));
#15326=CARTESIAN_POINT('Ctrl Pts',(2.90779856556226,-1.10735236224961,0.908178531628458));
#15327=CARTESIAN_POINT('Ctrl Pts',(2.94457150036789,-1.17994595536391,0.912418665441859));
#15328=CARTESIAN_POINT('Ctrl Pts',(2.98490935385601,-1.2505974043332,0.916658799255261));
#15329=CARTESIAN_POINT('Ctrl Pts',(3.02856276223632,-1.31895156700725,0.920898933068662));
#15330=CARTESIAN_POINT('Ctrl Pts',(3.07213335371174,-1.38717605183027,0.925131022727625));
#15331=CARTESIAN_POINT('Ctrl Pts',(3.11916947096479,-1.45336649920344,0.929363112386589));
#15332=CARTESIAN_POINT('Ctrl Pts',(3.16945507369053,-1.51714941285713,0.933595202045552));
#15333=CARTESIAN_POINT('Ctrl Pts',(3.21966880627985,-1.58084116549341,0.937821243037608));
#15334=CARTESIAN_POINT('Ctrl Pts',(3.27312251498275,-1.64213185662239,0.942047284029663));
#15335=CARTESIAN_POINT('Ctrl Pts',(3.32955626775376,-1.70067589058484,0.946273325021719));
#15336=CARTESIAN_POINT('Ctrl Pts',(3.38600554307584,-1.75923602754793,0.95050052841985));
#15337=CARTESIAN_POINT('Ctrl Pts',(3.44543622880785,-1.81504761766274,0.95472773181798));
#15338=CARTESIAN_POINT('Ctrl Pts',(3.50754704413301,-1.86779700675161,0.958954935216112));
#15339=CARTESIAN_POINT('Ctrl Pts',(3.56952966997029,-1.9204375272459,0.963173414158834));
#15340=CARTESIAN_POINT('Ctrl Pts',(3.63418103546849,-1.97002815426122,0.967391893101556));
#15341=CARTESIAN_POINT('Ctrl Pts',(3.70116537433347,-2.01629447586623,0.971610372044278));
#15342=CARTESIAN_POINT('Ctrl Pts',(3.76812774749006,-2.06254562567816,0.975827467650538));
#15343=CARTESIAN_POINT('Ctrl Pts',(3.83742119266738,-2.10547437106498,0.9800445632568));
#15344=CARTESIAN_POINT('Ctrl Pts',(3.90867922331487,-2.14484839299855,0.98426165886306));
#15345=CARTESIAN_POINT('Ctrl Pts',(3.97993569024395,-2.1842215508908,0.988478661927469));
#15346=CARTESIAN_POINT('Ctrl Pts',(4.05315624964188,-2.22003991669338,0.992695664991879));
#15347=CARTESIAN_POINT('Ctrl Pts',(4.12794922733446,-2.25211679936304,0.996912668056289));
#15348=CARTESIAN_POINT('Ctrl Pts',(4.20305184948507,-2.28432648098329,1.00114712959967));
#15349=CARTESIAN_POINT('Ctrl Pts',(4.27973950882047,-2.31276343604565,1.00538159114305));
#15350=CARTESIAN_POINT('Ctrl Pts',(4.35759648647079,-2.33728788386237,1.00961605268644));
#15351=CARTESIAN_POINT('Ctrl Pts',(4.43524487760027,-2.36174662826496,1.01383916968977));
#15352=CARTESIAN_POINT('Ctrl Pts',(4.51405586678778,-2.3823137244071,1.01806228669311));
#15353=CARTESIAN_POINT('Ctrl Pts',(4.5936047727015,-2.39890137725466,1.02228540369644));
#15354=CARTESIAN_POINT('Ctrl Pts',(4.67347421641284,-2.41555586910712,1.02652553750985));
#15355=CARTESIAN_POINT('Ctrl Pts',(4.75408706910114,-2.42819871555461,1.03076567132326));
#15356=CARTESIAN_POINT('Ctrl Pts',(4.835008060753,-2.43679357480658,1.03500580513666));
#15357=CARTESIAN_POINT('Ctrl Pts',(4.91592905240485,-2.44538843405855,1.03924593895007));
#15358=CARTESIAN_POINT('Ctrl Pts',(4.99715771294229,-2.44993534210655,1.04348607276348));
#15359=CARTESIAN_POINT('Ctrl Pts',(5.07826040200378,-2.45045055575236,1.04772620657688));
#15360=CARTESIAN_POINT('Ctrl Pts',(5.15920922739371,-2.45096479196247,1.05195829623585));
#15361=CARTESIAN_POINT('Ctrl Pts',(5.240334562324,-2.44746455166313,1.05619038589481));
#15362=CARTESIAN_POINT('Ctrl Pts',(5.32120547477968,-2.43992814441332,1.06042247555377));
#15363=CARTESIAN_POINT('Ctrl Pts',(5.40196080338606,-2.43240250848948,1.06464851654581));
#15364=CARTESIAN_POINT('Ctrl Pts',(5.48246197290976,-2.4208522055311,1.06887455753785));
#15365=CARTESIAN_POINT('Ctrl Pts',(5.56227761120284,-2.40530755216622,1.07310059852989));
#15366=CARTESIAN_POINT('Ctrl Pts',(5.64211520342029,-2.38975862312114,1.07732780192803));
#15367=CARTESIAN_POINT('Ctrl Pts',(5.72126642100674,-2.37021316962655,1.08155500532616));
#15368=CARTESIAN_POINT('Ctrl Pts',(5.79930422572347,-2.34675357746031,1.08578220872429));
#15369=CARTESIAN_POINT('Ctrl Pts',(5.87718096950144,-2.32334240315962,1.09000068766702));
#15370=CARTESIAN_POINT('Ctrl Pts',(5.95394843948697,-2.29603334055061,1.09421916660974));
#15371=CARTESIAN_POINT('Ctrl Pts',(6.02919379005196,-2.26495905236258,1.09843764555246));
#15372=CARTESIAN_POINT('Ctrl Pts',(6.10441446593258,-2.23389495414972,1.10265474115873));
#15373=CARTESIAN_POINT('Ctrl Pts',(6.17811358446272,-2.19906825960464,1.106871836765));
#15374=CARTESIAN_POINT('Ctrl Pts',(6.24989693204501,-2.16066029760598,1.11108893237127));
#15375=CARTESIAN_POINT('Ctrl Pts',(6.3216787043813,-2.12225317844887,1.1153059354357));
#15376=CARTESIAN_POINT('Ctrl Pts',(6.39154438017327,-2.08026516833278,1.11952293850013));
#15377=CARTESIAN_POINT('Ctrl Pts',(6.45912435248184,-2.03492354003424,1.12373994156455));
#15378=CARTESIAN_POINT('Ctrl Pts',(6.52698410725816,-1.98939419646706,1.12797440310793));
#15379=CARTESIAN_POINT('Ctrl Pts',(6.59253879355162,-1.940483659642,1.13220886465131));
#15380=CARTESIAN_POINT('Ctrl Pts',(6.65544510872166,-1.88846488398099,1.13644332619469));
#15381=CARTESIAN_POINT('Ctrl Pts',(6.71818289167012,-1.83658547174959,1.14066644319803));
#15382=CARTESIAN_POINT('Ctrl Pts',(6.77828615862655,-1.78161479991805,1.14488956020137));
#15383=CARTESIAN_POINT('Ctrl Pts',(6.83545036964668,-1.72386160401061,1.14911267720471));
#15384=CARTESIAN_POINT('Ctrl Pts',(6.89284492060773,-1.66587569488113,1.15335281101811));
#15385=CARTESIAN_POINT('Ctrl Pts',(6.94727637205012,-1.60508514727145,1.1575929448315));
#15386=CARTESIAN_POINT('Ctrl Pts',(6.99847761586214,-1.54183555337905,1.1618330786449));
#15387=CARTESIAN_POINT('Ctrl Pts',(7.04967885967416,-1.47858595948665,1.1660732124583));
#15388=CARTESIAN_POINT('Ctrl Pts',(7.09764967054028,-1.41287773343903,1.1703133462717));
#15389=CARTESIAN_POINT('Ctrl Pts',(7.14216797518797,-1.34508369115379,1.17455348008509));
#15390=CARTESIAN_POINT('Ctrl Pts',(7.18746672627468,-1.27610115754332,1.17886794730723));
#15391=CARTESIAN_POINT('Ctrl Pts',(7.2293551016474,-1.20470926392159,1.18318241452936));
#15392=CARTESIAN_POINT('Ctrl Pts',(7.26757389031839,-1.13127157776659,1.18749688175149));
#15393=CARTESIAN_POINT('Ctrl Pts',(7.30573175456377,-1.05795095834772,1.19180447129784));
#15394=CARTESIAN_POINT('Ctrl Pts',(7.34023145647742,-0.982591415569996,
1.19611206084419));
#15395=CARTESIAN_POINT('Ctrl Pts',(7.37085724304463,-0.90558502096874,1.20041965039054));
#15396=CARTESIAN_POINT('Ctrl Pts',(7.40143315944261,-0.828704021413996,
1.20472022557926));
#15397=CARTESIAN_POINT('Ctrl Pts',(7.42814755207704,-0.750181913787925,
1.20902080076798));
#15398=CARTESIAN_POINT('Ctrl Pts',(7.45083143436931,-0.670433500931087,
1.21332137595669));
#15399=CARTESIAN_POINT('Ctrl Pts',(7.47349353380038,-0.590761668819372,
1.21761782139235));
#15400=CARTESIAN_POINT('Ctrl Pts',(7.49213269474065,-0.50986629385648,1.221914266828));
#15401=CARTESIAN_POINT('Ctrl Pts',(7.50662893554611,-0.428179658531404,
1.22621071226366));
#15402=CARTESIAN_POINT('Ctrl Pts',(7.52111435624916,-0.346553994721007,
1.23050395080035));
#15403=CARTESIAN_POINT('Ctrl Pts',(7.53146292938334,-0.264138678010635,
1.23479718933704));
#15404=CARTESIAN_POINT('Ctrl Pts',(7.53760547669634,-0.181377414860852,
1.23909042787373));
#15405=CARTESIAN_POINT('Ctrl Pts',(7.54210976449271,-0.120689148475219,
1.24223863023382));
#15406=CARTESIAN_POINT('Ctrl Pts',(7.54435344337769,-0.0598151464494927,
1.2453868325939));
#15407=CARTESIAN_POINT('Ctrl Pts',(7.54432692296591,0.00106743604236301,
1.24853503495399));
#15408=CARTESIAN_POINT('',(7.54432671099194,0.00147590784950144,2.0485350349256));
#15409=CARTESIAN_POINT('Ctrl Pts',(7.54432692296551,0.0010674369623747,
1.24853503500156));
#15410=CARTESIAN_POINT('Ctrl Pts',(7.54428806046215,0.0902835300895766,
1.25314834645204));
#15411=CARTESIAN_POINT('Ctrl Pts',(7.5393728342159,0.17934237197442,1.25776165790251));
#15412=CARTESIAN_POINT('Ctrl Pts',(7.52965757937397,0.267731947853721,1.26237496935299));
#15413=CARTESIAN_POINT('Ctrl Pts',(7.5199136595364,0.356382318416006,1.26700189244358));
#15414=CARTESIAN_POINT('Ctrl Pts',(7.50534147059153,0.444359170624326,1.27162881553417));
#15415=CARTESIAN_POINT('Ctrl Pts',(7.48606828497608,0.531161583907084,1.27625573862477));
#15416=CARTESIAN_POINT('Ctrl Pts',(7.4667091059621,0.618351293543798,1.28090330619257));
#15417=CARTESIAN_POINT('Ctrl Pts',(7.44260702225187,0.704355770605615,1.28555087376038));
#15418=CARTESIAN_POINT('Ctrl Pts',(7.4139396961747,0.788687548010236,1.29019844132819));
#15419=CARTESIAN_POINT('Ctrl Pts',(7.39094795642238,0.856323234495913,1.2939258787499));
#15420=CARTESIAN_POINT('Ctrl Pts',(7.36502066814117,0.922883320604921,1.2976533161716));
#15421=CARTESIAN_POINT('Ctrl Pts',(7.33627098328141,0.988127486225723,1.30138075359331));
#15422=CARTESIAN_POINT('Ctrl Pts',(7.30362892112772,1.06220496289194,1.30561284325227));
#15423=CARTESIAN_POINT('Ctrl Pts',(7.26725138371584,1.13480142576407,1.30984493291123));
#15424=CARTESIAN_POINT('Ctrl Pts',(7.22729484661253,1.20551477003763,1.3140770225702));
#15425=CARTESIAN_POINT('Ctrl Pts',(7.18739541694394,1.27612704805308,1.31830306356224));
#15426=CARTESIAN_POINT('Ctrl Pts',(7.14392737370832,1.34486115174554,1.32252910455429));
#15427=CARTESIAN_POINT('Ctrl Pts',(7.09709482980959,1.41133584765583,1.32675514554634));
#15428=CARTESIAN_POINT('Ctrl Pts',(7.0502494042483,1.47782882795833,1.33098234894447));
#15429=CARTESIAN_POINT('Ctrl Pts',(7.00003783915847,1.54206074159131,1.33520955234261));
#15430=CARTESIAN_POINT('Ctrl Pts',(6.94670998865652,1.60367560822633,1.33943675574074));
#15431=CARTESIAN_POINT('Ctrl Pts',(6.89349220062614,1.6651633089538,1.34365523468346));
#15432=CARTESIAN_POINT('Ctrl Pts',(6.83717126285887,1.72404438670867,1.34787371362619));
#15433=CARTESIAN_POINT('Ctrl Pts',(6.77803710266946,1.77999637743943,1.35209219256891));
#15434=CARTESIAN_POINT('Ctrl Pts',(6.71892233393394,1.83593002022301,1.35630928817517));
#15435=CARTESIAN_POINT('Ctrl Pts',(6.65699651209806,1.88893616434786,1.36052638378143));
#15436=CARTESIAN_POINT('Ctrl Pts',(6.59258635189092,1.93872925420057,1.36474347938769));
#15437=CARTESIAN_POINT('Ctrl Pts',(6.52817760512931,1.98852125137131,1.36896048245211));
#15438=CARTESIAN_POINT('Ctrl Pts',(6.46128499673596,2.03510005115916,1.37317748551653));
#15439=CARTESIAN_POINT('Ctrl Pts',(6.39226710089324,2.0782213448248,1.37739448858095));
#15440=CARTESIAN_POINT('Ctrl Pts',(6.32296346954969,2.12152116152846,1.38162895012433));
#15441=CARTESIAN_POINT('Ctrl Pts',(6.25151730910752,2.16133452191954,1.38586341166772));
#15442=CARTESIAN_POINT('Ctrl Pts',(6.17831811948979,2.19745980598572,1.3900978732111));
#15443=CARTESIAN_POINT('Ctrl Pts',(6.10531503771946,2.23348830685345,1.39432099021443));
#15444=CARTESIAN_POINT('Ctrl Pts',(6.03056875330173,2.26584831961874,1.39854410721776));
#15445=CARTESIAN_POINT('Ctrl Pts',(5.95448556150857,2.29438823177031,1.40276722422109));
#15446=CARTESIAN_POINT('Ctrl Pts',(5.87809579681594,2.3230431438767,1.4070073580345));
#15447=CARTESIAN_POINT('Ctrl Pts',(5.8003587797785,2.34784696952838,1.41124749184791));
#15448=CARTESIAN_POINT('Ctrl Pts',(5.72169912686977,2.36869732923169,1.41548762566131));
#15449=CARTESIAN_POINT('Ctrl Pts',(5.64303947396105,2.389547688935,1.41972775947472));
#15450=CARTESIAN_POINT('Ctrl Pts',(5.56345765524226,2.40644454648053,1.42396789328813));
#15451=CARTESIAN_POINT('Ctrl Pts',(5.48338470822628,2.41933775299717,1.42820802710153));
#15452=CARTESIAN_POINT('Ctrl Pts',(5.40346367131056,2.43220649921394,1.43244011676049));
#15453=CARTESIAN_POINT('Ctrl Pts',(5.32275520129993,2.44113479794549,1.43667220641945));
#15454=CARTESIAN_POINT('Ctrl Pts',(5.24168186473874,2.4460354116288,1.44090429607841));
#15455=CARTESIAN_POINT('Ctrl Pts',(5.16072440133901,2.45092902116469,1.44513033707046));
#15456=CARTESIAN_POINT('Ctrl Pts',(5.07940356707361,2.4518063509304,1.44935637806251));
#15457=CARTESIAN_POINT('Ctrl Pts',(4.99815030471606,2.44863149335155,1.45358241905456));
#15458=CARTESIAN_POINT('Ctrl Pts',(4.9168746930044,2.44545576250295,1.45780962245269));
#15459=CARTESIAN_POINT('Ctrl Pts',(4.83566715474352,2.4382255669776,1.46203682585082));
#15460=CARTESIAN_POINT('Ctrl Pts',(4.7549623003575,2.4269571195184,1.46626402924896));
#15461=CARTESIAN_POINT('Ctrl Pts',(4.67442401139006,2.41571192882215,1.47048250819168));
#15462=CARTESIAN_POINT('Ctrl Pts',(4.59438679711928,2.40044517801082,1.4747009871344));
#15463=CARTESIAN_POINT('Ctrl Pts',(4.51527891886781,2.38122493434451,1.47891946607712));
#15464=CARTESIAN_POINT('Ctrl Pts',(4.43619698191265,2.36201099343903,1.48313656168339));
#15465=CARTESIAN_POINT('Ctrl Pts',(4.35804422697278,2.33884624391855,1.48735365728965));
#15466=CARTESIAN_POINT('Ctrl Pts',(4.28123793294673,2.31184969352821,1.49157075289591));
#15467=CARTESIAN_POINT('Ctrl Pts',(4.20443332439259,2.28485373556233,1.49578775596033));
#15468=CARTESIAN_POINT('Ctrl Pts',(4.12897555601967,2.25402629908896,1.50000475902475));
#15469=CARTESIAN_POINT('Ctrl Pts',(4.05526460406163,2.21953555431023,1.50422176208917));
#15470=CARTESIAN_POINT('Ctrl Pts',(3.98124848725441,2.18490201714246,1.50845622363255));
#15471=CARTESIAN_POINT('Ctrl Pts',(3.90899411417661,2.14657496300712,1.51269068517593));
#15472=CARTESIAN_POINT('Ctrl Pts',(3.83888244061972,2.10477172460857,1.51692514671931));
#15473=CARTESIAN_POINT('Ctrl Pts',(3.76895860315021,2.06308048120803,1.52114826372264));
#15474=CARTESIAN_POINT('Ctrl Pts',(3.70116636520278,2.01793194928828,1.52537138072598));
#15475=CARTESIAN_POINT('Ctrl Pts',(3.63585383805487,1.96958474195826,1.52959449772931));
#15476=CARTESIAN_POINT('Ctrl Pts',(3.5702781377889,1.92104272230266,1.53383463154272));
#15477=CARTESIAN_POINT('Ctrl Pts',(3.50720253317648,1.86927650081015,1.53807476535612));
#15478=CARTESIAN_POINT('Ctrl Pts',(3.44694377047309,1.81458683073496,1.54231489916953));
#15479=CARTESIAN_POINT('Ctrl Pts',(3.3866850077697,1.75989716065978,1.54655503298293));
#15480=CARTESIAN_POINT('Ctrl Pts',(3.32924337288416,1.70228441686834,1.55079516679634));
#15481=CARTESIAN_POINT('Ctrl Pts',(3.27489526229107,1.64208313371704,1.55503530060974));
#15482=CARTESIAN_POINT('Ctrl Pts',(3.22065025801833,1.58199606121111,1.5592673902687));
#15483=CARTESIAN_POINT('Ctrl Pts',(3.16928466213748,1.51910610009245,1.56349947992767));
#15484=CARTESIAN_POINT('Ctrl Pts',(3.12110139711795,1.45372051385435,1.56773156958663));
#15485=CARTESIAN_POINT('Ctrl Pts',(3.07298699749225,1.38842837923572,1.57195761057867));
#15486=CARTESIAN_POINT('Ctrl Pts',(3.02804616865433,1.32064807460014,1.57618365157072));
#15487=CARTESIAN_POINT('Ctrl Pts',(2.9865433020495,1.25072179607794,1.58040969256277));
#15488=CARTESIAN_POINT('Ctrl Pts',(2.94502901975208,1.18077628377831,1.5846368959609));
#15489=CARTESIAN_POINT('Ctrl Pts',(2.90695488381131,1.10868398065176,1.58886409935903));
#15490=CARTESIAN_POINT('Ctrl Pts',(2.87254353178807,1.03481849289501,1.59309130275716));
#15491=CARTESIAN_POINT('Ctrl Pts',(2.83820320078702,0.961105454900816,1.59730978169989));
#15492=CARTESIAN_POINT('Ctrl Pts',(2.80751076859186,0.885626954952128,1.60152826064261));
#15493=CARTESIAN_POINT('Ctrl Pts',(2.78064189706716,0.808779457198272,1.60574673958533));
#15494=CARTESIAN_POINT('Ctrl Pts',(2.75378183646462,0.731957159509874,1.6099638351916));
#15495=CARTESIAN_POINT('Ctrl Pts',(2.73074299978355,0.653767193853023,1.61418093079786));
#15496=CARTESIAN_POINT('Ctrl Pts',(2.71165232180658,0.574624496468033,1.61839802640412));
#15497=CARTESIAN_POINT('Ctrl Pts',(2.69256206276406,0.495483535826052,1.62261502946854));
#15498=CARTESIAN_POINT('Ctrl Pts',(2.677419898011,0.415390337026596,1.62683203253295));
#15499=CARTESIAN_POINT('Ctrl Pts',(2.6663020920874,0.334772036961452,1.63104903559737));
#15500=CARTESIAN_POINT('Ctrl Pts',(2.65513825821981,0.253819975484603,1.63528349714075));
#15501=CARTESIAN_POINT('Ctrl Pts',(2.64803225323112,0.172338921240921,1.63951795868414));
#15502=CARTESIAN_POINT('Ctrl Pts',(2.6450087376301,0.0907667699699964,1.64375242022752));
#15503=CARTESIAN_POINT('Ctrl Pts',(2.64199332232552,0.00941315853642459,
1.64797553723085));
#15504=CARTESIAN_POINT('Ctrl Pts',(2.64303850239018,-0.0720305954233467,
1.65219865423419));
#15505=CARTESIAN_POINT('Ctrl Pts',(2.64811643569602,-0.153131725208311,
1.65642177123752));
#15506=CARTESIAN_POINT('Ctrl Pts',(2.65321483024568,-0.234559647388847,
1.66066190505093));
#15507=CARTESIAN_POINT('Ctrl Pts',(2.66237848463236,-0.315641710899356,
1.66490203886433));
#15508=CARTESIAN_POINT('Ctrl Pts',(2.67552713668527,-0.395948568917046,
1.66914217267774));
#15509=CARTESIAN_POINT('Ctrl Pts',(2.68867578873818,-0.476255426934736,
1.67338230649115));
#15510=CARTESIAN_POINT('Ctrl Pts',(2.70580927922514,-0.555786635709915,
1.67762244030455));
#15511=CARTESIAN_POINT('Ctrl Pts',(2.72679705821168,-0.634128353532026,
1.68186257411796));
#15512=CARTESIAN_POINT('Ctrl Pts',(2.74774502030965,-0.712321445649074,
1.68609466377692));
#15513=CARTESIAN_POINT('Ctrl Pts',(2.7726107971626,-0.789621282590697,1.69032675343589));
#15514=CARTESIAN_POINT('Ctrl Pts',(2.8013011478423,-0.865606581784154,1.69455884309485));
#15515=CARTESIAN_POINT('Ctrl Pts',(2.82995049315847,-0.941483279836695,
1.6987848840869));
#15516=CARTESIAN_POINT('Ctrl Pts',(2.86241339300268,-1.01604874051948,1.70301092507894));
#15517=CARTESIAN_POINT('Ctrl Pts',(2.8985463407754,-1.08889503383382,1.70723696607099));
#15518=CARTESIAN_POINT('Ctrl Pts',(2.93468922720193,-1.16176136409881,1.71146416946912));
#15519=CARTESIAN_POINT('Ctrl Pts',(2.97450403450885,-1.23290713780912,1.71569137286725));
#15520=CARTESIAN_POINT('Ctrl Pts',(3.0177981952346,-1.30194239747158,1.71991857626539));
#15521=CARTESIAN_POINT('Ctrl Pts',(3.06100300185571,-1.37083517639963,1.72413705520811));
#15522=CARTESIAN_POINT('Ctrl Pts',(3.10767258855501,-1.43762573730366,1.72835553415083));
#15523=CARTESIAN_POINT('Ctrl Pts',(3.15756966680859,-1.50195112692391,1.73257401309355));
#15524=CARTESIAN_POINT('Ctrl Pts',(3.20745038266034,-1.56625542276655,1.73679110869982));
#15525=CARTESIAN_POINT('Ctrl Pts',(3.26055620364706,-1.62809578581825,1.74100820430608));
#15526=CARTESIAN_POINT('Ctrl Pts',(3.31660784946631,-1.68714012116001,1.74522529991234));
#15527=CARTESIAN_POINT('Ctrl Pts',(3.37265826526298,-1.74618316080625,1.74944230297676));
#15528=CARTESIAN_POINT('Ctrl Pts',(3.43165405659566,-1.80242995851394,1.75365930604117));
#15529=CARTESIAN_POINT('Ctrl Pts',(3.49327815909478,-1.8555843177437,1.75787630910559));
#15530=CARTESIAN_POINT('Ctrl Pts',(3.55515738663906,-1.90895873710819,1.76211077064897));
#15531=CARTESIAN_POINT('Ctrl Pts',(3.61968638538108,-1.95921474002239,1.76634523219235));
#15532=CARTESIAN_POINT('Ctrl Pts',(3.68651100948259,-2.00609359584509,1.77057969373574));
#15533=CARTESIAN_POINT('Ctrl Pts',(3.75315660382636,-2.05284685859018,1.77480281073907));
#15534=CARTESIAN_POINT('Ctrl Pts',(3.82208512119671,-2.09624083229109,1.77902592774241));
#15535=CARTESIAN_POINT('Ctrl Pts',(3.89291818142928,-2.13606364280399,1.78324904474574));
#15536=CARTESIAN_POINT('Ctrl Pts',(3.96403665945441,-2.17604691706972,1.78748917855914));
#15537=CARTESIAN_POINT('Ctrl Pts',(4.03707463540398,-2.21242998530242,1.79172931237255));
#15538=CARTESIAN_POINT('Ctrl Pts',(4.11162810508851,-2.24504683146318,1.79596944618596));
#15539=CARTESIAN_POINT('Ctrl Pts',(4.18618157477305,-2.27766367762394,1.80020957999936));
#15540=CARTESIAN_POINT('Ctrl Pts',(4.26225007917263,-2.30651419415162,1.80444971381277));
#15541=CARTESIAN_POINT('Ctrl Pts',(4.33941529296309,-2.33148300266897,1.80868984762617));
#15542=CARTESIAN_POINT('Ctrl Pts',(4.41643411304883,-2.35640444170205,1.81292193728513));
#15543=CARTESIAN_POINT('Ctrl Pts',(4.49483282171878,-2.37755187957483,1.81715402694409));
#15544=CARTESIAN_POINT('Ctrl Pts',(4.5742071285654,-2.3947745776288,1.82138611660305));
#15545=CARTESIAN_POINT('Ctrl Pts',(4.65346799056975,-2.41197266033378,1.8256121575951));
#15546=CARTESIAN_POINT('Ctrl Pts',(4.73370123106809,-2.42525704636647,1.82983819858715));
#15547=CARTESIAN_POINT('Ctrl Pts',(4.81448644377937,-2.43452644610848,1.83406423957919));
#15548=CARTESIAN_POINT('Ctrl Pts',(4.89529387710404,-2.4437983954724,1.83829144297732));
#15549=CARTESIAN_POINT('Ctrl Pts',(4.97665313471908,-2.44905303133571,1.84251864637546));
#15550=CARTESIAN_POINT('Ctrl Pts',(5.0581322271524,-2.45024001316067,1.84674584977359));
#15551=CARTESIAN_POINT('Ctrl Pts',(5.13944315623,-2.45142454519341,1.85096432871632));
#15552=CARTESIAN_POINT('Ctrl Pts',(5.22087296166411,-2.44855816498041,1.85518280765904));
#15553=CARTESIAN_POINT('Ctrl Pts',(5.30198801066615,-2.44164274789679,1.85940128660176));
#15554=CARTESIAN_POINT('Ctrl Pts',(5.38307646017434,-2.43472959853779,1.86361838220803));
#15555=CARTESIAN_POINT('Ctrl Pts',(5.46384989557651,-2.42377008858649,1.86783547781429));
#15556=CARTESIAN_POINT('Ctrl Pts',(5.54387775932526,-2.40881811350594,1.87205257342056));
#15557=CARTESIAN_POINT('Ctrl Pts',(5.62390386690647,-2.39386646653827,1.87626957648497));
#15558=CARTESIAN_POINT('Ctrl Pts',(5.70318397879108,-2.37492261511094,1.88048657954939));
#15559=CARTESIAN_POINT('Ctrl Pts',(5.78129713029502,-2.35209168267116,1.88470358261381));
#15560=CARTESIAN_POINT('Ctrl Pts',(5.85973367184437,-2.32916622970396,1.88893804415719));
#15561=CARTESIAN_POINT('Ctrl Pts',(5.93699311348128,-2.30232156197435,1.89317250570057));
#15562=CARTESIAN_POINT('Ctrl Pts',(6.01266578101148,-2.27171429325565,1.89740696724395));
#15563=CARTESIAN_POINT('Ctrl Pts',(6.08813571400305,-2.24118902442812,1.90163008424729));
#15564=CARTESIAN_POINT('Ctrl Pts',(6.1620269574203,-2.20692152369229,1.90585320125062));
#15565=CARTESIAN_POINT('Ctrl Pts',(6.23395599308187,-2.16911421635821,1.91007631825396));
#15566=CARTESIAN_POINT('Ctrl Pts',(6.30617486270674,-2.13115456662685,1.91431645206736));
#15567=CARTESIAN_POINT('Ctrl Pts',(6.37641527654647,-2.0896267705324,1.91855658588077));
#15568=CARTESIAN_POINT('Ctrl Pts',(6.4443182790114,-2.04477968866826,1.92279671969418));
#15569=CARTESIAN_POINT('Ctrl Pts',(6.51222128147632,-1.99993260680413,1.92703685350758));
#15570=CARTESIAN_POINT('Ctrl Pts',(6.57778653276988,-1.95176656598368,1.93127698732099));
#15571=CARTESIAN_POINT('Ctrl Pts',(6.64068979568123,-1.90056997299928,1.9355171211344));
#15572=CARTESIAN_POINT('Ctrl Pts',(6.70265595672201,-1.85013608167505,1.93969408751985));
#15573=CARTESIAN_POINT('Ctrl Pts',(6.76228324590583,-1.79656223509988,1.9438710539053));
#15574=CARTESIAN_POINT('Ctrl Pts',(6.81923004557809,-1.74009629525161,1.94804802029075));
#15575=CARTESIAN_POINT('Ctrl Pts',(6.8763130790926,-1.68349527192215,1.95223497923387));
#15576=CARTESIAN_POINT('Ctrl Pts',(6.93070236814598,-1.62398855423777,1.95642193817699));
#15577=CARTESIAN_POINT('Ctrl Pts',(6.98208507709209,-1.56186819910249,1.96060889712011));
#15578=CARTESIAN_POINT('Ctrl Pts',(7.0332127811925,-1.50005613817552,1.9647750768003));
#15579=CARTESIAN_POINT('Ctrl Pts',(7.08136334922856,-1.43565667276066,1.96894125648049));
#15580=CARTESIAN_POINT('Ctrl Pts',(7.1262649478876,-1.36899483924668,1.97310743616068));
#15581=CARTESIAN_POINT('Ctrl Pts',(7.17113945057062,-1.30237323297396,1.97727110174988));
#15582=CARTESIAN_POINT('Ctrl Pts',(7.21276860737517,-1.23349236269156,1.98143476733907));
#15583=CARTESIAN_POINT('Ctrl Pts',(7.25092218098948,-1.16270860528605,1.98559843292827));
#15584=CARTESIAN_POINT('Ctrl Pts',(7.28906513501693,-1.09194454968535,1.98976093961139));
#15585=CARTESIAN_POINT('Ctrl Pts',(7.32373420028611,-1.01927907926499,1.99392344629451));
#15586=CARTESIAN_POINT('Ctrl Pts',(7.35474445735159,-0.945094283114693,
1.99808595297763));
#15587=CARTESIAN_POINT('Ctrl Pts',(7.38606450716415,-0.870168380183437,
2.00229004313996));
#15588=CARTESIAN_POINT('Ctrl Pts',(7.4136520138649,-0.793693069530683,2.00649413330229));
#15589=CARTESIAN_POINT('Ctrl Pts',(7.43736645441978,-0.716082260776532,
2.01069822346462));
#15590=CARTESIAN_POINT('Ctrl Pts',(7.46086810650685,-0.639167849858183,
2.01486459053995));
#15591=CARTESIAN_POINT('Ctrl Pts',(7.48056585136317,-0.561138719230198,
2.01903095761529));
#15592=CARTESIAN_POINT('Ctrl Pts',(7.49637378505751,-0.482410553964721,
2.02319732469062));
#15593=CARTESIAN_POINT('Ctrl Pts',(7.5123964108495,-0.402613158825682,2.02742027639645));
#15594=CARTESIAN_POINT('Ctrl Pts',(7.52442268876795,-0.322098098698069,
2.03164322810228));
#15595=CARTESIAN_POINT('Ctrl Pts',(7.53241743836409,-0.241304127797537,
2.03586617980811));
#15596=CARTESIAN_POINT('Ctrl Pts',(7.54041218796023,-0.160510156897006,
2.04008913151394));
#15597=CARTESIAN_POINT('Ctrl Pts',(7.54437544438211,-0.079437782649294,
2.04431208321977));
#15598=CARTESIAN_POINT('Ctrl Pts',(7.54432671099194,0.00147590784949135,
2.0485350349256));
#15599=CARTESIAN_POINT('',(7.54432621659511,-0.002145073936182,2.84853503499689));
#15600=CARTESIAN_POINT('Ctrl Pts',(7.54432671099162,0.00147590839337491,
2.04853503495399));
#15601=CARTESIAN_POINT('Ctrl Pts',(7.54427359039347,0.0896737956893433,
2.0531381548502));
#15602=CARTESIAN_POINT('Ctrl Pts',(7.53945915089848,0.17772660136509,2.0577412747464));
#15603=CARTESIAN_POINT('Ctrl Pts',(7.52992837234614,0.265256688986949,2.0623443946426));
#15604=CARTESIAN_POINT('Ctrl Pts',(7.52116581341596,0.345731494558948,2.06657648430155));
#15605=CARTESIAN_POINT('Ctrl Pts',(7.5083949867179,0.425921753537977,2.0708085739605));
#15606=CARTESIAN_POINT('Ctrl Pts',(7.49164371171518,0.505396886135544,2.07504066361945));
#15607=CARTESIAN_POINT('Ctrl Pts',(7.47491637828531,0.584758429786803,2.07926670461149));
#15608=CARTESIAN_POINT('Ctrl Pts',(7.4542199905826,0.663406426132384,2.08349274560353));
#15609=CARTESIAN_POINT('Ctrl Pts',(7.42963408316964,0.740915816021938,2.08771878659557));
#15610=CARTESIAN_POINT('Ctrl Pts',(7.40504141320785,0.81844652548394,2.0919459899937));
#15611=CARTESIAN_POINT('Ctrl Pts',(7.37655716042474,0.894837541586089,2.09617319339183));
#15612=CARTESIAN_POINT('Ctrl Pts',(7.34431208924527,0.969674075540071,2.10040039678997));
#15613=CARTESIAN_POINT('Ctrl Pts',(7.31213356813673,1.04435615560513,2.10461887573268));
#15614=CARTESIAN_POINT('Ctrl Pts',(7.27620989784197,1.1174897269735,2.1088373546754));
#15615=CARTESIAN_POINT('Ctrl Pts',(7.23672016284678,1.18867985970291,2.11305583361812));
#15616=CARTESIAN_POINT('Ctrl Pts',(7.1972433774457,1.25984664754727,2.11727292922438));
#15617=CARTESIAN_POINT('Ctrl Pts',(7.1542030748911,1.32907085632596,2.12149002483064));
#15618=CARTESIAN_POINT('Ctrl Pts',(7.10782455095711,1.39598164060389,2.1257071204369));
#15619=CARTESIAN_POINT('Ctrl Pts',(7.06144704477438,1.46289095656135,2.12992412350132));
#15620=CARTESIAN_POINT('Ctrl Pts',(7.01173172852818,1.52748656769599,2.13414112656573));
#15621=CARTESIAN_POINT('Ctrl Pts',(6.9589467205048,1.58942733651507,2.13835812963014));
#15622=CARTESIAN_POINT('Ctrl Pts',(6.90594318146806,1.65162454138457,2.14259259117353));
#15623=CARTESIAN_POINT('Ctrl Pts',(6.84984477555372,1.71114450745861,2.14682705271692));
#15624=CARTESIAN_POINT('Ctrl Pts',(6.79096198855441,1.76767746160725,2.15106151426031));
#15625=CARTESIAN_POINT('Ctrl Pts',(6.73223695434822,1.82405895839669,2.15528463126365));
#15626=CARTESIAN_POINT('Ctrl Pts',(6.67074281928052,1.87746915229913,2.15950774826698));
#15627=CARTESIAN_POINT('Ctrl Pts',(6.60682117406737,1.92764087672924,2.16373086527032));
#15628=CARTESIAN_POINT('Ctrl Pts',(6.54264196021563,1.97801476527315,2.16797099908374));
#15629=CARTESIAN_POINT('Ctrl Pts',(6.47601602181197,2.02512376565215,2.17221113289716));
#15630=CARTESIAN_POINT('Ctrl Pts',(6.40731727544797,2.06874211893989,2.17645126671058));
#15631=CARTESIAN_POINT('Ctrl Pts',(6.33861852908397,2.11236047222762,2.180691400524));
#15632=CARTESIAN_POINT('Ctrl Pts',(6.26784741197262,2.15248800203392,2.18493153433742));
#15633=CARTESIAN_POINT('Ctrl Pts',(6.19539972605475,2.18894680650264,2.18917166815084));
#15634=CARTESIAN_POINT('Ctrl Pts',(6.12308948400096,2.22533644328293,2.1934037578098));
#15635=CARTESIAN_POINT('Ctrl Pts',(6.04883926109604,2.25820703877901,2.19763584746876));
#15636=CARTESIAN_POINT('Ctrl Pts',(5.97302558958405,2.28734788858663,2.20186793712773));
#15637=CARTESIAN_POINT('Ctrl Pts',(5.89732027391604,2.31644708915984,2.20609397811977));
#15638=CARTESIAN_POINT('Ctrl Pts',(5.82005637780858,2.34182696605905,2.21032001911182));
#15639=CARTESIAN_POINT('Ctrl Pts',(5.74163391104989,2.36332322321835,2.21454606010386));
#15640=CARTESIAN_POINT('Ctrl Pts',(5.66318987356978,2.38482539309366,2.21877326350199));
#15641=CARTESIAN_POINT('Ctrl Pts',(5.58358705627131,2.40244162072258,2.22300046690013));
#15642=CARTESIAN_POINT('Ctrl Pts',(5.50324469600782,2.41605619294878,2.22722767029826));
#15643=CARTESIAN_POINT('Ctrl Pts',(5.42306815301729,2.42964266628378,2.23144614924098));
#15644=CARTESIAN_POINT('Ctrl Pts',(5.34215557068417,2.43924388332878,2.2356646281837));
#15645=CARTESIAN_POINT('Ctrl Pts',(5.26093578305467,2.44479548358981,2.23988310712642));
#15646=CARTESIAN_POINT('Ctrl Pts',(5.17974262926524,2.45034526335317,2.24410020273269));
#15647=CARTESIAN_POINT('Ctrl Pts',(5.09824293348796,2.45184803188112,2.24831729833895));
#15648=CARTESIAN_POINT('Ctrl Pts',(5.01687043383599,2.44929130831715,2.25253439394521));
#15649=CARTESIAN_POINT('Ctrl Pts',(4.93549971985879,2.44673464085907,2.25675139700962));
#15650=CARTESIAN_POINT('Ctrl Pts',(4.85425666088054,2.44011867417226,2.26096840007404));
#15651=CARTESIAN_POINT('Ctrl Pts',(4.77357333693884,2.42948301943583,2.26518540313846));
#15652=CARTESIAN_POINT('Ctrl Pts',(4.69255598238529,2.41880333287118,2.26941986468184));
#15653=CARTESIAN_POINT('Ctrl Pts',(4.61210347680974,2.40407065306822,2.27365432622522));
#15654=CARTESIAN_POINT('Ctrl Pts',(4.53264460451389,2.38537720172751,2.2778887877686));
#15655=CARTESIAN_POINT('Ctrl Pts',(4.45339861037261,2.36673383198636,2.28211190477194));
#15656=CARTESIAN_POINT('Ctrl Pts',(4.3751413700557,2.34415105539868,2.28633502177527));
#15657=CARTESIAN_POINT('Ctrl Pts',(4.29828281380327,2.31777036189285,2.2905581387786));
#15658=CARTESIAN_POINT('Ctrl Pts',(4.22111456036433,2.29128336888108,2.29479827259201));
#15659=CARTESIAN_POINT('Ctrl Pts',(4.14535672112151,2.26096797051491,2.29903840640541));
#15660=CARTESIAN_POINT('Ctrl Pts',(4.07140204223235,2.22701529807397,2.30327854021882));
#15661=CARTESIAN_POINT('Ctrl Pts',(3.99744736334318,2.19306262563304,2.30751867403222));
#15662=CARTESIAN_POINT('Ctrl Pts',(3.92529623052251,2.15547295021277,2.31175880784563));
#15663=CARTESIAN_POINT('Ctrl Pts',(3.85531311721876,2.11448178689164,2.31599894165903));
#15664=CARTESIAN_POINT('Ctrl Pts',(3.78546277212388,2.07356838980691,2.320231031318));
#15665=CARTESIAN_POINT('Ctrl Pts',(3.71751162249775,2.02911377346404,2.32446312097696));
#15666=CARTESIAN_POINT('Ctrl Pts',(3.65184120019895,1.98131944795627,2.32869521063593));
#15667=CARTESIAN_POINT('Ctrl Pts',(3.58626463661834,1.93359343195486,2.33292125162797));
#15668=CARTESIAN_POINT('Ctrl Pts',(3.52296269881717,1.88253745812461,2.33714729262002));
#15669=CARTESIAN_POINT('Ctrl Pts',(3.46229072743443,1.82839796927475,2.34137333361207));
#15670=CARTESIAN_POINT('Ctrl Pts',(3.40160206774487,1.77424358892919,2.3456005370102));
#15671=CARTESIAN_POINT('Ctrl Pts',(3.34354521018637,1.71700425552848,2.34982774040833));
#15672=CARTESIAN_POINT('Ctrl Pts',(3.28844516845862,1.65696895898379,2.35405494380647));
#15673=CARTESIAN_POINT('Ctrl Pts',(3.23345884679868,1.59705756829797,2.35827342274919));
#15674=CARTESIAN_POINT('Ctrl Pts',(3.18141748076242,1.53436206949908,2.36249190169191));
#15675=CARTESIAN_POINT('Ctrl Pts',(3.13260819768634,1.46920742228462,2.36671038063464));
#15676=CARTESIAN_POINT('Ctrl Pts',(3.08381492029897,1.40407414078046,2.3709274762409));
#15677=CARTESIAN_POINT('Ctrl Pts',(3.03825189944832,1.33648368393925,2.37514457184717));
#15678=CARTESIAN_POINT('Ctrl Pts',(2.99616538269479,1.26679332849066,2.37936166745343));
#15679=CARTESIAN_POINT('Ctrl Pts',(2.95407978950675,1.19710450235861,2.38357867051785));
#15680=CARTESIAN_POINT('Ctrl Pts',(2.91547078796965,1.12531626761467,2.38779567358227));
#15681=CARTESIAN_POINT('Ctrl Pts',(2.880540000536,1.0518128254965,2.39201267664669));
#15682=CARTESIAN_POINT('Ctrl Pts',(2.84546459892773,0.978005077624156,2.39624713819007));
#15683=CARTESIAN_POINT('Ctrl Pts',(2.81409814620306,0.902468310741889,2.40048159973345));
#15684=CARTESIAN_POINT('Ctrl Pts',(2.78659631431134,0.825612557852792,2.40471606127683));
#15685=CARTESIAN_POINT('Ctrl Pts',(2.75916816253928,0.748962709104628,2.40893917828017));
#15686=CARTESIAN_POINT('Ctrl Pts',(2.73558404662123,0.671001392178894,2.41316229528351));
#15687=CARTESIAN_POINT('Ctrl Pts',(2.71594803617511,0.592149596049576,2.41738541228684));
#15688=CARTESIAN_POINT('Ctrl Pts',(2.69623290354033,0.512980071086965,2.42162554610025));
#15689=CARTESIAN_POINT('Ctrl Pts',(2.68049784333027,0.4329133397623,2.42586567991365));
#15690=CARTESIAN_POINT('Ctrl Pts',(2.668795917416,0.352382951551585,2.43010581372705));
#15691=CARTESIAN_POINT('Ctrl Pts',(2.65709399150174,0.271852563340869,2.43434594754046));
#15692=CARTESIAN_POINT('Ctrl Pts',(2.64942518200458,0.190858989358771,2.43858608135386));
#15693=CARTESIAN_POINT('Ctrl Pts',(2.64578992844836,0.109836174363986,2.44282621516727));
#15694=CARTESIAN_POINT('Ctrl Pts',(2.64216157150021,0.0289670715079627,
2.44705830482623));
#15695=CARTESIAN_POINT('Ctrl Pts',(2.6425379274089,-0.0522328669521755,
2.45129039448519));
#15696=CARTESIAN_POINT('Ctrl Pts',(2.6469572506401,-0.133333862616963,2.45552248414415));
#15697=CARTESIAN_POINT('Ctrl Pts',(2.65137025760289,-0.214318945588759,
2.4597485251362));
#15698=CARTESIAN_POINT('Ctrl Pts',(2.65981473035322,-0.295204906503504,
2.46397456612824));
#15699=CARTESIAN_POINT('Ctrl Pts',(2.67227697172963,-0.375559526185646,
2.46820060712029));
#15700=CARTESIAN_POINT('Ctrl Pts',(2.68474264094436,-0.455936248043137,
2.47242781051842));
#15701=CARTESIAN_POINT('Ctrl Pts',(2.70122828366821,-0.535780869538314,
2.47665501391656));
#15702=CARTESIAN_POINT('Ctrl Pts',(2.72166800539679,-0.614663498838233,
2.48088221731469));
#15703=CARTESIAN_POINT('Ctrl Pts',(2.74206554192063,-0.693383323579882,
2.48510069625741));
#15704=CARTESIAN_POINT('Ctrl Pts',(2.76640075986744,-0.771144666907021,
2.48931917520013));
#15705=CARTESIAN_POINT('Ctrl Pts',(2.7945569789483,-0.847529884685807,2.49353765414286));
#15706=CARTESIAN_POINT('Ctrl Pts',(2.82270396495606,-0.923890053991391,
2.49775474974912));
#15707=CARTESIAN_POINT('Ctrl Pts',(2.85466930317223,-0.998874558242367,
2.50197184535538));
#15708=CARTESIAN_POINT('Ctrl Pts',(2.89028696632634,-1.07208249911243,2.50618894096164));
#15709=CARTESIAN_POINT('Ctrl Pts',(2.92590384787039,-1.14528883347444,2.51040594402606));
#15710=CARTESIAN_POINT('Ctrl Pts',(2.96517269066384,-1.21671826461455,2.51462294709048));
#15711=CARTESIAN_POINT('Ctrl Pts',(3.00788061081696,-1.28599271495624,2.51883995015489));
#15712=CARTESIAN_POINT('Ctrl Pts',(3.05076534263331,-1.35555396293968,2.52307441169827));
#15713=CARTESIAN_POINT('Ctrl Pts',(3.09711745153451,-1.42294194041319,2.52730887324165));
#15714=CARTESIAN_POINT('Ctrl Pts',(3.14667739375335,-1.48780309702345,2.53154333478503));
#15715=CARTESIAN_POINT('Ctrl Pts',(3.19610455999973,-1.552490484199,2.53576645178837));
#15716=CARTESIAN_POINT('Ctrl Pts',(3.24872205982453,-1.61466424210871,2.5399895687917));
#15717=CARTESIAN_POINT('Ctrl Pts',(3.30423310345922,-1.6740081777184,2.54421268579504));
#15718=CARTESIAN_POINT('Ctrl Pts',(3.35996782569094,-1.73359123634561,2.54845281960844));
#15719=CARTESIAN_POINT('Ctrl Pts',(3.41861911483808,-1.79032129774357,2.55269295342185));
#15720=CARTESIAN_POINT('Ctrl Pts',(3.47985191156118,-1.84391815493638,2.55693308723525));
#15721=CARTESIAN_POINT('Ctrl Pts',(3.54108470828428,-1.89751501212919,2.56117322104866));
#15722=CARTESIAN_POINT('Ctrl Pts',(3.60489860743148,-1.94797842403459,2.56541335486206));
#15723=CARTESIAN_POINT('Ctrl Pts',(3.6709296133877,-1.99507213773944,2.56965348867547));
#15724=CARTESIAN_POINT('Ctrl Pts',(3.73683534886111,-2.0420765077766,2.57388557833443));
#15725=CARTESIAN_POINT('Ctrl Pts',(3.80519565810401,-2.08589933025433,2.57811766799339));
#15726=CARTESIAN_POINT('Ctrl Pts',(3.8756705980363,-2.12627487677921,2.58234975765236));
#15727=CARTESIAN_POINT('Ctrl Pts',(3.94604481244714,-2.16659271700477,2.5865757986444));
#15728=CARTESIAN_POINT('Ctrl Pts',(4.01852725507039,-2.20347283772714,2.59080183963645));
#15729=CARTESIAN_POINT('Ctrl Pts',(4.0927476942418,-2.2366917897513,2.59502788062849));
#15730=CARTESIAN_POINT('Ctrl Pts',(4.1669885483336,-2.26991987891165,2.59925508402663));
#15731=CARTESIAN_POINT('Ctrl Pts',(4.24296796032467,-2.29948453604172,2.60348228742476));
#15732=CARTESIAN_POINT('Ctrl Pts',(4.32028927855364,-2.3252073892455,2.60770949082289));
#15733=CARTESIAN_POINT('Ctrl Pts',(4.39745101458852,-2.35087715347658,2.61192796976561));
#15734=CARTESIAN_POINT('Ctrl Pts',(4.47594869025042,-2.37272078559758,2.61614644870834));
#15735=CARTESIAN_POINT('Ctrl Pts',(4.55536832789653,-2.39060919872454,2.62036492765106));
#15736=CARTESIAN_POINT('Ctrl Pts',(4.63476192201321,-2.40849174582859,2.62458202325732));
#15737=CARTESIAN_POINT('Ctrl Pts',(4.71507642472786,-2.42242154764815,2.62879911886358));
#15738=CARTESIAN_POINT('Ctrl Pts',(4.79588509004015,-2.43232003972698,2.63301621446985));
#15739=CARTESIAN_POINT('Ctrl Pts',(4.87669198205073,-2.44221831458884,2.63723321753426));
#15740=CARTESIAN_POINT('Ctrl Pts',(4.957992553717,-2.44808540024345,2.64145022059868));
#15741=CARTESIAN_POINT('Ctrl Pts',(5.03935374343876,-2.44989446658086,2.6456672236631));
#15742=CARTESIAN_POINT('Ctrl Pts',(5.12105177015058,-2.45171102248992,2.64990168520648));
#15743=CARTESIAN_POINT('Ctrl Pts',(5.20281044650658,-2.44943586357772,2.65413614674986));
#15744=CARTESIAN_POINT('Ctrl Pts',(5.28419193459196,-2.44309465655005,2.65837060829325));
#15745=CARTESIAN_POINT('Ctrl Pts',(5.36535539364545,-2.43677043824134,2.66259372529658));
#15746=CARTESIAN_POINT('Ctrl Pts',(5.44614322436628,-2.42640203104198,2.66681684229992));
#15747=CARTESIAN_POINT('Ctrl Pts',(5.52612869875607,-2.41206667106402,2.67103995930325));
#15748=CARTESIAN_POINT('Ctrl Pts',(5.60643647007138,-2.39767354756735,2.67528009311666));
#15749=CARTESIAN_POINT('Ctrl Pts',(5.68593494793452,-2.37928154924512,2.67952022693006));
#15750=CARTESIAN_POINT('Ctrl Pts',(5.76420680689366,-2.35701959536497,2.68376036074347));
#15751=CARTESIAN_POINT('Ctrl Pts',(5.84247866585281,-2.33475764148481,2.68800049455688));
#15752=CARTESIAN_POINT('Ctrl Pts',(5.91952348332117,-2.30862594106609,2.69224062837029));
#15753=CARTESIAN_POINT('Ctrl Pts',(5.99494509779225,-2.27880159381954,2.6964807621837));
#15754=CARTESIAN_POINT('Ctrl Pts',(6.07022362642169,-2.24903382772491,2.70071285184266));
#15755=CARTESIAN_POINT('Ctrl Pts',(6.14416596005127,-2.21547637032557,2.70494494150162));
#15756=CARTESIAN_POINT('Ctrl Pts',(6.21636427122024,-2.17827011036859,2.70917703116058));
#15757=CARTESIAN_POINT('Ctrl Pts',(6.28845939375874,-2.14111702704343,2.71340307215263));
#15758=CARTESIAN_POINT('Ctrl Pts',(6.35881503484576,-2.10032570982552,2.71762911314467));
#15759=CARTESIAN_POINT('Ctrl Pts',(6.42704239006815,-2.05608545255064,2.72185515413672));
#15760=CARTESIAN_POINT('Ctrl Pts',(6.49528851176561,-2.01183302664219,2.72608235753485));
#15761=CARTESIAN_POINT('Ctrl Pts',(6.56140475299464,-1.96412995919919,2.73030956093299));
#15762=CARTESIAN_POINT('Ctrl Pts',(6.62502578388396,-1.91321222301434,2.73453676433112));
#15763=CARTESIAN_POINT('Ctrl Pts',(6.68851550837637,-1.86239957510586,2.73875524327384));
#15764=CARTESIAN_POINT('Ctrl Pts',(6.74951993344176,-1.80838578546842,2.74297372221657));
#15765=CARTESIAN_POINT('Ctrl Pts',(6.80770567885512,-1.75144815995831,2.74719220115929));
#15766=CARTESIAN_POINT('Ctrl Pts',(6.86587234382169,-1.6945292056077,2.75140929676555));
#15767=CARTESIAN_POINT('Ctrl Pts',(6.92122183286099,-1.63468864421221,2.75562639237181));
#15768=CARTESIAN_POINT('Ctrl Pts',(6.97345623146411,-1.57224196185385,2.75984348797808));
#15769=CARTESIAN_POINT('Ctrl Pts',(7.02568948381206,-1.50979664985361,2.7640604910425));
#15770=CARTESIAN_POINT('Ctrl Pts',(7.07480748437652,-1.44474568777084,2.76827749410692));
#15771=CARTESIAN_POINT('Ctrl Pts',(7.1205523091914,-1.37743798452217,2.77249449717133));
#15772=CARTESIAN_POINT('Ctrl Pts',(7.16648651851691,-1.309851626005,2.77672895871472));
#15773=CARTESIAN_POINT('Ctrl Pts',(7.20901928670969,-1.23999018358204,2.78096342025809));
#15774=CARTESIAN_POINT('Ctrl Pts',(7.24793415705625,-1.16823511145844,2.78519788180148));
#15775=CARTESIAN_POINT('Ctrl Pts',(7.28674477062765,-1.09667227824904,2.78942099880481));
#15776=CARTESIAN_POINT('Ctrl Pts',(7.3219566819964,-1.02322638824702,2.79364411580814));
#15777=CARTESIAN_POINT('Ctrl Pts',(7.35340275872267,-0.948297602606365,
2.79786723281148));
#15778=CARTESIAN_POINT('Ctrl Pts',(7.38497554562883,-0.873066895680292,
2.80210736662488));
#15779=CARTESIAN_POINT('Ctrl Pts',(7.41275193301665,-0.796341763627506,
2.80634750043829));
#15780=CARTESIAN_POINT('Ctrl Pts',(7.4366132801029,-0.718542569475471,2.81058763425169));
#15781=CARTESIAN_POINT('Ctrl Pts',(7.46047462718915,-0.640743375323441,
2.8148277680651));
#15782=CARTESIAN_POINT('Ctrl Pts',(7.48042087970566,-0.561870587392187,
2.8190679018785));
#15783=CARTESIAN_POINT('Ctrl Pts',(7.49638534176926,-0.482352994564428,
2.82330803569191));
#15784=CARTESIAN_POINT('Ctrl Pts',(7.51922595399613,-0.368585897636371,
2.82937446322553));
#15785=CARTESIAN_POINT('Ctrl Pts',(7.53399165590758,-0.253147670603014,
2.83544089075915));
#15786=CARTESIAN_POINT('Ctrl Pts',(7.54049542395752,-0.136984064378373,
2.84150731829277));
#15787=CARTESIAN_POINT('Ctrl Pts',(7.5430068767487,-0.0921270813424802,
2.84384989051318));
#15788=CARTESIAN_POINT('Ctrl Pts',(7.54428681030232,-0.0471621918703228,
2.84619246273358));
#15789=CARTESIAN_POINT('Ctrl Pts',(7.54432621659438,-0.00214507476057291,
2.84853503495399));
#15790=CARTESIAN_POINT('',(7.54393141126483,8.94937218200234E-5,3.64853504140039));
#15791=CARTESIAN_POINT('Ctrl Pts',(7.54432621659511,-0.0021450739361722,
2.84853503499689));
#15792=CARTESIAN_POINT('Ctrl Pts',(7.54439742906591,0.0792069437731955,
2.85276837975536));
#15793=CARTESIAN_POINT('Ctrl Pts',(7.54041302387129,0.160689976852925,2.85700172451383));
#15794=CARTESIAN_POINT('Ctrl Pts',(7.53236234262213,0.241860271517619,2.86123506927229));
#15795=CARTESIAN_POINT('Ctrl Pts',(7.52445196900469,0.321615926668091,2.86539463510958));
#15796=CARTESIAN_POINT('Ctrl Pts',(7.51261596087071,0.401069158613188,2.86955420094686));
#15797=CARTESIAN_POINT('Ctrl Pts',(7.49689665975846,0.47979913242696,2.87371376678415));
#15798=CARTESIAN_POINT('Ctrl Pts',(7.48118511182867,0.558490274498245,2.87787128101158));
#15799=CARTESIAN_POINT('Ctrl Pts',(7.4615941642831,0.636458396846369,2.88202879523902));
#15800=CARTESIAN_POINT('Ctrl Pts',(7.4382176456193,0.713290599698551,2.88618630946646));
#15801=CARTESIAN_POINT('Ctrl Pts',(7.4148450175322,0.790110015292633,2.89034313175476));
#15802=CARTESIAN_POINT('Ctrl Pts',(7.38768820935883,0.86579342840745,2.89449995404307));
#15803=CARTESIAN_POINT('Ctrl Pts',(7.35689109022833,0.93994248607013,2.89865677633138));
#15804=CARTESIAN_POINT('Ctrl Pts',(7.32510818814065,1.01646497603422,2.90294665407044));
#15805=CARTESIAN_POINT('Ctrl Pts',(7.28944814638991,1.09135270273379,2.9072365318095));
#15806=CARTESIAN_POINT('Ctrl Pts',(7.2501222516031,1.16419143972094,2.91152640954857));
#15807=CARTESIAN_POINT('Ctrl Pts',(7.21196864925906,1.23485887707526,2.9156884073937));
#15808=CARTESIAN_POINT('Ctrl Pts',(7.17036499723827,1.30359738498866,2.91985040523883));
#15809=CARTESIAN_POINT('Ctrl Pts',(7.12554925654204,1.3700567703372,2.92401240308397));
#15810=CARTESIAN_POINT('Ctrl Pts',(7.07866802985336,1.43957916273128,2.92836622077));
#15811=CARTESIAN_POINT('Ctrl Pts',(7.028271843264,1.50660680265626,2.93272003845602));
#15812=CARTESIAN_POINT('Ctrl Pts',(6.97467977651935,1.57077804537378,2.93707385614205));
#15813=CARTESIAN_POINT('Ctrl Pts',(6.9210877097747,1.6349492880913,2.94142767382807));
#15814=CARTESIAN_POINT('Ctrl Pts',(6.86430022451701,1.69626375536157,2.9457814915141));
#15815=CARTESIAN_POINT('Ctrl Pts',(6.80467773584327,1.75440603669123,2.95013530920012));
#15816=CARTESIAN_POINT('Ctrl Pts',(6.7467222273782,1.81092272280643,2.95436739885909));
#15817=CARTESIAN_POINT('Ctrl Pts',(6.6858551205809,1.86466997352527,2.95859948851805));
#15818=CARTESIAN_POINT('Ctrl Pts',(6.62237179651115,1.91533326872707,2.96283157817702));
#15819=CARTESIAN_POINT('Ctrl Pts',(6.55897920527397,1.96592415397953,2.96705761916906));
#15820=CARTESIAN_POINT('Ctrl Pts',(6.49297818339017,2.01343955046757,2.9712836601611));
#15821=CARTESIAN_POINT('Ctrl Pts',(6.42470050117019,2.05760209653369,2.97550970115314));
#15822=CARTESIAN_POINT('Ctrl Pts',(6.35640403863222,2.10177678985834,2.97973690455128));
#15823=CARTESIAN_POINT('Ctrl Pts',(6.28583001538864,2.14259648168644,2.98396410794941));
#15824=CARTESIAN_POINT('Ctrl Pts',(6.21334319503753,2.17982432482831,2.98819131134754));
#15825=CARTESIAN_POINT('Ctrl Pts',(6.14100597904003,2.21697533403841,2.99240979029027));
#15826=CARTESIAN_POINT('Ctrl Pts',(6.0667642555964,2.25054907152295,2.99662826923299));
#15827=CARTESIAN_POINT('Ctrl Pts',(5.99100743671978,2.28035475154772,3.00084674817572));
#15828=CARTESIAN_POINT('Ctrl Pts',(5.91527546024984,2.31015065760316,3.00506384378198));
#15829=CARTESIAN_POINT('Ctrl Pts',(5.83802980710525,2.3361807900522,3.00928093938825));
#15830=CARTESIAN_POINT('Ctrl Pts',(5.7596802224845,2.35830234345066,3.01349803499451));
#15831=CARTESIAN_POINT('Ctrl Pts',(5.68133235720246,2.38042341140376,3.01771503805893));
#15832=CARTESIAN_POINT('Ctrl Pts',(5.60188105612782,2.39863594568312,3.02193204112334));
#15833=CARTESIAN_POINT('Ctrl Pts',(5.52175020561148,2.41284730414984,3.02614904418776));
#15834=CARTESIAN_POINT('Ctrl Pts',(5.44128761173451,2.42711749793138,3.03038350573114));
#15835=CARTESIAN_POINT('Ctrl Pts',(5.36014029203784,2.4373532203585,3.03461796727452));
#15836=CARTESIAN_POINT('Ctrl Pts',(5.27874486921614,2.44351298116803,3.0388524288179));
#15837=CARTESIAN_POINT('Ctrl Pts',(5.19756751275883,2.44965623937091,3.04307554582124));
#15838=CARTESIAN_POINT('Ctrl Pts',(5.11614384934191,2.45174537703917,3.04729866282457));
#15839=CARTESIAN_POINT('Ctrl Pts',(5.03490739645519,2.44979156501112,3.05152177982791));
#15840=CARTESIAN_POINT('Ctrl Pts',(4.95334360589618,2.44782988020849,3.05576191364131));
#15841=CARTESIAN_POINT('Ctrl Pts',(4.8719690072782,2.4417926387357,3.06000204745472));
#15842=CARTESIAN_POINT('Ctrl Pts',(4.79121571760324,2.43174352423985,3.06424218126812));
#15843=CARTESIAN_POINT('Ctrl Pts',(4.71046242792827,2.42169440974399,3.06848231508153));
#15844=CARTESIAN_POINT('Ctrl Pts',(4.6303308967439,2.4076335642661,3.07272244889494));
#15845=CARTESIAN_POINT('Ctrl Pts',(4.55123968223925,2.38967551854041,3.07696258270834));
#15846=CARTESIAN_POINT('Ctrl Pts',(4.4722985153445,2.37175154185586,3.08119467236731));
#15847=CARTESIAN_POINT('Ctrl Pts',(4.394099204526,2.34987828336001,3.08542676202628));
#15848=CARTESIAN_POINT('Ctrl Pts',(4.31706630786371,2.32413270611904,3.08965885168525));
#15849=CARTESIAN_POINT('Ctrl Pts',(4.2401435096094,2.29842392545705,3.09388489267729));
#15850=CARTESIAN_POINT('Ctrl Pts',(4.1643842515435,2.26885396417144,3.09811093366934));
#15851=CARTESIAN_POINT('Ctrl Pts',(4.09020168302746,2.23555052752077,3.10233697466138));
#15852=CARTESIAN_POINT('Ctrl Pts',(4.01599871000768,2.20223793049575,3.10656417805951));
#15853=CARTESIAN_POINT('Ctrl Pts',(3.94337374263367,2.16518993309172,3.11079138145764));
#15854=CARTESIAN_POINT('Ctrl Pts',(3.87272385868278,2.124583956594,3.11501858485578));
#15855=CARTESIAN_POINT('Ctrl Pts',(3.8022197878627,2.08406178610179,3.1192370637985));
#15856=CARTESIAN_POINT('Ctrl Pts',(3.73368307129303,2.03999651825496,3.12345554274123));
#15857=CARTESIAN_POINT('Ctrl Pts',(3.66748552315288,1.99261130127456,3.12767402168395));
#15858=CARTESIAN_POINT('Ctrl Pts',(3.60130968271429,1.9452416229988,3.13189111729022));
#15859=CARTESIAN_POINT('Ctrl Pts',(3.53747186494676,1.89455442789271,3.13610821289648));
#15860=CARTESIAN_POINT('Ctrl Pts',(3.47631466416858,1.8408160121366,3.14032530850274));
#15861=CARTESIAN_POINT('Ctrl Pts',(3.41515880545153,1.78707877564047,3.14454231156717));
#15862=CARTESIAN_POINT('Ctrl Pts',(3.35668379508049,1.73029075921571,3.14875931463159));
#15863=CARTESIAN_POINT('Ctrl Pts',(3.30119780931436,1.67075739632124,3.15297631769601));
#15864=CARTESIAN_POINT('Ctrl Pts',(3.24548211043202,1.61097756408647,3.15721077923939));
#15865=CARTESIAN_POINT('Ctrl Pts',(3.19278056921847,1.54842994173943,3.16144524078277));
#15866=CARTESIAN_POINT('Ctrl Pts',(3.14336535048291,1.48345845824964,3.16567970232615));
#15867=CARTESIAN_POINT('Ctrl Pts',(3.09408251999131,1.41866103977113,3.16990281932948));
#15868=CARTESIAN_POINT('Ctrl Pts',(3.04806865587466,1.35145314016491,3.17412593633281));
#15869=CARTESIAN_POINT('Ctrl Pts',(3.00555003355331,1.28220470758373,3.17834905333615));
#15870=CARTESIAN_POINT('Ctrl Pts',(2.9628600848586,1.21267724237716,3.18258918714955));
#15871=CARTESIAN_POINT('Ctrl Pts',(2.9236938239047,1.14109318278484,3.18682932096295));
#15872=CARTESIAN_POINT('Ctrl Pts',(2.8882326878449,1.06784984639978,3.19106945477635));
#15873=CARTESIAN_POINT('Ctrl Pts',(2.85277155178509,0.99460651001471,3.19530958858976));
#15874=CARTESIAN_POINT('Ctrl Pts',(2.82101566576165,0.919704351378521,3.19954972240316));
#15875=CARTESIAN_POINT('Ctrl Pts',(2.79309641776494,0.843556946896211,3.20378985621656));
#15876=CARTESIAN_POINT('Ctrl Pts',(2.76523013666798,0.767554005185249,3.20802194587553));
#15877=CARTESIAN_POINT('Ctrl Pts',(2.74108197119413,0.690026992125537,3.2122540355345));
#15878=CARTESIAN_POINT('Ctrl Pts',(2.72081810344039,0.61137409911254,3.21648612519346));
#15879=CARTESIAN_POINT('Ctrl Pts',(2.70058319759349,0.53283361986914,3.22071216618551));
#15880=CARTESIAN_POINT('Ctrl Pts',(2.68422167837404,0.453170902855609,3.22493820717756));
#15881=CARTESIAN_POINT('Ctrl Pts',(2.67185093551005,0.372802145957223,3.22916424816961));
#15882=CARTESIAN_POINT('Ctrl Pts',(2.65947678997514,0.292411282995037,3.23339145156774));
#15883=CARTESIAN_POINT('Ctrl Pts',(2.65109575197378,0.211314438421757,3.23761865496587));
#15884=CARTESIAN_POINT('Ctrl Pts',(2.64677474554041,0.129941345000103,3.241845858364));
#15885=CARTESIAN_POINT('Ctrl Pts',(2.64246265716099,0.048736196164606,3.24606433730672));
#15886=CARTESIAN_POINT('Ctrl Pts',(2.64219390782992,-0.0327435996276477,
3.25028281624944));
#15887=CARTESIAN_POINT('Ctrl Pts',(2.64598330755778,-0.11406465850992,3.25450129519216));
#15888=CARTESIAN_POINT('Ctrl Pts',(2.64977146465415,-0.195359050343041,
3.25871839079843));
#15889=CARTESIAN_POINT('Ctrl Pts',(2.65761510642675,-0.276494344813367,
3.26293548640469));
#15890=CARTESIAN_POINT('Ctrl Pts',(2.66947694299597,-0.357038229548362,
3.26715258201096));
#15891=CARTESIAN_POINT('Ctrl Pts',(2.68133851926371,-0.437580346792089,
3.27136958507538));
#15892=CARTESIAN_POINT('Ctrl Pts',(2.69721804616655,-0.517530620542038,
3.2755865881398));
#15893=CARTESIAN_POINT('Ctrl Pts',(2.71702667468682,-0.596464353192318,
3.27980359120422));
#15894=CARTESIAN_POINT('Ctrl Pts',(2.73691731133442,-0.675724873110627,
3.2840380527476));
#15895=CARTESIAN_POINT('Ctrl Pts',(2.76076954967438,-0.753959956249378,
3.28827251429097));
#15896=CARTESIAN_POINT('Ctrl Pts',(2.78844265408719,-0.830754206045222,
3.29250697583435));
#15897=CARTESIAN_POINT('Ctrl Pts',(2.81604161952438,-0.907342716472999,
3.29673009283769));
#15898=CARTESIAN_POINT('Ctrl Pts',(2.84744078598369,-0.982497688404951,
3.30095320984103));
#15899=CARTESIAN_POINT('Ctrl Pts',(2.88245263387824,-1.0558280993275,3.30517632684436));
#15900=CARTESIAN_POINT('Ctrl Pts',(2.91760556002501,-1.12945399097527,3.30941646065776));
#15901=CARTESIAN_POINT('Ctrl Pts',(2.9564001115301,-1.20124017598565,3.31365659447117));
#15902=CARTESIAN_POINT('Ctrl Pts',(2.99860142286126,-1.27081838965485,3.31789672828457));
#15903=CARTESIAN_POINT('Ctrl Pts',(3.04080273419242,-1.34039660332405,3.32213686209797));
#15904=CARTESIAN_POINT('Ctrl Pts',(3.08641049185188,-1.407766493533,3.32637699591137));
#15905=CARTESIAN_POINT('Ctrl Pts',(3.13514897760215,-1.47259296671226,3.33061712972477));
#15906=CARTESIAN_POINT('Ctrl Pts',(3.1837949993115,-1.5372964545838,3.33484921938374));
#15907=CARTESIAN_POINT('Ctrl Pts',(3.23574135673279,-1.59970757218609,3.3390813090427));
#15908=CARTESIAN_POINT('Ctrl Pts',(3.29074415854742,-1.65947038427012,3.34331339870166));
#15909=CARTESIAN_POINT('Ctrl Pts',(3.34566834822122,-1.71914778102173,3.3475394396937));
#15910=CARTESIAN_POINT('Ctrl Pts',(3.40363999413734,-1.77618405073565,3.35176548068574));
#15911=CARTESIAN_POINT('Ctrl Pts',(3.46437356851543,-1.83025442439458,3.35599152167778));
#15912=CARTESIAN_POINT('Ctrl Pts',(3.52512384814491,-1.88433967053869,3.36021872507591));
#15913=CARTESIAN_POINT('Ctrl Pts',(3.58863727450732,-1.93545703226086,3.36444592847404));
#15914=CARTESIAN_POINT('Ctrl Pts',(3.65458952705235,-1.98331674197425,3.36867313187218));
#15915=CARTESIAN_POINT('Ctrl Pts',(3.72040566183053,-2.0310776748217,3.3728916108149));
#15916=CARTESIAN_POINT('Ctrl Pts',(3.78865020450101,-2.0755940958847,3.37711008975762));
#15917=CARTESIAN_POINT('Ctrl Pts',(3.8589674417565,-2.11661799517276,3.38132856870035));
#15918=CARTESIAN_POINT('Ctrl Pts',(3.92926162036955,-2.15762844177891,3.38554566430662));
#15919=CARTESIAN_POINT('Ctrl Pts',(4.00162674271203,-2.19514840704296,3.38976275991289));
#15920=CARTESIAN_POINT('Ctrl Pts',(4.07567967434794,-2.22897419382083,3.39397985551915));
#15921=CARTESIAN_POINT('Ctrl Pts',(4.14973098093277,-2.2627992383103,3.39819685858357));
#15922=CARTESIAN_POINT('Ctrl Pts',(4.22546960001136,-2.29293007346957,3.40241386164798));
#15923=CARTESIAN_POINT('Ctrl Pts',(4.30249076210233,-2.31921041791352,3.4066308647124));
#15924=CARTESIAN_POINT('Ctrl Pts',(4.37983079338029,-2.34559956352118,3.41086532625578));
#15925=CARTESIAN_POINT('Ctrl Pts',(4.45846356743373,-2.36810610373114,3.41509978779916));
#15926=CARTESIAN_POINT('Ctrl Pts',(4.53796391712025,-2.38662236440332,3.41933424934254));
#15927=CARTESIAN_POINT('Ctrl Pts',(4.61725127753017,-2.40508901818721,3.42355736634588));
#15928=CARTESIAN_POINT('Ctrl Pts',(4.69740110343072,-2.41958670312452,3.42778048334921));
#15929=CARTESIAN_POINT('Ctrl Pts',(4.77798325534482,-2.43006026278452,3.43200360035255));
#15930=CARTESIAN_POINT('Ctrl Pts',(4.85889010846263,-2.44057602505823,3.43624373416596));
#15931=CARTESIAN_POINT('Ctrl Pts',(4.94023230836447,-2.44703513490168,3.44048386797936));
#15932=CARTESIAN_POINT('Ctrl Pts',(5.02157308115603,-2.44943454673675,3.44472400179277));
#15933=CARTESIAN_POINT('Ctrl Pts',(5.10291385394758,-2.45183395857182,3.44896413560618));
#15934=CARTESIAN_POINT('Ctrl Pts',(5.18425273366396,-2.45017374412986,3.45320426941959));
#15935=CARTESIAN_POINT('Ctrl Pts',(5.26515858208952,-2.4445031790216,3.45744440323299));
#15936=CARTESIAN_POINT('Ctrl Pts',(5.34591094027892,-2.43884337180533,3.46167649289195));
#15937=CARTESIAN_POINT('Ctrl Pts',(5.42653318044008,-2.42916731676783,3.46590858255091));
#15938=CARTESIAN_POINT('Ctrl Pts',(5.50659397124848,-2.41548624624073,3.47014067220987));
#15939=CARTESIAN_POINT('Ctrl Pts',(5.58654033606505,-2.40182472923102,3.47436671320191));
#15940=CARTESIAN_POINT('Ctrl Pts',(5.66592639105071,-2.38416964308185,3.47859275419396));
#15941=CARTESIAN_POINT('Ctrl Pts',(5.74432433169587,-2.3625841093388,3.482818795186));
#15942=CARTESIAN_POINT('Ctrl Pts',(5.82274383631637,-2.3409926383235,3.48704599858413));
#15943=CARTESIAN_POINT('Ctrl Pts',(5.9001742198754,-2.31546861631229,3.49127320198227));
#15944=CARTESIAN_POINT('Ctrl Pts',(5.97619596955483,-2.28612675193234,3.4955004053804));
#15945=CARTESIAN_POINT('Ctrl Pts',(6.05206081919819,-2.25684544574263,3.49971888432312));
#15946=CARTESIAN_POINT('Ctrl Pts',(6.12652240111848,-2.22376218462051,3.50393736326584));
#15947=CARTESIAN_POINT('Ctrl Pts',(6.19917918752779,-2.18704072554408,3.50815584220856));
#15948=CARTESIAN_POINT('Ctrl Pts',(6.27181214810253,-2.1503313082803,3.51237293781482));
#15949=CARTESIAN_POINT('Ctrl Pts',(6.34264107408638,-2.10998627179487,3.51659003342108));
#15950=CARTESIAN_POINT('Ctrl Pts',(6.4112867263889,-2.06621647678787,3.52080712902735));
#15951=CARTESIAN_POINT('Ctrl Pts',(6.47993087230009,-2.02244764228511,3.52502413209175));
#15952=CARTESIAN_POINT('Ctrl Pts',(6.5463914485901,-1.97525444948679,3.52924113515616));
#15953=CARTESIAN_POINT('Ctrl Pts',(6.61031725452029,-1.9248916929093,3.53345813822056));
#15954=CARTESIAN_POINT('Ctrl Pts',(6.67450771459521,-1.87432043348895,3.53769259976395));
#15955=CARTESIAN_POINT('Ctrl Pts',(6.73614199302411,-1.82055359212623,3.54192706130733));
#15956=CARTESIAN_POINT('Ctrl Pts',(6.79489860012048,-1.76388950621553,3.54616152285072));
#15957=CARTESIAN_POINT('Ctrl Pts',(6.85349779247216,-1.70737722897892,3.55038463985405));
#15958=CARTESIAN_POINT('Ctrl Pts',(6.90923442299243,-1.64798358050816,3.55460775685739));
#15959=CARTESIAN_POINT('Ctrl Pts',(6.96182838023185,-1.58603961937434,3.55883087386072));
#15960=CARTESIAN_POINT('Ctrl Pts',(7.01463426183454,-1.52384605856767,3.56307100767413));
#15961=CARTESIAN_POINT('Ctrl Pts',(7.06427181029833,-1.45908196846079,3.56731114148755));
#15962=CARTESIAN_POINT('Ctrl Pts',(7.11050104743682,-1.39211230272247,3.57155127530096));
#15963=CARTESIAN_POINT('Ctrl Pts',(7.15673028457532,-1.32514263698415,3.57579140911438));
#15964=CARTESIAN_POINT('Ctrl Pts',(7.19955101730721,-1.25596782571705,3.5800315429278));
#15965=CARTESIAN_POINT('Ctrl Pts',(7.23877024704368,-1.18497653303257,3.58427167674121));
#15966=CARTESIAN_POINT('Ctrl Pts',(7.27979763224545,-1.11071227209454,3.58870729682959));
#15967=CARTESIAN_POINT('Ctrl Pts',(7.31702493902605,-1.03420556025214,3.59314291691798));
#15968=CARTESIAN_POINT('Ctrl Pts',(7.35021345270096,-0.95586145836733,3.59757853700636));
#15969=CARTESIAN_POINT('Ctrl Pts',(7.38331144713053,-0.877731034294349,
3.60200205926515));
#15970=CARTESIAN_POINT('Ctrl Pts',(7.41239243550695,-0.797773568688574,
3.60642558152394));
#15971=CARTESIAN_POINT('Ctrl Pts',(7.43726394308904,-0.716417666137985,
3.61084910378273));
#15972=CARTESIAN_POINT('Ctrl Pts',(7.46209503840575,-0.635193954059309,
3.6152654385176));
#15973=CARTESIAN_POINT('Ctrl Pts',(7.48273014165557,-0.552576704786469,
3.61968177325247));
#15974=CARTESIAN_POINT('Ctrl Pts',(7.49902488252049,-0.469014012274587,
3.62409810798735));
#15975=CARTESIAN_POINT('Ctrl Pts',(7.51528614811596,-0.38562298764449,3.62850536997928));
#15976=CARTESIAN_POINT('Ctrl Pts',(7.52722473537349,-0.301290779277856,
3.63291263197121));
#15977=CARTESIAN_POINT('Ctrl Pts',(7.53474649504544,-0.216478700116522,
3.63731989396313));
#15978=CARTESIAN_POINT('Ctrl Pts',(7.54112669174313,-0.144538386813589,
3.64105827429342));
#15979=CARTESIAN_POINT('Ctrl Pts',(7.54432979256689,-0.0722532055566229,
3.6447966546237));
#15980=CARTESIAN_POINT('Ctrl Pts',(7.54432715382295,8.93836134977417E-5,
3.64853503495399));
#15981=CARTESIAN_POINT('',(7.54548616237095,0.00208864728292292,4.44853503495399));
#15982=CARTESIAN_POINT('Ctrl Pts',(7.54033669847616,9.04938866648818E-5,
3.64853509995607));
#15983=CARTESIAN_POINT('Ctrl Pts',(7.54046775454349,0.402997660035618,3.66938971672052));
#15984=CARTESIAN_POINT('Ctrl Pts',(7.2558289127575,1.62248954264943,3.73252009132105));
#15985=CARTESIAN_POINT('Ctrl Pts',(5.33475743839734,2.88488253211185,3.83792622375765));
#15986=CARTESIAN_POINT('Ctrl Pts',(2.80334611963393,1.77039296481798,3.96475349726585));
#15987=CARTESIAN_POINT('Ctrl Pts',(2.36277430168313,-0.960179636963284,
4.09158077077408));
#15988=CARTESIAN_POINT('Ctrl Pts',(4.41521294580189,-2.81426320371486,4.21840804428229));
#15989=CARTESIAN_POINT('Ctrl Pts',(6.92189640647373,-2.1435844429306,4.33739279900894));
#15990=CARTESIAN_POINT('Ctrl Pts',(7.5395029472068,-0.659618059205427,4.4141017958995));
#15991=CARTESIAN_POINT('Ctrl Pts',(7.54548616237095,0.00208864728292292,
4.44853503495399));
#15992=CARTESIAN_POINT('',(7.5469083499403,-0.00161708351646295,5.248535034954));
#15993=CARTESIAN_POINT('Ctrl Pts',(7.54548616237095,0.00208864728292292,
4.44853503495399));
#15994=CARTESIAN_POINT('Ctrl Pts',(7.54684890019601,0.152799048512293,4.45637755373557));
#15995=CARTESIAN_POINT('Ctrl Pts',(7.46563602800205,1.11446190020873,4.50649583035324));
#15996=CARTESIAN_POINT('Ctrl Pts',(6.1942094107571,2.67763954212219,4.59888986480693));
#15997=CARTESIAN_POINT('Ctrl Pts',(3.44447846030825,2.37912662696793,4.72571713831517));
#15998=CARTESIAN_POINT('Ctrl Pts',(2.20033666274626,-0.0911449062707706,
4.85254441182336));
#15999=CARTESIAN_POINT('Ctrl Pts',(3.59748467407956,-2.47821585092194,4.97937168533159));
#16000=CARTESIAN_POINT('Ctrl Pts',(6.36055186041318,-2.60307570907344,5.1061989588398));
#16001=CARTESIAN_POINT('Ctrl Pts',(7.49721259379224,-1.01042400560164,5.19592007538061));
#16002=CARTESIAN_POINT('Ctrl Pts',(7.54766539424022,-0.100812118607445,
5.24336543408534));
#16003=CARTESIAN_POINT('Ctrl Pts',(7.5469083499403,-0.00161708351646295,
5.248535034954));
#16004=CARTESIAN_POINT('',(7.54409000407149,-0.000907487779776068,6.04853499257024));
#16005=CARTESIAN_POINT('Ctrl Pts',(7.5469083499403,-0.00161708351646295,
5.248535034954));
#16006=CARTESIAN_POINT('Ctrl Pts',(7.54147446725997,0.710381122145878,5.28564119192141));
#16007=CARTESIAN_POINT('Ctrl Pts',(6.84050798882477,2.24289643598352,5.36502310672491));
#16008=CARTESIAN_POINT('Ctrl Pts',(4.2394355735632,2.76597354472522,5.48668077936444));
#16009=CARTESIAN_POINT('Ctrl Pts',(2.30775737354188,0.786390358311311,5.61350805287268));
#16010=CARTESIAN_POINT('Ctrl Pts',(2.91931121122073,-1.91104030140742,5.74033532638088));
#16011=CARTESIAN_POINT('Ctrl Pts',(5.5158471379227,-2.86399960888975,5.86716259988912));
#16012=CARTESIAN_POINT('Ctrl Pts',(7.30705098429824,-1.51821911474262,5.96989561711511));
#16013=CARTESIAN_POINT('Ctrl Pts',(7.54182188154817,-0.352067409384865,
6.03035287650504));
#16014=CARTESIAN_POINT('Ctrl Pts',(7.54065403856044,-0.000918084752164947,
6.0485343780589));
#16015=CARTESIAN_POINT('',(7.5443261628818,0.00220558177830445,6.84853503499609));
#16016=CARTESIAN_POINT('Ctrl Pts',(7.54432698768978,-0.000906756890932275,
6.04853503495399));
#16017=CARTESIAN_POINT('Ctrl Pts',(7.54435782807605,0.082439024249153,6.05284397718214));
#16018=CARTESIAN_POINT('Ctrl Pts',(7.54013222037993,0.165757790068247,6.05715291941028));
#16019=CARTESIAN_POINT('Ctrl Pts',(7.53168467216413,0.248598025365387,6.06146186163843));
#16020=CARTESIAN_POINT('Ctrl Pts',(7.5232318680157,0.331489802563786,6.06577348482317));
#16021=CARTESIAN_POINT('Ctrl Pts',(7.51055194191658,0.413902023722049,6.07008510800791));
#16022=CARTESIAN_POINT('Ctrl Pts',(7.49373099221601,0.495390577515068,6.07439673119265));
#16023=CARTESIAN_POINT('Ctrl Pts',(7.4768816418065,0.577016717635823,6.07871563417771));
#16024=CARTESIAN_POINT('Ctrl Pts',(7.45587739507284,0.65771564883538,6.08303453716278));
#16025=CARTESIAN_POINT('Ctrl Pts',(7.43085500839885,0.737055672629838,6.08735344014785));
#16026=CARTESIAN_POINT('Ctrl Pts',(7.40580967646488,0.81646845037444,6.09167630352059));
#16027=CARTESIAN_POINT('Ctrl Pts',(7.37673901636462,0.894519430353428,6.09599916689333));
#16028=CARTESIAN_POINT('Ctrl Pts',(7.34382811427782,0.97079654680468,6.10032203026608));
#16029=CARTESIAN_POINT('Ctrl Pts',(7.31084909359608,1.0472315407272,6.10465384105018));
#16030=CARTESIAN_POINT('Ctrl Pts',(7.27401414562568,1.12188494603015,6.10898565183427));
#16031=CARTESIAN_POINT('Ctrl Pts',(7.2335545487697,1.19436884264894,6.11331746261837));
#16032=CARTESIAN_POINT('Ctrl Pts',(7.21020525229535,1.23619941248367,6.11581735738076));
#16033=CARTESIAN_POINT('Ctrl Pts',(7.18564959734903,1.27730796117,6.11831725214315));
#16034=CARTESIAN_POINT('Ctrl Pts',(7.15993834715027,1.31762467855749,6.12081714690554));
#16035=CARTESIAN_POINT('Ctrl Pts',(7.11641158845541,1.38587713674324,6.1250492365645));
#16036=CARTESIAN_POINT('Ctrl Pts',(7.06941799814007,1.45209778396879,6.12928132622347));
#16037=CARTESIAN_POINT('Ctrl Pts',(7.01917337655042,1.51591298526872,6.13351341588243));
#16038=CARTESIAN_POINT('Ctrl Pts',(6.96900056652541,1.5796369794044,6.13773945687448));
#16039=CARTESIAN_POINT('Ctrl Pts',(6.91558623874065,1.64096199371702,6.14196549786652));
#16040=CARTESIAN_POINT('Ctrl Pts',(6.85919010319566,1.69954226565206,6.14619153885857));
#16041=CARTESIAN_POINT('Ctrl Pts',(6.8027784554464,1.75813865055541,6.15041874225671));
#16042=CARTESIAN_POINT('Ctrl Pts',(6.7433836323815,1.81398840427749,6.15464594565484));
#16043=CARTESIAN_POINT('Ctrl Pts',(6.68130671328082,1.86677767917852,6.15887314905297));
#16044=CARTESIAN_POINT('Ctrl Pts',(6.61935791371017,1.91945800316528,6.16309162799569));
#16045=CARTESIAN_POINT('Ctrl Pts',(6.5547384159393,1.96909014855915,6.16731010693841));
#16046=CARTESIAN_POINT('Ctrl Pts',(6.48778380992542,2.01539948780691,6.17152858588114));
#16047=CARTESIAN_POINT('Ctrl Pts',(6.42085115986981,2.06169364115514,6.1757456814874));
#16048=CARTESIAN_POINT('Ctrl Pts',(6.35158530413794,2.10466688812076,6.17996277709366));
#16049=CARTESIAN_POINT('Ctrl Pts',(6.28035257997533,2.14408667431202,6.18417987269992));
#16050=CARTESIAN_POINT('Ctrl Pts',(6.20912141897563,2.18350559545778,6.18839687576434));
#16051=CARTESIAN_POINT('Ctrl Pts',(6.1359238825023,2.21937098687609,6.19261387882877));
#16052=CARTESIAN_POINT('Ctrl Pts',(6.06115152472833,2.25149590597147,6.19683088189319));
#16053=CARTESIAN_POINT('Ctrl Pts',(5.98606960786345,2.28375382288914,6.20106534343657));
#16054=CARTESIAN_POINT('Ctrl Pts',(5.90940023074128,2.31224003217109,6.20529980497995));
#16055=CARTESIAN_POINT('Ctrl Pts',(5.83155902235822,2.33681448612266,6.20953426652333));
#16056=CARTESIAN_POINT('Ctrl Pts',(5.75392635824854,2.36132310268874,6.21375738352666));
#16057=CARTESIAN_POINT('Ctrl Pts',(5.67512859653218,2.38194081858858,6.21798050053));
#16058=CARTESIAN_POINT('Ctrl Pts',(5.59559036205847,2.39857956601342,6.22220361753333));
#16059=CARTESIAN_POINT('Ctrl Pts',(5.51573163278717,2.41528535832582,6.22644375134673));
#16060=CARTESIAN_POINT('Ctrl Pts',(5.43512691782398,2.4279799835874,6.23068388516014));
#16061=CARTESIAN_POINT('Ctrl Pts',(5.35421146374845,2.43662682042071,6.23492401897354));
#16062=CARTESIAN_POINT('Ctrl Pts',(5.27329600967292,2.44527365725403,6.23916415278694));
#16063=CARTESIAN_POINT('Ctrl Pts',(5.19207028658604,2.44987274134868,6.24340428660035));
#16064=CARTESIAN_POINT('Ctrl Pts',(5.11096794520242,2.4504400509555,6.24764442041375));
#16065=CARTESIAN_POINT('Ctrl Pts',(5.0300194668307,2.45100628429295,6.25187651007271));
#16066=CARTESIAN_POINT('Ctrl Pts',(4.94889190026816,2.44755815532954,6.25610859973168));
#16067=CARTESIAN_POINT('Ctrl Pts',(4.86801616350811,2.44007369682082,6.26034068939064));
#16068=CARTESIAN_POINT('Ctrl Pts',(4.78725601749245,2.43259993539092,6.26456673038268));
#16069=CARTESIAN_POINT('Ctrl Pts',(4.70674744527433,2.42110134449847,6.26879277137472));
#16070=CARTESIAN_POINT('Ctrl Pts',(4.62692183838648,2.40560796367465,6.27301881236676));
#16071=CARTESIAN_POINT('Ctrl Pts',(4.54707427483231,2.39011032127356,6.2772460157649));
#16072=CARTESIAN_POINT('Ctrl Pts',(4.46791051861213,2.37061571435678,6.28147321916303));
#16073=CARTESIAN_POINT('Ctrl Pts',(4.38985766079683,2.34720625437846,6.28570042256116));
#16074=CARTESIAN_POINT('Ctrl Pts',(4.31196589498814,2.32384510879872,6.28991890150388));
#16075=CARTESIAN_POINT('Ctrl Pts',(4.23518089894629,2.29658536317614,6.29413738044661));
#16076=CARTESIAN_POINT('Ctrl Pts',(4.15991560342966,2.26555941502251,6.29835585938933));
#16077=CARTESIAN_POINT('Ctrl Pts',(4.084674989138,2.23454364099232,6.30257295499559));
#16078=CARTESIAN_POINT('Ctrl Pts',(4.01095351499051,2.1997642940384,6.30679005060184));
#16079=CARTESIAN_POINT('Ctrl Pts',(3.9391455109793,2.16140244978007,6.3110071462081));
#16080=CARTESIAN_POINT('Ctrl Pts',(3.86733908275521,2.12304144735128,6.31522414927252));
#16081=CARTESIAN_POINT('Ctrl Pts',(3.79744645050563,2.08109832390347,6.31944115233693));
#16082=CARTESIAN_POINT('Ctrl Pts',(3.72983736708138,2.03580011475037,6.32365815540135));
#16083=CARTESIAN_POINT('Ctrl Pts',(3.66194838066842,1.99031437008456,6.32789261694473));
#16084=CARTESIAN_POINT('Ctrl Pts',(3.59636229036352,1.94144595220464,6.33212707848812));
#16085=CARTESIAN_POINT('Ctrl Pts',(3.53342257406784,1.8894675949568,6.3363615400315));
#16086=CARTESIAN_POINT('Ctrl Pts',(3.4706514794788,1.83762849285379,6.34058465703484));
#16087=CARTESIAN_POINT('Ctrl Pts',(3.410512914677,1.78269643951499,6.34480777403818));
#16088=CARTESIAN_POINT('Ctrl Pts',(3.35331161785923,1.72497997478066,6.34903089104151));
#16089=CARTESIAN_POINT('Ctrl Pts',(3.29587983166521,1.66703094483023,6.35327102485492));
#16090=CARTESIAN_POINT('Ctrl Pts',(3.24140934282751,1.60627537364017,6.35751115866834));
#16091=CARTESIAN_POINT('Ctrl Pts',(3.19016748139282,1.54305868176058,6.36175129248175));
#16092=CARTESIAN_POINT('Ctrl Pts',(3.13892561995814,1.47984198988098,6.36599142629516));
#16093=CARTESIAN_POINT('Ctrl Pts',(3.09091261150799,1.41416459129452,6.37023156010856));
#16094=CARTESIAN_POINT('Ctrl Pts',(3.04635076874625,1.34639915919381,6.37447169392197));
#16095=CARTESIAN_POINT('Ctrl Pts',(3.00187346632249,1.27876228803623,6.37870378358094));
#16096=CARTESIAN_POINT('Ctrl Pts',(2.96066829775085,1.20879296809753,6.3829358732399));
#16097=CARTESIAN_POINT('Ctrl Pts',(2.92298794009431,1.13684095240292,6.38716796289887));
#16098=CARTESIAN_POINT('Ctrl Pts',(2.88536143666844,1.06499177332378,6.39139400389091));
#16099=CARTESIAN_POINT('Ctrl Pts',(2.85124995232441,0.991165934832231,6.39562004488296));
#16100=CARTESIAN_POINT('Ctrl Pts',(2.82086276928559,0.915741857301564,6.399846085875));
#16101=CARTESIAN_POINT('Ctrl Pts',(2.79046722801111,0.840297033780277,6.40407328927313));
#16102=CARTESIAN_POINT('Ctrl Pts',(2.76379827099119,0.763253495899447,6.40830049267127));
#16103=CARTESIAN_POINT('Ctrl Pts',(2.74101913587277,0.685014359702361,6.4125276960694));
#16104=CARTESIAN_POINT('Ctrl Pts',(2.71828701423584,0.606936699968788,6.41674617501212));
#16105=CARTESIAN_POINT('Ctrl Pts',(2.69942882816891,0.527668811345367,6.42096465395484));
#16106=CARTESIAN_POINT('Ctrl Pts',(2.6845579100964,0.447629258849659,6.42518313289756));
#16107=CARTESIAN_POINT('Ctrl Pts',(2.66969186854063,0.367615953167742,6.42940022850382));
#16108=CARTESIAN_POINT('Ctrl Pts',(2.6588105831879,0.286831942657625,6.43361732411008));
#16109=CARTESIAN_POINT('Ctrl Pts',(2.65197641713916,0.205706640134927,6.43783441971634));
#16110=CARTESIAN_POINT('Ctrl Pts',(2.64514240106242,0.124583117862275,6.44205142278076));
#16111=CARTESIAN_POINT('Ctrl Pts',(2.64235536557133,0.0431187816130797,
6.44626842584518));
#16112=CARTESIAN_POINT('Ctrl Pts',(2.64362573752005,-0.0382526019874996,
6.4504854289096));
#16113=CARTESIAN_POINT('Ctrl Pts',(2.64490136883462,-0.119960864780948,
6.45471989045298));
#16114=CARTESIAN_POINT('Ctrl Pts',(2.65026808016464,-0.2015749316877,6.45895435199637));
#16115=CARTESIAN_POINT('Ctrl Pts',(2.65968365842977,-0.282658249302905,
6.46318881353975));
#16116=CARTESIAN_POINT('Ctrl Pts',(2.66907401143223,-0.363524336714368,
6.46741193054308));
#16117=CARTESIAN_POINT('Ctrl Pts',(2.68249144681185,-0.443862060656903,
6.47163504754642));
#16118=CARTESIAN_POINT('Ctrl Pts',(2.6998426393241,-0.523247920716893,6.47585816454975));
#16119=CARTESIAN_POINT('Ctrl Pts',(2.71726374748095,-0.602953661590481,
6.48009829836316));
#16120=CARTESIAN_POINT('Ctrl Pts',(2.73865024951101,-0.681699398717995,
6.48433843217656));
#16121=CARTESIAN_POINT('Ctrl Pts',(2.76385752974272,-0.759072982832983,
6.48857856598997));
#16122=CARTESIAN_POINT('Ctrl Pts',(2.78906480997442,-0.836446566947971,
6.49281869980338));
#16123=CARTESIAN_POINT('Ctrl Pts',(2.8180926435503,-0.912447583674034,6.49705883361678));
#16124=CARTESIAN_POINT('Ctrl Pts',(2.85074906954625,-0.986686855352001,
6.50129896743019));
#16125=CARTESIAN_POINT('Ctrl Pts',(2.88334354152236,-1.06078528426564,6.50553105708915));
#16126=CARTESIAN_POINT('Ctrl Pts',(2.91967443931074,-1.13340509916198,6.5097631467481));
#16127=CARTESIAN_POINT('Ctrl Pts',(2.95958554566773,-1.20414409480789,6.51399523640706));
#16128=CARTESIAN_POINT('Ctrl Pts',(2.99943960952137,-1.27478198753371,6.51822127739911));
#16129=CARTESIAN_POINT('Ctrl Pts',(3.04286349264541,-1.34354399861218,6.52244731839115));
#16130=CARTESIAN_POINT('Ctrl Pts',(3.08965332706221,-1.41004876355144,6.5266733593832));
#16131=CARTESIAN_POINT('Ctrl Pts',(3.13645603139403,-1.47657182115373,6.53090056278133));
#16132=CARTESIAN_POINT('Ctrl Pts',(3.1866263269493,-1.54083597478252,6.53512776617946));
#16133=CARTESIAN_POINT('Ctrl Pts',(3.23991458832602,-1.60248508368977,6.53935496957759));
#16134=CARTESIAN_POINT('Ctrl Pts',(3.29309286893847,-1.66400695601737,6.54357344852031));
#16135=CARTESIAN_POINT('Ctrl Pts',(3.34937597300401,-1.722924199209,6.54779192746304));
#16136=CARTESIAN_POINT('Ctrl Pts',(3.4084741804015,-1.77891416304573,6.55201040640576));
#16137=CARTESIAN_POINT('Ctrl Pts',(3.46755300813493,-1.83488576648309,6.55622750201202));
#16138=CARTESIAN_POINT('Ctrl Pts',(3.5294447688587,-1.88793167753714,6.56044459761829));
#16139=CARTESIAN_POINT('Ctrl Pts',(3.59382293133692,-1.93776613078916,6.56466169322456));
#16140=CARTESIAN_POINT('Ctrl Pts',(3.65819968107186,-1.98759949045158,6.56887869628898));
#16141=CARTESIAN_POINT('Ctrl Pts',(3.72506235591376,-2.03422124889501,6.57309569935341));
#16142=CARTESIAN_POINT('Ctrl Pts',(3.79405253868518,-2.0773868671015,6.57731270241784));
#16143=CARTESIAN_POINT('Ctrl Pts',(3.8633283422246,-2.12073119185039,6.58154716396122));
#16144=CARTESIAN_POINT('Ctrl Pts',(3.93474891393529,-2.16059043725309,6.58578162550459));
#16145=CARTESIAN_POINT('Ctrl Pts',(4.00792488348457,-2.19676273314475,6.59001608704798));
#16146=CARTESIAN_POINT('Ctrl Pts',(4.08090480739528,-2.23283811988862,6.59423920405131));
#16147=CARTESIAN_POINT('Ctrl Pts',(4.15563029003601,-2.26524613902785,6.59846232105464));
#16148=CARTESIAN_POINT('Ctrl Pts',(4.23169513360644,-2.29383491709987,6.60268543805797));
#16149=CARTESIAN_POINT('Ctrl Pts',(4.30806647614328,-2.32253889202919,6.60692557187138));
#16150=CARTESIAN_POINT('Ctrl Pts',(4.38578754448073,-2.34739264670177,6.61116570568478));
#16151=CARTESIAN_POINT('Ctrl Pts',(4.46443378799603,-2.36829352889397,6.61540583949819));
#16152=CARTESIAN_POINT('Ctrl Pts',(4.54308003151132,-2.38919441108616,6.61964597331159));
#16153=CARTESIAN_POINT('Ctrl Pts',(4.6226509801666,-2.40614238428662,6.623886107125));
#16154=CARTESIAN_POINT('Ctrl Pts',(4.70271562875089,-2.41908702275893,6.6281262409384));
#16155=CARTESIAN_POINT('Ctrl Pts',(4.7826283829782,-2.43200710335743,6.63235833059736));
#16156=CARTESIAN_POINT('Ctrl Pts',(4.86333110127249,-2.44098724308891,6.63659042025632));
#16157=CARTESIAN_POINT('Ctrl Pts',(4.94440127321341,-2.44593993297401,6.64082250991527));
#16158=CARTESIAN_POINT('Ctrl Pts',(5.02535557651603,-2.45088554428237,6.64504855090733));
#16159=CARTESIAN_POINT('Ctrl Pts',(5.10667583045455,-2.4518151100593,6.64927459189939));
#16160=CARTESIAN_POINT('Ctrl Pts',(5.18793111540945,-2.44869244592303,6.65350063289144));
#16161=CARTESIAN_POINT('Ctrl Pts',(5.26920875027467,-2.44556892287324,6.65772783628957));
#16162=CARTESIAN_POINT('Ctrl Pts',(5.35042091607628,-2.43839089225638,6.6619550396877));
#16163=CARTESIAN_POINT('Ctrl Pts',(5.43113299206567,-2.42717428764131,6.66618224308583));
#16164=CARTESIAN_POINT('Ctrl Pts',(5.51167848773203,-2.41598083279159,6.67040072202856));
#16165=CARTESIAN_POINT('Ctrl Pts',(5.59172549204208,-2.40076549679264,6.67461920097129));
#16166=CARTESIAN_POINT('Ctrl Pts',(5.67084570003875,-2.38159607179813,6.67883767991402));
#16167=CARTESIAN_POINT('Ctrl Pts',(5.74993996269581,-2.36243293289985,6.68305477552028));
#16168=CARTESIAN_POINT('Ctrl Pts',(5.82810758131926,-2.33931838934439,6.68727187112654));
#16169=CARTESIAN_POINT('Ctrl Pts',(5.90493120065239,-2.31237118081448,6.69148896673281));
#16170=CARTESIAN_POINT('Ctrl Pts',(5.98175313413311,-2.28542456362637,6.69570596979721));
#16171=CARTESIAN_POINT('Ctrl Pts',(6.05723068884913,-2.25464560358251,6.69992297286161));
#16172=CARTESIAN_POINT('Ctrl Pts',(6.13096378062568,-2.22020221392684,6.70413997592601));
#16173=CARTESIAN_POINT('Ctrl Pts',(6.20500212891104,-2.18561622793315,6.7083744374694));
#16174=CARTESIAN_POINT('Ctrl Pts',(6.2772811063499,-2.14733559408313,6.71260889901278));
#16175=CARTESIAN_POINT('Ctrl Pts',(6.34741961762635,-2.10557740033047,6.71684336055617));
#16176=CARTESIAN_POINT('Ctrl Pts',(6.41737022091445,-2.06393108089682,6.7210664775595));
#16177=CARTESIAN_POINT('Ctrl Pts',(6.48519144589907,-2.01882610443071,6.72528959456283));
#16178=CARTESIAN_POINT('Ctrl Pts',(6.55053501525523,-1.97052086037949,6.72951271156617));
#16179=CARTESIAN_POINT('Ctrl Pts',(6.61614188281239,-1.92202097309126,6.73375284537958));
#16180=CARTESIAN_POINT('Ctrl Pts',(6.67925072628806,-1.87029527870239,6.73799297919298));
#16181=CARTESIAN_POINT('Ctrl Pts',(6.73954460630421,-1.81564432694407,6.74223311300639));
#16182=CARTESIAN_POINT('Ctrl Pts',(6.79983848632034,-1.76099337518575,6.7464732468198));
#16183=CARTESIAN_POINT('Ctrl Pts',(6.85731711672737,-1.70341754074068,6.75071338063321));
#16184=CARTESIAN_POINT('Ctrl Pts',(6.9117038862206,-1.64325118035379,6.75495351444662));
#16185=CARTESIAN_POINT('Ctrl Pts',(6.96540918855507,-1.58383870549912,6.7591405193103));
#16186=CARTESIAN_POINT('Ctrl Pts',(7.01630972610998,-1.5216676940111,6.76332752417397));
#16187=CARTESIAN_POINT('Ctrl Pts',(7.06410492824271,-1.45703663236421,6.76751452903765));
#16188=CARTESIAN_POINT('Ctrl Pts',(7.11183727288988,-1.3924905697516,6.77169602739469));
#16189=CARTESIAN_POINT('Ctrl Pts',(7.1564721034002,-1.32549125271769,6.77587752575173));
#16190=CARTESIAN_POINT('Ctrl Pts',(7.19774685860048,-1.256372609025,6.78005902410877));
#16191=CARTESIAN_POINT('Ctrl Pts',(7.23898061525843,-1.18732262143034,6.78423636895026));
#16192=CARTESIAN_POINT('Ctrl Pts',(7.2768606772769,-1.1161578901549,6.78841371379175));
#16193=CARTESIAN_POINT('Ctrl Pts',(7.31116678822483,-1.04324263857445,6.79259105863324));
#16194=CARTESIAN_POINT('Ctrl Pts',(7.34544985857253,-0.97037635818648,6.79676559789491));
#16195=CARTESIAN_POINT('Ctrl Pts',(7.37616354180739,-0.895762320607005,
6.80094013715659));
#16196=CARTESIAN_POINT('Ctrl Pts',(7.40313346544009,-0.819789373348011,
6.80511467641826));
#16197=CARTESIAN_POINT('Ctrl Pts',(7.43010088435272,-0.74382348176215,6.80928882798687));
#16198=CARTESIAN_POINT('Ctrl Pts',(7.45332506264323,-0.666499374327774,
6.81346297955549));
#16199=CARTESIAN_POINT('Ctrl Pts',(7.4726802197878,-0.588224743023826,6.8176371311241));
#16200=CARTESIAN_POINT('Ctrl Pts',(7.4920341913564,-0.509954906334663,6.82181102701027));
#16201=CARTESIAN_POINT('Ctrl Pts',(7.50751950632716,-0.430735124921569,
6.82598492289644));
#16202=CARTESIAN_POINT('Ctrl Pts',(7.51906109382895,-0.350985176538865,
6.83015881878261));
#16203=CARTESIAN_POINT('Ctrl Pts',(7.53061059387715,-0.271180554120406,
6.83433557615944));
#16204=CARTESIAN_POINT('Ctrl Pts',(7.53821091093363,-0.190845511246944,
6.83851233353628));
#16205=CARTESIAN_POINT('Ctrl Pts',(7.54183875718171,-0.110405832283243,
6.84268909091312));
#16206=CARTESIAN_POINT('Ctrl Pts',(7.54353131309225,-0.0728770494291832,
6.84463773892675));
#16207=CARTESIAN_POINT('Ctrl Pts',(7.54435994289274,-0.0353255197729877,
6.84658638694037));
#16208=CARTESIAN_POINT('Ctrl Pts',(7.54432616288253,0.00220558096770259,
6.848535034954));
#16209=CARTESIAN_POINT('',(7.54432706310264,-0.000672762683564314,7.64853503499169));
#16210=CARTESIAN_POINT('Ctrl Pts',(7.5443261628818,0.002205581778286,6.84853503499609));
#16211=CARTESIAN_POINT('Ctrl Pts',(7.54423010976538,0.108924846857743,6.85407599382254));
#16212=CARTESIAN_POINT('Ctrl Pts',(7.53715829815171,0.215335078947657,6.859616952649));
#16213=CARTESIAN_POINT('Ctrl Pts',(7.52325695306015,0.320657306947781,6.86515791147546));
#16214=CARTESIAN_POINT('Ctrl Pts',(7.50935560796859,0.425979534947917,6.87069887030192));
#16215=CARTESIAN_POINT('Ctrl Pts',(7.48862491996705,0.530214102573731,6.87623982912838));
#16216=CARTESIAN_POINT('Ctrl Pts',(7.46126409479691,0.632607768076277,6.88178078795484));
#16217=CARTESIAN_POINT('Ctrl Pts',(7.4403663641171,0.710814299921889,6.8860128776138));
#16218=CARTESIAN_POINT('Ctrl Pts',(7.41555024571081,0.788130093372826,6.89024496727276));
#16219=CARTESIAN_POINT('Ctrl Pts',(7.38690870987745,0.864133806050236,6.89447705693173));
#16220=CARTESIAN_POINT('Ctrl Pts',(7.35830810963956,0.940028891269427,6.89870309792377));
#16221=CARTESIAN_POINT('Ctrl Pts',(7.32589311339101,1.0146151890146,6.90292913891582));
#16222=CARTESIAN_POINT('Ctrl Pts',(7.28980696566916,1.08748467719021,6.90715517990786));
#16223=CARTESIAN_POINT('Ctrl Pts',(7.25371089216619,1.16037420869643,6.91138238330599));
#16224=CARTESIAN_POINT('Ctrl Pts',(7.21394179334606,1.23154554265023,6.91560958670413));
#16225=CARTESIAN_POINT('Ctrl Pts',(7.17069198614259,1.30060859794372,6.91983679010226));
#16226=CARTESIAN_POINT('Ctrl Pts',(7.12753144150325,1.36952911513589,6.92405526904499));
#16227=CARTESIAN_POINT('Ctrl Pts',(7.08090476714711,1.43634964032875,6.92827374798771));
#16228=CARTESIAN_POINT('Ctrl Pts',(7.03104901840722,1.50070706791586,6.93249222693043));
#16229=CARTESIAN_POINT('Ctrl Pts',(6.98120961851626,1.56504339121936,6.9367093225367));
#16230=CARTESIAN_POINT('Ctrl Pts',(6.92814353145589,1.62691785387678,6.94092641814296));
#16231=CARTESIAN_POINT('Ctrl Pts',(6.87212982415079,1.68599818164277,6.94514351374923));
#16232=CARTESIAN_POINT('Ctrl Pts',(6.8161173460357,1.74507721292344,6.94936051681365));
#16233=CARTESIAN_POINT('Ctrl Pts',(6.75715769683468,1.80136189479551,6.95357751987806));
#16234=CARTESIAN_POINT('Ctrl Pts',(6.69556775059093,1.85455582711536,6.95779452294248));
#16235=CARTESIAN_POINT('Ctrl Pts',(6.63372282070967,1.90796998340331,6.96202898448586));
#16236=CARTESIAN_POINT('Ctrl Pts',(6.56922611707195,1.95826742595683,6.96626344602924));
#16237=CARTESIAN_POINT('Ctrl Pts',(6.5024316192481,2.0051891967036,6.97049790757262));
#16238=CARTESIAN_POINT('Ctrl Pts',(6.4358160704707,2.05198525939946,6.97472102457596));
#16239=CARTESIAN_POINT('Ctrl Pts',(6.36691544130852,2.09542350017289,6.9789441415793));
#16240=CARTESIAN_POINT('Ctrl Pts',(6.29610797575115,2.1352918018724,6.98316725858263));
#16241=CARTESIAN_POINT('Ctrl Pts',(6.22501519553358,2.17532075062886,6.98740739239603));
#16242=CARTESIAN_POINT('Ctrl Pts',(6.15200060520609,2.21175072707874,6.99164752620943));
#16243=CARTESIAN_POINT('Ctrl Pts',(6.07746810223493,2.24441545570649,6.99588766002284));
#16244=CARTESIAN_POINT('Ctrl Pts',(6.00293559926375,2.27708018433424,7.00012779383624));
#16245=CARTESIAN_POINT('Ctrl Pts',(5.92688564259963,2.3059795572839,7.00436792764965));
#16246=CARTESIAN_POINT('Ctrl Pts',(5.84973648336748,2.33099792749201,7.00860806146305));
#16247=CARTESIAN_POINT('Ctrl Pts',(5.77273368738217,2.35596883419008,7.01284015112201));
#16248=CARTESIAN_POINT('Ctrl Pts',(5.69434857887908,2.3771666268737,7.01707224078097));
#16249=CARTESIAN_POINT('Ctrl Pts',(5.61498535135583,2.39444030722076,7.02130433043993));
#16250=CARTESIAN_POINT('Ctrl Pts',(5.5357355528398,2.41168929935295,7.02553037143198));
#16251=CARTESIAN_POINT('Ctrl Pts',(5.45551086207915,2.42502522022466,7.02975641242403));
#16252=CARTESIAN_POINT('Ctrl Pts',(5.37473162020512,2.43434651019167,7.03398245341608));
#16253=CARTESIAN_POINT('Ctrl Pts',(5.29393015936008,2.44367036405341,7.03820965681421));
#16254=CARTESIAN_POINT('Ctrl Pts',(5.21257429382933,2.44897725970599,7.04243686021234));
#16255=CARTESIAN_POINT('Ctrl Pts',(5.13109598065973,2.45021657913494,7.04666406361047));
#16256=CARTESIAN_POINT('Ctrl Pts',(5.04978582923756,2.45145334075294,7.0508825425532));
#16257=CARTESIAN_POINT('Ctrl Pts',(4.96835419939216,2.4486392673208,7.05510102149592));
#16258=CARTESIAN_POINT('Ctrl Pts',(4.88723472502729,2.44177595567053,7.05931950043864));
#16259=CARTESIAN_POINT('Ctrl Pts',(4.80614185160747,2.43491489465832,7.0635365960449));
#16260=CARTESIAN_POINT('Ctrl Pts',(4.72536139306116,2.42400727154023,7.06775369165117));
#16261=CARTESIAN_POINT('Ctrl Pts',(4.64532394146655,2.40910670520086,7.07197078725743));
#16262=CARTESIAN_POINT('Ctrl Pts',(4.56528824624983,2.39420646584622,7.07618779032185));
#16263=CARTESIAN_POINT('Ctrl Pts',(4.48599598219533,2.37531354366745,7.08040479338627));
#16264=CARTESIAN_POINT('Ctrl Pts',(4.40786818142601,2.35253279168467,7.08462179645069));
#16265=CARTESIAN_POINT('Ctrl Pts',(4.32941692996306,2.32965772692261,7.08885625799407));
#16266=CARTESIAN_POINT('Ctrl Pts',(4.25214026067395,2.30286269210011,7.09309071953745));
#16267=CARTESIAN_POINT('Ctrl Pts',(4.17644794826881,2.27230403780522,7.09732518108083));
#16268=CARTESIAN_POINT('Ctrl Pts',(4.10095842303284,2.24182725315866,7.10154829808416));
#16269=CARTESIAN_POINT('Ctrl Pts',(4.02704518323414,2.20760722330936,7.1057714150875));
#16270=CARTESIAN_POINT('Ctrl Pts',(3.95509187700223,2.16984612717386,7.10999453209083));
#16271=CARTESIAN_POINT('Ctrl Pts',(3.88284863901015,2.13193287484649,7.11423466590424));
#16272=CARTESIAN_POINT('Ctrl Pts',(3.81258156440701,2.09045020603706,7.11847479971764));
#16273=CARTESIAN_POINT('Ctrl Pts',(3.74464976856326,2.04564675071359,7.12271493353105));
#16274=CARTESIAN_POINT('Ctrl Pts',(3.67671797271953,2.00084329539013,7.12695506734446));
#16275=CARTESIAN_POINT('Ctrl Pts',(3.6111217956416,1.95271938014768,7.13119520115786));
#16276=CARTESIAN_POINT('Ctrl Pts',(3.54818565973068,1.90156320344629,7.13543533497127));
#16277=CARTESIAN_POINT('Ctrl Pts',(3.48536892288112,1.85050407749949,7.13966742463023));
#16278=CARTESIAN_POINT('Ctrl Pts',(3.42496777694522,1.79623370603101,7.14389951428919));
#16279=CARTESIAN_POINT('Ctrl Pts',(3.36732867519254,1.73900927187233,7.14813160394815));
#16280=CARTESIAN_POINT('Ctrl Pts',(3.30977195348277,1.68186662509753,7.1523576449402));
#16281=CARTESIAN_POINT('Ctrl Pts',(3.25496976256563,1.62177862576476,7.15658368593224));
#16282=CARTESIAN_POINT('Ctrl Pts',(3.20323583655671,1.55904288424455,7.16080972692429));
#16283=CARTESIAN_POINT('Ctrl Pts',(3.1514876807212,1.49628988676115,7.16503693032242));
#16284=CARTESIAN_POINT('Ctrl Pts',(3.10280982282825,1.43088800491757,7.16926413372055));
#16285=CARTESIAN_POINT('Ctrl Pts',(3.05747955297212,1.36317228987018,7.17349133711868));
#16286=CARTESIAN_POINT('Ctrl Pts',(3.0122428395127,1.29559633217082,7.17770981606141));
#16287=CARTESIAN_POINT('Ctrl Pts',(2.97034018911735,1.22571645496427,7.18192829500413));
#16288=CARTESIAN_POINT('Ctrl Pts',(2.93200597649514,1.1538974998711,7.18614677394685));
#16289=CARTESIAN_POINT('Ctrl Pts',(2.89368433454466,1.08210209586836,7.19036386955312));
#16290=CARTESIAN_POINT('Ctrl Pts',(2.85892902515503,1.00836928638527,7.19458096515938));
#16291=CARTESIAN_POINT('Ctrl Pts',(2.82792910448836,0.933089638048864,7.19879806076564));
#16292=CARTESIAN_POINT('Ctrl Pts',(2.79692986409792,0.857811641682979,7.20301506383006));
#16293=CARTESIAN_POINT('Ctrl Pts',(2.76968602445695,0.780987304074674,7.20723206689447));
#16294=CARTESIAN_POINT('Ctrl Pts',(2.74633844139469,0.703027017523766,7.21144906995889));
#16295=CARTESIAN_POINT('Ctrl Pts',(2.72289419886087,0.624743973791483,7.21568353150227));
#16296=CARTESIAN_POINT('Ctrl Pts',(2.70337869048469,0.54531600365262,7.21991799304566));
#16297=CARTESIAN_POINT('Ctrl Pts',(2.68788342794357,0.465172043503783,7.22415245458904));
#16298=CARTESIAN_POINT('Ctrl Pts',(2.67242967873883,0.385242796927439,7.22837557159237));
#16299=CARTESIAN_POINT('Ctrl Pts',(2.6609746866025,0.304601860576321,7.23259868859571));
#16300=CARTESIAN_POINT('Ctrl Pts',(2.65355729498283,0.223681152715985,7.23682180559905));
#16301=CARTESIAN_POINT('Ctrl Pts',(2.64611001540496,0.142434379459981,7.24106193941245));
#16302=CARTESIAN_POINT('Ctrl Pts',(2.64273295449464,0.0609060466887959,
7.24530207322586));
#16303=CARTESIAN_POINT('Ctrl Pts',(2.64341263115474,-0.0204672691777702,
7.24954220703926));
#16304=CARTESIAN_POINT('Ctrl Pts',(2.64409230781484,-0.101840585044325,
7.25378234085267));
#16305=CARTESIAN_POINT('Ctrl Pts',(2.64882863273646,-0.183058421088772,
7.25802247466608));
#16306=CARTESIAN_POINT('Ctrl Pts',(2.65755605430675,-0.263691812006185,
7.26226260847948));
#16307=CARTESIAN_POINT('Ctrl Pts',(2.66626691868094,-0.344172229579233,
7.26649469813844));
#16308=CARTESIAN_POINT('Ctrl Pts',(2.67898623277375,-0.424370675316697,
7.2707267877974));
#16309=CARTESIAN_POINT('Ctrl Pts',(2.69568645370932,-0.503856551649172,
7.27495887745637));
#16310=CARTESIAN_POINT('Ctrl Pts',(2.71236280604048,-0.583228823679947,
7.27918491844841));
#16311=CARTESIAN_POINT('Ctrl Pts',(2.73300867017062,-0.661890098062268,
7.28341095944046));
#16312=CARTESIAN_POINT('Ctrl Pts',(2.757544784589,-0.739415264644689,7.2876370004325));
#16313=CARTESIAN_POINT('Ctrl Pts',(2.78208764786022,-0.816961755138957,
7.29186420383064));
#16314=CARTESIAN_POINT('Ctrl Pts',(2.8105228252285,-0.893371052254958,7.29609140722877));
#16315=CARTESIAN_POINT('Ctrl Pts',(2.84271981873416,-0.968228283293825,
7.3003186106269));
#16316=CARTESIAN_POINT('Ctrl Pts',(2.87485036139567,-1.04293101772751,7.30453708956963));
#16317=CARTESIAN_POINT('Ctrl Pts',(2.91072704715064,-1.11608764946923,7.30875556851234));
#16318=CARTESIAN_POINT('Ctrl Pts',(2.95017104523229,-1.18730313362382,7.31297404745507));
#16319=CARTESIAN_POINT('Ctrl Pts',(2.98960210871799,-1.25849526458,7.31719114306133));
#16320=CARTESIAN_POINT('Ctrl Pts',(3.03259793643184,-1.32774710588574,7.32140823866759));
#16321=CARTESIAN_POINT('Ctrl Pts',(3.07893347085764,-1.3946876674644,7.32562533427385));
#16322=CARTESIAN_POINT('Ctrl Pts',(3.12526798847559,-1.4616267600692,7.32984233733827));
#16323=CARTESIAN_POINT('Ctrl Pts',(3.17494180166971,-1.52625429236071,7.33405934040269));
#16324=CARTESIAN_POINT('Ctrl Pts',(3.22768701133766,-1.5882289546916,7.3382763434671));
#16325=CARTESIAN_POINT('Ctrl Pts',(3.28065058725282,-1.65046019339256,7.34251080501048));
#16326=CARTESIAN_POINT('Ctrl Pts',(3.33671074912334,-1.71001618182879,7.34674526655386));
#16327=CARTESIAN_POINT('Ctrl Pts',(3.39555721020248,-1.76658694749463,7.35097972809725));
#16328=CARTESIAN_POINT('Ctrl Pts',(3.45424601580931,-1.8230061545006,7.35520284510058));
#16329=CARTESIAN_POINT('Ctrl Pts',(3.51570583031381,-1.87645583795613,7.35942596210392));
#16330=CARTESIAN_POINT('Ctrl Pts',(3.57959523468405,-1.92666861191125,7.36364907910725));
#16331=CARTESIAN_POINT('Ctrl Pts',(3.64374207778003,-1.97708371538675,7.36788921292066));
#16332=CARTESIAN_POINT('Ctrl Pts',(3.71033774211421,-2.02423550301704,7.37212934673406));
#16333=CARTESIAN_POINT('Ctrl Pts',(3.77900845618769,-2.06789797573816,7.37636948054747));
#16334=CARTESIAN_POINT('Ctrl Pts',(3.84767917026118,-2.11156044845928,7.38060961436088));
#16335=CARTESIAN_POINT('Ctrl Pts',(3.91842449697439,-2.15173342960025,7.38484974817429));
#16336=CARTESIAN_POINT('Ctrl Pts',(3.99084874874287,-2.18823876309943,7.38908988198769));
#16337=CARTESIAN_POINT('Ctrl Pts',(4.06313560110557,-2.22467484063796,7.39332197164666));
#16338=CARTESIAN_POINT('Ctrl Pts',(4.13736469436473,-2.25759312375911,7.39755406130563));
#16339=CARTESIAN_POINT('Ctrl Pts',(4.21315963169929,-2.28678266623772,7.4017861509646));
#16340=CARTESIAN_POINT('Ctrl Pts',(4.28884623996552,-2.3159304898885,7.40601219195665));
#16341=CARTESIAN_POINT('Ctrl Pts',(4.36609381744599,-2.341359991782,7.41023823294871));
#16342=CARTESIAN_POINT('Ctrl Pts',(4.44450245997007,-2.36290661894114,7.41446427394076));
#16343=CARTESIAN_POINT('Ctrl Pts',(4.52293266941293,-2.38445917267091,7.41869147733889));
#16344=CARTESIAN_POINT('Ctrl Pts',(4.60252415455834,-2.4021265292947,7.42291868073702));
#16345=CARTESIAN_POINT('Ctrl Pts',(4.68285775296745,-2.41579270638451,7.42714588413515));
#16346=CARTESIAN_POINT('Ctrl Pts',(4.76302555218719,-2.42943067807672,7.43136436307788));
#16347=CARTESIAN_POINT('Ctrl Pts',(4.843931950515,-2.43908386709375,7.43558284202061));
#16348=CARTESIAN_POINT('Ctrl Pts',(4.92514815533494,-2.44468763749464,7.43980132096334));
#16349=CARTESIAN_POINT('Ctrl Pts',(5.00633772748967,-2.45028957029008,7.44401841656961));
#16350=CARTESIAN_POINT('Ctrl Pts',(5.08783644115445,-2.45184468959133,7.44823551217587));
#16351=CARTESIAN_POINT('Ctrl Pts',(5.16921056632264,-2.44934023593409,7.45245260778214));
#16352=CARTESIAN_POINT('Ctrl Pts',(5.25058290578035,-2.44683583723572,7.45666961084656));
#16353=CARTESIAN_POINT('Ctrl Pts',(5.33183019774403,-2.44027205814725,7.46088661391099));
#16354=CARTESIAN_POINT('Ctrl Pts',(5.41252033682111,-2.42968823229433,7.46510361697541));
#16355=CARTESIAN_POINT('Ctrl Pts',(5.49354453472467,-2.41906058918586,7.46933807851878));
#16356=CARTESIAN_POINT('Ctrl Pts',(5.57400648719473,-2.40437959084619,7.47357254006216));
#16357=CARTESIAN_POINT('Ctrl Pts',(5.65347735077971,-2.38573718352858,7.47780700160553));
#16358=CARTESIAN_POINT('Ctrl Pts',(5.7327353040845,-2.36714472105851,7.48203011860887));
#16359=CARTESIAN_POINT('Ctrl Pts',(5.81100703423499,-2.34461221743159,7.48625323561222));
#16360=CARTESIAN_POINT('Ctrl Pts',(5.88788252019001,-2.31828089922954,7.49047635261556));
#16361=CARTESIAN_POINT('Ctrl Pts',(5.96506777154849,-2.29184348047665,7.49471648642895));
#16362=CARTESIAN_POINT('Ctrl Pts',(6.04084506816645,-2.2615767511839,7.49895662024235));
#16363=CARTESIAN_POINT('Ctrl Pts',(6.11482154119478,-2.22767159031218,7.50319675405574));
#16364=CARTESIAN_POINT('Ctrl Pts',(6.18879801422311,-2.19376642944046,7.50743688786914));
#16365=CARTESIAN_POINT('Ctrl Pts',(6.26097327777291,-2.15622310783739,7.51167702168254));
#16366=CARTESIAN_POINT('Ctrl Pts',(6.33098270718856,-2.11527690641442,7.51591715549593));
#16367=CARTESIAN_POINT('Ctrl Pts',(6.40085931846993,-2.07440838592849,7.52014924515489));
#16368=CARTESIAN_POINT('Ctrl Pts',(6.46883900936586,-2.02999742697252,7.52438133481385));
#16369=CARTESIAN_POINT('Ctrl Pts',(6.53454011865709,-1.98224529452235,7.52861342447282));
#16370=CARTESIAN_POINT('Ctrl Pts',(6.60014732537101,-1.93456141127463,7.53283946546486));
#16371=CARTESIAN_POINT('Ctrl Pts',(6.66348204576312,-1.88354610978607,7.5370655064569));
#16372=CARTESIAN_POINT('Ctrl Pts',(6.72418878096595,-1.82944560456307,7.54129154744894));
#16373=CARTESIAN_POINT('Ctrl Pts',(6.78491221403776,-1.77533021856704,7.54551875084707));
#16374=CARTESIAN_POINT('Ctrl Pts',(6.84300582713173,-1.71812818962213,7.5497459542452));
#16375=CARTESIAN_POINT('Ctrl Pts',(6.89814442098345,-1.65812829880836,7.55397315764334));
#16376=CARTESIAN_POINT('Ctrl Pts',(6.95316921520019,-1.59825224078024,7.55819163658605));
#16377=CARTESIAN_POINT('Ctrl Pts',(7.00525084276425,-1.53559018353007,7.56241011552878));
#16378=CARTESIAN_POINT('Ctrl Pts',(7.0541019676615,-1.47046690225294,7.56662859447149));
#16379=CARTESIAN_POINT('Ctrl Pts',(7.10293707314914,-1.40536497640048,7.57084569007776));
#16380=CARTESIAN_POINT('Ctrl Pts',(7.14854350112565,-1.33780380077239,7.57506278568401));
#16381=CARTESIAN_POINT('Ctrl Pts',(7.19067477458579,-1.26814049384822,7.57927988129027));
#16382=CARTESIAN_POINT('Ctrl Pts',(7.23280512349825,-1.1984787156471,7.58349688435468));
#16383=CARTESIAN_POINT('Ctrl Pts',(7.27146023002579,-1.12671529608906,7.5877138874191));
#16384=CARTESIAN_POINT('Ctrl Pts',(7.30643822496701,-1.05323430682093,7.59193089048351));
#16385=CARTESIAN_POINT('Ctrl Pts',(7.34156102952299,-0.979449104753689,
7.59616535202689));
#16386=CARTESIAN_POINT('Ctrl Pts',(7.37297599659068,-0.903932501601114,
7.60039981357028));
#16387=CARTESIAN_POINT('Ctrl Pts',(7.40052719086937,-0.827094430286303,
7.60463427511366));
#16388=CARTESIAN_POINT('Ctrl Pts',(7.42800457278164,-0.750462215741914,
7.60885739211699));
#16389=CARTESIAN_POINT('Ctrl Pts',(7.45163876205057,-0.672516064085702,
7.61308050912032));
#16390=CARTESIAN_POINT('Ctrl Pts',(7.47132541865873,-0.593676897355996,
7.61730362612365));
#16391=CARTESIAN_POINT('Ctrl Pts',(7.49109140153145,-0.514520052682174,
7.62154375993706));
#16392=CARTESIAN_POINT('Ctrl Pts',(7.50687788911834,-0.434463445243895,
7.62578389375048));
#16393=CARTESIAN_POINT('Ctrl Pts',(7.51863154107007,-0.353940590343589,
7.63002402756389));
#16394=CARTESIAN_POINT('Ctrl Pts',(7.53038519302179,-0.273417735443293,
7.6342641613773));
#16395=CARTESIAN_POINT('Ctrl Pts',(7.53810602691443,-0.192429104207026,
7.63850429519071));
#16396=CARTESIAN_POINT('Ctrl Pts',(7.54179332448113,-0.111408641021635,
7.64274442900412));
#16397=CARTESIAN_POINT('Ctrl Pts',(7.5434718632701,-0.0745263477710347,
7.64467463098741));
#16398=CARTESIAN_POINT('Ctrl Pts',(7.54431692344925,-0.0376058353287276,
7.64660483297071));
#16399=CARTESIAN_POINT('Ctrl Pts',(7.54432706310245,-0.000672763404672779,
7.648535034954));
#16400=CARTESIAN_POINT('',(7.54432655273176,-0.00171870211734679,8.44853500454046));
#16401=CARTESIAN_POINT('Ctrl Pts',(7.54432706310264,-0.000672762683580638,
7.64853503499169));
#16402=CARTESIAN_POINT('Ctrl Pts',(7.54434913504306,0.0797230281083948,
7.65273669238839));
#16403=CARTESIAN_POINT('Ctrl Pts',(7.54041051570088,0.160277450484244,7.65693834978509));
#16404=CARTESIAN_POINT('Ctrl Pts',(7.53249050506243,0.240564580252856,7.6611400071818));
#16405=CARTESIAN_POINT('Ctrl Pts',(7.52458159021615,0.320739229199728,7.66533577813222));
#16406=CARTESIAN_POINT('Ctrl Pts',(7.51270240427672,0.400646863270518,7.66953154908264));
#16407=CARTESIAN_POINT('Ctrl Pts',(7.49688426185791,0.479861223019126,7.67372732003306));
#16408=CARTESIAN_POINT('Ctrl Pts',(7.48108343481771,0.558988870523393,7.67791849806981));
#16409=CARTESIAN_POINT('Ctrl Pts',(7.4613523092814,0.637424290795133,7.68210967610655));
#16410=CARTESIAN_POINT('Ctrl Pts',(7.43777386554785,0.714747556998992,7.6863008541433));
#16411=CARTESIAN_POINT('Ctrl Pts',(7.41420923082455,0.792025537865658,7.69048957756426));
#16412=CARTESIAN_POINT('Ctrl Pts',(7.38680188651039,0.868192206760459,7.69467830098522));
#16413=CARTESIAN_POINT('Ctrl Pts',(7.35568533976967,0.942840285541607,7.69886702440617));
#16414=CARTESIAN_POINT('Ctrl Pts',(7.32457715080152,1.01746831416521,7.70305462275377));
#16415=CARTESIAN_POINT('Ctrl Pts',(7.2897619191421,1.0905781271244,7.70724222110136));
#16416=CARTESIAN_POINT('Ctrl Pts',(7.25142167462184,1.16178145141548,7.71142981944896));
#16417=CARTESIAN_POINT('Ctrl Pts',(7.21307957177601,1.23298822688325,7.7156176207666));
#16418=CARTESIAN_POINT('Ctrl Pts',(7.17121234244202,1.30228791559096,7.71980542208424));
#16419=CARTESIAN_POINT('Ctrl Pts',(7.12604771747699,1.36931728875646,7.72399322340188));
#16420=CARTESIAN_POINT('Ctrl Pts',(7.08083722339248,1.43641473684407,7.72818527784371));
#16421=CARTESIAN_POINT('Ctrl Pts',(7.0323229128709,1.5012368744042,7.73237733228554));
#16422=CARTESIAN_POINT('Ctrl Pts',(6.98077516759307,1.56345049473307,7.73656938672737));
#16423=CARTESIAN_POINT('Ctrl Pts',(6.92919923522218,1.62569813441808,7.74076373344849));
#16424=CARTESIAN_POINT('Ctrl Pts',(6.874586885962,1.68533407022842,7.7449580801696));
#16425=CARTESIAN_POINT('Ctrl Pts',(6.81724628663355,1.7420610633044,7.74915242689072));
#16426=CARTESIAN_POINT('Ctrl Pts',(6.75980868398112,1.79888402166418,7.75335386920516));
#16427=CARTESIAN_POINT('Ctrl Pts',(6.69963396885006,1.85278789834029,7.7575553115196));
#16428=CARTESIAN_POINT('Ctrl Pts',(6.63706398365877,1.90351525921642,7.76175675383404));
#16429=CARTESIAN_POINT('Ctrl Pts',(6.59826927250347,1.93496729339612,7.76436173672682));
#16430=CARTESIAN_POINT('Ctrl Pts',(6.55855437060596,1.96519902747809,7.76696671961959));
#16431=CARTESIAN_POINT('Ctrl Pts',(6.51800593252806,1.99415773220909,7.76957170251236));
#16432=CARTESIAN_POINT('Ctrl Pts',(6.45213040376656,2.04120442689898,7.77380379217132));
#16433=CARTESIAN_POINT('Ctrl Pts',(6.3837982580845,2.08507115137388,7.77803588183027));
#16434=CARTESIAN_POINT('Ctrl Pts',(6.31334926780202,2.12549195893375,7.78226797148922));
#16435=CARTESIAN_POINT('Ctrl Pts',(6.24300096595278,2.16585499550547,7.78649401248125));
#16436=CARTESIAN_POINT('Ctrl Pts',(6.17054222811735,2.20278166749725,7.79072005347329));
#16437=CARTESIAN_POINT('Ctrl Pts',(6.09634314235166,2.236048287943,7.79494609446532));
#16438=CARTESIAN_POINT('Ctrl Pts',(6.02212364753879,2.26932405863662,7.79917329786346));
#16439=CARTESIAN_POINT('Ctrl Pts',(5.94616324199081,2.29893751481314,7.80340050126159));
#16440=CARTESIAN_POINT('Ctrl Pts',(5.86885846271062,2.32471002982538,7.80762770465973));
#16441=CARTESIAN_POINT('Ctrl Pts',(5.79171323149022,2.35042935336868,7.81184618360244));
#16442=CARTESIAN_POINT('Ctrl Pts',(5.71322960321401,2.37232340372805,7.81606466254516));
#16443=CARTESIAN_POINT('Ctrl Pts',(5.63382147252083,2.39026282812886,7.82028314148787));
#16444=CARTESIAN_POINT('Ctrl Pts',(5.55443938158367,2.40819636977899,7.82450023709413));
#16445=CARTESIAN_POINT('Ctrl Pts',(5.47413384320454,2.42217775850298,7.82871733270038));
#16446=CARTESIAN_POINT('Ctrl Pts',(5.39333155283008,2.43212815574177,7.83293442830664));
#16447=CARTESIAN_POINT('Ctrl Pts',(5.31253103561741,2.44207833462457,7.83715143137105));
#16448=CARTESIAN_POINT('Ctrl Pts',(5.23123424942869,2.44799764224542,7.84136843443547));
#16449=CARTESIAN_POINT('Ctrl Pts',(5.14987423854054,2.44985897032409,7.84558543749988));
#16450=CARTESIAN_POINT('Ctrl Pts',(5.0681773955425,2.45172800433909,7.84981989904327));
#16451=CARTESIAN_POINT('Ctrl Pts',(4.98641727461212,2.44950536333508,7.85405436058665));
#16452=CARTESIAN_POINT('Ctrl Pts',(4.90503173006084,2.44321643276869,7.85828882213004));
#16453=CARTESIAN_POINT('Ctrl Pts',(4.82386422540937,2.43694435086748,7.86251193913337));
#16454=CARTESIAN_POINT('Ctrl Pts',(4.74306975124056,2.42662783962624,7.8667350561367));
#16455=CARTESIAN_POINT('Ctrl Pts',(4.66307508507712,2.41234386103366,7.87095817314003));
#16456=CARTESIAN_POINT('Ctrl Pts',(4.58275808495003,2.39800232596067,7.87519830695345));
#16457=CARTESIAN_POINT('Ctrl Pts',(4.50324780944299,2.37966139703988,7.87943844076687));
#16458=CARTESIAN_POINT('Ctrl Pts',(4.42496166673264,2.35744972544458,7.88367857458029));
#16459=CARTESIAN_POINT('Ctrl Pts',(4.34667552402229,2.33523805384928,7.88791870839371));
#16460=CARTESIAN_POINT('Ctrl Pts',(4.26961393682959,2.30915584832735,7.89215884220713));
#16461=CARTESIAN_POINT('Ctrl Pts',(4.19417318033878,2.27937995407983,7.89639897602055));
#16462=CARTESIAN_POINT('Ctrl Pts',(4.11887554600507,2.24966054906191,7.90063106567951));
#16463=CARTESIAN_POINT('Ctrl Pts',(4.04491167209881,2.21615059522029,7.90486315533847));
#16464=CARTESIAN_POINT('Ctrl Pts',(3.97268947649604,2.17899071930625,7.90909524499743));
#16465=CARTESIAN_POINT('Ctrl Pts',(3.90057050366025,2.14188395373011,7.91332128598948));
#16466=CARTESIAN_POINT('Ctrl Pts',(3.83018867490852,2.10113783766115,7.91754732698153));
#16467=CARTESIAN_POINT('Ctrl Pts',(3.76193291616612,2.05694141514875,7.92177336797358));
#16468=CARTESIAN_POINT('Ctrl Pts',(3.69365838313604,2.01273283605988,7.92600057137171));
#16469=CARTESIAN_POINT('Ctrl Pts',(3.62751151362582,1.96507224802607,7.93022777476984));
#16470=CARTESIAN_POINT('Ctrl Pts',(3.56385778900778,1.91419538912277,7.93445497816798));
#16471=CARTESIAN_POINT('Ctrl Pts',(3.50033543826272,1.86342353412991,7.9386734571107));
#16472=CARTESIAN_POINT('Ctrl Pts',(3.43929633018822,1.80944894164393,7.94289193605342));
#16473=CARTESIAN_POINT('Ctrl Pts',(3.38107402306712,1.75254870331811,7.94711041499615));
#16474=CARTESIAN_POINT('Ctrl Pts',(3.32287080838226,1.6956671238917,7.95132751060241));
#16475=CARTESIAN_POINT('Ctrl Pts',(3.26748289235801,1.63586212841871,7.95554460620867));
#16476=CARTESIAN_POINT('Ctrl Pts',(3.21520839209335,1.57344901155158,7.95976170181493));
#16477=CARTESIAN_POINT('Ctrl Pts',(3.16293503896387,1.51103726430599,7.96397870487934));
#16478=CARTESIAN_POINT('Ctrl Pts',(3.11377526324372,1.44601786644287,7.96819570794376));
#16479=CARTESIAN_POINT('Ctrl Pts',(3.06798721296639,1.37873956113017,7.97241271100817));
#16480=CARTESIAN_POINT('Ctrl Pts',(3.02200959922407,1.31118272225693,7.97664717255156));
#16481=CARTESIAN_POINT('Ctrl Pts',(2.97943196451947,1.24134861504183,7.98088163409494));
#16482=CARTESIAN_POINT('Ctrl Pts',(2.94047101054738,1.169618554571,7.98511609563833));
#16483=CARTESIAN_POINT('Ctrl Pts',(2.90161443681309,1.09808066600576,7.98933921264166));
#16484=CARTESIAN_POINT('Ctrl Pts',(2.86635535496317,1.02465740942091,7.99356232964499));
#16485=CARTESIAN_POINT('Ctrl Pts',(2.83486115444528,0.949748838530843,7.99778544664832));
#16486=CARTESIAN_POINT('Ctrl Pts',(2.80324004983536,0.874538427809408,8.00202558046173));
#16487=CARTESIAN_POINT('Ctrl Pts',(2.77541438402111,0.797831153663802,8.00626571427514));
#16488=CARTESIAN_POINT('Ctrl Pts',(2.75150306778021,0.720047302826216,8.01050584808855));
#16489=CARTESIAN_POINT('Ctrl Pts',(2.7275917515393,0.642263451988641,8.01474598190196));
#16490=CARTESIAN_POINT('Ctrl Pts',(2.70759483944073,0.563403492744156,8.01898611571537));
#16491=CARTESIAN_POINT('Ctrl Pts',(2.69157930278514,0.483896171045126,8.02322624952878));
#16492=CARTESIAN_POINT('Ctrl Pts',(2.67559414994663,0.4045396863721,8.02745833918776));
#16493=CARTESIAN_POINT('Ctrl Pts',(2.66351562688301,0.324242233546056,8.03169042884674));
#16494=CARTESIAN_POINT('Ctrl Pts',(2.65544743384357,0.243422643242911,8.03592251850571));
#16495=CARTESIAN_POINT('Ctrl Pts',(2.64739077217901,0.162718563437469,8.04014855949777));
#16496=CARTESIAN_POINT('Ctrl Pts',(2.64333310249604,0.0814942868331558,
8.04437460048982));
#16497=CARTESIAN_POINT('Ctrl Pts',(2.64332716199235,0.000179021789542721,
8.04860064148187));
#16498=CARTESIAN_POINT('Ctrl Pts',(2.64332121985467,-0.0811586096623815,
8.05282784488));
#16499=CARTESIAN_POINT('Ctrl Pts',(2.64736930210422,-0.16258681747649,8.05705504827813));
#16500=CARTESIAN_POINT('Ctrl Pts',(2.65547220897873,-0.243670689669318,
8.06128225167626));
#16501=CARTESIAN_POINT('Ctrl Pts',(2.66355839239734,-0.32458721419525,8.065500730619));
#16502=CARTESIAN_POINT('Ctrl Pts',(2.67568265845143,-0.405160358115837,
8.06971920956173));
#16503=CARTESIAN_POINT('Ctrl Pts',(2.69179374419206,-0.484959525306589,
8.07393768850446));
#16504=CARTESIAN_POINT('Ctrl Pts',(2.7078995467364,-0.564732524511477,8.07815478411074));
#16505=CARTESIAN_POINT('Ctrl Pts',(2.72798948075756,-0.643731595873776,
8.08237187971702));
#16506=CARTESIAN_POINT('Ctrl Pts',(2.75196095221176,-0.721535124658506,
8.0865889753233));
#16507=CARTESIAN_POINT('Ctrl Pts',(2.77593189762514,-0.799336946087373,
8.09080597838772));
#16508=CARTESIAN_POINT('Ctrl Pts',(2.80378407319164,-0.875942833351775,
8.09502298145215));
#16509=CARTESIAN_POINT('Ctrl Pts',(2.83536508321222,-0.950946538060565,
8.09923998451657));
#16510=CARTESIAN_POINT('Ctrl Pts',(2.86707683926029,-1.0262607596411,8.10347444605994));
#16511=CARTESIAN_POINT('Ctrl Pts',(2.90254819921316,-1.09995906444261,8.10770890760331));
#16512=CARTESIAN_POINT('Ctrl Pts',(2.94157689847738,-1.17165228687862,8.11194336914668));
#16513=CARTESIAN_POINT('Ctrl Pts',(2.98050103600779,-1.2431534361023,8.11616648615003));
#16514=CARTESIAN_POINT('Ctrl Pts',(3.02296319737104,-1.31265985532268,8.12038960315338));
#16515=CARTESIAN_POINT('Ctrl Pts',(3.06871858439075,-1.37981358357199,8.12461272015673));
#16516=CARTESIAN_POINT('Ctrl Pts',(3.1146583401429,-1.44723790395399,8.12885285397011));
#16517=CARTESIAN_POINT('Ctrl Pts',(3.16391762583173,-1.51229016262488,8.1330929877835));
#16518=CARTESIAN_POINT('Ctrl Pts',(3.21620830848822,-1.57464209124558,8.13733312159688));
#16519=CARTESIAN_POINT('Ctrl Pts',(3.26849899114471,-1.63699401986627,8.14157325541026));
#16520=CARTESIAN_POINT('Ctrl Pts',(3.32382070737321,-1.69664531808319,8.14581338922364));
#16521=CARTESIAN_POINT('Ctrl Pts',(3.38184999060249,-1.75330671504732,8.15005352303702));
#16522=CARTESIAN_POINT('Ctrl Pts',(3.43976918378828,-1.80986061704842,8.15428561269597));
#16523=CARTESIAN_POINT('Ctrl Pts',(3.50060175364407,-1.86364695448092,8.15851770235492));
#16524=CARTESIAN_POINT('Ctrl Pts',(3.56405252120205,-1.91435101755191,8.16274979201387));
#16525=CARTESIAN_POINT('Ctrl Pts',(3.62741260245876,-1.96498261240673,8.16697583300592));
#16526=CARTESIAN_POINT('Ctrl Pts',(3.69338308935487,-2.01254039464917,8.17120187399797));
#16527=CARTESIAN_POINT('Ctrl Pts',(3.76163238981083,-2.05674678956728,8.17542791499001));
#16528=CARTESIAN_POINT('Ctrl Pts',(3.8299004627781,-2.10096534380487,8.17965511838815));
#16529=CARTESIAN_POINT('Ctrl Pts',(3.90044825105619,-2.14183036022231,8.18388232178627));
#16530=CARTESIAN_POINT('Ctrl Pts',(3.97291114326035,-2.17910475737397,8.18810952518441));
#16531=CARTESIAN_POINT('Ctrl Pts',(4.0452244804956,-2.2163022245117,8.19232800412712));
#16532=CARTESIAN_POINT('Ctrl Pts',(4.11944462263375,-2.24992364401651,8.19654648306983));
#16533=CARTESIAN_POINT('Ctrl Pts',(4.19518228029263,-2.27977798005591,8.20076496201255));
#16534=CARTESIAN_POINT('Ctrl Pts',(4.27089510182833,-2.30962252617058,8.20498205761881));
#16535=CARTESIAN_POINT('Ctrl Pts',(4.34812401865969,-2.33570227176141,8.20919915322506));
#16536=CARTESIAN_POINT('Ctrl Pts',(4.4264593774034,-2.35787414821508,8.21341624883132));
#16537=CARTESIAN_POINT('Ctrl Pts',(4.50479301712052,-2.38004553811905,8.21763325189573));
#16538=CARTESIAN_POINT('Ctrl Pts',(4.5842326030374,-2.3983091039443,8.22185025496013));
#16539=CARTESIAN_POINT('Ctrl Pts',(4.66435430839896,-2.41257193128893,8.22606725802453));
#16540=CARTESIAN_POINT('Ctrl Pts',(4.74480771926037,-2.42689380703065,8.23030171956792));
#16541=CARTESIAN_POINT('Ctrl Pts',(4.82594844733071,-2.43718165208182,8.23453618111131));
#16542=CARTESIAN_POINT('Ctrl Pts',(4.90733989665653,-2.44339369572456,8.2387706426547));
#16543=CARTESIAN_POINT('Ctrl Pts',(4.98851329026299,-2.44958909668977,8.24299375965802));
#16544=CARTESIAN_POINT('Ctrl Pts',(5.06993559493031,-2.4517305361713,8.24721687666135));
#16545=CARTESIAN_POINT('Ctrl Pts',(5.15117328608259,-2.4498289065365,8.25143999366467));
#16546=CARTESIAN_POINT('Ctrl Pts',(5.23273831989722,-2.4479196143931,8.25568012747809));
#16547=CARTESIAN_POINT('Ctrl Pts',(5.31411677973135,-2.44193464489345,8.25992026129152));
#16548=CARTESIAN_POINT('Ctrl Pts',(5.39487650776516,-2.43193740410244,8.26416039510494));
#16549=CARTESIAN_POINT('Ctrl Pts',(5.47563623579896,-2.42194016331143,8.26840052891836));
#16550=CARTESIAN_POINT('Ctrl Pts',(5.55577678239371,-2.40793079298131,8.27264066273178));
#16551=CARTESIAN_POINT('Ctrl Pts',(5.63487951587815,-2.39002355496311,8.2768807965452));
#16552=CARTESIAN_POINT('Ctrl Pts',(5.71383217989905,-2.37215028959648,8.28111288620416));
#16553=CARTESIAN_POINT('Ctrl Pts',(5.79204552480599,-2.35032726670433,8.28534497586312));
#16554=CARTESIAN_POINT('Ctrl Pts',(5.86909494316962,-2.32463117662332,8.28957706552208));
#16555=CARTESIAN_POINT('Ctrl Pts',(5.94603423951164,-2.2989718123924,8.2938031065141));
#16556=CARTESIAN_POINT('Ctrl Pts',(6.02181247612304,-2.26945052093793,8.29802914750613));
#16557=CARTESIAN_POINT('Ctrl Pts',(6.09601642169648,-2.23619474210691,8.30225518849815));
#16558=CARTESIAN_POINT('Ctrl Pts',(6.17024077765402,-2.20292981601,8.30648239189629));
#16559=CARTESIAN_POINT('Ctrl Pts',(6.24288952771448,-2.16592847667754,8.31070959529443));
#16560=CARTESIAN_POINT('Ctrl Pts',(6.31356548021642,-2.12536789029655,8.31493679869257));
#16561=CARTESIAN_POINT('Ctrl Pts',(6.38409556578478,-2.08489101624132,8.31915527763528));
#16562=CARTESIAN_POINT('Ctrl Pts',(6.45266057340652,-2.04086978183839,8.32337375657799));
#16563=CARTESIAN_POINT('Ctrl Pts',(6.51888854564062,-1.99352709642905,8.3275922355207));
#16564=CARTESIAN_POINT('Ctrl Pts',(6.5850948001965,-1.9461999357772,8.33180933112696));
#16565=CARTESIAN_POINT('Ctrl Pts',(6.64896516356059,-1.89555375715765,8.33602642673322));
#16566=CARTESIAN_POINT('Ctrl Pts',(6.71015687043073,-1.84185463663134,8.34024352233948));
#16567=CARTESIAN_POINT('Ctrl Pts',(6.77134723448216,-1.78815669450301,8.34446052540387));
#16568=CARTESIAN_POINT('Ctrl Pts',(6.82985871039997,-1.73140625104065,8.34867752846826));
#16569=CARTESIAN_POINT('Ctrl Pts',(6.88538292579458,-1.67190854168408,8.35289453153265));
#16570=CARTESIAN_POINT('Ctrl Pts',(6.94113701257752,-1.61216451059283,8.35712899307605));
#16571=CARTESIAN_POINT('Ctrl Pts',(6.99387872019512,-1.54965075382522,8.36136345461945));
#16572=CARTESIAN_POINT('Ctrl Pts',(7.04333566297255,-1.48471102545557,8.36559791616285));
#16573=CARTESIAN_POINT('Ctrl Pts',(7.09266010572292,-1.41994527702247,8.36982103316618));
#16574=CARTESIAN_POINT('Ctrl Pts',(7.13871713113803,-1.35276694814826,8.3740441501695));
#16575=CARTESIAN_POINT('Ctrl Pts',(7.18128022620912,-1.28354584156208,8.37826726717283));
#16576=CARTESIAN_POINT('Ctrl Pts',(7.22401482685434,-1.21404581245845,8.38250740098627));
#16577=CARTESIAN_POINT('Ctrl Pts',(7.26322706153285,-1.14248692596317,8.3867475347997));
#16578=CARTESIAN_POINT('Ctrl Pts',(7.29873523791302,-1.06926638304164,8.39098766861314));
#16579=CARTESIAN_POINT('Ctrl Pts',(7.3342434142932,-0.996045840120104,8.39522780242657));
#16580=CARTESIAN_POINT('Ctrl Pts',(7.36604740694082,-0.921164095233479,
8.39946793624001));
#16581=CARTESIAN_POINT('Ctrl Pts',(7.39401556223308,-0.84503464030478,8.40370807005344));
#16582=CARTESIAN_POINT('Ctrl Pts',(7.42616850853488,-0.757514163865443,
8.40858264234436));
#16583=CARTESIAN_POINT('Ctrl Pts',(7.45335219664532,-0.6680757325126,8.41345721463529));
#16584=CARTESIAN_POINT('Ctrl Pts',(7.47536636025846,-0.577253207851724,
8.41833178692621));
#16585=CARTESIAN_POINT('Ctrl Pts',(7.49809992997909,-0.483462672228121,
8.42336565652858));
#16586=CARTESIAN_POINT('Ctrl Pts',(7.5153201250636,-0.388196137854479,8.42839952613096));
#16587=CARTESIAN_POINT('Ctrl Pts',(7.52685978595068,-0.292065864034257,
8.43343339573333));
#16588=CARTESIAN_POINT('Ctrl Pts',(7.53839944683776,-0.195935590214034,
8.43846726533571));
#16589=CARTESIAN_POINT('Ctrl Pts',(7.54425836357543,-0.0989417664283526,
8.44350113493809));
#16590=CARTESIAN_POINT('Ctrl Pts',(7.54432655273176,-0.00171870211734679,
8.44853500454046));
#16591=CARTESIAN_POINT('',(7.54195686003335,0.00183542991444358,9.24853503495399));
#16592=CARTESIAN_POINT('Ctrl Pts',(7.54168864282551,-0.00171626520296555,
8.448535034954));
#16593=CARTESIAN_POINT('Ctrl Pts',(7.5382686113892,0.525630161723889,8.47586847115655));
#16594=CARTESIAN_POINT('Ctrl Pts',(7.11247508906639,1.87364192080501,8.54547766519524));
#16595=CARTESIAN_POINT('Ctrl Pts',(4.89327789020825,2.88797067463353,8.65736261706985));
#16596=CARTESIAN_POINT('Ctrl Pts',(2.56077430391188,1.40151271011197,8.78418989057805));
#16597=CARTESIAN_POINT('Ctrl Pts',(2.54053913495462,-1.36430015381262,8.91101716408634));
#16598=CARTESIAN_POINT('Ctrl Pts',(4.85104382663735,-2.88472717612166,9.03784443759448));
#16599=CARTESIAN_POINT('Ctrl Pts',(7.09724314960541,-1.89752823793867,9.15035039455043));
#16600=CARTESIAN_POINT('Ctrl Pts',(7.53818936996484,-0.537343409699177,
9.22058059367024));
#16601=CARTESIAN_POINT('Ctrl Pts',(7.54195686003335,0.00183542991444358,
9.24853503495399));
#16602=CARTESIAN_POINT('',(7.54821173167671,0.000461678744492038,10.048535034954));
#16603=CARTESIAN_POINT('Ctrl Pts',(7.54195686003335,0.00183542991444358,
9.24853503495399));
#16604=CARTESIAN_POINT('Ctrl Pts',(7.54388697973531,0.278061692569365,9.26285635150631));
#16605=CARTESIAN_POINT('Ctrl Pts',(7.37337365908062,1.36738067873508,9.3194534258947));
#16606=CARTESIAN_POINT('Ctrl Pts',(5.77424895855223,2.81382671743475,9.41832625811913));
#16607=CARTESIAN_POINT('Ctrl Pts',(3.10188641709578,2.10065863938698,9.54515353162742));
#16608=CARTESIAN_POINT('Ctrl Pts',(2.24784426931667,-0.530071728273779,
9.67198080513556));
#16609=CARTESIAN_POINT('Ctrl Pts',(3.99172515361836,-2.67693216321298,9.79880807864387));
#16610=CARTESIAN_POINT('Ctrl Pts',(6.71326072902087,-2.38324880778346,9.92432615524993));
#16611=CARTESIAN_POINT('Ctrl Pts',(7.54617390178795,-0.784506859752817,
10.00756847402));
#16612=CARTESIAN_POINT('Ctrl Pts',(7.54821173167671,0.000461678744492038,
10.048535034954));
#16613=CARTESIAN_POINT('',(7.54432619404612,-0.00217068071248294,10.848535034954));
#16614=CARTESIAN_POINT('Ctrl Pts',(7.54821173167671,0.000461678744492038,
10.048535034954));
#16615=CARTESIAN_POINT('Ctrl Pts',(7.54827685602488,0.0255474646978529,
10.0498442318561));
#16616=CARTESIAN_POINT('Ctrl Pts',(7.54792542615634,0.0506313813797534,
10.0511534287582));
#16617=CARTESIAN_POINT('Ctrl Pts',(7.52217079946011,0.885275564505149,10.0947383834963));
#16618=CARTESIAN_POINT('Ctrl Pts',(6.59176120172026,2.47725417354276,10.1792898991685));
#16619=CARTESIAN_POINT('Ctrl Pts',(3.82877479129759,2.60388883938323,10.3061171726766));
#16620=CARTESIAN_POINT('Ctrl Pts',(2.22057700338537,0.353593297184827,10.4329444461849));
#16621=CARTESIAN_POINT('Ctrl Pts',(3.23519287125426,-2.21947591850572,10.559771719693));
#16622=CARTESIAN_POINT('Ctrl Pts',(5.94644183489036,-2.76652172461777,10.6865989932015));
#16623=CARTESIAN_POINT('Ctrl Pts',(7.41343416718733,-1.26507931657609,10.7828532647379));
#16624=CARTESIAN_POINT('Ctrl Pts',(7.54521040552383,-0.227592870575658,
10.8368317784384));
#16625=CARTESIAN_POINT('Ctrl Pts',(7.54327304612934,-0.00217939107654637,
10.8485345343029));
#16626=CARTESIAN_POINT('',(7.5443269150918,0.00108536201693948,11.6485350350021));
#16627=CARTESIAN_POINT('Ctrl Pts',(7.54432619404612,-0.00217068071248294,
10.848535034954));
#16628=CARTESIAN_POINT('Ctrl Pts',(7.54439758870431,0.0784273272084078,
10.8527176653695));
#16629=CARTESIAN_POINT('Ctrl Pts',(7.54048835863867,0.159110489711957,10.8569002957851));
#16630=CARTESIAN_POINT('Ctrl Pts',(7.53260002673345,0.239451732729212,10.8610829262006));
#16631=CARTESIAN_POINT('Ctrl Pts',(7.52471552024031,0.319754014611907,10.8652635282678));
#16632=CARTESIAN_POINT('Ctrl Pts',(7.51285578733571,0.399714235407546,10.869444130335));
#16633=CARTESIAN_POINT('Ctrl Pts',(7.49707436666984,0.478908228973995,10.8736247324022));
#16634=CARTESIAN_POINT('Ctrl Pts',(7.48129555878778,0.558089111123662,10.8778046423258));
#16635=CARTESIAN_POINT('Ctrl Pts',(7.46159644552335,0.636503553587562,10.8819845522494));
#16636=CARTESIAN_POINT('Ctrl Pts',(7.43808179808031,0.713736940700719,10.886164462173));
#16637=CARTESIAN_POINT('Ctrl Pts',(7.41456353342076,0.790982208488829,10.8903450150847));
#16638=CARTESIAN_POINT('Ctrl Pts',(7.38722870974025,0.867045607888982,10.8945255679965));
#16639=CARTESIAN_POINT('Ctrl Pts',(7.35623167927006,0.941528555388835,10.8987061209082));
#16640=CARTESIAN_POINT('Ctrl Pts',(7.3252008460254,1.01609272777502,10.902891232782));
#16641=CARTESIAN_POINT('Ctrl Pts',(7.29050002116863,1.08907257212126,10.9070763446559));
#16642=CARTESIAN_POINT('Ctrl Pts',(7.2523310345847,1.16009105408751,10.9112614565297));
#16643=CARTESIAN_POINT('Ctrl Pts',(7.21413743490858,1.23115533198916,10.9154492671533));
#16644=CARTESIAN_POINT('Ctrl Pts',(7.17247147012247,1.30025532719584,10.919637077777));
#16645=CARTESIAN_POINT('Ctrl Pts',(7.12757877001081,1.36704228913517,10.9238248884006));
#16646=CARTESIAN_POINT('Ctrl Pts',(7.08261342784854,1.43393732080205,10.92801947543));
#16647=CARTESIAN_POINT('Ctrl Pts',(7.03441121891333,1.4985114758326,10.9322140624593));
#16648=CARTESIAN_POINT('Ctrl Pts',(6.98325807194982,1.56044899365099,10.9364086494887));
#16649=CARTESIAN_POINT('Ctrl Pts',(6.9676285428175,1.57937362090447,10.9376902797317));
#16650=CARTESIAN_POINT('Ctrl Pts',(6.95172377932987,1.59805236370055,10.9389719099747));
#16651=CARTESIAN_POINT('Ctrl Pts',(6.93555258950466,1.61647693319998,10.9402535402177));
#16652=CARTESIAN_POINT('Ctrl Pts',(6.88215346157301,1.67731697987681,10.9444856306234));
#16653=CARTESIAN_POINT('Ctrl Pts',(6.82563677562139,1.73562167331044,10.9487177210291));
#16654=CARTESIAN_POINT('Ctrl Pts',(6.76627263775363,1.79105453817927,10.9529498114348));
#16655=CARTESIAN_POINT('Ctrl Pts',(6.7069933456937,1.84640817598664,10.9571758531528));
#16656=CARTESIAN_POINT('Ctrl Pts',(6.64487502138773,1.89889782280003,10.9614018948708));
#16657=CARTESIAN_POINT('Ctrl Pts',(6.5802269316755,1.94822122851745,10.9656279365888));
#16658=CARTESIAN_POINT('Ctrl Pts',(6.5155610739181,1.99755819040497,10.9698551398029));
#16659=CARTESIAN_POINT('Ctrl Pts',(6.44836438740582,2.04372683777131,10.9740823430169));
#16660=CARTESIAN_POINT('Ctrl Pts',(6.37898217395731,2.08646275509856,10.978309546231));
#16661=CARTESIAN_POINT('Ctrl Pts',(6.30974314328738,2.12911047911107,10.9825280258447));
#16662=CARTESIAN_POINT('Ctrl Pts',(6.23832797970495,2.16833936204999,10.9867465054583));
#16663=CARTESIAN_POINT('Ctrl Pts',(6.16511013076783,2.20392899994552,10.990964985072));
#16664=CARTESIAN_POINT('Ctrl Pts',(6.09191629202919,2.23950696699463,10.9951820813272));
#16665=CARTESIAN_POINT('Ctrl Pts',(6.01692135951698,2.27144785601566,10.9993991775824));
#16666=CARTESIAN_POINT('Ctrl Pts',(5.94052277285337,2.29957752238866,11.0036162738377));
#16667=CARTESIAN_POINT('Ctrl Pts',(5.86412586312688,2.32770657131986,11.0078332775283));
#16668=CARTESIAN_POINT('Ctrl Pts',(5.78632579697358,2.35202440445222,11.0120502812188));
#16669=CARTESIAN_POINT('Ctrl Pts',(5.70753800194581,2.37240579305,11.0162672849094));
#16670=CARTESIAN_POINT('Ctrl Pts',(5.62842405069097,2.39287155406619,11.0205017456442));
#16671=CARTESIAN_POINT('Ctrl Pts',(5.54831462892302,2.40936807926501,11.0247362063789));
#16672=CARTESIAN_POINT('Ctrl Pts',(5.46764182776139,2.42182015037596,11.0289706671136));
#16673=CARTESIAN_POINT('Ctrl Pts',(5.38718513086499,2.43423886519286,11.0331937846817));
#16674=CARTESIAN_POINT('Ctrl Pts',(5.30616853838209,2.44263475937085,11.0374169022497));
#16675=CARTESIAN_POINT('Ctrl Pts',(5.22502512901692,2.44698535789096,11.0416400198178));
#16676=CARTESIAN_POINT('Ctrl Pts',(5.14355479652035,2.45135348477601,11.0458801521358));
#16677=CARTESIAN_POINT('Ctrl Pts',(5.06195709457966,2.45164365752031,11.0501202844539));
#16678=CARTESIAN_POINT('Ctrl Pts',(4.98066777652221,2.44788586436541,11.0543604167719));
#16679=CARTESIAN_POINT('Ctrl Pts',(4.89937845846479,2.4441280712105,11.0586005490899));
#16680=CARTESIAN_POINT('Ctrl Pts',(4.81839798349671,2.4363224189142,11.0628406814079));
#16681=CARTESIAN_POINT('Ctrl Pts',(4.73815252935017,2.42455064091195,11.067080813726));
#16682=CARTESIAN_POINT('Ctrl Pts',(4.65805914449168,2.41280117103816,11.0713129107738));
#16683=CARTESIAN_POINT('Ctrl Pts',(4.57839918700369,2.39705677527953,11.0755450078217));
#16684=CARTESIAN_POINT('Ctrl Pts',(4.49960190535111,2.3773612687476,11.0797771048696));
#16685=CARTESIAN_POINT('Ctrl Pts',(4.42091724289576,2.35769391156408,11.0840031532903));
#16686=CARTESIAN_POINT('Ctrl Pts',(4.34309325453466,2.33408677097203,11.0882292017111));
#16687=CARTESIAN_POINT('Ctrl Pts',(4.26655174843519,2.30663513606798,11.0924552501319));
#16688=CARTESIAN_POINT('Ctrl Pts',(4.18998935711926,2.27917601067456,11.0966824516778));
#16689=CARTESIAN_POINT('Ctrl Pts',(4.11471060530473,2.24787038661509,11.1009096532237));
#16690=CARTESIAN_POINT('Ctrl Pts',(4.04112512980976,2.21286436439434,11.1051368547697));
#16691=CARTESIAN_POINT('Ctrl Pts',(3.96769136394277,2.17793051335374,11.109355341183));
#16692=CARTESIAN_POINT('Ctrl Pts',(3.89594432977266,2.1393116840397,11.1135738275964));
#16693=CARTESIAN_POINT('Ctrl Pts',(3.82627202458665,2.09720152589447,11.1177923140098));
#16694=CARTESIAN_POINT('Ctrl Pts',(3.75662256652938,2.05510517662499,11.1220094170858));
#16695=CARTESIAN_POINT('Ctrl Pts',(3.68904688372532,2.00952001234369,11.1262265201618));
#16696=CARTESIAN_POINT('Ctrl Pts',(3.62390718692327,1.9606849660558,11.1304436232378));
#16697=CARTESIAN_POINT('Ctrl Pts',(3.55876891974422,1.91185099155222,11.1346606337609));
#16698=CARTESIAN_POINT('Ctrl Pts',(3.49606690338341,1.8597675565151,11.138877644284));
#16699=CARTESIAN_POINT('Ctrl Pts',(3.43613206856243,1.80471528194851,11.1430946548071));
#16700=CARTESIAN_POINT('Ctrl Pts',(3.37594933440138,1.74943530303311,11.1473291075094));
#16701=CARTESIAN_POINT('Ctrl Pts',(3.31855707759335,1.69116218289615,11.1515635602116));
#16702=CARTESIAN_POINT('Ctrl Pts',(3.26425330714429,1.63021771048669,11.1557980129139));
#16703=CARTESIAN_POINT('Ctrl Pts',(3.21009481444188,1.56943628155559,11.160021137273));
#16704=CARTESIAN_POINT('Ctrl Pts',(3.15900856526425,1.50599816532624,11.1642442616321));
#16705=CARTESIAN_POINT('Ctrl Pts',(3.11124883825198,1.4402546532346,11.1684673859912));
#16706=CARTESIAN_POINT('Ctrl Pts',(3.06329694122607,1.37424661007452,11.172707502865));
#16707=CARTESIAN_POINT('Ctrl Pts',(3.01869864295373,1.30591497909931,11.1769476197388));
#16708=CARTESIAN_POINT('Ctrl Pts',(2.97766563737836,1.23564180870493,11.1811877366127));
#16709=CARTESIAN_POINT('Ctrl Pts',(2.93663263180299,1.16536863831054,11.1854278534865));
#16710=CARTESIAN_POINT('Ctrl Pts',(2.89916507892861,1.09315437195268,11.1896679703603));
#16711=CARTESIAN_POINT('Ctrl Pts',(2.86542603596681,1.01940114806303,11.1939080872342));
#16712=CARTESIAN_POINT('Ctrl Pts',(2.83175100969359,0.945787864039777,11.1981401588816));
#16713=CARTESIAN_POINT('Ctrl Pts',(2.80166470758439,0.870366826279314,11.2023722305289));
#16714=CARTESIAN_POINT('Ctrl Pts',(2.77536368487898,0.793522139334085,11.2066043021763));
#16715=CARTESIAN_POINT('Ctrl Pts',(2.74910025282121,0.71678728239748,11.2108303251496));
#16716=CARTESIAN_POINT('Ctrl Pts',(2.72661150434788,0.638633253481783,11.2150563481229));
#16717=CARTESIAN_POINT('Ctrl Pts',(2.70804674541415,0.559465892681889,11.2192823710962));
#16718=CARTESIAN_POINT('Ctrl Pts',(2.68947678113385,0.480276334257343,11.2235095789981));
#16719=CARTESIAN_POINT('Ctrl Pts',(2.67483317695073,0.400073310493394,11.2277367869));
#16720=CARTESIAN_POINT('Ctrl Pts',(2.66421597596828,0.319280075360713,11.231963994802));
#16721=CARTESIAN_POINT('Ctrl Pts',(2.65362074391374,0.238654016187215,11.2361824558387));
#16722=CARTESIAN_POINT('Ctrl Pts',(2.64703535431247,0.157440643226408,11.2404009168754));
#16723=CARTESIAN_POINT('Ctrl Pts',(2.64450817448571,0.0760708845275549,
11.2446193779122));
#16724=CARTESIAN_POINT('Ctrl Pts',(2.64198182333396,-0.00527219261689159,
11.2488364556943));
#16725=CARTESIAN_POINT('Ctrl Pts',(2.64351105370798,-0.0867710895524872,
11.2530535334763));
#16726=CARTESIAN_POINT('Ctrl Pts',(2.64909220679532,-0.167991906981183,
11.2572706112584));
#16727=CARTESIAN_POINT('Ctrl Pts',(2.65467323754636,-0.249210944087131,
11.2614875966041));
#16728=CARTESIAN_POINT('Ctrl Pts',(2.66430598141719,-0.330151450284385,
11.2657045819498));
#16729=CARTESIAN_POINT('Ctrl Pts',(2.67793478526406,-0.41038312058654,11.2699215672955));
#16730=CARTESIAN_POINT('Ctrl Pts',(2.69162013879732,-0.490947694336733,
11.2741560500827));
#16731=CARTESIAN_POINT('Ctrl Pts',(2.70933471837483,-0.570797069989575,
11.27839053287));
#16732=CARTESIAN_POINT('Ctrl Pts',(2.73097041610576,-0.649506181125932,
11.2826250156572));
#16733=CARTESIAN_POINT('Ctrl Pts',(2.75254795311202,-0.728003707732052,
11.2868481153779));
#16734=CARTESIAN_POINT('Ctrl Pts',(2.77802536847771,-0.805366661228117,
11.2910712150986));
#16735=CARTESIAN_POINT('Ctrl Pts',(2.80724602416878,-0.881190660444427,
11.2952943148192));
#16736=CARTESIAN_POINT('Ctrl Pts',(2.83658482317548,-0.957321227000153,
11.2995344891398));
#16737=CARTESIAN_POINT('Ctrl Pts',(2.86969699642403,-1.03189994103223,11.3037746634603));
#16738=CARTESIAN_POINT('Ctrl Pts',(2.90637692938527,-1.10454142451776,11.3080148377808));
#16739=CARTESIAN_POINT('Ctrl Pts',(2.94305686234651,-1.17718290800332,11.3122550121013));
#16740=CARTESIAN_POINT('Ctrl Pts',(2.98330426974135,-1.24788678555084,11.3164951864219));
#16741=CARTESIAN_POINT('Ctrl Pts',(3.02687023336538,-1.31629758498359,11.3207353607424));
#16742=CARTESIAN_POINT('Ctrl Pts',(3.07035323835108,-1.38457811605323,11.3249674608908));
#16743=CARTESIAN_POINT('Ctrl Pts',(3.11730439207376,-1.45082905390806,11.3291995610392));
#16744=CARTESIAN_POINT('Ctrl Pts',(3.16750813329105,-1.51467662385626,11.3334316611877));
#16745=CARTESIAN_POINT('Ctrl Pts',(3.21764012001026,-1.5784329386465,11.3376577125394));
#16746=CARTESIAN_POINT('Ctrl Pts',(3.27101517634973,-1.63979234568297,11.3418837638912));
#16747=CARTESIAN_POINT('Ctrl Pts',(3.3273738135302,-1.69840891448714,11.346109815243));
#16748=CARTESIAN_POINT('Ctrl Pts',(3.38374777964987,-1.75704142636348,11.350337016035));
#16749=CARTESIAN_POINT('Ctrl Pts',(3.44310667705206,-1.81292922893659,11.3545642168269));
#16750=CARTESIAN_POINT('Ctrl Pts',(3.50514962997472,-1.86575828285442,11.3587914176189));
#16751=CARTESIAN_POINT('Ctrl Pts',(3.5670647180324,-1.9184784609124,11.3630099065358));
#16752=CARTESIAN_POINT('Ctrl Pts',(3.6316524718586,-1.96815216501466,11.3672283954526));
#16753=CARTESIAN_POINT('Ctrl Pts',(3.69857747712651,-2.01450455078402,11.3714468843695));
#16754=CARTESIAN_POINT('Ctrl Pts',(3.76548053355875,-2.06084173474809,11.3756639897837));
#16755=CARTESIAN_POINT('Ctrl Pts',(3.83471893746229,-2.10385949918518,11.379881095198));
#16756=CARTESIAN_POINT('Ctrl Pts',(3.90592650012927,-2.14332505306153,11.3840982006122));
#16757=CARTESIAN_POINT('Ctrl Pts',(3.9771324971775,-2.18278973922089,11.3883152133063));
#16758=CARTESIAN_POINT('Ctrl Pts',(4.05030715991266,-2.21870214584994,11.3925322260003));
#16759=CARTESIAN_POINT('Ctrl Pts',(4.12505905329797,-2.25087507744138,11.3967492386944));
#16760=CARTESIAN_POINT('Ctrl Pts',(4.20012003846211,-2.28318104096292,11.4009836883241));
#16761=CARTESIAN_POINT('Ctrl Pts',(4.27677089713528,-2.31171634061407,11.4052181379537));
#16762=CARTESIAN_POINT('Ctrl Pts',(4.35459609551625,-2.33634066223756,11.4094525875834));
#16763=CARTESIAN_POINT('Ctrl Pts',(4.43221317814195,-2.36089913488925,11.4136757136868));
#16764=CARTESIAN_POINT('Ctrl Pts',(4.51099786507144,-2.38156744102214,11.4178988397902));
#16765=CARTESIAN_POINT('Ctrl Pts',(4.59052558684527,-2.39825723829553,11.4221219658935));
#16766=CARTESIAN_POINT('Ctrl Pts',(4.6703731667867,-2.4150141614447,11.4263620772864));
#16767=CARTESIAN_POINT('Ctrl Pts',(4.75096930409871,-2.42776044033142,11.4306021886792));
#16768=CARTESIAN_POINT('Ctrl Pts',(4.83187878393395,-2.43645917278711,11.4348423000721));
#16769=CARTESIAN_POINT('Ctrl Pts',(4.91278826376918,-2.44515790524281,11.439082411465));
#16770=CARTESIAN_POINT('Ctrl Pts',(4.99401061602312,-2.4498091266491,11.4433225228578));
#16771=CARTESIAN_POINT('Ctrl Pts',(5.0751121874727,-2.45042853394534,11.4475626342507));
#16772=CARTESIAN_POINT('Ctrl Pts',(5.1560611600733,-2.45104677577907,11.4517947675476));
#16773=CARTESIAN_POINT('Ctrl Pts',(5.2371917788119,-2.44765068432874,11.4560269008445));
#16774=CARTESIAN_POINT('Ctrl Pts',(5.31807313171866,-2.44021802143348,11.4602590341414));
#16775=CARTESIAN_POINT('Ctrl Pts',(5.39883889267889,-2.43279598096157,11.4644851190661));
#16776=CARTESIAN_POINT('Ctrl Pts',(5.47935563647557,-2.42134886884991,11.4687112039909));
#16777=CARTESIAN_POINT('Ctrl Pts',(5.55919194504468,-2.40590645342008,11.4729372889156));
#16778=CARTESIAN_POINT('Ctrl Pts',(5.63904917625865,-2.39045999100737,11.4771644813674));
#16779=CARTESIAN_POINT('Ctrl Pts',(5.71822514934162,-2.37101615404332,11.4813916738192));
#16780=CARTESIAN_POINT('Ctrl Pts',(5.79629273058369,-2.3476567819331,11.485618866271));
#16781=CARTESIAN_POINT('Ctrl Pts',(5.87420020970802,-2.32434531555896,11.4898373895357));
#16782=CARTESIAN_POINT('Ctrl Pts',(5.9510033863069,-2.29713446733452,11.4940559128005));
#16783=CARTESIAN_POINT('Ctrl Pts',(6.0262892383907,-2.2661563745434,11.4982744360653));
#16784=CARTESIAN_POINT('Ctrl Pts',(6.10155040361138,-2.23518843972905,11.5024915760408));
#16785=CARTESIAN_POINT('Ctrl Pts',(6.17529480300427,-2.20045589024738,11.5067087160164));
#16786=CARTESIAN_POINT('Ctrl Pts',(6.24712798438816,-2.16213955330772,11.5109258559919));
#16787=CARTESIAN_POINT('Ctrl Pts',(6.31895958922144,-2.12382405731154,11.5151429034123));
#16788=CARTESIAN_POINT('Ctrl Pts',(6.38887964998971,-2.08192514995343,11.5193599508327));
#16789=CARTESIAN_POINT('Ctrl Pts',(6.45651826229098,-2.03666963382503,11.523576998253));
#16790=CARTESIAN_POINT('Ctrl Pts',(6.52443534469827,-1.99122779943927,11.5278114073785));
#16791=CARTESIAN_POINT('Ctrl Pts',(6.59005175412252,-1.9424019110021,11.532045816504));
#16792=CARTESIAN_POINT('Ctrl Pts',(6.6530238549092,-1.89046446737442,11.5362802256295));
#16793=CARTESIAN_POINT('Ctrl Pts',(6.71582867708937,-1.83866498997443,11.540503386503));
#16794=CARTESIAN_POINT('Ctrl Pts',(6.77600290369533,-1.78377081286643,11.5447265473765));
#16795=CARTESIAN_POINT('Ctrl Pts',(6.83324159173854,-1.72609028409346,11.54894970825));
#16796=CARTESIAN_POINT('Ctrl Pts',(6.89070895986495,-1.66817930999461,11.5531897415015));
#16797=CARTESIAN_POINT('Ctrl Pts',(6.94521697590909,-1.60746003023737,11.5574297747529));
#16798=CARTESIAN_POINT('Ctrl Pts',(6.99649810758367,-1.54427766218338,11.5616698080044));
#16799=CARTESIAN_POINT('Ctrl Pts',(7.04777923925826,-1.4810952941294,11.5659098412559));
#16800=CARTESIAN_POINT('Ctrl Pts',(7.0958332607517,-1.41545025153213,11.5701498745074));
#16801=CARTESIAN_POINT('Ctrl Pts',(7.14043763303792,-1.34771503035326,11.5743899077589));
#16802=CARTESIAN_POINT('Ctrl Pts',(7.18580626072282,-1.27881922769294,11.5787025901283));
#16803=CARTESIAN_POINT('Ctrl Pts',(7.22777065521348,-1.20751132097549,11.5830152724977));
#16804=CARTESIAN_POINT('Ctrl Pts',(7.26607126061476,-1.13415422125497,11.5873279548672));
#16805=CARTESIAN_POINT('Ctrl Pts',(7.30431097491278,-1.06091374618534,11.591633780844));
#16806=CARTESIAN_POINT('Ctrl Pts',(7.33889827398536,-0.985630940696496,
11.5959396068208));
#16807=CARTESIAN_POINT('Ctrl Pts',(7.36961701700286,-0.908697285165616,
11.6002454327976));
#16808=CARTESIAN_POINT('Ctrl Pts',(7.40028604158352,-0.831888147135061,
11.6045442897739));
#16809=CARTESIAN_POINT('Ctrl Pts',(7.42709880731689,-0.753433883498876,
11.6088431467502));
#16810=CARTESIAN_POINT('Ctrl Pts',(7.44988590611216,-0.673748776208844,
11.6131420037265));
#16811=CARTESIAN_POINT('Ctrl Pts',(7.47265125111263,-0.59413974062448,11.6174367567818));
#16812=CARTESIAN_POINT('Ctrl Pts',(7.49139844590941,-0.513302618978107,
11.6217315098371));
#16813=CARTESIAN_POINT('Ctrl Pts',(7.50600706647091,-0.431669233189206,
11.6260262628924));
#16814=CARTESIAN_POINT('Ctrl Pts',(7.52060499333906,-0.350095604061897,
11.6303178721347));
#16815=CARTESIAN_POINT('Ctrl Pts',(7.53107029247444,-0.267727303234328,
11.6346094813769));
#16816=CARTESIAN_POINT('Ctrl Pts',(7.53733332939813,-0.185007642795082,
11.6389010906192));
#16817=CARTESIAN_POINT('Ctrl Pts',(7.54201981921922,-0.123110379314718,
11.6421124053974));
#16818=CARTESIAN_POINT('Ctrl Pts',(7.54435442096618,-0.0610166788267173,
11.6453237201757));
#16819=CARTESIAN_POINT('Ctrl Pts',(7.54432691509222,0.00108536108698895,
11.648535034954));
#16820=CARTESIAN_POINT('',(7.54432661325899,0.0016301205695403,12.448535034954));
#16821=CARTESIAN_POINT('Ctrl Pts',(7.5443269150918,0.00108536201690472,
11.6485350350021));
#16822=CARTESIAN_POINT('Ctrl Pts',(7.54428737102145,0.0903668490952409,
11.653151807));
#16823=CARTESIAN_POINT('Ctrl Pts',(7.53936432127917,0.179489947527524,11.6577685789978));
#16824=CARTESIAN_POINT('Ctrl Pts',(7.52963449152874,0.26794191818403,11.6623853509957));
#16825=CARTESIAN_POINT('Ctrl Pts',(7.51987558796534,0.356658193162158,11.6670159184216));
#16826=CARTESIAN_POINT('Ctrl Pts',(7.50528126174495,0.444699028238786,11.6716464858474));
#16827=CARTESIAN_POINT('Ctrl Pts',(7.48597916961371,0.53156278194337,11.6762770532733));
#16828=CARTESIAN_POINT('Ctrl Pts',(7.466590452723,0.61881636653884,11.6809284019588));
#16829=CARTESIAN_POINT('Ctrl Pts',(7.44245175505355,0.704881992755861,11.6855797506444));
#16830=CARTESIAN_POINT('Ctrl Pts',(7.41374112037227,0.789271464942855,11.69023109933));
#16831=CARTESIAN_POINT('Ctrl Pts',(7.39113711119857,0.855711668186527,11.6938931266423));
#16832=CARTESIAN_POINT('Ctrl Pts',(7.36570018578957,0.921113268291848,11.6975551539547));
#16833=CARTESIAN_POINT('Ctrl Pts',(7.33753740077229,0.98524848898628,11.7012171812671));
#16834=CARTESIAN_POINT('Ctrl Pts',(7.30498972907498,1.05936942930224,11.7054493785671));
#16835=CARTESIAN_POINT('Ctrl Pts',(7.26870453044918,1.13201406351384,11.709681575867));
#16836=CARTESIAN_POINT('Ctrl Pts',(7.22883777515172,1.20278007290367,11.713913773167));
#16837=CARTESIAN_POINT('Ctrl Pts',(7.18902800487398,1.27344493028325,11.7181399210194));
#16838=CARTESIAN_POINT('Ctrl Pts',(7.14564707184775,1.34223609465023,11.7223660688718));
#16839=CARTESIAN_POINT('Ctrl Pts',(7.0988986101566,1.40877205804673,11.7265922167241));
#16840=CARTESIAN_POINT('Ctrl Pts',(7.05213876890876,1.47532421769314,11.7308193933096));
#16841=CARTESIAN_POINT('Ctrl Pts',(7.00200997126493,1.53961966245601,11.7350465698951));
#16842=CARTESIAN_POINT('Ctrl Pts',(6.94876160056616,1.60130211213661,11.7392737464805));
#16843=CARTESIAN_POINT('Ctrl Pts',(6.89562147843312,1.66285916761976,11.7434923296425));
#16844=CARTESIAN_POINT('Ctrl Pts',(6.83937473883501,1.72181347324932,11.7477109128044));
#16845=CARTESIAN_POINT('Ctrl Pts',(6.78031090407868,1.77784217961603,11.7519294959663));
#16846=CARTESIAN_POINT('Ctrl Pts',(6.72126645428652,1.83385249715867,11.756146694574));
#16847=CARTESIAN_POINT('Ctrl Pts',(6.65940708232636,1.88693880275201,11.7603638931816));
#16848=CARTESIAN_POINT('Ctrl Pts',(6.5950591456263,1.93681510776859,11.7645810917893));
#16849=CARTESIAN_POINT('Ctrl Pts',(6.53071264156319,1.98669030234337,11.7687981965056));
#16850=CARTESIAN_POINT('Ctrl Pts',(6.46387805088233,2.03335535468002,11.7730153012219));
#16851=CARTESIAN_POINT('Ctrl Pts',(6.39491364406077,2.07656548154942,11.7772324059383));
#16852=CARTESIAN_POINT('Ctrl Pts',(6.32566742255814,2.11995218135962,11.7814667433413));
#16853=CARTESIAN_POINT('Ctrl Pts',(6.25427433491571,2.1598553990506,11.7857010807444));
#16854=CARTESIAN_POINT('Ctrl Pts',(6.18112357072248,2.19607303051205,11.7899354181475));
#16855=CARTESIAN_POINT('Ctrl Pts',(6.10816496399789,2.2321955230032,11.7941586325013));
#16856=CARTESIAN_POINT('Ctrl Pts',(6.03345834856939,2.26465161919133,11.7983818468551));
#16857=CARTESIAN_POINT('Ctrl Pts',(5.95740983617412,2.29328916701726,11.8026050612089));
#16858=CARTESIAN_POINT('Ctrl Pts',(5.88106088034333,2.32203985266775,11.8068449601366));
#16859=CARTESIAN_POINT('Ctrl Pts',(5.80335985434953,2.34694162065989,11.8110848590643));
#16860=CARTESIAN_POINT('Ctrl Pts',(5.72473115689336,2.36789154966326,11.8153247579921));
#16861=CARTESIAN_POINT('Ctrl Pts',(5.6461024594372,2.38884147866663,11.8195646569198));
#16862=CARTESIAN_POINT('Ctrl Pts',(5.5665465603225,2.40583953184433,11.8238045558475));
#16863=CARTESIAN_POINT('Ctrl Pts',(5.48649434798162,2.41883499352721,11.8280444547753));
#16864=CARTESIAN_POINT('Ctrl Pts',(5.40658498862843,2.43180726483879,11.8322767876132));
#16865=CARTESIAN_POINT('Ctrl Pts',(5.32588318148657,2.44083959441903,11.8365091204511));
#16866=CARTESIAN_POINT('Ctrl Pts',(5.2448114322562,2.44584423015004,11.840741453289));
#16867=CARTESIAN_POINT('Ctrl Pts',(5.16385550657287,2.45084171598399,11.8449677395841));
#16868=CARTESIAN_POINT('Ctrl Pts',(5.08253114837649,2.4518229080577,11.8491940258792));
#16869=CARTESIAN_POINT('Ctrl Pts',(5.00126930042078,2.44875137436854,11.8534203121744));
#16870=CARTESIAN_POINT('Ctrl Pts',(4.91999099271485,2.44567921853408,11.8576474545122));
#16871=CARTESIAN_POINT('Ctrl Pts',(4.83877568474453,2.43855264724011,11.8618745968501));
#16872=CARTESIAN_POINT('Ctrl Pts',(4.75805795456608,2.42738733904082,11.866101739188));
#16873=CARTESIAN_POINT('Ctrl Pts',(4.67750090536055,2.4162442570932,11.8703204667533));
#16874=CARTESIAN_POINT('Ctrl Pts',(4.59743991853169,2.40107854053588,11.8745391943186));
#16875=CARTESIAN_POINT('Ctrl Pts',(4.51830338163993,2.38195773173578,11.8787579218839));
#16876=CARTESIAN_POINT('Ctrl Pts',(4.43919278099187,2.36284318959803,11.8829752668015));
#16877=CARTESIAN_POINT('Ctrl Pts',(4.36100647987066,2.3397762384881,11.8871926117192));
#16878=CARTESIAN_POINT('Ctrl Pts',(4.28416194662076,2.31287537485409,11.8914099566368));
#16879=CARTESIAN_POINT('Ctrl Pts',(4.20731909329354,2.28597509930839,11.8956272093577));
#16880=CARTESIAN_POINT('Ctrl Pts',(4.13181838766841,2.25524123248628,11.8998444620787));
#16881=CARTESIAN_POINT('Ctrl Pts',(4.05806005722665,2.22084145499663,11.9040617147996));
#16882=CARTESIAN_POINT('Ctrl Pts',(3.98400588791538,2.18630370270164,11.9082958825899));
#16883=CARTESIAN_POINT('Ctrl Pts',(3.91170853201712,2.14807076021067,11.9125300503802));
#16884=CARTESIAN_POINT('Ctrl Pts',(3.84154911436463,2.10635940850739,11.9167642181706));
#16885=CARTESIAN_POINT('Ctrl Pts',(3.77156869803521,2.06475447711647,11.9209875831113));
#16886=CARTESIAN_POINT('Ctrl Pts',(3.70371569113058,2.01968915628265,11.925210948052));
#16887=CARTESIAN_POINT('Ctrl Pts',(3.63833857592227,1.97142163041174,11.9294343129927));
#16888=CARTESIAN_POINT('Ctrl Pts',(3.57271062074898,1.92296891092285,11.9336738822079));
#16889=CARTESIAN_POINT('Ctrl Pts',(3.50957795267431,1.87128967049584,11.937913451423));
#16890=CARTESIAN_POINT('Ctrl Pts',(3.44925756636745,1.81668409930143,11.9421530206381));
#16891=CARTESIAN_POINT('Ctrl Pts',(3.38893718006058,1.762078528107,11.9463925898532));
#16892=CARTESIAN_POINT('Ctrl Pts',(3.33142936163524,1.70454700020993,11.9506321590683));
#16893=CARTESIAN_POINT('Ctrl Pts',(3.27701083306423,1.64442351622122,11.9548717282835));
#16894=CARTESIAN_POINT('Ctrl Pts',(3.22269978240752,1.58441877757217,11.9591029242465));
#16895=CARTESIAN_POINT('Ctrl Pts',(3.17126306813964,1.52160831074434,11.9633341202096));
#16896=CARTESIAN_POINT('Ctrl Pts',(3.12300397143216,1.45629881113922,11.9675653161726));
#16897=CARTESIAN_POINT('Ctrl Pts',(3.07481388079836,1.39108269811716,11.9717904619143));
#16898=CARTESIAN_POINT('Ctrl Pts',(3.02979265752206,1.3233750201322,11.9760156076559));
#16899=CARTESIAN_POINT('Ctrl Pts',(2.98820510569361,1.2535174644043,11.9802407533975));
#16900=CARTESIAN_POINT('Ctrl Pts',(2.94659509957854,1.18362219062113,11.9844681804139));
#16901=CARTESIAN_POINT('Ctrl Pts',(2.90842276915838,1.11157507936504,11.9886956074304));
#16902=CARTESIAN_POINT('Ctrl Pts',(2.87391138256914,1.03774958988234,11.9929230344468));
#16903=CARTESIAN_POINT('Ctrl Pts',(2.83948033164713,0.964095951505664,11.9971406208511));
#16904=CARTESIAN_POINT('Ctrl Pts',(2.80869341764964,0.888672616786132,12.0013582072554));
#16905=CARTESIAN_POINT('Ctrl Pts',(2.78172678220013,0.811875676445236,12.0055757936596));
#16906=CARTESIAN_POINT('Ctrl Pts',(2.75476897252166,0.735103870578877,12.0097919997118));
#16907=CARTESIAN_POINT('Ctrl Pts',(2.73162911231634,0.656959790173955,12.014008205764));
#16908=CARTESIAN_POINT('Ctrl Pts',(2.71243464087164,0.577858063450985,12.0182244118162));
#16909=CARTESIAN_POINT('Ctrl Pts',(2.69324057175096,0.498757994732792,12.0224405294949));
#16910=CARTESIAN_POINT('Ctrl Pts',(2.67799183547715,0.41870077167333,12.0266566471737));
#16911=CARTESIAN_POINT('Ctrl Pts',(2.66676521675643,0.338113288307206,12.0308727648524));
#16912=CARTESIAN_POINT('Ctrl Pts',(2.6554869344874,0.257154951040742,12.0351082845974));
#16913=CARTESIAN_POINT('Ctrl Pts',(2.64826795746175,0.175661927664486,12.0393438043423));
#16914=CARTESIAN_POINT('Ctrl Pts',(2.6451335020842,0.0940725355818836,12.0435793240872));
#16915=CARTESIAN_POINT('Ctrl Pts',(2.64200886630936,0.0127387462499724,
12.0478015748217));
#16916=CARTESIAN_POINT('Ctrl Pts',(2.64294314827754,-0.0686903414125342,
12.0520238255562));
#16917=CARTESIAN_POINT('Ctrl Pts',(2.64790900905182,-0.149782078717372,
12.0562460762907));
#16918=CARTESIAN_POINT('Ctrl Pts',(2.65289827868884,-0.231256079124994,
12.0604882305408));
#16919=CARTESIAN_POINT('Ctrl Pts',(2.66195717388358,-0.312389071043011,
12.064730384791));
#16920=CARTESIAN_POINT('Ctrl Pts',(2.67500575227409,-0.392750900092013,
12.0689725390412));
#16921=CARTESIAN_POINT('Ctrl Pts',(2.68805433066461,-0.473112729141016,
12.0732146932913));
#16922=CARTESIAN_POINT('Ctrl Pts',(2.70509243275337,-0.552702949733793,
12.0774568475415));
#16923=CARTESIAN_POINT('Ctrl Pts',(2.72598967865944,-0.631106911300591,
12.0816990017917));
#16924=CARTESIAN_POINT('Ctrl Pts',(2.74684212322271,-0.709342783599845,
12.0859320613407));
#16925=CARTESIAN_POINT('Ctrl Pts',(2.77161505752076,-0.78668975636709,12.0901651208897));
#16926=CARTESIAN_POINT('Ctrl Pts',(2.80021568143163,-0.862726292770211,
12.0943981804387));
#16927=CARTESIAN_POINT('Ctrl Pts',(2.8287754073789,-0.938654099394971,12.09862518685));
#16928=CARTESIAN_POINT('Ctrl Pts',(2.8611517897442,-1.01327476032922,12.1028521932613));
#16929=CARTESIAN_POINT('Ctrl Pts',(2.89720174783176,-1.08618003507352,12.1070791996726));
#16930=CARTESIAN_POINT('Ctrl Pts',(2.9332513227617,-1.15908453494283,12.111306161157));
#16931=CARTESIAN_POINT('Ctrl Pts',(2.97297424750053,-1.2302732431027,12.1155331226415));
#16932=CARTESIAN_POINT('Ctrl Pts',(3.01617852991393,-1.29935616318051,12.119760084126));
#16933=CARTESIAN_POINT('Ctrl Pts',(3.05930579810639,-1.36831593881585,12.1239795107985));
#16934=CARTESIAN_POINT('Ctrl Pts',(3.10590180028734,-1.4351770192821,12.1281989374709));
#16935=CARTESIAN_POINT('Ctrl Pts',(3.15572963307939,-1.49957602133697,12.1324183641434));
#16936=CARTESIAN_POINT('Ctrl Pts',(3.2055410269042,-1.56395377717211,12.1366363987622));
#16937=CARTESIAN_POINT('Ctrl Pts',(3.25858184986589,-1.62587070067144,12.1408544333811));
#16938=CARTESIAN_POINT('Ctrl Pts',(3.31457316612192,-1.68499421110253,12.1450724679999));
#16939=CARTESIAN_POINT('Ctrl Pts',(3.37056312203107,-1.74411628508797,12.1492904001387));
#16940=CARTESIAN_POINT('Ctrl Pts',(3.42950310851249,-1.80044474448912,12.1535083322775));
#16941=CARTESIAN_POINT('Ctrl Pts',(3.49107635611985,-1.85368285454567,12.1577262644163));
#16942=CARTESIAN_POINT('Ctrl Pts',(3.55287444314557,-1.90711536762894,12.1619595986566));
#16943=CARTESIAN_POINT('Ctrl Pts',(3.61732470858141,-1.95743460485067,12.1661929328969));
#16944=CARTESIAN_POINT('Ctrl Pts',(3.68407376652017,-2.00438160847482,12.1704262671372));
#16945=CARTESIAN_POINT('Ctrl Pts',(3.75067584475842,-2.05122523601029,12.174650279685));
#16946=CARTESIAN_POINT('Ctrl Pts',(3.81956618752025,-2.09471124759712,12.1788742922327));
#16947=CARTESIAN_POINT('Ctrl Pts',(3.8903665996224,-2.13462711979391,12.1830983047804));
#16948=CARTESIAN_POINT('Ctrl Pts',(3.96140137881133,-2.17467512351939,12.187336299867));
#16949=CARTESIAN_POINT('Ctrl Pts',(4.0343584686729,-2.21112911292004,12.1915742949536));
#16950=CARTESIAN_POINT('Ctrl Pts',(4.10883484332294,-2.24382271916577,12.1958122900402));
#16951=CARTESIAN_POINT('Ctrl Pts',(4.18331121797297,-2.27651632541149,12.2000502851268));
#16952=CARTESIAN_POINT('Ctrl Pts',(4.25930642045452,-2.30544944046707,12.2042882802134));
#16953=CARTESIAN_POINT('Ctrl Pts',(4.3364030504409,-2.33050616286386,12.2085262753));
#16954=CARTESIAN_POINT('Ctrl Pts',(4.41341479090877,-2.35553529581738,12.2127596040171));
#16955=CARTESIAN_POINT('Ctrl Pts',(4.49181138361709,-2.37678948157706,12.2169929327342));
#16956=CARTESIAN_POINT('Ctrl Pts',(4.57118843361084,-2.39411758617472,12.2212262614513));
#16957=CARTESIAN_POINT('Ctrl Pts',(4.65045234877213,-2.41142099330365,12.2254535564731));
#16958=CARTESIAN_POINT('Ctrl Pts',(4.73069349579421,-2.42480933510125,12.2296808514949));
#16959=CARTESIAN_POINT('Ctrl Pts',(4.81149132896875,-2.43418091584898,12.2339081465167));
#16960=CARTESIAN_POINT('Ctrl Pts',(4.8922814544946,-2.4435516026018,12.2381350382788));
#16961=CARTESIAN_POINT('Ctrl Pts',(4.97362770864029,-2.44890617950953,12.242361930041));
#16962=CARTESIAN_POINT('Ctrl Pts',(5.05509840725034,-2.45019393805116,12.2465888218031));
#16963=CARTESIAN_POINT('Ctrl Pts',(5.1364316409545,-2.45147952376735,12.2508085815621));
#16964=CARTESIAN_POINT('Ctrl Pts',(5.21788843608424,-2.44871196858668,12.2550283413211));
#16965=CARTESIAN_POINT('Ctrl Pts',(5.29903493442271,-2.44189271210886,12.2592481010801));
#16966=CARTESIAN_POINT('Ctrl Pts',(5.38015496866996,-2.43507567957698,12.2634664846601));
#16967=CARTESIAN_POINT('Ctrl Pts',(5.46096444471608,-2.42420960878395,12.2676848682401));
#16968=CARTESIAN_POINT('Ctrl Pts',(5.54103252799396,-2.40934796257631,12.2719032518201));
#16969=CARTESIAN_POINT('Ctrl Pts',(5.62109895630628,-2.39448662355115,12.2761215482084));
#16970=CARTESIAN_POINT('Ctrl Pts',(5.70042356596385,-2.37562995920312,12.2803398445966));
#16971=CARTESIAN_POINT('Ctrl Pts',(5.77858506014438,-2.35288267067502,12.2845581409848));
#16972=CARTESIAN_POINT('Ctrl Pts',(5.85701808554136,-2.33005635859461,12.2887910916367));
#16973=CARTESIAN_POINT('Ctrl Pts',(5.93427944615126,-2.30331246618675,12.2930240422887));
#16974=CARTESIAN_POINT('Ctrl Pts',(6.00995988304162,-2.27280687156679,12.2972569929406));
#16975=CARTESIAN_POINT('Ctrl Pts',(6.08548762263293,-2.24236282682811,12.3014814029425));
#16976=CARTESIAN_POINT('Ctrl Pts',(6.15944040314804,-2.20817247345499,12.3057058129443));
#16977=CARTESIAN_POINT('Ctrl Pts',(6.23143424151941,-2.17043782858016,12.3099302229461));
#16978=CARTESIAN_POINT('Ctrl Pts',(6.30364640890595,-2.13258874935872,12.3141674439231));
#16979=CARTESIAN_POINT('Ctrl Pts',(6.37388733787049,-2.09117409937537,12.3184046649001));
#16980=CARTESIAN_POINT('Ctrl Pts',(6.44179859361809,-2.04644160725183,12.3226418858771));
#16981=CARTESIAN_POINT('Ctrl Pts',(6.50970984936569,-2.00170911512828,12.3268791068541));
#16982=CARTESIAN_POINT('Ctrl Pts',(6.57529109347342,-1.95365910527841,12.3311163278311));
#16983=CARTESIAN_POINT('Ctrl Pts',(6.63821840765248,-1.90257875267492,12.3353535488081));
#16984=CARTESIAN_POINT('Ctrl Pts',(6.70017387946119,-1.85228727929821,12.3395253306204));
#16985=CARTESIAN_POINT('Ctrl Pts',(6.75980227254098,-1.79885891033061,12.3436971124327));
#16986=CARTESIAN_POINT('Ctrl Pts',(6.81676197200124,-1.74254006207211,12.347868894245));
#16987=CARTESIAN_POINT('Ctrl Pts',(6.87403079799516,-1.68591556524967,12.3520633167745));
#16988=CARTESIAN_POINT('Ctrl Pts',(6.92860144877801,-1.62636936367116,12.3562577393041));
#16989=CARTESIAN_POINT('Ctrl Pts',(6.98015816947068,-1.56419485856316,12.3604521618336));
#16990=CARTESIAN_POINT('Ctrl Pts',(7.03130373206592,-1.50251618699318,12.3646131343926));
#16991=CARTESIAN_POINT('Ctrl Pts',(7.07948293519092,-1.43825134120083,12.3687741069517));
#16992=CARTESIAN_POINT('Ctrl Pts',(7.12442385468376,-1.37172420517886,12.3729350795107));
#16993=CARTESIAN_POINT('Ctrl Pts',(7.16933765947029,-1.30523720771605,12.3770935415837));
#16994=CARTESIAN_POINT('Ctrl Pts',(7.21101678911364,-1.2364910238531,12.3812520036568));
#16995=CARTESIAN_POINT('Ctrl Pts',(7.24923085639673,-1.16584095654534,12.3854104657298));
#16996=CARTESIAN_POINT('Ctrl Pts',(7.28743434581261,-1.09521044557071,12.3895677767173));
#16997=CARTESIAN_POINT('Ctrl Pts',(7.32217444962915,-1.02267751879693,12.3937250877048));
#16998=CARTESIAN_POINT('Ctrl Pts',(7.35326605810788,-0.9486232630345,12.3978823986923));
#16999=CARTESIAN_POINT('Ctrl Pts',(7.38483437914912,-0.873433569263015,
12.4021034517141));
#17000=CARTESIAN_POINT('Ctrl Pts',(7.41264114922194,-0.796675953919252,
12.4063245047359));
#17001=CARTESIAN_POINT('Ctrl Pts',(7.43654351869195,-0.71876998505293,12.4105455577577));
#17002=CARTESIAN_POINT('Ctrl Pts',(7.46010721060141,-0.641967881789596,
12.4147068018162));
#17003=CARTESIAN_POINT('Ctrl Pts',(7.47987637177058,-0.564050245634618,
12.4188680458746));
#17004=CARTESIAN_POINT('Ctrl Pts',(7.49576514167452,-0.485431931733643,
12.423029289933));
#17005=CARTESIAN_POINT('Ctrl Pts',(7.51199646209124,-0.405118663226077,
12.4272802474365));
#17006=CARTESIAN_POINT('Ctrl Pts',(7.52417803290927,-0.324074672379063,
12.43153120494));
#17007=CARTESIAN_POINT('Ctrl Pts',(7.53227410577428,-0.242748265636235,
12.4357821624435));
#17008=CARTESIAN_POINT('Ctrl Pts',(7.54037017863928,-0.161421858893407,
12.440033119947));
#17009=CARTESIAN_POINT('Ctrl Pts',(7.54438079120497,-0.0798135650836431,
12.4442840774505));
#17010=CARTESIAN_POINT('Ctrl Pts',(7.54432661325899,0.0016301205695403,
12.448535034954));
#17011=CARTESIAN_POINT('',(4.01701573214483,2.20564849764805,12.7063139509272));
#17012=CARTESIAN_POINT('Ctrl Pts',(7.54716442798305,0.00163200833986455,
12.448535034954));
#17013=CARTESIAN_POINT('Ctrl Pts',(7.54778238923041,0.0888794869590354,
12.4530836307415));
#17014=CARTESIAN_POINT('Ctrl Pts',(7.50402124842324,0.986360506775624,12.4999079843645));
#17015=CARTESIAN_POINT('Ctrl Pts',(6.43805666178856,2.52634553668383,12.5858342896898));
#17016=CARTESIAN_POINT('Ctrl Pts',(4.69254186919481,2.53083748163268,12.6672119992262));
#17017=CARTESIAN_POINT('Ctrl Pts',(4.01701573214483,2.20564849764805,12.7063139509272));
#17018=CARTESIAN_POINT('',(6.16891561580437,2.2020751695661,12.7063625311661));
#17019=CARTESIAN_POINT('Origin',(5.09382715545311,0.,12.7063625311661));
#17020=CARTESIAN_POINT('',(7.54449188652341,0.00262105217720109,12.5641900273781));
#17021=CARTESIAN_POINT('Ctrl Pts',(6.16891561580437,2.2020751695661,12.7063625311661));
#17022=CARTESIAN_POINT('Ctrl Pts',(6.90007729696916,1.84511029528064,12.66408677333));
#17023=CARTESIAN_POINT('Ctrl Pts',(7.49776343645215,1.00822659690667,12.616695938734));
#17024=CARTESIAN_POINT('Ctrl Pts',(7.54732991511167,0.100698102860481,12.569305104138));
#17025=CARTESIAN_POINT('Ctrl Pts',(7.5465663696151,0.00262327089294606,
12.5641900273781));
#17026=CARTESIAN_POINT('',(7.54432697499987,0.000940426119431302,11.7641900274209));
#17027=CARTESIAN_POINT('Ctrl Pts',(7.54432575390545,0.00262087449387521,
12.5641900273781));
#17028=CARTESIAN_POINT('Ctrl Pts',(7.54441039363029,-0.0765166529131762,
12.5600588096074));
#17029=CARTESIAN_POINT('Ctrl Pts',(7.54065735796923,-0.155830075205808,
12.5559275918367));
#17030=CARTESIAN_POINT('Ctrl Pts',(7.53304219039848,-0.234904796239755,
12.551796374066));
#17031=CARTESIAN_POINT('Ctrl Pts',(7.52543169538823,-0.313930998128938,
12.5476676911528));
#17032=CARTESIAN_POINT('Ctrl Pts',(7.51396376930776,-0.392718305017181,
12.5435390082396));
#17033=CARTESIAN_POINT('Ctrl Pts',(7.49866605561368,-0.470850416028822,
12.5394103253264));
#17034=CARTESIAN_POINT('Ctrl Pts',(7.48339408899119,-0.548851025490896,
12.5352885912617));
#17035=CARTESIAN_POINT('Ctrl Pts',(7.46430526170117,-0.626198157536901,
12.531166857197));
#17036=CARTESIAN_POINT('Ctrl Pts',(7.44147889145808,-0.702482438522753,
12.5270451231323));
#17037=CARTESIAN_POINT('Ctrl Pts',(7.41866359048101,-0.77872972672389,12.5229253878336));
#17038=CARTESIAN_POINT('Ctrl Pts',(7.39211447967603,-0.853914719635981,
12.5188056525348));
#17039=CARTESIAN_POINT('Ctrl Pts',(7.36196141833813,-0.927640671557172,
12.514685917236));
#17040=CARTESIAN_POINT('Ctrl Pts',(7.33181284675423,-1.00135564577416,12.5105667953608));
#17041=CARTESIAN_POINT('Ctrl Pts',(7.29806157496909,-1.07361155940243,12.5064476734855));
#17042=CARTESIAN_POINT('Ctrl Pts',(7.26088591303975,-1.14403085236677,12.5023285516103));
#17043=CARTESIAN_POINT('Ctrl Pts',(7.22356652198715,-1.21472240149854,12.4981935043219));
#17044=CARTESIAN_POINT('Ctrl Pts',(7.18279642730905,-1.28356265622267,12.4940584570335));
#17045=CARTESIAN_POINT('Ctrl Pts',(7.13880198786701,-1.35019560982612,12.4899234097451));
#17046=CARTESIAN_POINT('Ctrl Pts',(7.09492050179105,-1.41665748689135,12.4857989789691));
#17047=CARTESIAN_POINT('Ctrl Pts',(7.04783153069711,-1.48092301251295,12.4816745481931));
#17048=CARTESIAN_POINT('Ctrl Pts',(6.99780120556054,-1.54267075765295,12.477550117417));
#17049=CARTESIAN_POINT('Ctrl Pts',(6.94757770919841,-1.60465691594679,12.4734097618725));
#17050=CARTESIAN_POINT('Ctrl Pts',(6.89439044087583,-1.66410545488232,12.4692694063279));
#17051=CARTESIAN_POINT('Ctrl Pts',(6.83854558294449,-1.72072887427741,12.4651290507833));
#17052=CARTESIAN_POINT('Ctrl Pts',(6.78270072501315,-1.7773522936725,12.4609886952388));
#17053=CARTESIAN_POINT('Ctrl Pts',(6.72419868715357,-1.8311503181936,12.4568483396942));
#17054=CARTESIAN_POINT('Ctrl Pts',(6.66337686356165,-1.88187777599301,12.4527079841497));
#17055=CARTESIAN_POINT('Ctrl Pts',(6.60111156302209,-1.93380914238347,12.4484693660501));
#17056=CARTESIAN_POINT('Ctrl Pts',(6.53615211630521,-1.9827420585461,12.4442307479506));
#17057=CARTESIAN_POINT('Ctrl Pts',(6.46881878398513,-2.02838563184293,12.4399921298511));
#17058=CARTESIAN_POINT('Ctrl Pts',(6.40158139194111,-2.07396416963846,12.4357595511703));
#17059=CARTESIAN_POINT('Ctrl Pts',(6.33197721295795,-2.11626241632434,12.4315269724895));
#17060=CARTESIAN_POINT('Ctrl Pts',(6.26035982944157,-2.15502941291235,12.4272943938088));
#17061=CARTESIAN_POINT('Ctrl Pts',(6.18882535891484,-2.19375152811222,12.4230667152756));
#17062=CARTESIAN_POINT('Ctrl Pts',(6.11528272169359,-2.22895029989725,12.4188390367425));
#17063=CARTESIAN_POINT('Ctrl Pts',(6.0401135269968,-2.26041862340379,12.4146113582094));
#17064=CARTESIAN_POINT('Ctrl Pts',(5.96499220158081,-2.29186690723823,12.4103863719484));
#17065=CARTESIAN_POINT('Ctrl Pts',(5.88824680106865,-2.3195892808155,12.4061613856875));
#17066=CARTESIAN_POINT('Ctrl Pts',(5.81028151198016,-2.34342557061525,12.4019363994265));
#17067=CARTESIAN_POINT('Ctrl Pts',(5.73234222836054,-2.36725390977569,12.3977128224177));
#17068=CARTESIAN_POINT('Ctrl Pts',(5.65318430674542,-2.38719860433681,12.3934892454088));
#17069=CARTESIAN_POINT('Ctrl Pts',(5.57322846081274,-2.40314890059261,12.3892656684));
#17070=CARTESIAN_POINT('Ctrl Pts',(5.4932750370186,-2.41909871365889,12.3850422193379));
#17071=CARTESIAN_POINT('Ctrl Pts',(5.41252419124509,-2.43105427952477,12.3808187702757));
#17072=CARTESIAN_POINT('Ctrl Pts',(5.33140684309925,-2.43895595327549,12.3765953212136));
#17073=CARTESIAN_POINT('Ctrl Pts',(5.25021173823486,-2.44686520133968,12.3723678236767));
#17074=CARTESIAN_POINT('Ctrl Pts',(5.16864989101269,-2.45071274847713,12.3681403261398));
#17075=CARTESIAN_POINT('Ctrl Pts',(5.08715683549386,-2.45049092159747,12.3639128286029));
#17076=CARTESIAN_POINT('Ctrl Pts',(5.00562695682094,-2.45026899448393,12.3596834208444));
#17077=CARTESIAN_POINT('Ctrl Pts',(4.92416639489778,-2.4459740532487,12.3554540130859));
#17078=CARTESIAN_POINT('Ctrl Pts',(4.84320769004459,-2.4376505355687,12.3512246053274));
#17079=CARTESIAN_POINT('Ctrl Pts',(4.76210461051928,-2.42931217445539,12.346987655213));
#17080=CARTESIAN_POINT('Ctrl Pts',(4.68150563575141,-2.41693094920283,12.3427507050987));
#17081=CARTESIAN_POINT('Ctrl Pts',(4.60183511267227,-2.40060285758397,12.3385137549844));
#17082=CARTESIAN_POINT('Ctrl Pts',(4.52265227094791,-2.38437471391994,12.3343027402034));
#17083=CARTESIAN_POINT('Ctrl Pts',(4.44438695422857,-2.36424809348003,12.3300917254224));
#17084=CARTESIAN_POINT('Ctrl Pts',(4.36743897176698,-2.34036545364205,12.3258807106414));
#17085=CARTESIAN_POINT('Ctrl Pts',(4.28997218984913,-2.31632179203111,12.3216413043145));
#17086=CARTESIAN_POINT('Ctrl Pts',(4.21356169799378,-2.28838468318746,12.3174018979875));
#17087=CARTESIAN_POINT('Ctrl Pts',(4.13862575067865,-2.2566657985437,12.3131624916606));
#17088=CARTESIAN_POINT('Ctrl Pts',(4.06379404581372,-2.22499103763991,12.3089289827183));
#17089=CARTESIAN_POINT('Ctrl Pts',(3.99043323388083,-2.18954512970591,12.304695473776));
#17090=CARTESIAN_POINT('Ctrl Pts',(3.91894603217246,-2.15048938526997,12.3004619648337));
#17091=CARTESIAN_POINT('Ctrl Pts',(3.84753799270652,-2.11147688969865,12.2962331439202));
#17092=CARTESIAN_POINT('Ctrl Pts',(3.77799984390751,-2.06886272354524,12.2920043230067));
#17093=CARTESIAN_POINT('Ctrl Pts',(3.71071262565826,-2.02285551818967,12.2877755020932));
#17094=CARTESIAN_POINT('Ctrl Pts',(3.64346620254492,-1.97687620624748,12.2835492450444));
#17095=CARTESIAN_POINT('Ctrl Pts',(3.57846838168398,-1.92750819977463,12.2793229879955));
#17096=CARTESIAN_POINT('Ctrl Pts',(3.51607296767334,-1.87500452611278,12.2750967309467));
#17097=CARTESIAN_POINT('Ctrl Pts',(3.45369648481703,-1.82251678239007,12.2708717561705));
#17098=CARTESIAN_POINT('Ctrl Pts',(3.39392119442706,-1.7668955588495,12.2666467813942));
#17099=CARTESIAN_POINT('Ctrl Pts',(3.33706830103246,-1.70843453998526,12.2624218066179));
#17100=CARTESIAN_POINT('Ctrl Pts',(3.28021543825759,-1.64997355260686,12.2581968341171));
#17101=CARTESIAN_POINT('Ctrl Pts',(3.22628529105744,-1.58867310563953,12.2539718616163));
#17102=CARTESIAN_POINT('Ctrl Pts',(3.17556162418357,-1.52486314190592,12.2497468891155));
#17103=CARTESIAN_POINT('Ctrl Pts',(3.1247870695095,-1.46098916173017,12.2455176779708));
#17104=CARTESIAN_POINT('Ctrl Pts',(3.07722571031335,-1.39460099831619,12.2412884668262));
#17105=CARTESIAN_POINT('Ctrl Pts',(3.03312013232558,-1.32606063769078,12.2370592556816));
#17106=CARTESIAN_POINT('Ctrl Pts',(2.9889935273383,-1.25748760096871,12.2328280282927));
#17107=CARTESIAN_POINT('Ctrl Pts',(2.94832621731021,-1.1867607243928,12.2285968009038));
#17108=CARTESIAN_POINT('Ctrl Pts',(2.91131535792414,-1.11426769837721,12.2243655735148));
#17109=CARTESIAN_POINT('Ctrl Pts',(2.87423710327715,-1.04164266552676,12.2201266412339));
#17110=CARTESIAN_POINT('Ctrl Pts',(2.84082879585868,-0.967245479317497,
12.215887708953));
#17111=CARTESIAN_POINT('Ctrl Pts',(2.81123981787899,-0.891484882847885,
12.2116487766721));
#17112=CARTESIAN_POINT('Ctrl Pts',(2.78193344231364,-0.816447870933587,
12.2074503301591));
#17113=CARTESIAN_POINT('Ctrl Pts',(2.75637379469379,-0.740073828005492,
12.2032518836462));
#17114=CARTESIAN_POINT('Ctrl Pts',(2.73465698606719,-0.662771726825782,
12.1990534371333));
#17115=CARTESIAN_POINT('Ctrl Pts',(2.71279593603056,-0.58495619090229,12.1948271048542));
#17116=CARTESIAN_POINT('Ctrl Pts',(2.69474720806299,-0.505908885358544,
12.1906007725752));
#17117=CARTESIAN_POINT('Ctrl Pts',(2.68064634693347,-0.426038302729327,
12.1863744402962));
#17118=CARTESIAN_POINT('Ctrl Pts',(2.66656593634664,-0.346283556767435,
12.182154237486));
#17119=CARTESIAN_POINT('Ctrl Pts',(2.65642210231356,-0.265708359974596,
12.1779340346759));
#17120=CARTESIAN_POINT('Ctrl Pts',(2.65030039347467,-0.184735523100296,
12.1737138318657));
#17121=CARTESIAN_POINT('Ctrl Pts',(2.64416642725262,-0.103600555828764,
12.1694851790223));
#17122=CARTESIAN_POINT('Ctrl Pts',(2.64207082699148,-0.0220668115723537,
12.165256526179));
#17123=CARTESIAN_POINT('Ctrl Pts',(2.64404793756445,0.0594309145210368,
12.1610278733356));
#17124=CARTESIAN_POINT('Ctrl Pts',(2.64601748951117,0.140617069344841,12.1568153869155));
#17125=CARTESIAN_POINT('Ctrl Pts',(2.65202867048672,0.221767012350393,12.1526029004954));
#17126=CARTESIAN_POINT('Ctrl Pts',(2.66206336155539,0.302448509151835,12.1483904140753));
#17127=CARTESIAN_POINT('Ctrl Pts',(2.67209465002971,0.383102648219714,12.1441793560382));
#17128=CARTESIAN_POINT('Ctrl Pts',(2.68614668199914,0.463288194291076,12.1399682980012));
#17129=CARTESIAN_POINT('Ctrl Pts',(2.70414947098843,0.54257793391506,12.1357572399641));
#17130=CARTESIAN_POINT('Ctrl Pts',(2.72215170586108,0.621865233041374,12.1315463115413));
#17131=CARTESIAN_POINT('Ctrl Pts',(2.74410435173223,0.700256326194733,12.1273353831184));
#17132=CARTESIAN_POINT('Ctrl Pts',(2.769886593912,0.777335523711612,12.1231244546956));
#17133=CARTESIAN_POINT('Ctrl Pts',(2.79585616513128,0.85497476453021,12.1188829304397));
#17134=CARTESIAN_POINT('Ctrl Pts',(2.82571107356269,0.93128250825446,12.1146414061838));
#17135=CARTESIAN_POINT('Ctrl Pts',(2.85927779811455,1.00585258344243,12.1103998819279));
#17136=CARTESIAN_POINT('Ctrl Pts',(2.89265053975843,1.07999171637356,12.1061828695427));
#17137=CARTESIAN_POINT('Ctrl Pts',(2.92969204340042,1.15241281953426,12.1019658571574));
#17138=CARTESIAN_POINT('Ctrl Pts',(2.97018556120639,1.22274144003761,12.0977488447721));
#17139=CARTESIAN_POINT('Ctrl Pts',(3.01103213887281,1.2936832503621,12.093495064581));
#17140=CARTESIAN_POINT('Ctrl Pts',(3.05539095687902,1.36249550563928,12.0892412843898));
#17141=CARTESIAN_POINT('Ctrl Pts',(3.10299605367378,1.42882531269155,12.0849875041986));
#17142=CARTESIAN_POINT('Ctrl Pts',(3.15060115046855,1.49515511974382,12.0807337240074));
#17143=CARTESIAN_POINT('Ctrl Pts',(3.2014521767119,1.55900214351023,12.0764799438162));
#17144=CARTESIAN_POINT('Ctrl Pts',(3.25524434129407,1.62005045769539,12.072226163625));
#17145=CARTESIAN_POINT('Ctrl Pts',(3.30877838497379,1.68080583245204,12.0679927951348));
#17146=CARTESIAN_POINT('Ctrl Pts',(3.36542656841756,1.7390176940597,12.0637594266447));
#17147=CARTESIAN_POINT('Ctrl Pts',(3.42491785484029,1.79435002057236,12.0595260581545));
#17148=CARTESIAN_POINT('Ctrl Pts',(3.48432422738297,1.84960336942596,12.0552987320912));
#17149=CARTESIAN_POINT('Ctrl Pts',(3.54656530581361,1.9019850327265,12.0510714060278));
#17150=CARTESIAN_POINT('Ctrl Pts',(3.61133097407495,1.95119330723513,12.0468440799645));
#17151=CARTESIAN_POINT('Ctrl Pts',(3.67608985291409,2.00039642321209,12.0426171970542));
#17152=CARTESIAN_POINT('Ctrl Pts',(3.74337246252358,2.04642648679026,12.0383903141439));
#17153=CARTESIAN_POINT('Ctrl Pts',(3.81283313979633,2.08902000513435,12.0341634312335));
#17154=CARTESIAN_POINT('Ctrl Pts',(3.88217692046509,2.13154184209205,12.0299436618193));
#17155=CARTESIAN_POINT('Ctrl Pts',(3.95369106289455,2.17063842488001,12.0257238924051));
#17156=CARTESIAN_POINT('Ctrl Pts',(4.02700146581783,2.20609002489341,12.0215041229909));
#17157=CARTESIAN_POINT('Ctrl Pts',(4.1002878200654,2.24152999539724,12.0172857378259));
#17158=CARTESIAN_POINT('Ctrl Pts',(4.17536884687027,2.27332715571786,12.0130673526609));
#17159=CARTESIAN_POINT('Ctrl Pts',(4.25184654972842,2.30130808662888,12.0088489674958));
#17160=CARTESIAN_POINT('Ctrl Pts',(4.32832252564945,2.32928838570465,12.0046306775859));
#17161=CARTESIAN_POINT('Ctrl Pts',(4.40619467843011,2.35345246823344,12.0004123876759));
#17162=CARTESIAN_POINT('Ctrl Pts',(4.48504712189463,2.37367586682355,11.9961940977659));
#17163=CARTESIAN_POINT('Ctrl Pts',(4.56417330661427,2.39396947222362,11.9919611637951));
#17164=CARTESIAN_POINT('Ctrl Pts',(4.64428614693988,2.41029485983171,11.9877282298244));
#17165=CARTESIAN_POINT('Ctrl Pts',(4.72495405036333,2.42257773504617,11.9834952958536));
#17166=CARTESIAN_POINT('Ctrl Pts',(4.80545901304841,2.43483580013576,11.9792709119673));
#17167=CARTESIAN_POINT('Ctrl Pts',(4.88651633050828,2.44306765643798,11.975046528081));
#17168=CARTESIAN_POINT('Ctrl Pts',(4.96769266192047,2.44725158893426,11.9708221441947));
#17169=CARTESIAN_POINT('Ctrl Pts',(5.04911544269933,2.45144822374778,11.9665849351817));
#17170=CARTESIAN_POINT('Ctrl Pts',(5.13065749219384,2.45157233176375,11.9623477261687));
#17171=CARTESIAN_POINT('Ctrl Pts',(5.21188416609952,2.44765454920363,11.9581105171557));
#17172=CARTESIAN_POINT('Ctrl Pts',(5.29311084000522,2.44373676664352,11.9538733081427));
#17173=CARTESIAN_POINT('Ctrl Pts',(5.37402168182735,2.43577720026681,11.9496360991297));
#17174=CARTESIAN_POINT('Ctrl Pts',(5.45419165729818,2.42385801477932,11.9453988901167));
#17175=CARTESIAN_POINT('Ctrl Pts',(5.53428104988045,2.41195080986674,11.9411659401364));
#17176=CARTESIAN_POINT('Ctrl Pts',(5.61392831550511,2.39604775568114,11.936932990156));
#17177=CARTESIAN_POINT('Ctrl Pts',(5.69270414619543,2.37619372105042,11.9327000401757));
#17178=CARTESIAN_POINT('Ctrl Pts',(5.77136776588927,2.35636796718792,11.9284731197545));
#17179=CARTESIAN_POINT('Ctrl Pts',(5.84916196939663,2.33260252326163,11.9242461993334));
#17180=CARTESIAN_POINT('Ctrl Pts',(5.92566501726814,2.30499371401551,11.9200192789123));
#17181=CARTESIAN_POINT('Ctrl Pts',(6.00216925077248,2.27738447689217,11.9157922929829));
#17182=CARTESIAN_POINT('Ctrl Pts',(6.07738183278321,2.24593185252719,11.9115653070536));
#17183=CARTESIAN_POINT('Ctrl Pts',(6.15089363736988,2.21078282579002,11.9073383211243));
#17184=CARTESIAN_POINT('Ctrl Pts',(6.22427348762946,2.17569689186082,11.9031189226714));
#17185=CARTESIAN_POINT('Ctrl Pts',(6.29595823061345,2.13692799014802,11.8988995242185));
#17186=CARTESIAN_POINT('Ctrl Pts',(6.3655601667511,2.09467071349531,11.8946801257656));
#17187=CARTESIAN_POINT('Ctrl Pts',(6.43513949964716,2.05242715990098,11.8904620975631));
#17188=CARTESIAN_POINT('Ctrl Pts',(6.50263697224862,2.00669772199978,11.8862440693606));
#17189=CARTESIAN_POINT('Ctrl Pts',(6.56769077542748,1.95772221719938,11.8820260411582));
#17190=CARTESIAN_POINT('Ctrl Pts',(6.63274333409962,1.90874764932106,11.8778080936483));
#17191=CARTESIAN_POINT('Ctrl Pts',(6.69535194593625,1.85652741830497,11.8735901461385));
#17192=CARTESIAN_POINT('Ctrl Pts',(6.7551861750095,1.80134295961058,11.8693721986287));
#17193=CARTESIAN_POINT('Ctrl Pts',(6.81523934965934,1.74595656979225,11.8651388167937));
#17194=CARTESIAN_POINT('Ctrl Pts',(6.87249744720056,1.68758453051007,11.8609054349587));
#17195=CARTESIAN_POINT('Ctrl Pts',(6.92666345787223,1.62654890443989,11.8566720531237));
#17196=CARTESIAN_POINT('Ctrl Pts',(6.98071046469252,1.56564737490892,11.8524479721165));
#17197=CARTESIAN_POINT('Ctrl Pts',(7.03167869416211,1.50209433807564,11.8482238911094));
#17198=CARTESIAN_POINT('Ctrl Pts',(7.07931449339184,1.43624172091085,11.8439998101023));
#17199=CARTESIAN_POINT('Ctrl Pts',(7.12710762354254,1.37017160654704,11.8397617778533));
#17200=CARTESIAN_POINT('Ctrl Pts',(7.17154602850335,1.30178709692435,11.8355237456044));
#17201=CARTESIAN_POINT('Ctrl Pts',(7.21241913883921,1.23146995819311,11.8312857133554));
#17202=CARTESIAN_POINT('Ctrl Pts',(7.25329224917508,1.16115281946187,11.8270476811065));
#17203=CARTESIAN_POINT('Ctrl Pts',(7.29059990638921,1.0889034935897,11.8228096488575));
#17204=CARTESIAN_POINT('Ctrl Pts',(7.3241800758682,1.01512368724007,11.8185716166086));
#17205=CARTESIAN_POINT('Ctrl Pts',(7.36071057463849,0.934861640712458,11.8139612339255));
#17206=CARTESIAN_POINT('Ctrl Pts',(7.39294885099948,0.852528858115445,11.8093508512425));
#17207=CARTESIAN_POINT('Ctrl Pts',(7.42067707427349,0.768582920240606,11.8047404685595));
#17208=CARTESIAN_POINT('Ctrl Pts',(7.4483340584941,0.68485265536771,11.8001419308221));
#17209=CARTESIAN_POINT('Ctrl Pts',(7.47150396342862,0.599517796048167,11.7955433930847));
#17210=CARTESIAN_POINT('Ctrl Pts',(7.49001656496528,0.513056101943753,11.7909448553474));
#17211=CARTESIAN_POINT('Ctrl Pts',(7.50844941034667,0.426966902882021,11.7863661290714));
#17212=CARTESIAN_POINT('Ctrl Pts',(7.52226486289349,0.339760859350498,11.7817874027954));
#17213=CARTESIAN_POINT('Ctrl Pts',(7.53134272764655,0.25192873062537,11.7772086765193));
#17214=CARTESIAN_POINT('Ctrl Pts',(7.53994639663354,0.168684643768949,11.7728691268199));
#17215=CARTESIAN_POINT('Ctrl Pts',(7.54429476214579,0.0848785383195788,
11.7685295771204));
#17216=CARTESIAN_POINT('Ctrl Pts',(7.54432697499987,0.000940426119398955,
11.7641900274209));
#17217=CARTESIAN_POINT('',(7.54432616501525,-0.00220321015044804,10.9641900273343));
#17218=CARTESIAN_POINT('Ctrl Pts',(7.54432697500019,0.000940425291412725,
11.7641900273781));
#17219=CARTESIAN_POINT('Ctrl Pts',(7.54435894248202,-0.0823583855581014,
11.7598835291724));
#17220=CARTESIAN_POINT('Ctrl Pts',(7.54013925275364,-0.165631393861959,
11.7555770309666));
#17221=CARTESIAN_POINT('Ctrl Pts',(7.5317020525233,-0.248427527128179,11.7512705327609));
#17222=CARTESIAN_POINT('Ctrl Pts',(7.52325973069101,-0.331273919820025,
11.7469614203977));
#17223=CARTESIAN_POINT('Ctrl Pts',(7.51059484986504,-0.413642427628778,
11.7426523080346));
#17224=CARTESIAN_POINT('Ctrl Pts',(7.49379315404187,-0.495089341046485,
11.7383431956714));
#17225=CARTESIAN_POINT('Ctrl Pts',(7.47696331328709,-0.576672688180899,
11.7340268650087));
#17226=CARTESIAN_POINT('Ctrl Pts',(7.45598290886903,-0.657330930030507,
11.729710534346));
#17227=CARTESIAN_POINT('Ctrl Pts',(7.43098835149548,-0.736632740050166,
11.7253942036833));
#17228=CARTESIAN_POINT('Ctrl Pts',(7.40597111894622,-0.816006493031197,
11.7210739572259));
#17229=CARTESIAN_POINT('Ctrl Pts',(7.37693263106896,-0.89402095405243,11.7167537107685));
#17230=CARTESIAN_POINT('Ctrl Pts',(7.34405763962233,-0.970264406291163,
11.7124334643111));
#17231=CARTESIAN_POINT('Ctrl Pts',(7.31111457303057,-1.04666573793454,11.708104271801));
#17232=CARTESIAN_POINT('Ctrl Pts',(7.27431932589656,-1.12128834332108,11.703775079291));
#17233=CARTESIAN_POINT('Ctrl Pts',(7.23390285759931,-1.1937446289234,11.6994458867809));
#17234=CARTESIAN_POINT('Ctrl Pts',(7.20993617133476,-1.23671070532952,11.696878705554));
#17235=CARTESIAN_POINT('Ctrl Pts',(7.18469695746452,-1.27891555142926,11.6943115243272));
#17236=CARTESIAN_POINT('Ctrl Pts',(7.15824029078737,-1.32028355161283,11.6917443431004));
#17237=CARTESIAN_POINT('Ctrl Pts',(7.1146230199284,-1.388484103516,11.6875120095157));
#17238=CARTESIAN_POINT('Ctrl Pts',(7.06754118944877,-1.45464801043107,11.6832796759311));
#17239=CARTESIAN_POINT('Ctrl Pts',(7.01721113515328,-1.5184018956234,11.6790473423465));
#17240=CARTESIAN_POINT('Ctrl Pts',(6.96695298744288,-1.58206469559369,11.6748210554999));
#17241=CARTESIAN_POINT('Ctrl Pts',(6.91345611845769,-1.64332395079541,11.6705947686533));
#17242=CARTESIAN_POINT('Ctrl Pts',(6.85698073508804,-1.70183421772525,11.6663684818068));
#17243=CARTESIAN_POINT('Ctrl Pts',(6.8004939220552,-1.76035632614434,11.6621413396311));
#17244=CARTESIAN_POINT('Ctrl Pts',(6.7410276628384,-1.81612795572645,11.6579141974555));
#17245=CARTESIAN_POINT('Ctrl Pts',(6.67888342250527,-1.86883570178833,11.6536870552799));
#17246=CARTESIAN_POINT('Ctrl Pts',(6.61686288630514,-1.92143852797358,11.6494683276405));
#17247=CARTESIAN_POINT('Ctrl Pts',(6.55217535804114,-1.97098933681526,11.6452496000011));
#17248=CARTESIAN_POINT('Ctrl Pts',(6.48515682533867,-2.0172139201622,11.6410308723616));
#17249=CARTESIAN_POINT('Ctrl Pts',(6.41816026017511,-2.06342335187432,11.6368135275496));
#17250=CARTESIAN_POINT('Ctrl Pts',(6.34883459011881,-2.10630845969896,11.6325961827375));
#17251=CARTESIAN_POINT('Ctrl Pts',(6.27754649415294,-2.14563714947053,11.6283788379255));
#17252=CARTESIAN_POINT('Ctrl Pts',(6.20625995967156,-2.18496497779198,11.6241615854896));
#17253=CARTESIAN_POINT('Ctrl Pts',(6.13301149212449,-2.22073631951311,11.6199443330537));
#17254=CARTESIAN_POINT('Ctrl Pts',(6.05819292752296,-2.25276472532311,11.6157270806178));
#17255=CARTESIAN_POINT('Ctrl Pts',(5.98307427009332,-2.28492159517049,11.6114929130323));
#17256=CARTESIAN_POINT('Ctrl Pts',(5.90637332325196,-2.31330524527914,11.6072587454468));
#17257=CARTESIAN_POINT('Ctrl Pts',(5.82850577622104,-2.33777620275905,11.6030245778614));
#17258=CARTESIAN_POINT('Ctrl Pts',(5.75083690615525,-2.36218472324497,11.5988012136413));
#17259=CARTESIAN_POINT('Ctrl Pts',(5.67200784425064,-2.38270041420456,11.5945778494213));
#17260=CARTESIAN_POINT('Ctrl Pts',(5.59244336822967,-2.39923573713722,11.5903544852012));
#17261=CARTESIAN_POINT('Ctrl Pts',(5.51257360332114,-2.41583450610252,11.5861149159331));
#17262=CARTESIAN_POINT('Ctrl Pts',(5.43196323625491,-2.42842223747161,11.5818753466649));
#17263=CARTESIAN_POINT('Ctrl Pts',(5.35104735266986,-2.43696286802729,11.5776357773967));
#17264=CARTESIAN_POINT('Ctrl Pts',(5.2701314690848,-2.44550349858296,11.5733962081285));
#17265=CARTESIAN_POINT('Ctrl Pts',(5.18891053852849,-2.44999706453427,11.5691566388603));
#17266=CARTESIAN_POINT('Ctrl Pts',(5.10781798894077,-2.45046006018836,11.5649170695921));
#17267=CARTESIAN_POINT('Ctrl Pts',(5.02686672690311,-2.45092224916511,11.5606848869255));
#17268=CARTESIAN_POINT('Ctrl Pts',(4.94574161846151,-2.44736963806486,11.5564527042589));
#17269=CARTESIAN_POINT('Ctrl Pts',(4.86487362920176,-2.43978083704604,11.5522205215923));
#17270=CARTESIAN_POINT('Ctrl Pts',(4.78412117184545,-2.43220287775377,11.5479943852257));
#17271=CARTESIAN_POINT('Ctrl Pts',(4.70362556287672,-2.42060022410224,11.543768248859));
#17272=CARTESIAN_POINT('Ctrl Pts',(4.62381817115424,-2.40500349369358,11.5395421124924));
#17273=CARTESIAN_POINT('Ctrl Pts',(4.54399107403052,-2.38940291226531,11.535314932642));
#17274=CARTESIAN_POINT('Ctrl Pts',(4.46485300016943,-2.3698063056605,11.5310877527917));
#17275=CARTESIAN_POINT('Ctrl Pts',(4.38683091139602,-2.34629634975831,11.5268605729413));
#17276=CARTESIAN_POINT('Ctrl Pts',(4.30896756342745,-2.32283422632741,11.522641993552));
#17277=CARTESIAN_POINT('Ctrl Pts',(4.232216116107,-2.29547477175723,11.5184234141626));
#17278=CARTESIAN_POINT('Ctrl Pts',(4.15698934085871,-2.26435093551021,11.5142048347733));
#17279=CARTESIAN_POINT('Ctrl Pts',(4.08178720342966,-2.23323729275414,11.5099876370276));
#17280=CARTESIAN_POINT('Ctrl Pts',(4.00810917544068,-2.19836189423427,11.5057704392819));
#17281=CARTESIAN_POINT('Ctrl Pts',(3.93634936282974,-2.15990634278057,11.5015532415362));
#17282=CARTESIAN_POINT('Ctrl Pts',(3.86459109838284,-2.12145162097649,11.4973361347733));
#17283=CARTESIAN_POINT('Ctrl Pts',(3.79475137604953,-2.0794171203074,11.4931190280105));
#17284=CARTESIAN_POINT('Ctrl Pts',(3.72719966382234,-2.03403037074646,11.4889019212477));
#17285=CARTESIAN_POINT('Ctrl Pts',(3.65937184074846,-1.98845810740006,11.484667577484));
#17286=CARTESIAN_POINT('Ctrl Pts',(3.59385116959799,-1.93950638628338,11.4804332337204));
#17287=CARTESIAN_POINT('Ctrl Pts',(3.53098073004293,-1.88744835706375,11.4761988899567));
#17288=CARTESIAN_POINT('Ctrl Pts',(3.46827540144395,-1.83552704314364,11.4719756664676));
#17289=CARTESIAN_POINT('Ctrl Pts',(3.4082067189857,-1.78051606215411,11.4677524429785));
#17290=CARTESIAN_POINT('Ctrl Pts',(3.35107903103002,-1.72272436124291,11.4635292194894));
#17291=CARTESIAN_POINT('Ctrl Pts',(3.29372570657613,-1.66470440119003,11.4592893155884));
#17292=CARTESIAN_POINT('Ctrl Pts',(3.23933696398529,-1.60388206723264,11.4550494116875));
#17293=CARTESIAN_POINT('Ctrl Pts',(3.18817963370037,-1.54060305492286,11.4508095077866));
#17294=CARTESIAN_POINT('Ctrl Pts',(3.13702230341543,-1.47732404261306,11.4465696038857));
#17295=CARTESIAN_POINT('Ctrl Pts',(3.0890966103807,-1.41158876603943,11.4423296999848));
#17296=CARTESIAN_POINT('Ctrl Pts',(3.04462434700435,-1.3437701067689,11.4380897960839));
#17297=CARTESIAN_POINT('Ctrl Pts',(3.00023530859849,-1.27607836269198,11.4338578266988));
#17298=CARTESIAN_POINT('Ctrl Pts',(2.9591211361363,-1.20605844318704,11.4296258573137));
#17299=CARTESIAN_POINT('Ctrl Pts',(2.92153406383363,-1.13406039261685,11.4253938879286));
#17300=CARTESIAN_POINT('Ctrl Pts',(2.88400073066575,-1.06216527937874,11.4211679690912));
#17301=CARTESIAN_POINT('Ctrl Pts',(2.84998469543737,-0.988298060653317,
11.4169420502538));
#17302=CARTESIAN_POINT('Ctrl Pts',(2.81969476265982,-0.912837395185082,
11.4127161314163));
#17303=CARTESIAN_POINT('Ctrl Pts',(2.78939540538737,-0.83735325067308,11.4084888977147));
#17304=CARTESIAN_POINT('Ctrl Pts',(2.76282470333167,-0.760275071916644,
11.404261664013));
#17305=CARTESIAN_POINT('Ctrl Pts',(2.74014540308181,-0.682006201257992,
11.4000344303113));
#17306=CARTESIAN_POINT('Ctrl Pts',(2.7175137475928,-0.603901758142695,11.3958160771983));
#17307=CARTESIAN_POINT('Ctrl Pts',(2.69875731349992,-0.524612060407832,
11.3915977240854));
#17308=CARTESIAN_POINT('Ctrl Pts',(2.68398890437622,-0.444555793626262,
11.3873793709724));
#17309=CARTESIAN_POINT('Ctrl Pts',(2.66922534216965,-0.364525800906284,
11.3831624023016));
#17310=CARTESIAN_POINT('Ctrl Pts',(2.65844728992316,-0.283730195416169,
11.3789454336308));
#17311=CARTESIAN_POINT('Ctrl Pts',(2.65171656842196,-0.202598446959399,
11.37472846496));
#17312=CARTESIAN_POINT('Ctrl Pts',(2.64498599611946,-0.121468496935655,
11.370511589766));
#17313=CARTESIAN_POINT('Ctrl Pts',(2.64230261346029,-0.040002881983545,
11.366294714572));
#17314=CARTESIAN_POINT('Ctrl Pts',(2.64367629956648,0.0413646394644267,
11.362077839378));
#17315=CARTESIAN_POINT('Ctrl Pts',(2.645055762863,0.123074361110238,11.3578432296445));
#17316=CARTESIAN_POINT('Ctrl Pts',(2.65052649910699,0.20468469025959,11.353608619911));
#17317=CARTESIAN_POINT('Ctrl Pts',(2.66004573388368,0.285759062889458,11.3493740101774));
#17318=CARTESIAN_POINT('Ctrl Pts',(2.66953884376968,0.366610932432473,11.3451510220415));
#17319=CARTESIAN_POINT('Ctrl Pts',(2.68305814087799,0.44692932916564,11.3409280339056));
#17320=CARTESIAN_POINT('Ctrl Pts',(2.70050976198522,0.526290893065881,11.3367050457697));
#17321=CARTESIAN_POINT('Ctrl Pts',(2.71803342297704,0.605980059649459,11.3324646252374));
#17322=CARTESIAN_POINT('Ctrl Pts',(2.7395218114061,0.684704023793716,11.328224204705));
#17323=CARTESIAN_POINT('Ctrl Pts',(2.76482974318002,0.762050722475371,11.3239837841727));
#17324=CARTESIAN_POINT('Ctrl Pts',(2.79013767495394,0.839397421157049,11.3197433636403));
#17325=CARTESIAN_POINT('Ctrl Pts',(2.81926492454934,0.915366440063504,11.315502943108));
#17326=CARTESIAN_POINT('Ctrl Pts',(2.8520189741217,0.989568758659821,11.3112625225756));
#17327=CARTESIAN_POINT('Ctrl Pts',(2.8847090062452,1.06362604959703,11.3070303899011));
#17328=CARTESIAN_POINT('Ctrl Pts',(2.92113363162592,1.13619986823533,11.3027982572265));
#17329=CARTESIAN_POINT('Ctrl Pts',(2.96113610676575,1.20688820561344,11.2985661245519));
#17330=CARTESIAN_POINT('Ctrl Pts',(3.00108141338179,1.27747552054522,11.2943400401225));
#17331=CARTESIAN_POINT('Ctrl Pts',(3.04459418744791,1.34618230492972,11.2901139556932));
#17332=CARTESIAN_POINT('Ctrl Pts',(3.09147006192824,1.4126274526607,11.2858878712638));
#17333=CARTESIAN_POINT('Ctrl Pts',(3.13835822818122,1.47909002361115,11.2816606786723));
#17334=CARTESIAN_POINT('Ctrl Pts',(3.18861104620899,1.54328935610522,11.2774334860807));
#17335=CARTESIAN_POINT('Ctrl Pts',(3.24197843436488,1.60486964087551,11.2732062934892));
#17336=CARTESIAN_POINT('Ctrl Pts',(3.29523637183308,1.66632363120365,11.2689877704083));
#17337=CARTESIAN_POINT('Ctrl Pts',(3.35159583145433,1.72516893830252,11.2647692473274));
#17338=CARTESIAN_POINT('Ctrl Pts',(3.41076667089988,1.78108328141484,11.2605507242464));
#17339=CARTESIAN_POINT('Ctrl Pts',(3.46991810937903,1.83697929130251,11.2563335843371));
#17340=CARTESIAN_POINT('Ctrl Pts',(3.53187875959856,1.88994592677056,11.2521164444277));
#17341=CARTESIAN_POINT('Ctrl Pts',(3.59632171586831,1.9396978394621,11.2478993045184));
#17342=CARTESIAN_POINT('Ctrl Pts',(3.66076325958014,1.98944866161617,11.2436822570467));
#17343=CARTESIAN_POINT('Ctrl Pts',(3.72768663263984,2.03598461804152,11.239465209575));
#17344=CARTESIAN_POINT('Ctrl Pts',(3.79673309666712,2.07906162791344,11.2352481621033));
#17345=CARTESIAN_POINT('Ctrl Pts',(3.86606383093863,2.12231598954826,11.2310137526836));
#17346=CARTESIAN_POINT('Ctrl Pts',(3.93753478158874,2.1620826022527,11.226779343264));
#17347=CARTESIAN_POINT('Ctrl Pts',(4.01075633896331,2.19816010710506,11.2225449338443));
#17348=CARTESIAN_POINT('Ctrl Pts',(4.08378339192877,2.23414177633174,11.2183217726326));
#17349=CARTESIAN_POINT('Ctrl Pts',(4.15855131738468,2.26645376439695,11.2140986114209));
#17350=CARTESIAN_POINT('Ctrl Pts',(4.23465371604348,2.29494471633045,11.2098754502092));
#17351=CARTESIAN_POINT('Ctrl Pts',(4.31106015789206,2.3235494948983,11.2056354166855));
#17352=CARTESIAN_POINT('Ctrl Pts',(4.38881130635894,2.34830250738448,11.2013953831619));
#17353=CARTESIAN_POINT('Ctrl Pts',(4.46748251584643,2.36910165303981,11.1971553496383));
#17354=CARTESIAN_POINT('Ctrl Pts',(4.5461537253339,2.38990079869514,11.1929153161147));
#17355=CARTESIAN_POINT('Ctrl Pts',(4.62574452584903,2.40674604161226,11.1886752825911));
#17356=CARTESIAN_POINT('Ctrl Pts',(4.70582388448333,2.41958750858834,11.1844352490674));
#17357=CARTESIAN_POINT('Ctrl Pts',(4.78575337372431,2.43240494261888,11.1802031508128));
#17358=CARTESIAN_POINT('Ctrl Pts',(4.86646775897929,2.4412814027134,11.1759710525582));
#17359=CARTESIAN_POINT('Ctrl Pts',(4.94754441548954,2.44612992500169,11.1717389543036));
#17360=CARTESIAN_POINT('Ctrl Pts',(5.02850519965063,2.45097151792593,11.1675129044381));
#17361=CARTESIAN_POINT('Ctrl Pts',(5.10982676678235,2.45179657878873,11.1632868545726));
#17362=CARTESIAN_POINT('Ctrl Pts',(5.19107814923646,2.44856947914658,11.1590608047071));
#17363=CARTESIAN_POINT('Ctrl Pts',(5.27235166789332,2.44534150031038,11.1548336034926));
#17364=CARTESIAN_POINT('Ctrl Pts',(5.35355449923363,2.43805910519284,11.1506064022781));
#17365=CARTESIAN_POINT('Ctrl Pts',(5.43425204526809,2.42673878783738,11.1463792010636));
#17366=CARTESIAN_POINT('Ctrl Pts',(5.51478326366659,2.4154418030579,11.1421607126343));
#17367=CARTESIAN_POINT('Ctrl Pts',(5.5948108139099,2.40012356453679,11.137942224205));
#17368=CARTESIAN_POINT('Ctrl Pts',(5.67390647719009,2.38085241678126,11.1337237357757));
#17369=CARTESIAN_POINT('Ctrl Pts',(5.75297620718848,2.36158758750243,11.1295066304722));
#17370=CARTESIAN_POINT('Ctrl Pts',(5.83111420586797,2.33837253274122,11.1252895251686));
#17371=CARTESIAN_POINT('Ctrl Pts',(5.90790326982822,2.31132653037253,11.1210724198651));
#17372=CARTESIAN_POINT('Ctrl Pts',(5.98469065230795,2.28428112024086,11.1168554069052));
#17373=CARTESIAN_POINT('Ctrl Pts',(6.06012872088491,2.25340508474976,11.1126383939453));
#17374=CARTESIAN_POINT('Ctrl Pts',(6.13381760662518,2.21886685302902,11.1084213809854));
#17375=CARTESIAN_POINT('Ctrl Pts',(6.20781119841862,2.18418580454337,11.1041869305332));
#17376=CARTESIAN_POINT('Ctrl Pts',(6.28004067809311,2.14581239738208,11.099952480081));
#17377=CARTESIAN_POINT('Ctrl Pts',(6.35012523456467,2.10396420749513,11.0957180296288));
#17378=CARTESIAN_POINT('Ctrl Pts',(6.42002238088403,2.06222792208515,11.0914949023417));
#17379=CARTESIAN_POINT('Ctrl Pts',(6.48778569450197,2.01703570745296,11.0872717750547));
#17380=CARTESIAN_POINT('Ctrl Pts',(6.55306722968888,1.96864640190776,11.0830486477676));
#17381=CARTESIAN_POINT('Ctrl Pts',(6.61861131684873,1.92006248225609,11.0788085357329));
#17382=CARTESIAN_POINT('Ctrl Pts',(6.68165326216365,1.86825600713603,11.0745684236981));
#17383=CARTESIAN_POINT('Ctrl Pts',(6.74187651914453,1.81352792777952,11.0703283116634));
#17384=CARTESIAN_POINT('Ctrl Pts',(6.8020997761254,1.75879984842303,11.0660881996287));
#17385=CARTESIAN_POINT('Ctrl Pts',(6.85950405911743,1.70115053986479,11.061848087594));
#17386=CARTESIAN_POINT('Ctrl Pts',(6.91381319192505,1.64091470742607,11.0576079755592));
#17387=CARTESIAN_POINT('Ctrl Pts',(6.96744889695082,1.58142579324822,11.0534204404871));
#17388=CARTESIAN_POINT('Ctrl Pts',(7.0182754860553,1.51918136673991,11.0492329054149));
#17389=CARTESIAN_POINT('Ctrl Pts',(7.06599273028175,1.45448038675701,11.0450453703427));
#17390=CARTESIAN_POINT('Ctrl Pts',(7.11364716714047,1.38986456882209,11.0408633470737));
#17391=CARTESIAN_POINT('Ctrl Pts',(7.15820009828966,1.32279898971227,11.0366813238046));
#17392=CARTESIAN_POINT('Ctrl Pts',(7.19938935247714,1.25361799782205,11.0324993005356));
#17393=CARTESIAN_POINT('Ctrl Pts',(7.24053764073229,1.18450581183491,11.0283214366155));
#17394=CARTESIAN_POINT('Ctrl Pts',(7.27832864894172,1.11328279391638,11.0241435726954));
#17395=CARTESIAN_POINT('Ctrl Pts',(7.31254255077461,1.04031353185631,11.0199657087753));
#17396=CARTESIAN_POINT('Ctrl Pts',(7.3467334246522,0.96739338237375,11.0157906568018));
#17397=CARTESIAN_POINT('Ctrl Pts',(7.37735177122243,0.892729751330217,11.0116156048283));
#17398=CARTESIAN_POINT('Ctrl Pts',(7.40422367988037,0.816711791217957,11.0074405528548));
#17399=CARTESIAN_POINT('Ctrl Pts',(7.43109295644617,0.740701277032877,11.0032659098258));
#17400=CARTESIAN_POINT('Ctrl Pts',(7.45421635323715,0.663337140612717,10.9990912667969));
#17401=CARTESIAN_POINT('Ctrl Pts',(7.47346857645307,0.585027313431843,10.994916623768));
#17402=CARTESIAN_POINT('Ctrl Pts',(7.49271959479406,0.506722387167932,10.9907422420035));
#17403=CARTESIAN_POINT('Ctrl Pts',(7.50809981523551,0.427472351205318,10.9865678602391));
#17404=CARTESIAN_POINT('Ctrl Pts',(7.51953466754609,0.347697161011841,10.9823934784747));
#17405=CARTESIAN_POINT('Ctrl Pts',(7.53097725214843,0.267868026523438,10.978216273977));
#17406=CARTESIAN_POINT('Ctrl Pts',(7.53846908540081,0.187513500945867,10.9740390694793));
#17407=CARTESIAN_POINT('Ctrl Pts',(7.54198738688373,0.107059475253671,10.9698618649817));
#17408=CARTESIAN_POINT('Ctrl Pts',(7.54357977837128,0.0706457948815983,
10.9679712524472));
#17409=CARTESIAN_POINT('Ctrl Pts',(7.54435890520214,0.0342117574601048,
10.9660806399126));
#17410=CARTESIAN_POINT('Ctrl Pts',(7.54432616501601,-0.00220320930647693,
10.9641900273781));
#17411=CARTESIAN_POINT('',(7.54432706806737,0.000654429156073597,10.1641900273412));
#17412=CARTESIAN_POINT('Ctrl Pts',(7.54432616501525,-0.00220321015041382,
10.9641900273343));
#17413=CARTESIAN_POINT('Ctrl Pts',(7.54422973877533,-0.109452355392079,
10.9586218064537));
#17414=CARTESIAN_POINT('Ctrl Pts',(7.53708802523116,-0.216389415989995,
10.9530535855732));
#17415=CARTESIAN_POINT('Ctrl Pts',(7.52304979361354,-0.32222294184132,10.9474853646926));
#17416=CARTESIAN_POINT('Ctrl Pts',(7.50901156199592,-0.428056467692646,
10.9419171438121));
#17417=CARTESIAN_POINT('Ctrl Pts',(7.48807700937725,-0.532786801160541,
10.9363489229316));
#17418=CARTESIAN_POINT('Ctrl Pts',(7.46044938521055,-0.635648858740374,
10.930780702051));
#17419=CARTESIAN_POINT('Ctrl Pts',(7.43945115546565,-0.713828622011396,
10.926548605197));
#17420=CARTESIAN_POINT('Ctrl Pts',(7.41453567237304,-0.79111260545169,10.922316508343));
#17421=CARTESIAN_POINT('Ctrl Pts',(7.38579644898933,-0.867079585440167,
10.918084411489));
#17422=CARTESIAN_POINT('Ctrl Pts',(7.35709830020516,-0.942937992095254,
10.9138583632216));
#17423=CARTESIAN_POINT('Ctrl Pts',(7.32458742817768,-1.01748270272683,10.9096323149543));
#17424=CARTESIAN_POINT('Ctrl Pts',(7.28840760300555,-1.09030587874254,10.9054062666869));
#17425=CARTESIAN_POINT('Ctrl Pts',(7.25221790407295,-1.163148928779,10.9011790650976));
#17426=CARTESIAN_POINT('Ctrl Pts',(7.21235739572926,-1.23426906122187,10.8969518635082));
#17427=CARTESIAN_POINT('Ctrl Pts',(7.16901889602631,-1.30327644414251,10.8927246619189));
#17428=CARTESIAN_POINT('Ctrl Pts',(7.12576974739914,-1.37214155439699,10.88850617556));
#17429=CARTESIAN_POINT('Ctrl Pts',(7.07905716023836,-1.43890221131252,10.884287689201));
#17430=CARTESIAN_POINT('Ctrl Pts',(7.0291186574484,-1.50319561345315,10.8800692028421));
#17431=CARTESIAN_POINT('Ctrl Pts',(6.97919653018364,-1.56746793289871,10.8758520997831));
#17432=CARTESIAN_POINT('Ctrl Pts',(6.92605087285857,-1.62927423755848,10.8716349967241));
#17433=CARTESIAN_POINT('Ctrl Pts',(6.86996118027363,-1.68828261137608,10.8674178936651));
#17434=CARTESIAN_POINT('Ctrl Pts',(6.81387271819393,-1.74728969065792,10.8632008831217));
#17435=CARTESIAN_POINT('Ctrl Pts',(6.75484067025096,-1.80349862512478,10.8589838725782));
#17436=CARTESIAN_POINT('Ctrl Pts',(6.69318229220123,-1.85661342140937,10.8547668620348));
#17437=CARTESIAN_POINT('Ctrl Pts',(6.63126888498284,-1.90994790920659,10.8505324092438));
#17438=CARTESIAN_POINT('Ctrl Pts',(6.56670772462401,-1.9601622909648,10.8462979564528));
#17439=CARTESIAN_POINT('Ctrl Pts',(6.49985312011632,-2.00699806594149,10.8420635036618));
#17440=CARTESIAN_POINT('Ctrl Pts',(6.43317736997772,-2.05370854239843,10.8378403791912));
#17441=CARTESIAN_POINT('Ctrl Pts',(6.36422084896978,-2.09705825239817,10.8336172547207));
#17442=CARTESIAN_POINT('Ctrl Pts',(6.29336207432357,-2.13683556419544,10.8293941302501));
#17443=CARTESIAN_POINT('Ctrl Pts',(6.22221818699229,-2.17677292697056,10.8251540132989));
#17444=CARTESIAN_POINT('Ctrl Pts',(6.14915713162086,-2.21310888042652,10.8209138963477));
#17445=CARTESIAN_POINT('Ctrl Pts',(6.07458301303673,-2.24567767006207,10.8166737793965));
#17446=CARTESIAN_POINT('Ctrl Pts',(6.00000889445258,-2.27824645969764,10.8124336624453));
#17447=CARTESIAN_POINT('Ctrl Pts',(5.92392217172948,-2.30704797824904,10.8081935454941));
#17448=CARTESIAN_POINT('Ctrl Pts',(5.84674123807394,-2.33196711687606,10.8039534285428));
#17449=CARTESIAN_POINT('Ctrl Pts',(5.76970641228079,-2.35683908216758,10.7997213383723));
#17450=CARTESIAN_POINT('Ctrl Pts',(5.69129412275253,-2.37793615913651,10.7954892482017));
#17451=CARTESIAN_POINT('Ctrl Pts',(5.61190875683385,-2.39510786903446,10.7912571580311));
#17452=CARTESIAN_POINT('Ctrl Pts',(5.53263685098873,-2.41225503658199,10.7870311164975));
#17453=CARTESIAN_POINT('Ctrl Pts',(5.45239508132609,-2.42548788221857,10.782805074964));
#17454=CARTESIAN_POINT('Ctrl Pts',(5.37160391926511,-2.43470538658913,10.7785790334304));
#17455=CARTESIAN_POINT('Ctrl Pts',(5.29079054782651,-2.44392542483877,10.7743518301639));
#17456=CARTESIAN_POINT('Ctrl Pts',(5.20942793358248,-2.44912779598901,10.7701246268974));
#17457=CARTESIAN_POINT('Ctrl Pts',(5.12794809816666,-2.45026243722348,10.7658974236309));
#17458=CARTESIAN_POINT('Ctrl Pts',(5.04663641333607,-2.45139473688979,10.7616789440775));
#17459=CARTESIAN_POINT('Ctrl Pts',(4.9652084549966,-2.44847604761776,10.757460464524));
#17460=CARTESIAN_POINT('Ctrl Pts',(4.88409785474619,-2.44150852352086,10.7532419849706));
#17461=CARTESIAN_POINT('Ctrl Pts',(4.80301385204959,-2.43454328419433,10.7490248887288));
#17462=CARTESIAN_POINT('Ctrl Pts',(4.72224746339989,-2.42353188643918,10.744807792487));
#17463=CARTESIAN_POINT('Ctrl Pts',(4.64222921171153,-2.40852850246958,10.7405906962452));
#17464=CARTESIAN_POINT('Ctrl Pts',(4.56221271552293,-2.39352544765536,10.7363736925211));
#17465=CARTESIAN_POINT('Ctrl Pts',(4.48294478017963,-2.37453066752338,10.7321566887971));
#17466=CARTESIAN_POINT('Ctrl Pts',(4.40484630280279,-2.35164955609488,10.7279396850731));
#17467=CARTESIAN_POINT('Ctrl Pts',(4.3264245214889,-2.32867372382601,10.7237052242365));
#17468=CARTESIAN_POINT('Ctrl Pts',(4.24918235755605,-2.3017794355617,10.7194707634));
#17469=CARTESIAN_POINT('Ctrl Pts',(4.1735293841398,-2.27112356821811,10.7152363025635));
#17470=CARTESIAN_POINT('Ctrl Pts',(4.09807906717904,-2.24054982070584,10.7110131848478));
#17471=CARTESIAN_POINT('Ctrl Pts',(4.02420984418272,-2.20623485547402,10.7067900671322));
#17472=CARTESIAN_POINT('Ctrl Pts',(3.95230510324244,-2.16838134430195,10.7025669494165));
#17473=CARTESIAN_POINT('Ctrl Pts',(3.88011066252651,-2.13037532366319,10.6983268170196));
#17474=CARTESIAN_POINT('Ctrl Pts',(3.80989696810958,-2.08880243134801,10.6940866846226));
#17475=CARTESIAN_POINT('Ctrl Pts',(3.7420228151154,-2.04391175823325,10.6898465522256));
#17476=CARTESIAN_POINT('Ctrl Pts',(3.67414866212122,-1.99902108511848,10.6856064198286));
#17477=CARTESIAN_POINT('Ctrl Pts',(3.60861439013521,-1.95081295823496,10.6813662874316));
#17478=CARTESIAN_POINT('Ctrl Pts',(3.545744050563,-1.89957599225559,10.6771261550346));
#17479=CARTESIAN_POINT('Ctrl Pts',(3.48299299799072,-1.84843624070195,10.6728940676502));
#17480=CARTESIAN_POINT('Ctrl Pts',(3.42266165538615,-1.79408835227847,10.6686619802658));
#17481=CARTESIAN_POINT('Ctrl Pts',(3.36509614527464,-1.736789954038,10.6644298928814));
#17482=CARTESIAN_POINT('Ctrl Pts',(3.30761291060314,-1.67957344946821,10.6602038542031));
#17483=CARTESIAN_POINT('Ctrl Pts',(3.25288798380879,-1.61941513560699,10.6559778155248));
#17484=CARTESIAN_POINT('Ctrl Pts',(3.20123471640633,-1.55661302502033,10.6517517768465));
#17485=CARTESIAN_POINT('Ctrl Pts',(3.1495672060652,-1.49379359729859,10.6475245728748));
#17486=CARTESIAN_POINT('Ctrl Pts',(3.1009733938187,-1.42832922967434,10.6432973689031));
#17487=CARTESIAN_POINT('Ctrl Pts',(3.05573013969367,-1.3605553293977,10.6390701649314));
#17488=CARTESIAN_POINT('Ctrl Pts',(3.01058029410279,-1.29292135408445,10.6348516883808));
#17489=CARTESIAN_POINT('Ctrl Pts',(2.9687674642413,-1.22298774567671,10.6306332118301));
#17490=CARTESIAN_POINT('Ctrl Pts',(2.93052555595295,-1.15111964608378,10.6264147352795));
#17491=CARTESIAN_POINT('Ctrl Pts',(2.89229618829429,-1.0792751141229,10.6221976420895));
#17492=CARTESIAN_POINT('Ctrl Pts',(2.85763563481092,-1.00549776069986,10.6179805488995));
#17493=CARTESIAN_POINT('Ctrl Pts',(2.82673244980861,-0.930178394523694,
10.6137634557095));
#17494=CARTESIAN_POINT('Ctrl Pts',(2.79582994311389,-0.854860681565405,
10.6095464550823));
#17495=CARTESIAN_POINT('Ctrl Pts',(2.76868481625073,-0.778001453495694,
10.6053294544552));
#17496=CARTESIAN_POINT('Ctrl Pts',(2.74543739777439,-0.700011282787416,
10.601112453828));
#17497=CARTESIAN_POINT('Ctrl Pts',(2.72209370549917,-0.621698133851823,
10.5968779894696));
#17498=CARTESIAN_POINT('Ctrl Pts',(2.70268022044022,-0.542245103709113,
10.5926435251111));
#17499=CARTESIAN_POINT('Ctrl Pts',(2.68728790353319,-0.462081247151078,
10.5884090607526));
#17500=CARTESIAN_POINT('Ctrl Pts',(2.67193684332346,-0.382132257268758,
10.5841859462133));
#17501=CARTESIAN_POINT('Ctrl Pts',(2.66058544696529,-0.3014767153737,10.5799628316741));
#17502=CARTESIAN_POINT('Ctrl Pts',(2.65327200300634,-0.220546588877568,
10.5757397171348));
#17503=CARTESIAN_POINT('Ctrl Pts',(2.64592907620976,-0.13929020709157,10.5714995778668));
#17504=CARTESIAN_POINT('Ctrl Pts',(2.64265673743915,-0.0577574935697764,
10.5672594385987));
#17505=CARTESIAN_POINT('Ctrl Pts',(2.64344094462743,0.0236149909031273,
10.5630192993306));
#17506=CARTESIAN_POINT('Ctrl Pts',(2.64422515181571,0.104987475376031,10.5587791600625));
#17507=CARTESIAN_POINT('Ctrl Pts',(2.64906581505827,0.186199267992801,10.5545390207944));
#17508=CARTESIAN_POINT('Ctrl Pts',(2.65789683120662,0.266821486047086,10.5502988815263));
#17509=CARTESIAN_POINT('Ctrl Pts',(2.66671108469566,0.347290670435662,10.5460667907103));
#17510=CARTESIAN_POINT('Ctrl Pts',(2.67953342465925,0.42747273257862,10.5418346998942));
#17511=CARTESIAN_POINT('Ctrl Pts',(2.69633575483152,0.506937110444215,10.5376026090782));
#17512=CARTESIAN_POINT('Ctrl Pts',(2.71311407052352,0.586287915030661,10.5333765669149));
#17513=CARTESIAN_POINT('Ctrl Pts',(2.73386098343242,0.664922621732558,10.5291505247517));
#17514=CARTESIAN_POINT('Ctrl Pts',(2.75849668575241,0.74241622240325,10.5249244825884));
#17515=CARTESIAN_POINT('Ctrl Pts',(2.7831391557917,0.819931111484143,10.5206972794814));
#17516=CARTESIAN_POINT('Ctrl Pts',(2.81167247496008,0.8963038070958,10.5164700763743));
#17517=CARTESIAN_POINT('Ctrl Pts',(2.84396561234774,0.971119604814727,10.5122428732672));
#17518=CARTESIAN_POINT('Ctrl Pts',(2.87619211182324,1.04578101776465,10.5080243931276));
#17519=CARTESIAN_POINT('Ctrl Pts',(2.91216276679483,1.11889151524476,10.503805912988));
#17520=CARTESIAN_POINT('Ctrl Pts',(2.95169823893658,1.19005628229245,10.4995874328485));
#17521=CARTESIAN_POINT('Ctrl Pts',(2.99122074655504,1.26119771289744,10.4953703360384));
#17522=CARTESIAN_POINT('Ctrl Pts',(3.03430552436084,1.3303942742741,10.4911532392283));
#17523=CARTESIAN_POINT('Ctrl Pts',(3.08072703822684,1.39727526565942,10.4869361424183));
#17524=CARTESIAN_POINT('Ctrl Pts',(3.12714753345736,1.46415478946331,10.4827191381447));
#17525=CARTESIAN_POINT('Ctrl Pts',(3.1769043532607,1.52871846321255,10.4785021338711));
#17526=CARTESIAN_POINT('Ctrl Pts',(3.22972916009567,1.59062532159663,10.4742851295976));
#17527=CARTESIAN_POINT('Ctrl Pts',(3.28277262981773,1.65278843709163,10.4700506694659));
#17528=CARTESIAN_POINT('Ctrl Pts',(3.33890924345049,1.71227232788743,10.4658162093343));
#17529=CARTESIAN_POINT('Ctrl Pts',(3.39782831669486,1.76876742081334,10.4615817492027));
#17530=CARTESIAN_POINT('Ctrl Pts',(3.45658957635809,1.8251111927418,10.4573586309894));
#17531=CARTESIAN_POINT('Ctrl Pts',(3.51811802895034,1.87848188195073,10.4531355127761));
#17532=CARTESIAN_POINT('Ctrl Pts',(3.58207191205862,1.92861254119879,10.4489123945629));
#17533=CARTESIAN_POINT('Ctrl Pts',(3.64628343407846,1.97894515235121,10.4446722634721));
#17534=CARTESIAN_POINT('Ctrl Pts',(3.71293957951195,2.02601130857226,10.4404321323813));
#17535=CARTESIAN_POINT('Ctrl Pts',(3.78166628772297,2.0695854916378,10.4361920012905));
#17536=CARTESIAN_POINT('Ctrl Pts',(3.85039299593399,2.11315967470334,10.4319518701997));
#17537=CARTESIAN_POINT('Ctrl Pts',(3.92118982959871,2.15324170850486,10.4277117391089));
#17538=CARTESIAN_POINT('Ctrl Pts',(3.99366087354392,2.18965394575264,10.4234716080181));
#17539=CARTESIAN_POINT('Ctrl Pts',(4.06599447518361,2.22599712670477,10.4192395183927));
#17540=CARTESIAN_POINT('Ctrl Pts',(4.14026579677943,2.25882002096268,10.4150074287673));
#17541=CARTESIAN_POINT('Ctrl Pts',(4.21609817081611,2.28791216604312,10.410775339142));
#17542=CARTESIAN_POINT('Ctrl Pts',(4.29182216232673,2.31696273151837,10.4065492981807));
#17543=CARTESIAN_POINT('Ctrl Pts',(4.36910234480826,2.34229297295076,10.4023232572195));
#17544=CARTESIAN_POINT('Ctrl Pts',(4.4475386030181,2.36373885126751,10.3980972162583));
#17545=CARTESIAN_POINT('Ctrl Pts',(4.52599643646458,2.38519062864052,10.3938700128521));
#17546=CARTESIAN_POINT('Ctrl Pts',(4.60561055333585,2.40275572018599,10.389642809446));
#17547=CARTESIAN_POINT('Ctrl Pts',(4.68596164252641,2.41631868207922,10.3854156060398));
#17548=CARTESIAN_POINT('Ctrl Pts',(4.76614689582192,2.42985365149657,10.3811971271209));
#17549=CARTESIAN_POINT('Ctrl Pts',(4.84706562833794,2.4394028926821,10.3769786482021));
#17550=CARTESIAN_POINT('Ctrl Pts',(4.92828896477675,2.44490232063115,10.3727601692833));
#17551=CARTESIAN_POINT('Ctrl Pts',(5.00948566626339,2.45039994519454,10.3685430736982));
#17552=CARTESIAN_POINT('Ctrl Pts',(5.09098631003848,2.4518503624904,10.3643259781131));
#17553=CARTESIAN_POINT('Ctrl Pts',(5.17235715006545,2.44924137029126,10.360108882528));
#17554=CARTESIAN_POINT('Ctrl Pts',(5.2537262045067,2.44663243534332,10.3558918794821));
#17555=CARTESIAN_POINT('Ctrl Pts',(5.33496499644998,2.43996428405307,10.3516748764361));
#17556=CARTESIAN_POINT('Ctrl Pts',(5.41564147139757,2.42927680515276,10.3474578733902));
#17557=CARTESIAN_POINT('Ctrl Pts',(5.49665194953007,2.41854507974821,10.3432234118168));
#17558=CARTESIAN_POINT('Ctrl Pts',(5.57709497531964,2.40376072474435,10.3389889502435));
#17559=CARTESIAN_POINT('Ctrl Pts',(5.65654182378683,2.38501623727011,10.3347544886701));
#17560=CARTESIAN_POINT('Ctrl Pts',(5.73577582553562,2.36632196830955,10.3305313716783));
#17561=CARTESIAN_POINT('Ctrl Pts',(5.81401854315967,2.34368892850853,10.3263082546865));
#17562=CARTESIAN_POINT('Ctrl Pts',(5.89086013740065,2.31725887109917,10.3220851376947));
#17563=CARTESIAN_POINT('Ctrl Pts',(5.96801136161381,2.29072231488509,10.3178450038305));
#17564=CARTESIAN_POINT('Ctrl Pts',(6.04374971268874,2.26035826005573,10.3136048699664));
#17565=CARTESIAN_POINT('Ctrl Pts',(6.11768256731956,2.22635809015346,10.3093647361023));
#17566=CARTESIAN_POINT('Ctrl Pts',(6.19161542195039,2.19235792025119,10.3051246022382));
#17567=CARTESIAN_POINT('Ctrl Pts',(6.26374239459648,2.15472190661922,10.3008844683741));
#17568=CARTESIAN_POINT('Ctrl Pts',(6.33369916316996,2.11368579842894,10.29664433451));
#17569=CARTESIAN_POINT('Ctrl Pts',(6.40352320773505,2.07272754513217,10.2924122451507));
#17570=CARTESIAN_POINT('Ctrl Pts',(6.47144578305982,2.02822929369221,10.2881801557914));
#17571=CARTESIAN_POINT('Ctrl Pts',(6.53708548682375,1.98039279915102,10.2839480664321));
#17572=CARTESIAN_POINT('Ctrl Pts',(6.60263137568237,1.9326246744523,10.2797220257452));
#17573=CARTESIAN_POINT('Ctrl Pts',(6.66590050079519,1.88152805407527,10.2754959850582));
#17574=CARTESIAN_POINT('Ctrl Pts',(6.72653767991026,1.82734960894921,10.2712699443713));
#17575=CARTESIAN_POINT('Ctrl Pts',(6.78719154322635,1.77315625673015,10.2670427408976));
#17576=CARTESIAN_POINT('Ctrl Pts',(6.84521162343385,1.71587964234996,10.2628155374239));
#17577=CARTESIAN_POINT('Ctrl Pts',(6.90027309244994,1.65580896443631,10.2585883339501));
#17578=CARTESIAN_POINT('Ctrl Pts',(6.95522091590697,1.59586227096944,10.2543698553236));
#17579=CARTESIAN_POINT('Ctrl Pts',(7.00722199653962,1.53313336189751,10.250151376697));
#17580=CARTESIAN_POINT('Ctrl Pts',(7.05598941581168,1.46794738121793,10.2459328980704));
#17581=CARTESIAN_POINT('Ctrl Pts',(7.10474084308195,1.40278277657864,10.2417158027838));
#17582=CARTESIAN_POINT('Ctrl Pts',(7.1502604366871,1.33516307224067,10.2374987074971));
#17583=CARTESIAN_POINT('Ctrl Pts',(7.19230217861376,1.26544570297225,10.2332816122105));
#17584=CARTESIAN_POINT('Ctrl Pts',(7.23434299792718,1.19572986366344,10.2290646094687));
#17585=CARTESIAN_POINT('Ctrl Pts',(7.27290587832797,1.12391684947886,10.224847606727));
#17586=CARTESIAN_POINT('Ctrl Pts',(7.30778944419396,1.05039099102828,10.2206306039852));
#17587=CARTESIAN_POINT('Ctrl Pts',(7.34281743449282,0.97656072188617,10.2163961420699));
#17588=CARTESIAN_POINT('Ctrl Pts',(7.37413536539507,0.901003816020216,10.2121616801546));
#17589=CARTESIAN_POINT('Ctrl Pts',(7.40158782829095,0.82413040649102,10.2079272182393));
#17590=CARTESIAN_POINT('Ctrl Pts',(7.42896673880807,0.747462961073511,10.2037041015628));
#17591=CARTESIAN_POINT('Ctrl Pts',(7.45250077239823,0.669486517032942,10.1994809848863));
#17592=CARTESIAN_POINT('Ctrl Pts',(7.47208612989054,0.590622130052558,10.1952578682098));
#17593=CARTESIAN_POINT('Ctrl Pts',(7.49175041033514,0.51143994390748,10.1910177336751));
#17594=CARTESIAN_POINT('Ctrl Pts',(7.50743404144642,0.431363107756696,10.1867775991404));
#17595=CARTESIAN_POINT('Ctrl Pts',(7.51908423982532,0.350825205340769,10.1825374646058));
#17596=CARTESIAN_POINT('Ctrl Pts',(7.53073443820423,0.270287302924853,10.1782973300711));
#17597=CARTESIAN_POINT('Ctrl Pts',(7.5383512220321,0.189288805347542,10.1740571955364));
#17598=CARTESIAN_POINT('Ctrl Pts',(7.5419344305523,0.108263657828534,10.1698170610017));
#17599=CARTESIAN_POINT('Ctrl Pts',(7.54351950878181,0.0724211449937457,
10.1679413831272));
#17600=CARTESIAN_POINT('Ctrl Pts',(7.54431748352344,0.0365435678285603,
10.1660657052527));
#17601=CARTESIAN_POINT('Ctrl Pts',(7.54432706806718,0.000654429861452634,
10.1641900273781));
#17602=CARTESIAN_POINT('',(7.54432654498802,0.00172970778312925,9.36419005773998));
#17603=CARTESIAN_POINT('Ctrl Pts',(7.54432706806737,0.000654429156057273,
10.1641900273412));
#17604=CARTESIAN_POINT('Ctrl Pts',(7.54434854189879,-0.0797540024219345,
10.1599876328403));
#17605=CARTESIAN_POINT('Ctrl Pts',(7.5404080790334,-0.160320975644378,10.1557852383394));
#17606=CARTESIAN_POINT('Ctrl Pts',(7.53248499309329,-0.240620449912523,
10.1515828438385));
#17607=CARTESIAN_POINT('Ctrl Pts',(7.52457302027542,-0.320807294091884,
10.1473863437232));
#17608=CARTESIAN_POINT('Ctrl Pts',(7.51268956108762,-0.400726918673235,
10.1431898436079));
#17609=CARTESIAN_POINT('Ctrl Pts',(7.4968659434941,-0.479952948913191,10.1389933434927));
#17610=CARTESIAN_POINT('Ctrl Pts',(7.4810596902607,-0.559092038900001,10.1348014484899));
#17611=CARTESIAN_POINT('Ctrl Pts',(7.46132196055936,-0.637538586265839,
10.1306095534871));
#17612=CARTESIAN_POINT('Ctrl Pts',(7.43773574775956,-0.714872548718988,
10.1264176584843));
#17613=CARTESIAN_POINT('Ctrl Pts',(7.41416339532711,-0.792161066100588,
10.1222282268361));
#17614=CARTESIAN_POINT('Ctrl Pts',(7.38674718491712,-0.86833784573309,10.1180387951878));
#17615=CARTESIAN_POINT('Ctrl Pts',(7.35562063746299,-0.942995490306101,
10.1138493635396));
#17616=CARTESIAN_POINT('Ctrl Pts',(7.32450251973879,-1.01763291600382,10.1096610664784));
#17617=CARTESIAN_POINT('Ctrl Pts',(7.28967624166735,-1.09075158826702,10.1054727694172));
#17618=CARTESIAN_POINT('Ctrl Pts',(7.25132384904031,-1.16196310920799,10.101284472356));
#17619=CARTESIAN_POINT('Ctrl Pts',(7.21296969209431,-1.23317790608111,10.0970959826212));
#17620=CARTESIAN_POINT('Ctrl Pts',(7.17108932405904,-1.30248496297156,10.0929074928865));
#17621=CARTESIAN_POINT('Ctrl Pts',(7.12591049597306,-1.36952091885494,10.0887190031517));
#17622=CARTESIAN_POINT('Ctrl Pts',(7.08068583939756,-1.43662487465625,10.0845262646977));
#17623=CARTESIAN_POINT('Ctrl Pts',(7.03215630761541,-1.50145273844476,10.0803335262436));
#17624=CARTESIAN_POINT('Ctrl Pts',(6.98059231048667,-1.56367116100259,10.0761407877896));
#17625=CARTESIAN_POINT('Ctrl Pts',(6.92900025391363,-1.6259234407953,10.0719457677841));
#17626=CARTESIAN_POINT('Ctrl Pts',(6.87437076456973,-1.68556310551769,10.0677507477787));
#17627=CARTESIAN_POINT('Ctrl Pts',(6.81701204751294,-1.74229276465718,10.0635557277732));
#17628=CARTESIAN_POINT('Ctrl Pts',(6.75955608575016,-1.79911860201171,10.0593535956232));
#17629=CARTESIAN_POINT('Ctrl Pts',(6.69936201018658,-1.85302426969885,10.0551514634732));
#17630=CARTESIAN_POINT('Ctrl Pts',(6.63677172159038,-1.90375216764879,10.0509493313232));
#17631=CARTESIAN_POINT('Ctrl Pts',(6.59725288308932,-1.93578121962386,10.0482961500466));
#17632=CARTESIAN_POINT('Ctrl Pts',(6.55677941399393,-1.96654429046505,10.0456429687701));
#17633=CARTESIAN_POINT('Ctrl Pts',(6.51544287596879,-1.99598571968405,10.0429897874936));
#17634=CARTESIAN_POINT('Ctrl Pts',(6.44950696129102,-2.04294774547818,10.0387576978549));
#17635=CARTESIAN_POINT('Ctrl Pts',(6.38111851702476,-2.08672664771397,10.0345256082162));
#17636=CARTESIAN_POINT('Ctrl Pts',(6.31061765686637,-2.12705691641537,10.0302935185776));
#17637=CARTESIAN_POINT('Ctrl Pts',(6.24021755927349,-2.1673295435315,10.0260674776057));
#17638=CARTESIAN_POINT('Ctrl Pts',(6.16771144212542,-2.20416309767322,10.0218414366338));
#17639=CARTESIAN_POINT('Ctrl Pts',(6.09346968053859,-2.23733436750986,10.0176153956619));
#17640=CARTESIAN_POINT('Ctrl Pts',(6.01920749772374,-2.27051476156514,10.0133881922587));
#17641=CARTESIAN_POINT('Ctrl Pts',(5.94320911055227,-2.30003060757941,10.0091609888555));
#17642=CARTESIAN_POINT('Ctrl Pts',(5.86587128518421,-2.32570378847947,10.0049337854523));
#17643=CARTESIAN_POINT('Ctrl Pts',(5.78869307653,-2.35132398277498,10.0007153065292));
#17644=CARTESIAN_POINT('Ctrl Pts',(5.71018138623775,-2.37311718764668,9.99649682760604));
#17645=CARTESIAN_POINT('Ctrl Pts',(5.63075027478033,-2.39095458215582,9.99227834868292));
#17646=CARTESIAN_POINT('Ctrl Pts',(5.55134521061032,-2.40878612737326,9.98806125309601));
#17647=CARTESIAN_POINT('Ctrl Pts',(5.47102177707208,-2.42266433661333,9.98384415750909));
#17648=CARTESIAN_POINT('Ctrl Pts',(5.39020677054033,-2.43251091955632,9.97962706192218));
#17649=CARTESIAN_POINT('Ctrl Pts',(5.30939353744409,-2.44235728642212,9.97541005887684));
#17650=CARTESIAN_POINT('Ctrl Pts',(5.22808921421871,-2.44817214783398,9.97119305583149));
#17651=CARTESIAN_POINT('Ctrl Pts',(5.14672687960594,-2.44992895186464,9.96697605278615));
#17652=CARTESIAN_POINT('Ctrl Pts',(5.06502770244309,-2.45169302911763,9.96274159121941));
#17653=CARTESIAN_POINT('Ctrl Pts',(4.98327050394719,-2.44936535339008,9.95850712965267));
#17654=CARTESIAN_POINT('Ctrl Pts',(4.90189310546524,-2.44297187262876,9.95427266808593));
#17655=CARTESIAN_POINT('Ctrl Pts',(4.82073372585589,-2.4365955206955,9.95004955110078));
#17656=CARTESIAN_POINT('Ctrl Pts',(4.73995257227418,-2.4261752220265,9.94582643411564));
#17657=CARTESIAN_POINT('Ctrl Pts',(4.65997632301412,-2.41178848682715,9.94160331713049));
#17658=CARTESIAN_POINT('Ctrl Pts',(4.57967781281918,-2.39734378088301,9.93736318327295));
#17659=CARTESIAN_POINT('Ctrl Pts',(4.50019116459454,-2.37890072070671,9.93312304941542));
#17660=CARTESIAN_POINT('Ctrl Pts',(4.4219336209088,-2.35658849361477,9.92888291555789));
#17661=CARTESIAN_POINT('Ctrl Pts',(4.34367607722305,-2.33427626652284,9.92464278170035));
#17662=CARTESIAN_POINT('Ctrl Pts',(4.26664806052866,-2.30809508180606,9.92040264784281));
#17663=CARTESIAN_POINT('Ctrl Pts',(4.19124561850282,-2.27822229362203,9.91616251398528));
#17664=CARTESIAN_POINT('Ctrl Pts',(4.11598622740603,-2.24840617906805,9.91193042436439));
#17665=CARTESIAN_POINT('Ctrl Pts',(4.04206546527135,-2.21480123235798,9.90769833474351));
#17666=CARTESIAN_POINT('Ctrl Pts',(3.9698910689718,-2.17754860416595,9.90346624512263));
#17667=CARTESIAN_POINT('Ctrl Pts',(3.8978198271362,-2.14034921888399,9.89924020416939));
#17668=CARTESIAN_POINT('Ctrl Pts',(3.82749040333833,-2.09951271786708,9.89501416321616));
#17669=CARTESIAN_POINT('Ctrl Pts',(3.75929148031584,-2.05522864464903,9.89078812226293));
#17670=CARTESIAN_POINT('Ctrl Pts',(3.69107379785709,-2.01093239023792,9.88656091885518));
#17671=CARTESIAN_POINT('Ctrl Pts',(3.62498821191902,-1.96318686309364,9.88233371544744));
#17672=CARTESIAN_POINT('Ctrl Pts',(3.56139990073167,-1.91222827062747,9.8781065120397));
#17673=CARTESIAN_POINT('Ctrl Pts',(3.49794282916259,-1.86137485136212,9.87388803313731));
#17674=CARTESIAN_POINT('Ctrl Pts',(3.43697311268567,-1.80732188749472,9.86966955423492));
#17675=CARTESIAN_POINT('Ctrl Pts',(3.37882395332888,-1.75034689896135,9.86545107533253));
#17676=CARTESIAN_POINT('Ctrl Pts',(3.32069386242832,-1.69339059384641,9.86123397976709));
#17677=CARTESIAN_POINT('Ctrl Pts',(3.26538282349114,-1.6335144919276,9.85701688420164));
#17678=CARTESIAN_POINT('Ctrl Pts',(3.21318854831214,-1.5710342705781,9.8527997886362));
#17679=CARTESIAN_POINT('Ctrl Pts',(3.16099541851314,-1.50855542032909,9.84858278561303));
#17680=CARTESIAN_POINT('Ctrl Pts',(3.1119192135165,-1.44347292163379,9.84436578258986));
#17681=CARTESIAN_POINT('Ctrl Pts',(3.06621763311378,-1.37613584900578,9.84014877956669));
#17682=CARTESIAN_POINT('Ctrl Pts',(3.0203268462704,-1.30851999810087,9.83591431797588));
#17683=CARTESIAN_POINT('Ctrl Pts',(2.97783896132303,-1.23863124858803,9.83167985638508));
#17684=CARTESIAN_POINT('Ctrl Pts',(2.93897018992724,-1.16685119365095,9.82744539479428));
#17685=CARTESIAN_POINT('Ctrl Pts',(2.9002055526215,-1.09526344607108,9.82322227783283));
#17686=CARTESIAN_POINT('Ctrl Pts',(2.86504082628364,-1.02179495372241,9.81899916087137));
#17687=CARTESIAN_POINT('Ctrl Pts',(2.83364288627533,-0.94684598502676,9.81477604390992));
#17688=CARTESIAN_POINT('Ctrl Pts',(2.80211842905418,-0.871595011338996,
9.81053591000444));
#17689=CARTESIAN_POINT('Ctrl Pts',(2.77439133067801,-0.794852051357482,
9.80629577609897));
#17690=CARTESIAN_POINT('Ctrl Pts',(2.75057996189576,-0.71703754426502,9.80205564219349));
#17691=CARTESIAN_POINT('Ctrl Pts',(2.72676859311351,-0.639223037172568,
9.79781550828802));
#17692=CARTESIAN_POINT('Ctrl Pts',(2.70687300789252,-0.56033745132404,9.79357537438254));
#17693=CARTESIAN_POINT('Ctrl Pts',(2.69095962667345,-0.480809618389983,
9.78933524047707));
#17694=CARTESIAN_POINT('Ctrl Pts',(2.67507643571004,-0.401432662606144,
9.78510315079078));
#17695=CARTESIAN_POINT('Ctrl Pts',(2.66310108021354,-0.32111975827553,9.7808710611045));
#17696=CARTESIAN_POINT('Ctrl Pts',(2.65513672227462,-0.240289868957742,
9.77663897141822));
#17697=CARTESIAN_POINT('Ctrl Pts',(2.64718374730463,-0.159575504849292,
9.77241293039847));
#17698=CARTESIAN_POINT('Ctrl Pts',(2.64323042936645,-0.0783460818642417,
9.76818688937873));
#17699=CARTESIAN_POINT('Ctrl Pts',(2.64332895420887,0.00296912423532622,
9.76396084835899));
#17700=CARTESIAN_POINT('Ctrl Pts',(2.64342750615052,0.0843066960617253,
9.75973364496773));
#17701=CARTESIAN_POINT('Ctrl Pts',(2.64758019548308,0.165729635975825,9.75550644157648));
#17702=CARTESIAN_POINT('Ctrl Pts',(2.655787263711,0.246803031330851,9.75127923818523));
#17703=CARTESIAN_POINT('Ctrl Pts',(2.66397739357458,0.327709101318281,9.74706075921409));
#17704=CARTESIAN_POINT('Ctrl Pts',(2.67620516165238,0.408266603264365,9.74284228024295));
#17705=CARTESIAN_POINT('Ctrl Pts',(2.69241875184998,0.488045007252681,9.73862380127181));
#17706=CARTESIAN_POINT('Ctrl Pts',(2.70862702523854,0.567797250067942,9.73440670563693));
#17707=CARTESIAN_POINT('Ctrl Pts',(2.72881843260256,0.646770447266115,9.73018961000204));
#17708=CARTESIAN_POINT('Ctrl Pts',(2.75288983833351,0.724543116258019,9.72597251436715));
#17709=CARTESIAN_POINT('Ctrl Pts',(2.77696071583163,0.802314078574487,9.72175551127394));
#17710=CARTESIAN_POINT('Ctrl Pts',(2.80491128391425,0.878884121492782,9.71753850818074));
#17711=CARTESIAN_POINT('Ctrl Pts',(2.83658862509982,0.953847192735038,9.71332150508754));
#17712=CARTESIAN_POINT('Ctrl Pts',(2.86839711065726,1.02912061151669,9.70908704357765));
#17713=CARTESIAN_POINT('Ctrl Pts',(2.9039631209882,1.10277328492846,9.70485258206775));
#17714=CARTESIAN_POINT('Ctrl Pts',(2.94308389171338,1.17441630756651,9.70061812055787));
#17715=CARTESIAN_POINT('Ctrl Pts',(2.98209985461162,1.2458673925362,9.69639500352563));
#17716=CARTESIAN_POINT('Ctrl Pts',(3.02465127584591,1.31531920384112,9.69217188649339));
#17717=CARTESIAN_POINT('Ctrl Pts',(3.07049289756892,1.38241409529569,9.68794876946115));
#17718=CARTESIAN_POINT('Ctrl Pts',(3.11651923448535,1.44977934031515,9.68370863571243));
#17719=CARTESIAN_POINT('Ctrl Pts',(3.16586205111719,1.51476826107213,9.67946850196373));
#17720=CARTESIAN_POINT('Ctrl Pts',(3.21823279302563,1.57705295967836,9.67522836821501));
#17721=CARTESIAN_POINT('Ctrl Pts',(3.27060353493407,1.63933765828457,9.6709882344663));
#17722=CARTESIAN_POINT('Ctrl Pts',(3.32600183833794,1.69891783485359,9.66674810071759));
#17723=CARTESIAN_POINT('Ctrl Pts',(3.38410386532814,1.75550463434428,9.66250796696887));
#17724=CARTESIAN_POINT('Ctrl Pts',(3.44209566508421,1.81198408118793,9.658275877315));
#17725=CARTESIAN_POINT('Ctrl Pts',(3.50299728362813,1.8656922229589,9.65404378766113));
#17726=CARTESIAN_POINT('Ctrl Pts',(3.56651313793106,1.91631472933875,9.64981169800726));
#17727=CARTESIAN_POINT('Ctrl Pts',(3.62993821290765,1.96686488406598,9.64558565702032));
#17728=CARTESIAN_POINT('Ctrl Pts',(3.69596974245763,2.01433787515468,9.64135961603339));
#17729=CARTESIAN_POINT('Ctrl Pts',(3.76427577817759,2.0584565541164,9.63713357504646));
#17730=CARTESIAN_POINT('Ctrl Pts',(3.83260060211758,2.10258736833731,9.63290637164705));
#17731=CARTESIAN_POINT('Ctrl Pts',(3.90320083122195,2.14336171876855,9.62867916824763));
#17732=CARTESIAN_POINT('Ctrl Pts',(3.97571154982909,2.18054299257319,9.62445196484822));
#17733=CARTESIAN_POINT('Ctrl Pts',(4.04807261465002,2.21764752850365,9.6202334859106));
#17734=CARTESIAN_POINT('Ctrl Pts',(4.12233588867171,2.25117357010085,9.61601500697299));
#17735=CARTESIAN_POINT('Ctrl Pts',(4.19811183741161,2.28093058180774,9.61179652803537));
#17736=CARTESIAN_POINT('Ctrl Pts',(4.27386293747197,2.31067783550486,9.60757943243419));
#17737=CARTESIAN_POINT('Ctrl Pts',(4.35112529495952,2.33665834407588,9.60336233683301));
#17738=CARTESIAN_POINT('Ctrl Pts',(4.42948907303053,2.35872956530483,9.59914524123183));
#17739=CARTESIAN_POINT('Ctrl Pts',(4.5078511314518,2.38080030219303,9.59492823817248));
#17740=CARTESIAN_POINT('Ctrl Pts',(4.58731411480222,2.39896179743436,9.59071123511313));
#17741=CARTESIAN_POINT('Ctrl Pts',(4.66745407731082,2.41312168119129,9.58649423205378));
#17742=CARTESIAN_POINT('Ctrl Pts',(4.74792582111546,2.42734018719407,9.58225977050435));
#17743=CARTESIAN_POINT('Ctrl Pts',(4.82907969907151,2.43752378283135,9.57802530895492));
#17744=CARTESIAN_POINT('Ctrl Pts',(4.91047906192067,2.4436312583117,9.57379084740549));
#17745=CARTESIAN_POINT('Ctrl Pts',(4.9916603476385,2.44972237124711,9.56956773040712));
#17746=CARTESIAN_POINT('Ctrl Pts',(5.07308533611265,2.451759206279,9.56534461340874));
#17747=CARTESIAN_POINT('Ctrl Pts',(5.15432051711923,2.44975321271232,9.56112149641036));
#17748=CARTESIAN_POINT('Ctrl Pts',(5.23588303099101,2.44773913610067,9.55688136258541));
#17749=CARTESIAN_POINT('Ctrl Pts',(5.31725373503828,2.44164962516437,9.55264122876045));
#17750=CARTESIAN_POINT('Ctrl Pts',(5.39800055325116,2.43154864110755,9.5484010949355));
#17751=CARTESIAN_POINT('Ctrl Pts',(5.47874737146404,2.42144765705074,9.54416096111054));
#17752=CARTESIAN_POINT('Ctrl Pts',(5.55886985438629,2.4073353422032,9.53992082728559));
#17753=CARTESIAN_POINT('Ctrl Pts',(5.63794951747986,2.38932649613702,9.53568069346063));
#17754=CARTESIAN_POINT('Ctrl Pts',(5.71687915457687,2.37135181555629,9.5314486038063));
#17755=CARTESIAN_POINT('Ctrl Pts',(5.79506439894742,2.34942833051714,9.52721651415196));
#17756=CARTESIAN_POINT('Ctrl Pts',(5.87208074203687,2.32363327678218,9.52298442449763));
#17757=CARTESIAN_POINT('Ctrl Pts',(5.94898701037536,2.29787509034061,9.51875838351032));
#17758=CARTESIAN_POINT('Ctrl Pts',(6.02472725855453,2.26825647147654,9.51453234252301));
#17759=CARTESIAN_POINT('Ctrl Pts',(6.09888841932976,2.23490539080621,9.5103063015357));
#17760=CARTESIAN_POINT('Ctrl Pts',(6.173069978824,2.20154513661007,9.5060790981364));
#17761=CARTESIAN_POINT('Ctrl Pts',(6.24567113357773,2.16445049642907,9.50185189473709));
#17762=CARTESIAN_POINT('Ctrl Pts',(6.31629491986031,2.12379914657325,9.49762469133779));
#17763=CARTESIAN_POINT('Ctrl Pts',(6.38677294677289,2.08323169642682,9.49340621239999));
#17764=CARTESIAN_POINT('Ctrl Pts',(6.45528134395035,2.03912241338701,9.48918773346218));
#17765=CARTESIAN_POINT('Ctrl Pts',(6.5214484406292,1.99169468446149,9.48496925452438));
#17766=CARTESIAN_POINT('Ctrl Pts',(6.58759383959105,1.94428250818211,9.48075215892311));
#17767=CARTESIAN_POINT('Ctrl Pts',(6.65139908537499,1.89355431758388,9.47653506332184));
#17768=CARTESIAN_POINT('Ctrl Pts',(6.71252175478821,1.83977662885563,9.47231796772057));
#17769=CARTESIAN_POINT('Ctrl Pts',(6.77364308289735,1.7860001202498,9.4681009646612));
#17770=CARTESIAN_POINT('Ctrl Pts',(6.83208160356233,1.72917455438392,9.46388396160181));
#17771=CARTESIAN_POINT('Ctrl Pts',(6.88752933678227,1.66960556260902,9.45966695854244));
#17772=CARTESIAN_POINT('Ctrl Pts',(6.94320662489477,1.60978995383625,9.45543249699327));
#17773=CARTESIAN_POINT('Ctrl Pts',(6.99586797807153,1.54720849164653,9.45119803544411));
#17774=CARTESIAN_POINT('Ctrl Pts',(7.04524145247934,1.48220527976446,9.44696357389494));
#17775=CARTESIAN_POINT('Ctrl Pts',(7.09448265035309,1.41737621806471,9.44274045689675));
#17776=CARTESIAN_POINT('Ctrl Pts',(7.14045333416895,1.35013877554875,9.43851733989857));
#17777=CARTESIAN_POINT('Ctrl Pts',(7.18292746618856,1.28086304563956,9.43429422290038));
#17778=CARTESIAN_POINT('Ctrl Pts',(7.2255727454755,1.21130817284262,9.43005408907572));
#17779=CARTESIAN_POINT('Ctrl Pts',(7.26469301668231,1.13969896950125,9.42581395525107));
#17780=CARTESIAN_POINT('Ctrl Pts',(7.30010709790708,1.06643286967595,9.42157382142642));
#17781=CARTESIAN_POINT('Ctrl Pts',(7.33552117913186,0.993166769850654,9.41733368760177));
#17782=CARTESIAN_POINT('Ctrl Pts',(7.36722894552435,0.91824422816336,9.41309355377711));
#17783=CARTESIAN_POINT('Ctrl Pts',(7.39509927477985,0.842078905334526,9.40885341995246));
#17784=CARTESIAN_POINT('Ctrl Pts',(7.42717646113868,0.754416889142964,9.40397326365316));
#17785=CARTESIAN_POINT('Ctrl Pts',(7.45427036000665,0.664839421432015,9.39909310735387));
#17786=CARTESIAN_POINT('Ctrl Pts',(7.47618097156191,0.573881995598245,9.39421295105457));
#17787=CARTESIAN_POINT('Ctrl Pts',(7.49864678047041,0.480619781422444,9.38920913550214));
#17788=CARTESIAN_POINT('Ctrl Pts',(7.51566290806526,0.385906846858317,9.3842053199497));
#17789=CARTESIAN_POINT('Ctrl Pts',(7.52706584652707,0.290344144526261,9.37920150439727));
#17790=CARTESIAN_POINT('Ctrl Pts',(7.53846878498888,0.194781442194193,9.37419768884484));
#17791=CARTESIAN_POINT('Ctrl Pts',(7.54425833113838,0.0983691508998505,
9.36919387329241));
#17792=CARTESIAN_POINT('Ctrl Pts',(7.54432654498802,0.00172970778312925,
9.36419005773998));
#17793=CARTESIAN_POINT('',(7.54193256524886,-0.00182552700443595,8.56419002737812));
#17794=CARTESIAN_POINT('Ctrl Pts',(7.54171142860237,0.00172727612123974,
9.36419002737812));
#17795=CARTESIAN_POINT('Ctrl Pts',(7.538260521488,-0.526658746908139,9.33680206706682));
#17796=CARTESIAN_POINT('Ctrl Pts',(7.11114849623935,-1.87574082982533,9.26713834891945));
#17797=CARTESIAN_POINT('Ctrl Pts',(4.88956789508618,-2.88771068875909,9.15519887293596));
#17798=CARTESIAN_POINT('Ctrl Pts',(2.55897584314901,-1.39825737663462,9.02837159942777));
#17799=CARTESIAN_POINT('Ctrl Pts',(2.54229391302319,1.36757924066726,8.9015443259196));
#17800=CARTESIAN_POINT('Ctrl Pts',(4.85475001434308,2.88503673937529,8.77471705241131));
#17801=CARTESIAN_POINT('Ctrl Pts',(7.09859130083223,1.89543275086705,8.66226561956423));
#17802=CARTESIAN_POINT('Ctrl Pts',(7.53819517521869,0.536315141057368,8.59208994455313));
#17803=CARTESIAN_POINT('Ctrl Pts',(7.54193256524886,-0.00182552700443595,
8.56419002737812));
#17804=CARTESIAN_POINT('',(7.54820287115862,-0.000480549575520677,7.76419002737812));
#17805=CARTESIAN_POINT('Ctrl Pts',(7.54193256524886,-0.00182552700443595,
8.56419002737812));
#17806=CARTESIAN_POINT('Ctrl Pts',(7.54385831016147,-0.27911038232396,8.54981418671706));
#17807=CARTESIAN_POINT('Ctrl Pts',(7.37249801786638,-1.36951156998236,8.49316258821991));
#17808=CARTESIAN_POINT('Ctrl Pts',(5.77063350138978,-2.81469856946862,8.3942352318867));
#17809=CARTESIAN_POINT('Ctrl Pts',(3.09918932920222,-2.09809790261087,8.26740795837852));
#17810=CARTESIAN_POINT('Ctrl Pts',(2.24852755674676,0.533727515180221,8.14058068487021));
#17811=CARTESIAN_POINT('Ctrl Pts',(3.99516508500167,2.67834585552468,8.01375341136209));
#17812=CARTESIAN_POINT('Ctrl Pts',(6.71513911122288,2.38129549316238,7.88828985886462));
#17813=CARTESIAN_POINT('Ctrl Pts',(7.546090913882,0.783450873209182,7.80510206420335));
#17814=CARTESIAN_POINT('Ctrl Pts',(7.54820287115862,-0.000480549575520677,
7.76419002737812));
#17815=CARTESIAN_POINT('',(7.54432619069004,0.00217446611858361,6.96419002737812));
#17816=CARTESIAN_POINT('Ctrl Pts',(7.54820287115862,-0.000480549575520677,
7.76419002737812));
#17817=CARTESIAN_POINT('Ctrl Pts',(7.54827326903503,-0.026611337364743,
7.76282630636728));
#17818=CARTESIAN_POINT('Ctrl Pts',(7.53607095936906,-0.862736996768992,
7.71918682752067));
#17819=CARTESIAN_POINT('Ctrl Pts',(6.58857747519914,-2.47917654645346,7.63327159083716));
#17820=CARTESIAN_POINT('Ctrl Pts',(3.8254306157284,-2.60226153275734,7.50644431732927));
#17821=CARTESIAN_POINT('Ctrl Pts',(2.22012507713375,-0.349901746089773,
7.37961704382094));
#17822=CARTESIAN_POINT('Ctrl Pts',(3.23804571895806,2.22186186042716,7.25278977031274));
#17823=CARTESIAN_POINT('Ctrl Pts',(5.94999528816588,2.76542419809011,7.12596249680452));
#17824=CARTESIAN_POINT('Ctrl Pts',(7.41422767974903,1.26294973299729,7.02976274506699));
#17825=CARTESIAN_POINT('Ctrl Pts',(7.54523659556225,0.226539321624495,6.97583875116552));
#17826=CARTESIAN_POINT('Ctrl Pts',(7.54330299861202,0.00218295211155193,
6.96419051510012));
#17827=CARTESIAN_POINT('',(7.54432692296551,-0.00106743696241274,6.16419002733055));
#17828=CARTESIAN_POINT('Ctrl Pts',(7.54432619069003,0.00217446611858361,
6.96419002737812));
#17829=CARTESIAN_POINT('Ctrl Pts',(7.54439769743544,-0.0784095490258181,
6.9600079418362));
#17830=CARTESIAN_POINT('Ctrl Pts',(7.54048996103695,-0.159079511651253,
6.95582585629429));
#17831=CARTESIAN_POINT('Ctrl Pts',(7.53260427432529,-0.239408467823362,
6.95164377075237));
#17832=CARTESIAN_POINT('Ctrl Pts',(7.52472246292544,-0.319697947439344,
6.94746374043864));
#17833=CARTESIAN_POINT('Ctrl Pts',(7.51286662670644,-0.399646282378628,
6.9432837101249));
#17834=CARTESIAN_POINT('Ctrl Pts',(7.49709007549609,-0.478829392525642,
6.93910367981117));
#17835=CARTESIAN_POINT('Ctrl Pts',(7.48131623537896,-0.557998895592756,
6.93492436780727));
#17836=CARTESIAN_POINT('Ctrl Pts',(7.46162311120077,-0.63640297047287,6.93074505580337));
#17837=CARTESIAN_POINT('Ctrl Pts',(7.43811525099532,-0.713627056030715,
6.92656574379946));
#17838=CARTESIAN_POINT('Ctrl Pts',(7.41460391741899,-0.790862551724909,
6.92238581428718));
#17839=CARTESIAN_POINT('Ctrl Pts',(7.38727686924611,-0.866917259459429,
6.91820588477491));
#17840=CARTESIAN_POINT('Ctrl Pts',(7.35628824494099,-0.94139262189232,6.91402595526263));
#17841=CARTESIAN_POINT('Ctrl Pts',(7.32526596372123,-1.01594887242441,6.909841485906));
#17842=CARTESIAN_POINT('Ctrl Pts',(7.29057435498374,-1.08892191757205,6.90565701654937));
#17843=CARTESIAN_POINT('Ctrl Pts',(7.25241504782298,-1.15993472269529,6.90147254719275));
#17844=CARTESIAN_POINT('Ctrl Pts',(7.214231326336,-1.23099296181404,6.89728540061246));
#17845=CARTESIAN_POINT('Ctrl Pts',(7.17257573845094,-1.30008806150181,6.89309825403218));
#17846=CARTESIAN_POINT('Ctrl Pts',(7.12769372870001,-1.36687124932412,6.8889111074519));
#17847=CARTESIAN_POINT('Ctrl Pts',(7.08273896064388,-1.43376269949007,6.8847171730809));
#17848=CARTESIAN_POINT('Ctrl Pts',(7.03454762087581,-1.49833438387594,6.88052323870991));
#17849=CARTESIAN_POINT('Ctrl Pts',(6.98340547657638,-1.56027049524785,6.87632930433892));
#17850=CARTESIAN_POINT('Ctrl Pts',(6.96705959253493,-1.580066311562,6.87498885282198));
#17851=CARTESIAN_POINT('Ctrl Pts',(6.95041254789922,-1.59959317725488,6.87364840130504));
#17852=CARTESIAN_POINT('Ctrl Pts',(6.93347442743153,-1.61884161198753,6.8723079497881));
#17853=CARTESIAN_POINT('Ctrl Pts',(6.87999718967411,-1.67961300174232,6.86807586012913));
#17854=CARTESIAN_POINT('Ctrl Pts',(6.82340565434217,-1.73784503569689,6.86384377047017));
#17855=CARTESIAN_POINT('Ctrl Pts',(6.7639703595767,-1.79320158591269,6.8596116808112));
#17856=CARTESIAN_POINT('Ctrl Pts',(6.70462001204295,-1.8484790183969,6.85538563981915));
#17857=CARTESIAN_POINT('Ctrl Pts',(6.64243431464168,-1.90088881549508,6.8511595988271));
#17858=CARTESIAN_POINT('Ctrl Pts',(6.57772292224269,-1.95012912477712,6.84693355783504));
#17859=CARTESIAN_POINT('Ctrl Pts',(6.51299373046219,-1.9993829779966,6.84270635443691));
#17860=CARTESIAN_POINT('Ctrl Pts',(6.4457377819112,-2.04546526724344,6.83847915103878));
#17861=CARTESIAN_POINT('Ctrl Pts',(6.37630071801608,-2.08811202078027,6.83425194764065));
#17862=CARTESIAN_POINT('Ctrl Pts',(6.30700696413248,-2.13067075638548,6.83003346869793));
#17863=CARTESIAN_POINT('Ctrl Pts',(6.23554147196011,-2.16980785869417,6.82581498975521));
#17864=CARTESIAN_POINT('Ctrl Pts',(6.16227797187641,-2.20530340381644,6.82159651081248));
#17865=CARTESIAN_POINT('Ctrl Pts',(6.08903849658266,-2.24078730913151,6.81737941520622));
#17866=CARTESIAN_POINT('Ctrl Pts',(6.01400260215468,-2.2726318262804,6.81316231959995));
#17867=CARTESIAN_POINT('Ctrl Pts',(5.93756795157072,-2.30066332151552,6.80894522399368));
#17868=CARTESIAN_POINT('Ctrl Pts',(5.86113497830319,-2.32869420161487,6.80472822092926));
#17869=CARTESIAN_POINT('Ctrl Pts',(5.78330374658018,-2.35291206724811,6.80051121786484));
#17870=CARTESIAN_POINT('Ctrl Pts',(5.70448984443593,-2.37319222362713,6.79629421480041));
#17871=CARTESIAN_POINT('Ctrl Pts',(5.62534965112445,-2.39355634026844,6.79205975325704));
#17872=CARTESIAN_POINT('Ctrl Pts',(5.5452190872179,-2.40994994376381,6.78782529171366));
#17873=CARTESIAN_POINT('Ctrl Pts',(5.46453034046881,-2.42229837109701,6.78359083017028));
#17874=CARTESIAN_POINT('Ctrl Pts',(5.38405776682911,-2.43461371577568,6.77936771316695));
#17875=CARTESIAN_POINT('Ctrl Pts',(5.30303046671893,-2.44290552482377,6.77514459616361));
#17876=CARTESIAN_POINT('Ctrl Pts',(5.22188154726461,-2.44715187978552,6.77092147916028));
#17877=CARTESIAN_POINT('Ctrl Pts',(5.14040564284918,-2.45141534519336,6.76668134534688));
#17878=CARTESIAN_POINT('Ctrl Pts',(5.05880760837002,-2.45160069338739,6.76244121153348));
#17879=CARTESIAN_POINT('Ctrl Pts',(4.97752315877344,-2.4477384726225,6.75820107772008));
#17880=CARTESIAN_POINT('Ctrl Pts',(4.89623870917688,-2.44387625185761,6.75396094390668));
#17881=CARTESIAN_POINT('Ctrl Pts',(4.8152683035326,-2.43596656948219,6.74972081009328));
#17882=CARTESIAN_POINT('Ctrl Pts',(4.73503801466492,-2.4240917066919,6.74548067627989));
#17883=CARTESIAN_POINT('Ctrl Pts',(4.65495993439775,-2.41223937225435,6.74124858662092));
#17884=CARTESIAN_POINT('Ctrl Pts',(4.57532040791192,-2.39639268582382,6.73701649696195));
#17885=CARTESIAN_POINT('Ctrl Pts',(4.49654862582741,-2.37659601279817,6.73278440730299));
#17886=CARTESIAN_POINT('Ctrl Pts',(4.41788942743332,-2.3568276339465,6.72855836631093));
#17887=CARTESIAN_POINT('Ctrl Pts',(4.34009595714923,-2.33312059334013,6.72433232531888));
#17888=CARTESIAN_POINT('Ctrl Pts',(4.26358989930911,-2.30557072077837,6.72010628432683));
#17889=CARTESIAN_POINT('Ctrl Pts',(4.18706279787122,-2.27801327040573,6.71587908092869));
#17890=CARTESIAN_POINT('Ctrl Pts',(4.11182427435442,-2.24661096831282,6.71165187753056));
#17891=CARTESIAN_POINT('Ctrl Pts',(4.03828377926908,-2.21151044107732,6.70742467413243));
#17892=CARTESIAN_POINT('Ctrl Pts',(3.96489506319927,-2.17648235724137,6.70320619518971));
#17893=CARTESIAN_POINT('Ctrl Pts',(3.89319780366043,-2.13777147604273,6.69898771624699));
#17894=CARTESIAN_POINT('Ctrl Pts',(3.82357974790947,-2.09557194427408,6.69476923730427));
#17895=CARTESIAN_POINT('Ctrl Pts',(3.75398452152329,-2.05338625070436,6.690552141698));
#17896=CARTESIAN_POINT('Ctrl Pts',(3.68646754197144,-2.00771441915321,6.68633504609174));
#17897=CARTESIAN_POINT('Ctrl Pts',(3.62139071185994,-1.95879584683516,6.68211795048548));
#17898=CARTESIAN_POINT('Ctrl Pts',(3.5563153098237,-1.9098783480083,6.67790094742106));
#17899=CARTESIAN_POINT('Ctrl Pts',(3.49368032151697,-1.85771453021127,6.67368394435664));
#17900=CARTESIAN_POINT('Ctrl Pts',(3.43381631600644,-1.8025854384521,6.66946694129222));
#17901=CARTESIAN_POINT('Ctrl Pts',(3.37370447228837,-1.74722811112519,6.66523247974884));
#17902=CARTESIAN_POINT('Ctrl Pts',(3.31638695987383,-1.68888121507957,6.66099801820546));
#17903=CARTESIAN_POINT('Ctrl Pts',(3.26216137660258,-1.62786692471709,6.65676355666208));
#17904=CARTESIAN_POINT('Ctrl Pts',(3.20808106901624,-1.56701609765528,6.65254043965875));
#17905=CARTESIAN_POINT('Ctrl Pts',(3.1570764052606,-1.50351254078169,6.64831732265541));
#17906=CARTESIAN_POINT('Ctrl Pts',(3.10940121141798,-1.43770787110605,6.64409420565208));
#17907=CARTESIAN_POINT('Ctrl Pts',(3.06153391308996,-1.37163804525199,6.63985407183868));
#17908=CARTESIAN_POINT('Ctrl Pts',(3.01702322307941,-1.30324892287414,6.63561393802528));
#17909=CARTESIAN_POINT('Ctrl Pts',(2.97608034673313,-1.23292282976524,6.63137380421188));
#17910=CARTESIAN_POINT('Ctrl Pts',(2.93513747038684,-1.16259673665634,6.62713367039847));
#17911=CARTESIAN_POINT('Ctrl Pts',(2.89776256714265,-1.09033411649224,6.62289353658507));
#17912=CARTESIAN_POINT('Ctrl Pts',(2.86411817867461,-1.01653732291213,6.61865340277167));
#17913=CARTESIAN_POINT('Ctrl Pts',(2.83053761853579,-0.942880532650582,
6.61442131311271));
#17914=CARTESIAN_POINT('Ctrl Pts',(2.80054813471462,-0.867420592882331,
6.61018922345375));
#17915=CARTESIAN_POINT('Ctrl Pts',(2.77434578854561,-0.790541863893945,
6.60595713379479));
#17916=CARTESIAN_POINT('Ctrl Pts',(2.74818089178745,-0.713773012971022,
6.60173109280275));
#17917=CARTESIAN_POINT('Ctrl Pts',(2.72579253108134,-0.63558983640461,6.59750505181071));
#17918=CARTESIAN_POINT('Ctrl Pts',(2.7073294904886,-0.556398369083661,6.59327901081866));
#17919=CARTESIAN_POINT('Ctrl Pts',(2.68886137149012,-0.477185119521554,
6.58905180742053));
#17920=CARTESIAN_POINT('Ctrl Pts',(2.67432090143951,-0.396963459550963,
6.5848246040224));
#17921=CARTESIAN_POINT('Ctrl Pts',(2.66380757770076,-0.316156767664846,
6.58059740062426));
#17922=CARTESIAN_POINT('Ctrl Pts',(2.65331595223757,-0.235516851378036,
6.57637892168154));
#17923=CARTESIAN_POINT('Ctrl Pts',(2.6468349513143,-0.154294773248997,6.57216044273881));
#17924=CARTESIAN_POINT('Ctrl Pts',(2.64441238840444,-0.0729215260666718,
6.56794196379609));
#17925=CARTESIAN_POINT('Ctrl Pts',(2.64199061990878,0.00842503695261541,
6.56372486818982));
#17926=CARTESIAN_POINT('Ctrl Pts',(2.64362466028642,0.0899222064561095,
6.55950777258356));
#17927=CARTESIAN_POINT('Ctrl Pts',(2.64931029310316,0.1711360852852,6.55529067697729));
#17928=CARTESIAN_POINT('Ctrl Pts',(2.6549958011518,0.252348181920348,6.55107367391288));
#17929=CARTESIAN_POINT('Ctrl Pts',(2.66473269126401,0.333276536767597,6.54685667084846));
#17930=CARTESIAN_POINT('Ctrl Pts',(2.67846475733505,0.413490913754334,6.54263966778404));
#17931=CARTESIAN_POINT('Ctrl Pts',(2.69225367444059,0.494037379902969,6.53840520624066));
#17932=CARTESIAN_POINT('Ctrl Pts',(2.71007085127474,0.573863476620917,6.53417074469728));
#17933=CARTESIAN_POINT('Ctrl Pts',(2.73180763696923,0.652544285318017,6.5299362831539));
#17934=CARTESIAN_POINT('Ctrl Pts',(2.7534861876713,0.731014300369605,6.52571316615056));
#17935=CARTESIAN_POINT('Ctrl Pts',(2.77906318609842,0.80834472524806,6.52149004914723));
#17936=CARTESIAN_POINT('Ctrl Pts',(2.80838147504338,0.88413137705688,6.5172669321439));
#17937=CARTESIAN_POINT('Ctrl Pts',(2.83781790036826,0.960223406874211,6.51302679833049));
#17938=CARTESIAN_POINT('Ctrl Pts',(2.87102563075637,1.03475876913479,6.50878666451708));
#17939=CARTESIAN_POINT('Ctrl Pts',(2.90779856556206,1.10735236224923,6.50454653070368));
#17940=CARTESIAN_POINT('Ctrl Pts',(2.94457150036774,1.17994595536366,6.50030639689027));
#17941=CARTESIAN_POINT('Ctrl Pts',(2.98490935385593,1.25059740433307,6.49606626307686));
#17942=CARTESIAN_POINT('Ctrl Pts',(3.02856276223631,1.31895156700724,6.49182612926345));
#17943=CARTESIAN_POINT('Ctrl Pts',(3.07213335371169,1.38717605183019,6.48759403960449));
#17944=CARTESIAN_POINT('Ctrl Pts',(3.11916947096469,1.45336649920331,6.48336194994553));
#17945=CARTESIAN_POINT('Ctrl Pts',(3.16945507369038,1.51714941285694,6.47912986028657));
#17946=CARTESIAN_POINT('Ctrl Pts',(3.21966880627954,1.58084116549303,6.47490381929453));
#17947=CARTESIAN_POINT('Ctrl Pts',(3.27312251498226,1.64213185662184,6.47067777830248));
#17948=CARTESIAN_POINT('Ctrl Pts',(3.32955626775308,1.70067589058414,6.46645173731044));
#17949=CARTESIAN_POINT('Ctrl Pts',(3.38600554307516,1.75923602754727,6.46222453391231));
#17950=CARTESIAN_POINT('Ctrl Pts',(3.44543622880718,1.81504761766214,6.45799733051417));
#17951=CARTESIAN_POINT('Ctrl Pts',(3.50754704413236,1.86779700675106,6.45377012711604));
#17952=CARTESIAN_POINT('Ctrl Pts',(3.56952966996961,1.92043752724536,6.44955164817332));
#17953=CARTESIAN_POINT('Ctrl Pts',(3.6341810354678,1.97002815426071,6.4453331692306));
#17954=CARTESIAN_POINT('Ctrl Pts',(3.70116537433277,2.01629447586574,6.44111469028788));
#17955=CARTESIAN_POINT('Ctrl Pts',(3.76812774748944,2.06254562567776,6.43689759468161));
#17956=CARTESIAN_POINT('Ctrl Pts',(3.83742119266684,2.10547437106466,6.43268049907535));
#17957=CARTESIAN_POINT('Ctrl Pts',(3.90867922331442,2.1448483929983,6.42846340346908));
#17958=CARTESIAN_POINT('Ctrl Pts',(3.97993569024362,2.18422155089064,6.42424640040467));
#17959=CARTESIAN_POINT('Ctrl Pts',(4.05315624964168,2.22003991669329,6.42002939734025));
#17960=CARTESIAN_POINT('Ctrl Pts',(4.12794922733439,2.25211679936301,6.41581239427583));
#17961=CARTESIAN_POINT('Ctrl Pts',(4.203051849485,2.28432648098327,6.41157793273245));
#17962=CARTESIAN_POINT('Ctrl Pts',(4.27973950882041,2.31276343604563,6.40734347118907));
#17963=CARTESIAN_POINT('Ctrl Pts',(4.35759648647074,2.33728788386236,6.40310900964568));
#17964=CARTESIAN_POINT('Ctrl Pts',(4.43524487760014,2.36174662826492,6.39888589264235));
#17965=CARTESIAN_POINT('Ctrl Pts',(4.51405586678756,2.38231372440704,6.39466277563902));
#17966=CARTESIAN_POINT('Ctrl Pts',(4.5936047727012,2.3989013772546,6.39043965863569));
#17967=CARTESIAN_POINT('Ctrl Pts',(4.67347421641258,2.41555586910707,6.38619952482228));
#17968=CARTESIAN_POINT('Ctrl Pts',(4.75408706910091,2.42819871555458,6.38195939100887));
#17969=CARTESIAN_POINT('Ctrl Pts',(4.83500806075281,2.43679357480656,6.37771925719546));
#17970=CARTESIAN_POINT('Ctrl Pts',(4.91592905240472,2.44538843405854,6.37347912338205));
#17971=CARTESIAN_POINT('Ctrl Pts',(4.99715771294223,2.44993534210655,6.36923898956864));
#17972=CARTESIAN_POINT('Ctrl Pts',(5.07826040200378,2.45045055575236,6.36499885575523));
#17973=CARTESIAN_POINT('Ctrl Pts',(5.15920922739352,2.45096479196247,6.36076676609628));
#17974=CARTESIAN_POINT('Ctrl Pts',(5.24033456232364,2.44746455166315,6.35653467643732));
#17975=CARTESIAN_POINT('Ctrl Pts',(5.32120547477914,2.43992814441337,6.35230258677837));
#17976=CARTESIAN_POINT('Ctrl Pts',(5.40196080338581,2.43240250848952,6.34807654578631));
#17977=CARTESIAN_POINT('Ctrl Pts',(5.4824619729098,2.42085220553111,6.34385050479426));
#17978=CARTESIAN_POINT('Ctrl Pts',(5.56227761120317,2.40530755216616,6.3396244638022));
#17979=CARTESIAN_POINT('Ctrl Pts',(5.64211520342061,2.38975862312107,6.33539726040407));
#17980=CARTESIAN_POINT('Ctrl Pts',(5.72126642100705,2.37021316962647,6.33117005700593));
#17981=CARTESIAN_POINT('Ctrl Pts',(5.79930422572376,2.34675357746022,6.3269428536078));
#17982=CARTESIAN_POINT('Ctrl Pts',(5.87718096950162,2.32334240315956,6.32272437466508));
#17983=CARTESIAN_POINT('Ctrl Pts',(5.95394843948702,2.29603334055059,6.31850589572237));
#17984=CARTESIAN_POINT('Ctrl Pts',(6.0291937900519,2.26495905236261,6.31428741677965));
#17985=CARTESIAN_POINT('Ctrl Pts',(6.10441446593234,2.23389495414982,6.31007032117339));
#17986=CARTESIAN_POINT('Ctrl Pts',(6.1781135844623,2.19906825960485,6.30585322556713));
#17987=CARTESIAN_POINT('Ctrl Pts',(6.24989693204442,2.16066029760629,6.30163612996087));
#17988=CARTESIAN_POINT('Ctrl Pts',(6.32167870438045,2.12225317844935,6.29741912689646));
#17989=CARTESIAN_POINT('Ctrl Pts',(6.39154438017218,2.08026516833344,6.29320212383205));
#17990=CARTESIAN_POINT('Ctrl Pts',(6.45912435248052,2.03492354003513,6.28898512076764));
#17991=CARTESIAN_POINT('Ctrl Pts',(6.52698410725699,1.98939419646791,6.28475065922425));
#17992=CARTESIAN_POINT('Ctrl Pts',(6.59253879355058,1.94048365964281,6.28051619768086));
#17993=CARTESIAN_POINT('Ctrl Pts',(6.65544510872075,1.88846488398174,6.27628173613747));
#17994=CARTESIAN_POINT('Ctrl Pts',(6.71818289166911,1.83658547175047,6.27205861913414));
#17995=CARTESIAN_POINT('Ctrl Pts',(6.77828615862546,1.78161479991907,6.26783550213081));
#17996=CARTESIAN_POINT('Ctrl Pts',(6.83545036964551,1.72386160401179,6.26361238512748));
#17997=CARTESIAN_POINT('Ctrl Pts',(6.8928449206068,1.66587569488215,6.25937225131407));
#17998=CARTESIAN_POINT('Ctrl Pts',(6.9472763720494,1.60508514727229,6.25513211750066));
#17999=CARTESIAN_POINT('Ctrl Pts',(6.99847761586162,1.54183555337969,6.25089198368725));
#18000=CARTESIAN_POINT('Ctrl Pts',(7.04967885967384,1.47858595948709,6.24665184987383));
#18001=CARTESIAN_POINT('Ctrl Pts',(7.09764967054014,1.41287773343925,6.24241171606042));
#18002=CARTESIAN_POINT('Ctrl Pts',(7.14216797518798,1.34508369115378,6.23817158224701));
#18003=CARTESIAN_POINT('Ctrl Pts',(7.18746672627465,1.27610115754336,6.23385711502488));
#18004=CARTESIAN_POINT('Ctrl Pts',(7.22935510164734,1.20470926392168,6.22954264780275));
#18005=CARTESIAN_POINT('Ctrl Pts',(7.26757389031831,1.13127157776675,6.22522818058062));
#18006=CARTESIAN_POINT('Ctrl Pts',(7.30573175456386,1.05795095834756,6.22092059103425));
#18007=CARTESIAN_POINT('Ctrl Pts',(7.34023145647764,0.982591415569505,6.21661300148789));
#18008=CARTESIAN_POINT('Ctrl Pts',(7.37085724304496,0.905585020967907,6.21230541194152));
#18009=CARTESIAN_POINT('Ctrl Pts',(7.40143315944292,0.828704021413127,6.2080048367528));
#18010=CARTESIAN_POINT('Ctrl Pts',(7.42814755207734,0.750181913787023,6.20370426156408));
#18011=CARTESIAN_POINT('Ctrl Pts',(7.45083143436958,0.670433500930149,6.19940368637536));
#18012=CARTESIAN_POINT('Ctrl Pts',(7.47349353380069,0.590761668818158,6.19510724093969));
#18013=CARTESIAN_POINT('Ctrl Pts',(7.49213269474097,0.509866293854989,6.19081079550403));
#18014=CARTESIAN_POINT('Ctrl Pts',(7.50662893554642,0.42817965852963,6.18651435006836));
#18015=CARTESIAN_POINT('Ctrl Pts',(7.52111435624942,0.346553994719236,6.18222111153167));
#18016=CARTESIAN_POINT('Ctrl Pts',(7.53146292938353,0.264138678008879,6.17792787299498));
#18017=CARTESIAN_POINT('Ctrl Pts',(7.53760547669647,0.181377414859107,6.17363463445829));
#18018=CARTESIAN_POINT('Ctrl Pts',(7.54210976449276,0.120689148474039,6.17048643209823));
#18019=CARTESIAN_POINT('Ctrl Pts',(7.54435344337769,0.0598151464488679,
6.16733822973817));
#18020=CARTESIAN_POINT('Ctrl Pts',(7.54432692296591,-0.0010674360424196,
6.16419002737812));
#18021=CARTESIAN_POINT('',(7.54432671099194,-0.00147590784951504,5.36419002740651));
#18022=CARTESIAN_POINT('Ctrl Pts',(7.54432692296551,-0.00106743696241388,
6.16419002733055));
#18023=CARTESIAN_POINT('Ctrl Pts',(7.54428806046215,-0.0902835300895011,
6.15957671588008));
#18024=CARTESIAN_POINT('Ctrl Pts',(7.53937283421591,-0.179342371974235,
6.15496340442961));
#18025=CARTESIAN_POINT('Ctrl Pts',(7.529657579374,-0.267731947853424,6.15035009297914));
#18026=CARTESIAN_POINT('Ctrl Pts',(7.51991365953643,-0.356382318415845,
6.14572316988854));
#18027=CARTESIAN_POINT('Ctrl Pts',(7.50534147059154,-0.444359170624297,
6.14109624679794));
#18028=CARTESIAN_POINT('Ctrl Pts',(7.48606828497605,-0.531161583907186,
6.13646932370734));
#18029=CARTESIAN_POINT('Ctrl Pts',(7.46670910596212,-0.618351293543685,
6.13182175613954));
#18030=CARTESIAN_POINT('Ctrl Pts',(7.44260702225196,-0.70435577060529,6.12717418857175));
#18031=CARTESIAN_POINT('Ctrl Pts',(7.41393969617488,-0.78868754800971,6.12252662100395));
#18032=CARTESIAN_POINT('Ctrl Pts',(7.39094795642252,-0.856323234495553,
6.11879918358224));
#18033=CARTESIAN_POINT('Ctrl Pts',(7.36502066814126,-0.922883320604722,
6.11507174616052));
#18034=CARTESIAN_POINT('Ctrl Pts',(7.33627098328143,-0.988127486225679,
6.1113443087388));
#18035=CARTESIAN_POINT('Ctrl Pts',(7.30362892112772,-1.06220496289194,6.10711221907984));
#18036=CARTESIAN_POINT('Ctrl Pts',(7.26725138371582,-1.13480142576412,6.10288012942087));
#18037=CARTESIAN_POINT('Ctrl Pts',(7.22729484661249,-1.20551477003771,6.09864803976191));
#18038=CARTESIAN_POINT('Ctrl Pts',(7.18739541694389,-1.27612704805317,6.09442199876986));
#18039=CARTESIAN_POINT('Ctrl Pts',(7.14392737370826,-1.34486115174563,6.09019595777781));
#18040=CARTESIAN_POINT('Ctrl Pts',(7.09709482980952,-1.41133584765593,6.08596991678576));
#18041=CARTESIAN_POINT('Ctrl Pts',(7.05024940424823,-1.47782882795843,6.08174271338763));
#18042=CARTESIAN_POINT('Ctrl Pts',(7.0000378391584,-1.54206074159141,6.0775155099895));
#18043=CARTESIAN_POINT('Ctrl Pts',(6.94670998865645,-1.60367560822642,6.07328830659137));
#18044=CARTESIAN_POINT('Ctrl Pts',(6.89349220062604,-1.66516330895391,6.06906982764864));
#18045=CARTESIAN_POINT('Ctrl Pts',(6.83717126285874,-1.7240443867088,6.06485134870591));
#18046=CARTESIAN_POINT('Ctrl Pts',(6.77803710266931,-1.77999637743957,6.06063286976319));
#18047=CARTESIAN_POINT('Ctrl Pts',(6.71892233393374,-1.83593002022319,6.05641577415692));
#18048=CARTESIAN_POINT('Ctrl Pts',(6.65699651209779,-1.88893616434808,6.05219867855066));
#18049=CARTESIAN_POINT('Ctrl Pts',(6.59258635189059,-1.93872925420082,6.0479815829444));
#18050=CARTESIAN_POINT('Ctrl Pts',(6.52817760512899,-1.98852125137154,6.04376457987998));
#18051=CARTESIAN_POINT('Ctrl Pts',(6.46128499673565,-2.03510005115936,6.03954757681556));
#18052=CARTESIAN_POINT('Ctrl Pts',(6.39226710089295,-2.07822134482499,6.03533057375114));
#18053=CARTESIAN_POINT('Ctrl Pts',(6.32296346954942,-2.12152116152861,6.03109611220776));
#18054=CARTESIAN_POINT('Ctrl Pts',(6.25151730910728,-2.16133452191967,6.02686165066438));
#18055=CARTESIAN_POINT('Ctrl Pts',(6.17831811948958,-2.19745980598582,6.022627189121));
#18056=CARTESIAN_POINT('Ctrl Pts',(6.10531503771918,-2.23348830685357,6.01840407211766));
#18057=CARTESIAN_POINT('Ctrl Pts',(6.0305687533014,-2.26584831961888,6.01418095511433));
#18058=CARTESIAN_POINT('Ctrl Pts',(5.95448556150817,-2.29438823177046,6.00995783811099));
#18059=CARTESIAN_POINT('Ctrl Pts',(5.87809579681561,-2.32304314387681,6.00571770429759));
#18060=CARTESIAN_POINT('Ctrl Pts',(5.80035877977824,-2.34784696952846,6.00147757048419));
#18061=CARTESIAN_POINT('Ctrl Pts',(5.72169912686958,-2.36869732923174,5.99723743667079));
#18062=CARTESIAN_POINT('Ctrl Pts',(5.64303947396092,-2.38954768893503,5.99299730285739));
#18063=CARTESIAN_POINT('Ctrl Pts',(5.5634576552422,-2.40644454648054,5.98875716904398));
#18064=CARTESIAN_POINT('Ctrl Pts',(5.48338470822629,-2.41933775299716,5.98451703523058));
#18065=CARTESIAN_POINT('Ctrl Pts',(5.40346367131052,-2.43220649921395,5.98028494557161));
#18066=CARTESIAN_POINT('Ctrl Pts',(5.32275520129984,-2.44113479794551,5.97605285591265));
#18067=CARTESIAN_POINT('Ctrl Pts',(5.2416818647386,-2.44603541162881,5.97182076625369));
#18068=CARTESIAN_POINT('Ctrl Pts',(5.16072440133893,-2.45092902116469,5.96759472526164));
#18069=CARTESIAN_POINT('Ctrl Pts',(5.07940356707358,-2.4518063509304,5.9633686842696));
#18070=CARTESIAN_POINT('Ctrl Pts',(4.99815030471609,-2.44863149335155,5.95914264327755));
#18071=CARTESIAN_POINT('Ctrl Pts',(4.91687469300443,-2.44545576250295,5.95491543987942));
#18072=CARTESIAN_POINT('Ctrl Pts',(4.83566715474355,-2.4382255669776,5.95068823648129));
#18073=CARTESIAN_POINT('Ctrl Pts',(4.75496230035753,-2.4269571195184,5.94646103308316));
#18074=CARTESIAN_POINT('Ctrl Pts',(4.67442401139009,-2.41571192882215,5.94224255414043));
#18075=CARTESIAN_POINT('Ctrl Pts',(4.59438679711931,-2.40044517801083,5.93802407519771));
#18076=CARTESIAN_POINT('Ctrl Pts',(4.51527891886783,-2.38122493434452,5.93380559625499));
#18077=CARTESIAN_POINT('Ctrl Pts',(4.43619698191265,-2.36201099343903,5.92958850064872));
#18078=CARTESIAN_POINT('Ctrl Pts',(4.35804422697275,-2.33884624391854,5.92537140504246));
#18079=CARTESIAN_POINT('Ctrl Pts',(4.28123793294667,-2.31184969352819,5.92115430943619));
#18080=CARTESIAN_POINT('Ctrl Pts',(4.20443332439258,-2.28485373556233,5.91693730637178));
#18081=CARTESIAN_POINT('Ctrl Pts',(4.1289755560197,-2.25402629908897,5.91272030330736));
#18082=CARTESIAN_POINT('Ctrl Pts',(4.0552646040617,-2.21953555431026,5.90850330024295));
#18083=CARTESIAN_POINT('Ctrl Pts',(3.98124848725447,-2.18490201714249,5.90426883869957));
#18084=CARTESIAN_POINT('Ctrl Pts',(3.90899411417667,-2.14657496300716,5.90003437715618));
#18085=CARTESIAN_POINT('Ctrl Pts',(3.83888244061978,-2.10477172460861,5.8957999156128));
#18086=CARTESIAN_POINT('Ctrl Pts',(3.76895860315025,-2.06308048120806,5.89157679860947));
#18087=CARTESIAN_POINT('Ctrl Pts',(3.70116636520282,-2.0179319492883,5.88735368160613));
#18088=CARTESIAN_POINT('Ctrl Pts',(3.63585383805489,-1.96958474195827,5.8831305646028));
#18089=CARTESIAN_POINT('Ctrl Pts',(3.57027813778892,-1.92104272230268,5.87889043078939));
#18090=CARTESIAN_POINT('Ctrl Pts',(3.5072025331765,-1.86927650081016,5.87465029697599));
#18091=CARTESIAN_POINT('Ctrl Pts',(3.44694377047311,-1.81458683073498,5.87041016316258));
#18092=CARTESIAN_POINT('Ctrl Pts',(3.38668500776971,-1.75989716065979,5.86617002934918));
#18093=CARTESIAN_POINT('Ctrl Pts',(3.32924337288418,-1.70228441686835,5.86192989553577));
#18094=CARTESIAN_POINT('Ctrl Pts',(3.27489526229108,-1.64208313371705,5.85768976172237));
#18095=CARTESIAN_POINT('Ctrl Pts',(3.22065025801835,-1.58199606121114,5.8534576720634));
#18096=CARTESIAN_POINT('Ctrl Pts',(3.16928466213752,-1.5191061000925,5.84922558240444));
#18097=CARTESIAN_POINT('Ctrl Pts',(3.12110139711799,-1.45372051385441,5.84499349274548));
#18098=CARTESIAN_POINT('Ctrl Pts',(3.07298699749229,-1.38842837923577,5.84076745175344));
#18099=CARTESIAN_POINT('Ctrl Pts',(3.02804616865437,-1.3206480746002,5.83654141076139));
#18100=CARTESIAN_POINT('Ctrl Pts',(2.98654330204953,-1.25072179607799,5.83231536976935));
#18101=CARTESIAN_POINT('Ctrl Pts',(2.94502901975211,-1.18077628377836,5.82808816637121));
#18102=CARTESIAN_POINT('Ctrl Pts',(2.90695488381134,-1.10868398065182,5.82386096297308));
#18103=CARTESIAN_POINT('Ctrl Pts',(2.8725435317881,-1.03481849289507,5.81963375957495));
#18104=CARTESIAN_POINT('Ctrl Pts',(2.83820320078704,-0.961105454900868,
5.81541528063222));
#18105=CARTESIAN_POINT('Ctrl Pts',(2.80751076859188,-0.885626954952176,
5.8111968016895));
#18106=CARTESIAN_POINT('Ctrl Pts',(2.78064189706718,-0.808779457198316,
5.80697832274678));
#18107=CARTESIAN_POINT('Ctrl Pts',(2.75378183646463,-0.731957159509913,
5.80276122714051));
#18108=CARTESIAN_POINT('Ctrl Pts',(2.73074299978356,-0.653767193853057,
5.79854413153425));
#18109=CARTESIAN_POINT('Ctrl Pts',(2.71165232180659,-0.574624496468061,
5.79432703592799));
#18110=CARTESIAN_POINT('Ctrl Pts',(2.69256206276406,-0.49548353582608,5.79011003286357));
#18111=CARTESIAN_POINT('Ctrl Pts',(2.67741989801101,-0.415390337026624,
5.78589302979915));
#18112=CARTESIAN_POINT('Ctrl Pts',(2.66630209208741,-0.334772036961481,
5.78167602673474));
#18113=CARTESIAN_POINT('Ctrl Pts',(2.65513825821981,-0.253819975484631,
5.77744156519135));
#18114=CARTESIAN_POINT('Ctrl Pts',(2.64803225323112,-0.172338921240949,
5.77320710364797));
#18115=CARTESIAN_POINT('Ctrl Pts',(2.6450087376301,-0.0907667699700236,
5.76897264210459));
#18116=CARTESIAN_POINT('Ctrl Pts',(2.64199332232552,-0.00941315853644546,
5.76474952510125));
#18117=CARTESIAN_POINT('Ctrl Pts',(2.64303850239018,0.0720305954233322,
5.76052640809792));
#18118=CARTESIAN_POINT('Ctrl Pts',(2.64811643569602,0.153131725208303,5.75630329109459));
#18119=CARTESIAN_POINT('Ctrl Pts',(2.65321483024567,0.23455964738884,5.75206315728118));
#18120=CARTESIAN_POINT('Ctrl Pts',(2.66237848463236,0.31564171089935,5.74782302346777));
#18121=CARTESIAN_POINT('Ctrl Pts',(2.67552713668527,0.395948568917041,5.74358288965437));
#18122=CARTESIAN_POINT('Ctrl Pts',(2.68867578873818,0.476255426934721,5.73934275584096));
#18123=CARTESIAN_POINT('Ctrl Pts',(2.70580927922513,0.555786635709889,5.73510262202755));
#18124=CARTESIAN_POINT('Ctrl Pts',(2.72679705821167,0.634128353531991,5.73086248821415));
#18125=CARTESIAN_POINT('Ctrl Pts',(2.74774502030964,0.712321445649041,5.72663039855518));
#18126=CARTESIAN_POINT('Ctrl Pts',(2.77261079716259,0.789621282590665,5.72239830889622));
#18127=CARTESIAN_POINT('Ctrl Pts',(2.80130114784229,0.865606581784123,5.71816621923726));
#18128=CARTESIAN_POINT('Ctrl Pts',(2.82995049315846,0.941483279836682,5.71394017824521));
#18129=CARTESIAN_POINT('Ctrl Pts',(2.86241339300269,1.01604874051948,5.70971413725316));
#18130=CARTESIAN_POINT('Ctrl Pts',(2.89854634077541,1.08889503383384,5.70548809626112));
#18131=CARTESIAN_POINT('Ctrl Pts',(2.93468922720194,1.16176136409883,5.70126089286298));
#18132=CARTESIAN_POINT('Ctrl Pts',(2.97450403450886,1.23290713780914,5.69703368946485));
#18133=CARTESIAN_POINT('Ctrl Pts',(3.01779819523461,1.3019423974716,5.69280648606672));
#18134=CARTESIAN_POINT('Ctrl Pts',(3.06100300185573,1.37083517639966,5.688588007124));
#18135=CARTESIAN_POINT('Ctrl Pts',(3.10767258855504,1.4376257373037,5.68436952818128));
#18136=CARTESIAN_POINT('Ctrl Pts',(3.15756966680863,1.50195112692396,5.68015104923855));
#18137=CARTESIAN_POINT('Ctrl Pts',(3.20745038266037,1.56625542276659,5.67593395363229));
#18138=CARTESIAN_POINT('Ctrl Pts',(3.26055620364708,1.62809578581827,5.67171685802603));
#18139=CARTESIAN_POINT('Ctrl Pts',(3.31660784946632,1.68714012116002,5.66749976241976));
#18140=CARTESIAN_POINT('Ctrl Pts',(3.37265826526298,1.74618316080626,5.66328275935535));
#18141=CARTESIAN_POINT('Ctrl Pts',(3.43165405659566,1.80242995851394,5.65906575629093));
#18142=CARTESIAN_POINT('Ctrl Pts',(3.49327815909478,1.8555843177437,5.65484875322651));
#18143=CARTESIAN_POINT('Ctrl Pts',(3.55515738663906,1.90895873710819,5.65061429168313));
#18144=CARTESIAN_POINT('Ctrl Pts',(3.61968638538108,1.95921474002239,5.64637983013975));
#18145=CARTESIAN_POINT('Ctrl Pts',(3.68651100948259,2.00609359584509,5.64214536859637));
#18146=CARTESIAN_POINT('Ctrl Pts',(3.75315660382636,2.05284685859018,5.63792225159303));
#18147=CARTESIAN_POINT('Ctrl Pts',(3.82208512119672,2.0962408322911,5.6336991345897));
#18148=CARTESIAN_POINT('Ctrl Pts',(3.8929181814293,2.136063642804,5.62947601758637));
#18149=CARTESIAN_POINT('Ctrl Pts',(3.96403665945442,2.17604691706972,5.62523588377296));
#18150=CARTESIAN_POINT('Ctrl Pts',(4.03707463540399,2.21242998530243,5.62099574995956));
#18151=CARTESIAN_POINT('Ctrl Pts',(4.11162810508852,2.24504683146319,5.61675561614615));
#18152=CARTESIAN_POINT('Ctrl Pts',(4.18618157477304,2.27766367762394,5.61251548233275));
#18153=CARTESIAN_POINT('Ctrl Pts',(4.26225007917262,2.30651419415162,5.60827534851934));
#18154=CARTESIAN_POINT('Ctrl Pts',(4.33941529296307,2.33148300266897,5.60403521470594));
#18155=CARTESIAN_POINT('Ctrl Pts',(4.41643411304883,2.35640444170205,5.59980312504697));
#18156=CARTESIAN_POINT('Ctrl Pts',(4.49483282171879,2.37755187957483,5.59557103538801));
#18157=CARTESIAN_POINT('Ctrl Pts',(4.57420712856542,2.39477457762881,5.59133894572905));
#18158=CARTESIAN_POINT('Ctrl Pts',(4.65346799056978,2.41197266033379,5.587112904737));
#18159=CARTESIAN_POINT('Ctrl Pts',(4.73370123106812,2.42525704636648,5.58288686374496));
#18160=CARTESIAN_POINT('Ctrl Pts',(4.8144864437794,2.43452644610849,5.57866082275291));
#18161=CARTESIAN_POINT('Ctrl Pts',(4.89529387710407,2.44379839547241,5.57443361935478));
#18162=CARTESIAN_POINT('Ctrl Pts',(4.97665313471911,2.44905303133571,5.57020641595664));
#18163=CARTESIAN_POINT('Ctrl Pts',(5.05813222715243,2.45024001316067,5.56597921255851));
#18164=CARTESIAN_POINT('Ctrl Pts',(5.13944315623001,2.45142454519341,5.56176073361579));
#18165=CARTESIAN_POINT('Ctrl Pts',(5.22087296166409,2.44855816498041,5.55754225467306));
#18166=CARTESIAN_POINT('Ctrl Pts',(5.3019880106661,2.44164274789679,5.55332377573034));
#18167=CARTESIAN_POINT('Ctrl Pts',(5.38307646017424,2.4347295985378,5.54910668012408));
#18168=CARTESIAN_POINT('Ctrl Pts',(5.46384989557637,2.42377008858651,5.54488958451781));
#18169=CARTESIAN_POINT('Ctrl Pts',(5.54387775932507,2.40881811350597,5.54067248891155));
#18170=CARTESIAN_POINT('Ctrl Pts',(5.62390386690628,2.39386646653832,5.53645548584714));
#18171=CARTESIAN_POINT('Ctrl Pts',(5.70318397879088,2.37492261511099,5.53223848278272));
#18172=CARTESIAN_POINT('Ctrl Pts',(5.78129713029482,2.35209168267122,5.52802147971831));
#18173=CARTESIAN_POINT('Ctrl Pts',(5.85973367184419,2.32916622970402,5.52378701817492));
#18174=CARTESIAN_POINT('Ctrl Pts',(5.93699311348111,2.30232156197441,5.51955255663154));
#18175=CARTESIAN_POINT('Ctrl Pts',(6.01266578101133,2.27171429325571,5.51531809508815));
#18176=CARTESIAN_POINT('Ctrl Pts',(6.08813571400291,2.24118902442819,5.51109497808482));
#18177=CARTESIAN_POINT('Ctrl Pts',(6.16202695742016,2.20692152369236,5.50687186108149));
#18178=CARTESIAN_POINT('Ctrl Pts',(6.23395599308173,2.16911421635828,5.50264874407815));
#18179=CARTESIAN_POINT('Ctrl Pts',(6.30617486270662,2.13115456662692,5.49840861026474));
#18180=CARTESIAN_POINT('Ctrl Pts',(6.37641527654636,2.08962677053247,5.49416847645134));
#18181=CARTESIAN_POINT('Ctrl Pts',(6.44431827901129,2.04477968866833,5.48992834263793));
#18182=CARTESIAN_POINT('Ctrl Pts',(6.51222128147624,1.99993260680418,5.48568820882453));
#18183=CARTESIAN_POINT('Ctrl Pts',(6.57778653276982,1.95176656598373,5.48144807501112));
#18184=CARTESIAN_POINT('Ctrl Pts',(6.64068979568119,1.90056997299931,5.47720794119771));
#18185=CARTESIAN_POINT('Ctrl Pts',(6.70265595672198,1.85013608167508,5.47303097481226));
#18186=CARTESIAN_POINT('Ctrl Pts',(6.76228324590581,1.7965622350999,5.46885400842681));
#18187=CARTESIAN_POINT('Ctrl Pts',(6.81923004557808,1.74009629525162,5.46467704204135));
#18188=CARTESIAN_POINT('Ctrl Pts',(6.8763130790926,1.68349527192215,5.46049008309823));
#18189=CARTESIAN_POINT('Ctrl Pts',(6.93070236814598,1.62398855423778,5.45630312415511));
#18190=CARTESIAN_POINT('Ctrl Pts',(6.98208507709208,1.56186819910249,5.45211616521199));
#18191=CARTESIAN_POINT('Ctrl Pts',(7.03321278119249,1.50005613817553,5.44794998553181));
#18192=CARTESIAN_POINT('Ctrl Pts',(7.08136334922854,1.43565667276068,5.44378380585162));
#18193=CARTESIAN_POINT('Ctrl Pts',(7.12626494788757,1.36899483924671,5.43961762617143));
#18194=CARTESIAN_POINT('Ctrl Pts',(7.17113945057057,1.30237323297402,5.43545396058224));
#18195=CARTESIAN_POINT('Ctrl Pts',(7.21276860737512,1.23349236269166,5.43129029499304));
#18196=CARTESIAN_POINT('Ctrl Pts',(7.25092218098941,1.16270860528618,5.42712662940384));
#18197=CARTESIAN_POINT('Ctrl Pts',(7.28906513501681,1.0919445496856,5.42296412272073));
#18198=CARTESIAN_POINT('Ctrl Pts',(7.32373420028594,1.01927907926535,5.41880161603762));
#18199=CARTESIAN_POINT('Ctrl Pts',(7.35474445735139,0.945094283115184,5.41463910935451));
#18200=CARTESIAN_POINT('Ctrl Pts',(7.38606450716398,0.870168380183887,5.41043501919218));
#18201=CARTESIAN_POINT('Ctrl Pts',(7.41365201386476,0.793693069531089,5.40623092902985));
#18202=CARTESIAN_POINT('Ctrl Pts',(7.43736645441967,0.716082260776893,5.40202683886751));
#18203=CARTESIAN_POINT('Ctrl Pts',(7.46086810650679,0.639167849858436,5.39786047179217));
#18204=CARTESIAN_POINT('Ctrl Pts',(7.48056585136314,0.561138719230343,5.39369410471683));
#18205=CARTESIAN_POINT('Ctrl Pts',(7.4963737850575,0.482410553964754,5.38952773764149));
#18206=CARTESIAN_POINT('Ctrl Pts',(7.5123964108495,0.402613158825711,5.38530478593566));
#18207=CARTESIAN_POINT('Ctrl Pts',(7.52442268876795,0.322098098698098,5.38108183422983));
#18208=CARTESIAN_POINT('Ctrl Pts',(7.53241743836409,0.241304127797563,5.376858882524));
#18209=CARTESIAN_POINT('Ctrl Pts',(7.54041218796023,0.160510156897017,5.37263593081816));
#18210=CARTESIAN_POINT('Ctrl Pts',(7.54437544438211,0.0794377826492872,
5.36841297911234));
#18211=CARTESIAN_POINT('Ctrl Pts',(7.54432671099194,-0.00147590784951311,
5.3641900274065));
#18212=CARTESIAN_POINT('',(7.54432621659511,0.0021450739360106,4.56419002733521));
#18213=CARTESIAN_POINT('Ctrl Pts',(7.54432671099162,-0.00147590839339668,
5.36419002737812));
#18214=CARTESIAN_POINT('Ctrl Pts',(7.54427359039347,-0.0896737956893541,
5.35958690748191));
#18215=CARTESIAN_POINT('Ctrl Pts',(7.53945915089848,-0.177726601365087,
5.35498378758571));
#18216=CARTESIAN_POINT('Ctrl Pts',(7.52992837234614,-0.265256688986924,
5.35038066768951));
#18217=CARTESIAN_POINT('Ctrl Pts',(7.52116581341593,-0.345731494559209,
5.34614857803055));
#18218=CARTESIAN_POINT('Ctrl Pts',(7.50839498671782,-0.42592175353851,5.34191648837158));
#18219=CARTESIAN_POINT('Ctrl Pts',(7.49164371171501,-0.505396886136336,
5.33768439871262));
#18220=CARTESIAN_POINT('Ctrl Pts',(7.47491637828506,-0.584758429787849,
5.33345835772057));
#18221=CARTESIAN_POINT('Ctrl Pts',(7.45421999058225,-0.663406426133667,
5.32923231672851));
#18222=CARTESIAN_POINT('Ctrl Pts',(7.42963408316916,-0.740915816023442,
5.32500627573646));
#18223=CARTESIAN_POINT('Ctrl Pts',(7.40504141320734,-0.818446525485383,
5.32077907233833));
#18224=CARTESIAN_POINT('Ctrl Pts',(7.3765571604242,-0.894837541587461,5.3165518689402));
#18225=CARTESIAN_POINT('Ctrl Pts',(7.34431208924471,-0.969674075541368,
5.31232466554207));
#18226=CARTESIAN_POINT('Ctrl Pts',(7.31213356813603,-1.04435615560664,5.30810618659934));
#18227=CARTESIAN_POINT('Ctrl Pts',(7.2762098978411,-1.11748972697521,5.3038877076566));
#18228=CARTESIAN_POINT('Ctrl Pts',(7.23672016284573,-1.18867985970479,5.29966922871387));
#18229=CARTESIAN_POINT('Ctrl Pts',(7.19724337744447,-1.25984664754935,5.2954521331076));
#18230=CARTESIAN_POINT('Ctrl Pts',(7.15420307488966,-1.32907085632821,5.29123503750133));
#18231=CARTESIAN_POINT('Ctrl Pts',(7.10782455095544,-1.39598164060628,5.28701794189505));
#18232=CARTESIAN_POINT('Ctrl Pts',(7.06144704477249,-1.4628909565639,5.28280093883063));
#18233=CARTESIAN_POINT('Ctrl Pts',(7.01173172852606,-1.52748656769867,5.2785839357662));
#18234=CARTESIAN_POINT('Ctrl Pts',(6.95894672050242,-1.58942733651786,5.27436693270178));
#18235=CARTESIAN_POINT('Ctrl Pts',(6.9059431814658,-1.65162454138703,5.2701324711584));
#18236=CARTESIAN_POINT('Ctrl Pts',(6.84984477555161,-1.71114450746076,5.26589800961503));
#18237=CARTESIAN_POINT('Ctrl Pts',(6.79096198855247,-1.7676774616091,5.26166354807165));
#18238=CARTESIAN_POINT('Ctrl Pts',(6.73223695434608,-1.82405895839863,5.25744043106831));
#18239=CARTESIAN_POINT('Ctrl Pts',(6.67074281927816,-1.87746915230112,5.25321731406496));
#18240=CARTESIAN_POINT('Ctrl Pts',(6.60682117406478,-1.92764087673128,5.24899419706162));
#18241=CARTESIAN_POINT('Ctrl Pts',(6.54264196021344,-1.97801476527473,5.24475406324823));
#18242=CARTESIAN_POINT('Ctrl Pts',(6.4760160218102,-2.02512376565333,5.24051392943484));
#18243=CARTESIAN_POINT('Ctrl Pts',(6.40731727544667,-2.06874211894071,5.23627379562145));
#18244=CARTESIAN_POINT('Ctrl Pts',(6.33861852908312,-2.1123604722281,5.23203366180806));
#18245=CARTESIAN_POINT('Ctrl Pts',(6.26784741197225,-2.15248800203411,5.22779352799467));
#18246=CARTESIAN_POINT('Ctrl Pts',(6.19539972605487,-2.18894680650258,5.22355339418128));
#18247=CARTESIAN_POINT('Ctrl Pts',(6.12308948400112,-2.22533644328286,5.21932130452231));
#18248=CARTESIAN_POINT('Ctrl Pts',(6.04883926109623,-2.25820703877894,5.21508921486335));
#18249=CARTESIAN_POINT('Ctrl Pts',(5.97302558958426,-2.28734788858655,5.21085712520439));
#18250=CARTESIAN_POINT('Ctrl Pts',(5.89732027391621,-2.31644708915979,5.20663108421235));
#18251=CARTESIAN_POINT('Ctrl Pts',(5.82005637780871,-2.34182696605901,5.2024050432203));
#18252=CARTESIAN_POINT('Ctrl Pts',(5.74163391104998,-2.36332322321833,5.19817900222826));
#18253=CARTESIAN_POINT('Ctrl Pts',(5.66318987356985,-2.38482539309364,5.19395179883012));
#18254=CARTESIAN_POINT('Ctrl Pts',(5.58358705627138,-2.40244162072257,5.18972459543199));
#18255=CARTESIAN_POINT('Ctrl Pts',(5.50324469600788,-2.41605619294877,5.18549739203386));
#18256=CARTESIAN_POINT('Ctrl Pts',(5.42306815301737,-2.42964266628376,5.18127891309114));
#18257=CARTESIAN_POINT('Ctrl Pts',(5.34215557068428,-2.43924388332877,5.17706043414842));
#18258=CARTESIAN_POINT('Ctrl Pts',(5.2609357830548,-2.4447954835898,5.1728419552057));
#18259=CARTESIAN_POINT('Ctrl Pts',(5.17974262926538,-2.45034526335317,5.16862485959944));
#18260=CARTESIAN_POINT('Ctrl Pts',(5.09824293348812,-2.45184803188112,5.16440776399318));
#18261=CARTESIAN_POINT('Ctrl Pts',(5.01687043383617,-2.44929130831716,5.16019066838692));
#18262=CARTESIAN_POINT('Ctrl Pts',(4.93549971985906,-2.44673464085909,5.1559736653225));
#18263=CARTESIAN_POINT('Ctrl Pts',(4.85425666088092,-2.4401186741723,5.15175666225809));
#18264=CARTESIAN_POINT('Ctrl Pts',(4.77357333693932,-2.42948301943589,5.14753965919367));
#18265=CARTESIAN_POINT('Ctrl Pts',(4.69255598238572,-2.41880333287126,5.14330519765029));
#18266=CARTESIAN_POINT('Ctrl Pts',(4.61210347681013,-2.4040706530683,5.13907073610691));
#18267=CARTESIAN_POINT('Ctrl Pts',(4.53264460451424,-2.38537720172759,5.13483627456353));
#18268=CARTESIAN_POINT('Ctrl Pts',(4.453398610373,-2.36673383198646,5.1306131575602));
#18269=CARTESIAN_POINT('Ctrl Pts',(4.37514137005613,-2.34415105539881,5.12639004055687));
#18270=CARTESIAN_POINT('Ctrl Pts',(4.29828281380373,-2.31777036189301,5.12216692355353));
#18271=CARTESIAN_POINT('Ctrl Pts',(4.22111456036471,-2.29128336888123,5.11792678974013));
#18272=CARTESIAN_POINT('Ctrl Pts',(4.14535672112182,-2.26096797051504,5.11368665592671));
#18273=CARTESIAN_POINT('Ctrl Pts',(4.07140204223259,-2.22701529807408,5.1094465221133));
#18274=CARTESIAN_POINT('Ctrl Pts',(3.99744736334334,-2.19306262563312,5.10520638829989));
#18275=CARTESIAN_POINT('Ctrl Pts',(3.92529623052259,-2.15547295021282,5.10096625448648));
#18276=CARTESIAN_POINT('Ctrl Pts',(3.85531311721876,-2.11448178689164,5.09672612067307));
#18277=CARTESIAN_POINT('Ctrl Pts',(3.78546277212392,-2.07356838980693,5.09249403101411));
#18278=CARTESIAN_POINT('Ctrl Pts',(3.71751162249781,-2.02911377346407,5.08826194135515));
#18279=CARTESIAN_POINT('Ctrl Pts',(3.65184120019903,-1.98131944795633,5.08402985169619));
#18280=CARTESIAN_POINT('Ctrl Pts',(3.58626463661845,-1.93359343195494,5.07980381070414));
#18281=CARTESIAN_POINT('Ctrl Pts',(3.52296269881731,-1.88253745812472,5.07557776971209));
#18282=CARTESIAN_POINT('Ctrl Pts',(3.46229072743459,-1.8283979692749,5.07135172872005));
#18283=CARTESIAN_POINT('Ctrl Pts',(3.40160206774502,-1.77424358892935,5.06712452532191));
#18284=CARTESIAN_POINT('Ctrl Pts',(3.34354521018652,-1.71700425552863,5.06289732192378));
#18285=CARTESIAN_POINT('Ctrl Pts',(3.28844516845876,-1.65696895898394,5.05867011852565));
#18286=CARTESIAN_POINT('Ctrl Pts',(3.23345884679883,-1.59705756829815,5.05445163958293));
#18287=CARTESIAN_POINT('Ctrl Pts',(3.18141748076258,-1.53436206949927,5.0502331606402));
#18288=CARTESIAN_POINT('Ctrl Pts',(3.13260819768649,-1.46920742228482,5.04601468169748));
#18289=CARTESIAN_POINT('Ctrl Pts',(3.08381492029912,-1.40407414078066,5.04179758609121));
#18290=CARTESIAN_POINT('Ctrl Pts',(3.03825189944845,-1.33648368393946,5.03758049048495));
#18291=CARTESIAN_POINT('Ctrl Pts',(2.99616538269492,-1.26679332849086,5.03336339487868));
#18292=CARTESIAN_POINT('Ctrl Pts',(2.95407978950688,-1.19710450235885,5.02914639181427));
#18293=CARTESIAN_POINT('Ctrl Pts',(2.91547078796979,-1.12531626761495,5.02492938874985));
#18294=CARTESIAN_POINT('Ctrl Pts',(2.88054000053615,-1.05181282549681,5.02071238568544));
#18295=CARTESIAN_POINT('Ctrl Pts',(2.84546459892786,-0.97800507762445,5.01647792414205));
#18296=CARTESIAN_POINT('Ctrl Pts',(2.81409814620316,-0.902468310742165,
5.01224346259867));
#18297=CARTESIAN_POINT('Ctrl Pts',(2.78659631431143,-0.825612557853047,
5.00800900105529));
#18298=CARTESIAN_POINT('Ctrl Pts',(2.75916816253937,-0.74896270910489,5.00378588405195));
#18299=CARTESIAN_POINT('Ctrl Pts',(2.73558404662131,-0.671001392179162,
4.99956276704862));
#18300=CARTESIAN_POINT('Ctrl Pts',(2.71594803617518,-0.592149596049849,
4.99533965004528));
#18301=CARTESIAN_POINT('Ctrl Pts',(2.69623290354037,-0.512980071087197,
4.99109951623188));
#18302=CARTESIAN_POINT('Ctrl Pts',(2.6804978433303,-0.432913339762491,4.98685938241847));
#18303=CARTESIAN_POINT('Ctrl Pts',(2.66879591741602,-0.352382951551732,
4.98261924860506));
#18304=CARTESIAN_POINT('Ctrl Pts',(2.65709399150175,-0.271852563340974,
4.97837911479166));
#18305=CARTESIAN_POINT('Ctrl Pts',(2.64942518200459,-0.190858989358832,
4.97413898097825));
#18306=CARTESIAN_POINT('Ctrl Pts',(2.64578992844837,-0.109836174364002,
4.96989884716485));
#18307=CARTESIAN_POINT('Ctrl Pts',(2.64216157150021,-0.028967071507964,
4.96566675750589));
#18308=CARTESIAN_POINT('Ctrl Pts',(2.6425379274089,0.0522328669521893,4.96143466784692));
#18309=CARTESIAN_POINT('Ctrl Pts',(2.6469572506401,0.133333862616992,4.95720257818796));
#18310=CARTESIAN_POINT('Ctrl Pts',(2.65137025760289,0.214318945588814,4.95297653719591));
#18311=CARTESIAN_POINT('Ctrl Pts',(2.65981473035323,0.295204906503583,4.94875049620386));
#18312=CARTESIAN_POINT('Ctrl Pts',(2.67227697172965,0.37555952618575,4.94452445521182));
#18313=CARTESIAN_POINT('Ctrl Pts',(2.68474264094438,0.455936248043244,4.94029725181368));
#18314=CARTESIAN_POINT('Ctrl Pts',(2.70122828366823,0.535780869538422,4.93607004841555));
#18315=CARTESIAN_POINT('Ctrl Pts',(2.72166800539681,0.614663498838341,4.93184284501742));
#18316=CARTESIAN_POINT('Ctrl Pts',(2.74206554192066,0.693383323580008,4.92762436607469));
#18317=CARTESIAN_POINT('Ctrl Pts',(2.76640075986749,0.771144666907163,4.92340588713197));
#18318=CARTESIAN_POINT('Ctrl Pts',(2.79455697894836,0.847529884685964,4.91918740818925));
#18319=CARTESIAN_POINT('Ctrl Pts',(2.82270396495613,0.923890053991553,4.91497031258298));
#18320=CARTESIAN_POINT('Ctrl Pts',(2.85466930317231,0.998874558242534,4.91075321697672));
#18321=CARTESIAN_POINT('Ctrl Pts',(2.89028696632642,1.0720824991126,4.90653612137046));
#18322=CARTESIAN_POINT('Ctrl Pts',(2.92590384787049,1.14528883347462,4.90231911830604));
#18323=CARTESIAN_POINT('Ctrl Pts',(2.96517269066395,1.21671826461475,4.89810211524162));
#18324=CARTESIAN_POINT('Ctrl Pts',(3.00788061081709,1.28599271495644,4.89388511217721));
#18325=CARTESIAN_POINT('Ctrl Pts',(3.05076534263344,1.35555396293986,4.88965065063383));
#18326=CARTESIAN_POINT('Ctrl Pts',(3.09711745153464,1.42294194041336,4.88541618909044));
#18327=CARTESIAN_POINT('Ctrl Pts',(3.14667739375347,1.48780309702361,4.88118172754706));
#18328=CARTESIAN_POINT('Ctrl Pts',(3.19610455999986,1.55249048419915,4.87695861054373));
#18329=CARTESIAN_POINT('Ctrl Pts',(3.24872205982467,1.61466424210887,4.8727354935404));
#18330=CARTESIAN_POINT('Ctrl Pts',(3.30423310345936,1.67400817771856,4.86851237653707));
#18331=CARTESIAN_POINT('Ctrl Pts',(3.35996782569106,1.73359123634573,4.86427224272366));
#18332=CARTESIAN_POINT('Ctrl Pts',(3.41861911483818,1.79032129774366,4.86003210891026));
#18333=CARTESIAN_POINT('Ctrl Pts',(3.47985191156125,1.84391815493645,4.85579197509685));
#18334=CARTESIAN_POINT('Ctrl Pts',(3.54108470828434,1.89751501212924,4.85155184128345));
#18335=CARTESIAN_POINT('Ctrl Pts',(3.60489860743153,1.94797842403463,4.84731170747004));
#18336=CARTESIAN_POINT('Ctrl Pts',(3.67092961338773,1.99507213773946,4.84307157365664));
#18337=CARTESIAN_POINT('Ctrl Pts',(3.73683534886111,2.0420765077766,4.83883948399768));
#18338=CARTESIAN_POINT('Ctrl Pts',(3.80519565810399,2.08589933025432,4.83460739433872));
#18339=CARTESIAN_POINT('Ctrl Pts',(3.87567059803625,2.12627487677918,4.83037530467976));
#18340=CARTESIAN_POINT('Ctrl Pts',(3.9460448124471,2.16659271700475,4.82614926368771));
#18341=CARTESIAN_POINT('Ctrl Pts',(4.01852725507035,2.20347283772712,4.82192322269567));
#18342=CARTESIAN_POINT('Ctrl Pts',(4.09274769424177,2.23669178975129,4.81769718170362));
#18343=CARTESIAN_POINT('Ctrl Pts',(4.16698854833357,2.26991987891164,4.81346997830549));
#18344=CARTESIAN_POINT('Ctrl Pts',(4.24296796032465,2.29948453604171,4.80924277490735));
#18345=CARTESIAN_POINT('Ctrl Pts',(4.32028927855363,2.32520738924549,4.80501557150922));
#18346=CARTESIAN_POINT('Ctrl Pts',(4.3974510145885,2.35087715347657,4.8007970925665));
#18347=CARTESIAN_POINT('Ctrl Pts',(4.47594869025038,2.37272078559757,4.79657861362378));
#18348=CARTESIAN_POINT('Ctrl Pts',(4.55536832789648,2.39060919872453,4.79236013468106));
#18349=CARTESIAN_POINT('Ctrl Pts',(4.63476192201317,2.40849174582859,4.78814303907479));
#18350=CARTESIAN_POINT('Ctrl Pts',(4.71507642472783,2.42242154764815,4.78392594346853));
#18351=CARTESIAN_POINT('Ctrl Pts',(4.79588509004013,2.43232003972698,4.77970884786227));
#18352=CARTESIAN_POINT('Ctrl Pts',(4.87669198205068,2.44221831458884,4.77549184479785));
#18353=CARTESIAN_POINT('Ctrl Pts',(4.95799255371693,2.44808540024345,4.77127484173343));
#18354=CARTESIAN_POINT('Ctrl Pts',(5.03935374343865,2.44989446658086,4.76705783866902));
#18355=CARTESIAN_POINT('Ctrl Pts',(5.12105177015047,2.45171102248992,4.76282337712563));
#18356=CARTESIAN_POINT('Ctrl Pts',(5.20281044650648,2.44943586357772,4.75858891558225));
#18357=CARTESIAN_POINT('Ctrl Pts',(5.28419193459185,2.44309465655006,4.75435445403887));
#18358=CARTESIAN_POINT('Ctrl Pts',(5.36535539364532,2.43677043824136,4.75013133703554));
#18359=CARTESIAN_POINT('Ctrl Pts',(5.44614322436611,2.426402031042,4.7459082200322));
#18360=CARTESIAN_POINT('Ctrl Pts',(5.52612869875587,2.41206667106406,4.74168510302887));
#18361=CARTESIAN_POINT('Ctrl Pts',(5.60643647007122,2.39767354756739,4.73744496921546));
#18362=CARTESIAN_POINT('Ctrl Pts',(5.68593494793438,2.37928154924516,4.73320483540205));
#18363=CARTESIAN_POINT('Ctrl Pts',(5.76420680689355,2.357019595365,4.72896470158864));
#18364=CARTESIAN_POINT('Ctrl Pts',(5.84247866585271,2.33475764148485,4.72472456777523));
#18365=CARTESIAN_POINT('Ctrl Pts',(5.9195234833211,2.30862594106612,4.72048443396183));
#18366=CARTESIAN_POINT('Ctrl Pts',(5.99494509779219,2.27880159381956,4.71624430014842));
#18367=CARTESIAN_POINT('Ctrl Pts',(6.07022362642167,2.24903382772493,4.71201221048946));
#18368=CARTESIAN_POINT('Ctrl Pts',(6.14416596005128,2.21547637032556,4.70778012083049));
#18369=CARTESIAN_POINT('Ctrl Pts',(6.21636427122028,2.17827011036857,4.70354803117153));
#18370=CARTESIAN_POINT('Ctrl Pts',(6.28845939375883,2.14111702704338,4.69932199017948));
#18371=CARTESIAN_POINT('Ctrl Pts',(6.35881503484589,2.10032570982544,4.69509594918743));
#18372=CARTESIAN_POINT('Ctrl Pts',(6.42704239006832,2.05608545255053,4.69086990819538));
#18373=CARTESIAN_POINT('Ctrl Pts',(6.49528851176577,2.01183302664207,4.68664270479725));
#18374=CARTESIAN_POINT('Ctrl Pts',(6.56140475299479,1.96412995919908,4.68241550139911));
#18375=CARTESIAN_POINT('Ctrl Pts',(6.6250257838841,1.91321222301423,4.67818829800098));
#18376=CARTESIAN_POINT('Ctrl Pts',(6.68851550837652,1.86239957510574,4.67396981905826));
#18377=CARTESIAN_POINT('Ctrl Pts',(6.74951993344191,1.80838578546829,4.66975134011554));
#18378=CARTESIAN_POINT('Ctrl Pts',(6.80770567885527,1.75144815995816,4.66553286117281));
#18379=CARTESIAN_POINT('Ctrl Pts',(6.86587234382183,1.69452920560756,4.66131576556655));
#18380=CARTESIAN_POINT('Ctrl Pts',(6.92122183286112,1.63468864421207,4.65709866996029));
#18381=CARTESIAN_POINT('Ctrl Pts',(6.97345623146422,1.57224196185371,4.65288157435402));
#18382=CARTESIAN_POINT('Ctrl Pts',(7.02568948381219,1.50979664985344,4.6486645712896));
#18383=CARTESIAN_POINT('Ctrl Pts',(7.07480748437667,1.44474568777064,4.64444756822518));
#18384=CARTESIAN_POINT('Ctrl Pts',(7.12055230919156,1.37743798452194,4.64023056516076));
#18385=CARTESIAN_POINT('Ctrl Pts',(7.16648651851705,1.30985162600478,4.63599610361738));
#18386=CARTESIAN_POINT('Ctrl Pts',(7.2090192867098,1.23999018358184,4.631761642074));
#18387=CARTESIAN_POINT('Ctrl Pts',(7.24793415705635,1.16823511145826,4.62752718053062));
#18388=CARTESIAN_POINT('Ctrl Pts',(7.28674477062775,1.09667227824884,4.62330406352729));
#18389=CARTESIAN_POINT('Ctrl Pts',(7.32195668199649,1.02322638824681,4.61908094652395));
#18390=CARTESIAN_POINT('Ctrl Pts',(7.35340275872277,0.948297602606147,4.61485782952062));
#18391=CARTESIAN_POINT('Ctrl Pts',(7.3849755456289,0.873066895680105,4.61061769570722));
#18392=CARTESIAN_POINT('Ctrl Pts',(7.4127519330167,0.79634176362735,4.60637756189381));
#18393=CARTESIAN_POINT('Ctrl Pts',(7.43661328010294,0.718542569475346,4.60213742808041));
#18394=CARTESIAN_POINT('Ctrl Pts',(7.46047462718918,0.640743375323342,4.597897294267));
#18395=CARTESIAN_POINT('Ctrl Pts',(7.48042087970568,0.561870587392111,4.5936571604536));
#18396=CARTESIAN_POINT('Ctrl Pts',(7.49638534176927,0.482352994564379,4.5894170266402));
#18397=CARTESIAN_POINT('Ctrl Pts',(7.51922595399674,0.368585897633325,4.58335059910642));
#18398=CARTESIAN_POINT('Ctrl Pts',(7.53399165590837,0.253147670596884,4.57728417157264));
#18399=CARTESIAN_POINT('Ctrl Pts',(7.54049542395804,0.136984064369133,4.57121774403885));
#18400=CARTESIAN_POINT('Ctrl Pts',(7.54300687674887,0.0921270813362655,
4.5688751718186));
#18401=CARTESIAN_POINT('Ctrl Pts',(7.54428681030233,0.047162191867149,4.56653259959836));
#18402=CARTESIAN_POINT('Ctrl Pts',(7.54432621659438,0.00214507476044559,
4.56419002737811));
#18403=CARTESIAN_POINT('',(7.54393144410385,-8.94937127778141E-5,3.76419002093224));
#18404=CARTESIAN_POINT('Ctrl Pts',(7.54432621659511,0.00214507393599264,
4.56419002733521));
#18405=CARTESIAN_POINT('Ctrl Pts',(7.5443974290659,-0.0792069437733646,
4.55995668257674));
#18406=CARTESIAN_POINT('Ctrl Pts',(7.54041302387128,-0.160689976853086,
4.55572333781828));
#18407=CARTESIAN_POINT('Ctrl Pts',(7.53236234262211,-0.24186027151777,4.55148999305981));
#18408=CARTESIAN_POINT('Ctrl Pts',(7.52445196900467,-0.321615926668248,
4.54733042722253));
#18409=CARTESIAN_POINT('Ctrl Pts',(7.51261596087068,-0.401069158613352,
4.54317086138524));
#18410=CARTESIAN_POINT('Ctrl Pts',(7.49689665975842,-0.479799132427131,
4.53901129554796));
#18411=CARTESIAN_POINT('Ctrl Pts',(7.48118511182865,-0.558490274498342,
4.53485378132053));
#18412=CARTESIAN_POINT('Ctrl Pts',(7.46159416428309,-0.636458396846393,
4.53069626709309));
#18413=CARTESIAN_POINT('Ctrl Pts',(7.43821764561932,-0.713290599698506,
4.52653875286566));
#18414=CARTESIAN_POINT('Ctrl Pts',(7.4148450175322,-0.79011001529264,4.52238193057735));
#18415=CARTESIAN_POINT('Ctrl Pts',(7.38768820935881,-0.865793428407507,
4.51822510828904));
#18416=CARTESIAN_POINT('Ctrl Pts',(7.35689109022829,-0.939942486070237,
4.51406828600073));
#18417=CARTESIAN_POINT('Ctrl Pts',(7.3251081881406,-1.01646497603433,4.50977840826167));
#18418=CARTESIAN_POINT('Ctrl Pts',(7.28944814638986,-1.09135270273389,4.5054885305226));
#18419=CARTESIAN_POINT('Ctrl Pts',(7.25012225160305,-1.16419143972103,4.50119865278354));
#18420=CARTESIAN_POINT('Ctrl Pts',(7.21196864925899,-1.23485887707538,4.49703665493841));
#18421=CARTESIAN_POINT('Ctrl Pts',(7.17036499723818,-1.30359738498881,4.49287465709327));
#18422=CARTESIAN_POINT('Ctrl Pts',(7.12554925654193,-1.37005677033736,4.48871265924813));
#18423=CARTESIAN_POINT('Ctrl Pts',(7.07866802985326,-1.43957916273142,4.48435884156211));
#18424=CARTESIAN_POINT('Ctrl Pts',(7.0282718432639,-1.50660680265638,4.48000502387608));
#18425=CARTESIAN_POINT('Ctrl Pts',(6.97467977651927,-1.57077804537387,4.47565120619006));
#18426=CARTESIAN_POINT('Ctrl Pts',(6.92108770977463,-1.63494928809137,4.47129738850404));
#18427=CARTESIAN_POINT('Ctrl Pts',(6.86430022451696,-1.69626375536162,4.46694357081801));
#18428=CARTESIAN_POINT('Ctrl Pts',(6.80467773584324,-1.75440603669126,4.46258975313199));
#18429=CARTESIAN_POINT('Ctrl Pts',(6.7467222273782,-1.81092272280642,4.45835766347302));
#18430=CARTESIAN_POINT('Ctrl Pts',(6.68585512058094,-1.86466997352523,4.45412557381406));
#18431=CARTESIAN_POINT('Ctrl Pts',(6.62237179651123,-1.91533326872701,4.4498934841551));
#18432=CARTESIAN_POINT('Ctrl Pts',(6.5589792052739,-1.96592415397959,4.44566744316305));
#18433=CARTESIAN_POINT('Ctrl Pts',(6.49297818338994,-2.01343955046774,4.44144140217099));
#18434=CARTESIAN_POINT('Ctrl Pts',(6.42470050116979,-2.05760209653395,4.43721536117894));
#18435=CARTESIAN_POINT('Ctrl Pts',(6.35640403863182,-2.10177678985858,4.43298815778081));
#18436=CARTESIAN_POINT('Ctrl Pts',(6.28583001538824,-2.14259648168666,4.42876095438268));
#18437=CARTESIAN_POINT('Ctrl Pts',(6.21334319503714,-2.17982432482852,4.42453375098454));
#18438=CARTESIAN_POINT('Ctrl Pts',(6.14100597903965,-2.21697533403859,4.42031527204182));
#18439=CARTESIAN_POINT('Ctrl Pts',(6.06676425559604,-2.25054907152311,4.4160967930991));
#18440=CARTESIAN_POINT('Ctrl Pts',(5.99100743671944,-2.28035475154785,4.41187831415638));
#18441=CARTESIAN_POINT('Ctrl Pts',(5.91527546024961,-2.31015065760323,4.40766121855012));
#18442=CARTESIAN_POINT('Ctrl Pts',(5.83802980710514,-2.33618079005223,4.40344412294386));
#18443=CARTESIAN_POINT('Ctrl Pts',(5.75968022248452,-2.35830234345066,4.3992270273376));
#18444=CARTESIAN_POINT('Ctrl Pts',(5.68133235720239,-2.38042341140378,4.39501002427318));
#18445=CARTESIAN_POINT('Ctrl Pts',(5.60188105612765,-2.39863594568316,4.39079302120876));
#18446=CARTESIAN_POINT('Ctrl Pts',(5.52175020561123,-2.41284730414989,4.38657601814434));
#18447=CARTESIAN_POINT('Ctrl Pts',(5.44128761173427,-2.42711749793142,4.38234155660096));
#18448=CARTESIAN_POINT('Ctrl Pts',(5.36014029203761,-2.43735322035853,4.37810709505758));
#18449=CARTESIAN_POINT('Ctrl Pts',(5.27874486921592,-2.44351298116804,4.3738726335142));
#18450=CARTESIAN_POINT('Ctrl Pts',(5.19756751275862,-2.44965623937092,4.36964951651086));
#18451=CARTESIAN_POINT('Ctrl Pts',(5.11614384934172,-2.45174537703917,4.36542639950753));
#18452=CARTESIAN_POINT('Ctrl Pts',(5.03490739645501,-2.44979156501111,4.36120328250419));
#18453=CARTESIAN_POINT('Ctrl Pts',(4.95334360589602,-2.44782988020848,4.35696314869079));
#18454=CARTESIAN_POINT('Ctrl Pts',(4.87196900727807,-2.44179263873569,4.35272301487739));
#18455=CARTESIAN_POINT('Ctrl Pts',(4.79121571760313,-2.43174352423983,4.34848288106398));
#18456=CARTESIAN_POINT('Ctrl Pts',(4.7104624279282,-2.42169440974398,4.34424274725058));
#18457=CARTESIAN_POINT('Ctrl Pts',(4.63033089674386,-2.40763356426609,4.34000261343717));
#18458=CARTESIAN_POINT('Ctrl Pts',(4.55123968223925,-2.38967551854041,4.33576247962377));
#18459=CARTESIAN_POINT('Ctrl Pts',(4.47229851534452,-2.37175154185586,4.3315303899648));
#18460=CARTESIAN_POINT('Ctrl Pts',(4.39409920452606,-2.34987828336003,4.32729830030584));
#18461=CARTESIAN_POINT('Ctrl Pts',(4.3170663078638,-2.32413270611907,4.32306621064687));
#18462=CARTESIAN_POINT('Ctrl Pts',(4.24014350960956,-2.29842392545711,4.31884016965483));
#18463=CARTESIAN_POINT('Ctrl Pts',(4.16438425154372,-2.26885396417153,4.31461412866279));
#18464=CARTESIAN_POINT('Ctrl Pts',(4.09020168302774,-2.23555052752089,4.31038808767075));
#18465=CARTESIAN_POINT('Ctrl Pts',(4.01599871000794,-2.20223793049588,4.30616088427261));
#18466=CARTESIAN_POINT('Ctrl Pts',(3.94337374263392,-2.16518993309185,4.30193368087448));
#18467=CARTESIAN_POINT('Ctrl Pts',(3.87272385868301,-2.12458395659414,4.29770647747635));
#18468=CARTESIAN_POINT('Ctrl Pts',(3.802219787863,-2.08406178610197,4.29348799853363));
#18469=CARTESIAN_POINT('Ctrl Pts',(3.73368307129339,-2.0399965182552,4.28926951959091));
#18470=CARTESIAN_POINT('Ctrl Pts',(3.6674855231533,-1.99261130127486,4.28505104064819));
#18471=CARTESIAN_POINT('Ctrl Pts',(3.60130968271473,-1.94524162299914,4.28083394504193));
#18472=CARTESIAN_POINT('Ctrl Pts',(3.53747186494722,-1.8945544278931,4.27661684943566));
#18473=CARTESIAN_POINT('Ctrl Pts',(3.47631466416907,-1.84081601213703,4.2723997538294));
#18474=CARTESIAN_POINT('Ctrl Pts',(3.41515880545205,-1.78707877564095,4.26818275076498));
#18475=CARTESIAN_POINT('Ctrl Pts',(3.35668379508103,-1.73029075921625,4.26396574770056));
#18476=CARTESIAN_POINT('Ctrl Pts',(3.30119780931492,-1.67075739632185,4.25974874463614));
#18477=CARTESIAN_POINT('Ctrl Pts',(3.24548211043251,-1.61097756408703,4.25551428309276));
#18478=CARTESIAN_POINT('Ctrl Pts',(3.1927805692189,-1.54842994173995,4.25127982154938));
#18479=CARTESIAN_POINT('Ctrl Pts',(3.14336535048328,-1.48345845825012,4.247045360006));
#18480=CARTESIAN_POINT('Ctrl Pts',(3.09408251999165,-1.41866103977161,4.24282224300266));
#18481=CARTESIAN_POINT('Ctrl Pts',(3.04806865587497,-1.35145314016538,4.23859912599933));
#18482=CARTESIAN_POINT('Ctrl Pts',(3.00555003355359,-1.28220470758419,4.23437600899599));
#18483=CARTESIAN_POINT('Ctrl Pts',(2.96286008485882,-1.21267724237755,4.23013587518259));
#18484=CARTESIAN_POINT('Ctrl Pts',(2.92369382390486,-1.14109318278515,4.22589574136918));
#18485=CARTESIAN_POINT('Ctrl Pts',(2.88823268784501,-1.06784984640001,4.22165560755577));
#18486=CARTESIAN_POINT('Ctrl Pts',(2.85277155178516,-0.994606510014861,
4.21741547374237));
#18487=CARTESIAN_POINT('Ctrl Pts',(2.82101566576168,-0.919704351378593,
4.21317533992896));
#18488=CARTESIAN_POINT('Ctrl Pts',(2.79309641776494,-0.843556946896196,
4.20893520611555));
#18489=CARTESIAN_POINT('Ctrl Pts',(2.76523013666801,-0.767554005185311,
4.20470311645659));
#18490=CARTESIAN_POINT('Ctrl Pts',(2.74108197119417,-0.690026992125681,
4.20047102679762));
#18491=CARTESIAN_POINT('Ctrl Pts',(2.72081810344044,-0.611374099112766,
4.19623893713866));
#18492=CARTESIAN_POINT('Ctrl Pts',(2.70058319759358,-0.532833619869503,
4.19201289614662));
#18493=CARTESIAN_POINT('Ctrl Pts',(2.68422167837414,-0.453170902856112,
4.18778685515458));
#18494=CARTESIAN_POINT('Ctrl Pts',(2.67185093551015,-0.372802145957868,
4.18356081416254));
#18495=CARTESIAN_POINT('Ctrl Pts',(2.65947678997521,-0.292411282995653,
4.1793336107644));
#18496=CARTESIAN_POINT('Ctrl Pts',(2.65109575197383,-0.211314438422341,
4.17510640736627));
#18497=CARTESIAN_POINT('Ctrl Pts',(2.64677474554044,-0.129941345000655,
4.17087920396814));
#18498=CARTESIAN_POINT('Ctrl Pts',(2.642462657161,-0.0487361961651143,4.16666072502541));
#18499=CARTESIAN_POINT('Ctrl Pts',(2.64219390782991,0.0327435996271821,
4.16244224608269));
#18500=CARTESIAN_POINT('Ctrl Pts',(2.64598330755776,0.114064658509501,4.15822376713997));
#18501=CARTESIAN_POINT('Ctrl Pts',(2.64977146465412,0.195359050342644,4.15400667153371));
#18502=CARTESIAN_POINT('Ctrl Pts',(2.6576151064267,0.276494344812994,4.14978957592744));
#18503=CARTESIAN_POINT('Ctrl Pts',(2.66947694299592,0.357038229548013,4.14557248032117));
#18504=CARTESIAN_POINT('Ctrl Pts',(2.68133851926364,0.437580346791695,4.14135547725675));
#18505=CARTESIAN_POINT('Ctrl Pts',(2.69721804616645,0.517530620541599,4.13713847419234));
#18506=CARTESIAN_POINT('Ctrl Pts',(2.7170266746867,0.596464353191837,4.13292147112792));
#18507=CARTESIAN_POINT('Ctrl Pts',(2.73691731133429,0.675724873110183,4.12868700958454));
#18508=CARTESIAN_POINT('Ctrl Pts',(2.76076954967425,0.753959956248967,4.12445254804115));
#18509=CARTESIAN_POINT('Ctrl Pts',(2.78844265408706,0.830754206044847,4.12021808649777));
#18510=CARTESIAN_POINT('Ctrl Pts',(2.81604161952421,0.907342716472562,4.11599496949444));
#18511=CARTESIAN_POINT('Ctrl Pts',(2.84744078598348,0.982497688404455,4.11177185249111));
#18512=CARTESIAN_POINT('Ctrl Pts',(2.88245263387798,1.05582809932695,4.10754873548778));
#18513=CARTESIAN_POINT('Ctrl Pts',(2.91760556002476,1.12945399097481,4.10330860167437));
#18514=CARTESIAN_POINT('Ctrl Pts',(2.95640011152989,1.20124017598528,4.09906846786097));
#18515=CARTESIAN_POINT('Ctrl Pts',(2.99860142286109,1.27081838965457,4.09482833404756));
#18516=CARTESIAN_POINT('Ctrl Pts',(3.04080273419228,1.34039660332386,4.09058820023415));
#18517=CARTESIAN_POINT('Ctrl Pts',(3.08641049185181,1.4077664935329,4.08634806642074));
#18518=CARTESIAN_POINT('Ctrl Pts',(3.13514897760213,1.47259296671225,4.08210793260734));
#18519=CARTESIAN_POINT('Ctrl Pts',(3.18379499931147,1.53729645458376,4.07787584294837));
#18520=CARTESIAN_POINT('Ctrl Pts',(3.23574135673275,1.59970757218604,4.07364375328941));
#18521=CARTESIAN_POINT('Ctrl Pts',(3.29074415854736,1.65947038427004,4.06941166363045));
#18522=CARTESIAN_POINT('Ctrl Pts',(3.34566834822134,1.71914778102187,4.06518562263839));
#18523=CARTESIAN_POINT('Ctrl Pts',(3.40363999413768,1.77618405073598,4.06095958164635));
#18524=CARTESIAN_POINT('Ctrl Pts',(3.464373568516,1.83025442439509,4.0567335406543));
#18525=CARTESIAN_POINT('Ctrl Pts',(3.52512384814549,1.88433967053916,4.05250633725616));
#18526=CARTESIAN_POINT('Ctrl Pts',(3.58863727450789,1.9354570322613,4.04827913385803));
#18527=CARTESIAN_POINT('Ctrl Pts',(3.6545895270529,1.98331674197465,4.04405193045989));
#18528=CARTESIAN_POINT('Ctrl Pts',(3.72040566183107,2.03107767482206,4.03983345151717));
#18529=CARTESIAN_POINT('Ctrl Pts',(3.78865020450153,2.07559409588503,4.03561497257445));
#18530=CARTESIAN_POINT('Ctrl Pts',(3.85896744175701,2.11661799517305,4.03139649363173));
#18531=CARTESIAN_POINT('Ctrl Pts',(3.92926162036989,2.15762844177908,4.02717939802547));
#18532=CARTESIAN_POINT('Ctrl Pts',(4.00162674271221,2.19514840704304,4.02296230241921));
#18533=CARTESIAN_POINT('Ctrl Pts',(4.07567967434793,2.22897419382082,4.01874520681295));
#18534=CARTESIAN_POINT('Ctrl Pts',(4.14973098093263,2.26279923831024,4.01452820374855));
#18535=CARTESIAN_POINT('Ctrl Pts',(4.22546960001108,2.29293007346946,4.01031120068414));
#18536=CARTESIAN_POINT('Ctrl Pts',(4.30249076210192,2.31921041791338,4.00609419761973));
#18537=CARTESIAN_POINT('Ctrl Pts',(4.3798307933799,2.34559956352106,4.00185973607635));
#18538=CARTESIAN_POINT('Ctrl Pts',(4.45846356743338,2.36810610373105,3.99762527453296));
#18539=CARTESIAN_POINT('Ctrl Pts',(4.53796391711992,2.38662236440325,3.99339081298958));
#18540=CARTESIAN_POINT('Ctrl Pts',(4.61725127752986,2.40508901818715,3.98916769598624));
#18541=CARTESIAN_POINT('Ctrl Pts',(4.69740110343043,2.41958670312448,3.98494457898291));
#18542=CARTESIAN_POINT('Ctrl Pts',(4.77798325534455,2.43006026278449,3.98072146197957));
#18543=CARTESIAN_POINT('Ctrl Pts',(4.85889010846239,2.44057602505821,3.97648132816616));
#18544=CARTESIAN_POINT('Ctrl Pts',(4.94023230836427,2.44703513490167,3.97224119435275));
#18545=CARTESIAN_POINT('Ctrl Pts',(5.02157308115586,2.44943454673675,3.96800106053934));
#18546=CARTESIAN_POINT('Ctrl Pts',(5.10291385394746,2.45183395857182,3.96376092672594));
#18547=CARTESIAN_POINT('Ctrl Pts',(5.18425273366386,2.45017374412987,3.95952079291253));
#18548=CARTESIAN_POINT('Ctrl Pts',(5.26515858208946,2.44450317902161,3.95528065909912));
#18549=CARTESIAN_POINT('Ctrl Pts',(5.34591094027888,2.43884337180533,3.95104856944016));
#18550=CARTESIAN_POINT('Ctrl Pts',(5.42653318044006,2.42916731676783,3.9468164797812));
#18551=CARTESIAN_POINT('Ctrl Pts',(5.50659397124849,2.41548624624073,3.94258439012223));
#18552=CARTESIAN_POINT('Ctrl Pts',(5.58654033606508,2.40182472923101,3.93835834913019));
#18553=CARTESIAN_POINT('Ctrl Pts',(5.66592639105077,2.38416964308183,3.93413230813815));
#18554=CARTESIAN_POINT('Ctrl Pts',(5.74432433169595,2.36258410933877,3.9299062671461));
#18555=CARTESIAN_POINT('Ctrl Pts',(5.82274383631645,2.34099263832347,3.92567906374797));
#18556=CARTESIAN_POINT('Ctrl Pts',(5.90017421987549,2.31546861631226,3.92145186034983));
#18557=CARTESIAN_POINT('Ctrl Pts',(5.97619596955491,2.28612675193231,3.9172246569517));
#18558=CARTESIAN_POINT('Ctrl Pts',(6.05206081919822,2.25684544574262,3.91300617800898));
#18559=CARTESIAN_POINT('Ctrl Pts',(6.12652240111848,2.22376218462051,3.90878769906627));
#18560=CARTESIAN_POINT('Ctrl Pts',(6.19917918752775,2.1870407255441,3.90456922012355));
#18561=CARTESIAN_POINT('Ctrl Pts',(6.27181214810243,2.15033130828035,3.90035212451729));
#18562=CARTESIAN_POINT('Ctrl Pts',(6.34264107408625,2.10998627179495,3.89613502891103));
#18563=CARTESIAN_POINT('Ctrl Pts',(6.41128672638872,2.06621647678798,3.89191793330477));
#18564=CARTESIAN_POINT('Ctrl Pts',(6.47993087230028,2.022447642285,3.88770093024034));
#18565=CARTESIAN_POINT('Ctrl Pts',(6.54639144859062,1.97525444948642,3.88348392717592));
#18566=CARTESIAN_POINT('Ctrl Pts',(6.61031725452114,1.92489169290863,3.87926692411149));
#18567=CARTESIAN_POINT('Ctrl Pts',(6.67450771459596,1.87432043348831,3.87503246256811));
#18568=CARTESIAN_POINT('Ctrl Pts',(6.73614199302478,1.82055359212562,3.87079800102473));
#18569=CARTESIAN_POINT('Ctrl Pts',(6.79489860012106,1.76388950621497,3.86656353948135));
#18570=CARTESIAN_POINT('Ctrl Pts',(6.85349779247285,1.70737722897821,3.86234042247801));
#18571=CARTESIAN_POINT('Ctrl Pts',(6.90923442299321,1.6479835805073,3.85811730547466));
#18572=CARTESIAN_POINT('Ctrl Pts',(6.96182838023272,1.58603961937333,3.85389418847132));
#18573=CARTESIAN_POINT('Ctrl Pts',(7.01463426183523,1.5238460585668,3.84965405465792));
#18574=CARTESIAN_POINT('Ctrl Pts',(7.06427181029886,1.45908196846006,3.84541392084452));
#18575=CARTESIAN_POINT('Ctrl Pts',(7.11050104743721,1.39211230272191,3.84117378703111));
#18576=CARTESIAN_POINT('Ctrl Pts',(7.15673028457556,1.32514263698376,3.83693365321771));
#18577=CARTESIAN_POINT('Ctrl Pts',(7.19955101730732,1.25596782571684,3.8326935194043));
#18578=CARTESIAN_POINT('Ctrl Pts',(7.23877024704368,1.18497653303256,3.8284533855909));
#18579=CARTESIAN_POINT('Ctrl Pts',(7.27979763224546,1.11071227209453,3.82401776550252));
#18580=CARTESIAN_POINT('Ctrl Pts',(7.31702493902606,1.03420556025212,3.81958214541413));
#18581=CARTESIAN_POINT('Ctrl Pts',(7.35021345270098,0.95586145836729,3.81514652532574));
#18582=CARTESIAN_POINT('Ctrl Pts',(7.38331144713044,0.877731034294547,3.81072300306697));
#18583=CARTESIAN_POINT('Ctrl Pts',(7.41239243550678,0.797773568689021,3.8062994808082));
#18584=CARTESIAN_POINT('Ctrl Pts',(7.43726394308882,0.716417666138689,3.80187595854942));
#18585=CARTESIAN_POINT('Ctrl Pts',(7.46209503840555,0.635193954060035,3.79745962381455));
#18586=CARTESIAN_POINT('Ctrl Pts',(7.4827301416554,0.552576704787212,3.79304328907968));
#18587=CARTESIAN_POINT('Ctrl Pts',(7.49902488252034,0.469014012275352,3.7886269543448));
#18588=CARTESIAN_POINT('Ctrl Pts',(7.51528614811584,0.385622987645243,3.78421969235287));
#18589=CARTESIAN_POINT('Ctrl Pts',(7.5272247353734,0.301290779278597,3.77981243036094));
#18590=CARTESIAN_POINT('Ctrl Pts',(7.53474649504538,0.216478700117246,3.77540516836901));
#18591=CARTESIAN_POINT('Ctrl Pts',(7.54112669174311,0.144538386814042,3.77166678803871));
#18592=CARTESIAN_POINT('Ctrl Pts',(7.54432979256689,0.0722532055568052,
3.76792840770841));
#18593=CARTESIAN_POINT('Ctrl Pts',(7.54432715382295,-8.9383613589154E-5,
3.76419002737811));
#18594=CARTESIAN_POINT('',(7.5454861976999,-0.00208864731307865,2.96419002737811));
#18595=CARTESIAN_POINT('Ctrl Pts',(7.54033673373089,-9.04938769800744E-5,
3.7641899623766));
#18596=CARTESIAN_POINT('Ctrl Pts',(7.54046778980184,-0.402997665835575,
3.74333534561196));
#18597=CARTESIAN_POINT('Ctrl Pts',(7.25582894391592,-1.62248956602737,3.68020497101128));
#18598=CARTESIAN_POINT('Ctrl Pts',(5.3347574418693,-2.88488257368372,3.57479883857445));
#18599=CARTESIAN_POINT('Ctrl Pts',(2.80334608662769,-1.77039299032977,3.44797156506626));
#18600=CARTESIAN_POINT('Ctrl Pts',(2.36277426232799,0.960179650799704,3.32114429155803));
#18601=CARTESIAN_POINT('Ctrl Pts',(4.41521293602296,2.81426324426903,3.19431701804983));
#18602=CARTESIAN_POINT('Ctrl Pts',(6.92189643281657,2.14358447382013,3.07533226332317));
#18603=CARTESIAN_POINT('Ctrl Pts',(7.53950298244955,0.659618068710635,2.99862326643261));
#18604=CARTESIAN_POINT('Ctrl Pts',(7.5454861976999,-0.00208864731307865,
2.96419002737811));
#18605=CARTESIAN_POINT('',(7.54690838528974,0.00161708353963758,2.16419002737811));
#18606=CARTESIAN_POINT('Ctrl Pts',(7.5454861976999,-0.00208864731307865,
2.96419002737811));
#18607=CARTESIAN_POINT('Ctrl Pts',(7.5468489355446,-0.152799050714208,2.95634750859654));
#18608=CARTESIAN_POINT('Ctrl Pts',(7.46563606218028,-1.11446191626834,2.90622923197887));
#18609=CARTESIAN_POINT('Ctrl Pts',(6.19420942661396,-2.67763958070757,2.81383519752519));
#18610=CARTESIAN_POINT('Ctrl Pts',(3.4444784365408,-2.3791266612517,2.68700792401695));
#18611=CARTESIAN_POINT('Ctrl Pts',(2.2003366210504,0.0911449075841722,2.56018065050874));
#18612=CARTESIAN_POINT('Ctrl Pts',(3.59748465251696,2.47821588663366,2.43335337700052));
#18613=CARTESIAN_POINT('Ctrl Pts',(6.36055187866693,2.6030757465843,2.30652610349231));
#18614=CARTESIAN_POINT('Ctrl Pts',(7.49721262842552,1.01042402016213,2.2168049869515));
#18615=CARTESIAN_POINT('Ctrl Pts',(7.54766542960058,0.100812120060077,2.16935962824677));
#18616=CARTESIAN_POINT('Ctrl Pts',(7.54690838528974,0.00161708353963758,
2.16419002737811));
#18617=CARTESIAN_POINT('',(7.54409003691263,0.000907487678406939,1.36419006975599));
#18618=CARTESIAN_POINT('Ctrl Pts',(7.54690838528974,0.00161708353963758,
2.16419002737811));
#18619=CARTESIAN_POINT('Ctrl Pts',(7.54147450253107,-0.710381132382711,
2.1270838704107));
#18620=CARTESIAN_POINT('Ctrl Pts',(6.84050801399482,-2.24289646830409,2.0477019556072));
#18621=CARTESIAN_POINT('Ctrl Pts',(4.2394355612513,-2.76597358458354,1.92604428296767));
#18622=CARTESIAN_POINT('Ctrl Pts',(2.30775733339397,-0.786390369643382,
1.79921700945943));
#18623=CARTESIAN_POINT('Ctrl Pts',(2.91931117988549,1.91104032894591,1.67238973595123));
#18624=CARTESIAN_POINT('Ctrl Pts',(5.51584714400404,2.86399965016062,1.545562462443));
#18625=CARTESIAN_POINT('Ctrl Pts',(7.30705101622796,1.51821913659295,1.4428294452149));
#18626=CARTESIAN_POINT('Ctrl Pts',(7.54182191684067,0.352067414377056,1.38237218582286));
#18627=CARTESIAN_POINT('Ctrl Pts',(7.54065407381936,0.00091808464348145,
1.3641906842669));
#18628=CARTESIAN_POINT('',(7.5443261628818,-0.00220558177832077,0.564190027336024));
#18629=CARTESIAN_POINT('Ctrl Pts',(7.54432698768978,0.000906756890839775,
1.36419002737811));
#18630=CARTESIAN_POINT('Ctrl Pts',(7.54435782807604,-0.0824390242491621,
1.35988108514997));
#18631=CARTESIAN_POINT('Ctrl Pts',(7.54013222037994,-0.165757790068172,
1.35557214292182));
#18632=CARTESIAN_POINT('Ctrl Pts',(7.53168467216415,-0.24859802536523,1.35126320069368));
#18633=CARTESIAN_POINT('Ctrl Pts',(7.52323186801572,-0.33148980256364,1.34695157750894));
#18634=CARTESIAN_POINT('Ctrl Pts',(7.5105519419166,-0.413902023721914,1.34263995432421));
#18635=CARTESIAN_POINT('Ctrl Pts',(7.49373099221603,-0.495390577514945,
1.33832833113947));
#18636=CARTESIAN_POINT('Ctrl Pts',(7.47688164180653,-0.577016717635693,
1.3340094281544));
#18637=CARTESIAN_POINT('Ctrl Pts',(7.45587739507288,-0.657715648835246,
1.32969052516934));
#18638=CARTESIAN_POINT('Ctrl Pts',(7.43085500839889,-0.7370556726297,1.32537162218427));
#18639=CARTESIAN_POINT('Ctrl Pts',(7.40580967646491,-0.816468450374359,
1.32104875881153));
#18640=CARTESIAN_POINT('Ctrl Pts',(7.37673901636463,-0.894519430353402,
1.31672589543878));
#18641=CARTESIAN_POINT('Ctrl Pts',(7.34382811427781,-0.970796546804707,
1.31240303206603));
#18642=CARTESIAN_POINT('Ctrl Pts',(7.31084909359606,-1.04723154072724,1.30807122128194));
#18643=CARTESIAN_POINT('Ctrl Pts',(7.27401414562565,-1.12188494603021,1.30373941049784));
#18644=CARTESIAN_POINT('Ctrl Pts',(7.23355454876966,-1.19436884264902,1.29940759971374));
#18645=CARTESIAN_POINT('Ctrl Pts',(7.21020525229532,-1.23619941248372,1.29690770495135));
#18646=CARTESIAN_POINT('Ctrl Pts',(7.18564959734902,-1.27730796117003,1.29440781018896));
#18647=CARTESIAN_POINT('Ctrl Pts',(7.15993834715027,-1.3176246785575,1.29190791542657));
#18648=CARTESIAN_POINT('Ctrl Pts',(7.11641158845541,-1.38587713674324,1.28767582576761));
#18649=CARTESIAN_POINT('Ctrl Pts',(7.06941799814008,-1.45209778396878,1.28344373610865));
#18650=CARTESIAN_POINT('Ctrl Pts',(7.01917337655043,-1.5159129852687,1.27921164644969));
#18651=CARTESIAN_POINT('Ctrl Pts',(6.96900056652542,-1.57963697940439,1.27498560545764));
#18652=CARTESIAN_POINT('Ctrl Pts',(6.91558623874066,-1.64096199371701,1.27075956446559));
#18653=CARTESIAN_POINT('Ctrl Pts',(6.85919010319566,-1.69954226565206,1.26653352347354));
#18654=CARTESIAN_POINT('Ctrl Pts',(6.80277845544641,-1.7581386505554,1.26230632007541));
#18655=CARTESIAN_POINT('Ctrl Pts',(6.74338363238152,-1.81398840427747,1.25807911667728));
#18656=CARTESIAN_POINT('Ctrl Pts',(6.68130671328084,-1.8667776791785,1.25385191327915));
#18657=CARTESIAN_POINT('Ctrl Pts',(6.61935791371015,-1.91945800316529,1.24963343433642));
#18658=CARTESIAN_POINT('Ctrl Pts',(6.55473841593925,-1.96909014855919,1.2454149553937));
#18659=CARTESIAN_POINT('Ctrl Pts',(6.48778380992533,-2.01539948780698,1.24119647645097));
#18660=CARTESIAN_POINT('Ctrl Pts',(6.42085115986977,-2.06169364115517,1.23697938084471));
#18661=CARTESIAN_POINT('Ctrl Pts',(6.35158530413795,-2.10466688812074,1.23276228523846));
#18662=CARTESIAN_POINT('Ctrl Pts',(6.2803525799754,-2.14408667431198,1.2285451896322));
#18663=CARTESIAN_POINT('Ctrl Pts',(6.20912141897576,-2.18350559545771,1.22432818656778));
#18664=CARTESIAN_POINT('Ctrl Pts',(6.13592388250251,-2.21937098687598,1.22011118350336));
#18665=CARTESIAN_POINT('Ctrl Pts',(6.06115152472861,-2.25149590597135,1.21589418043894));
#18666=CARTESIAN_POINT('Ctrl Pts',(5.98606960786372,-2.28375382288903,1.21165971889556));
#18667=CARTESIAN_POINT('Ctrl Pts',(5.90940023074154,-2.312240032171,1.20742525735218));
#18668=CARTESIAN_POINT('Ctrl Pts',(5.83155902235847,-2.33681448612258,1.2031907958088));
#18669=CARTESIAN_POINT('Ctrl Pts',(5.7539263582488,-2.36132310268867,1.19896767880546));
#18670=CARTESIAN_POINT('Ctrl Pts',(5.67512859653247,-2.38194081858851,1.19474456180213));
#18671=CARTESIAN_POINT('Ctrl Pts',(5.59559036205877,-2.39857956601335,1.19052144479879));
#18672=CARTESIAN_POINT('Ctrl Pts',(5.51573163278742,-2.41528535832578,1.18628131098539));
#18673=CARTESIAN_POINT('Ctrl Pts',(5.43512691782418,-2.42797998358737,1.18204117717198));
#18674=CARTESIAN_POINT('Ctrl Pts',(5.3542114637486,-2.4366268204207,1.17780104335858));
#18675=CARTESIAN_POINT('Ctrl Pts',(5.27329600967303,-2.44527365725402,1.17356090954517));
#18676=CARTESIAN_POINT('Ctrl Pts',(5.1920702865861,-2.44987274134868,1.16932077573176));
#18677=CARTESIAN_POINT('Ctrl Pts',(5.11096794520243,-2.45044005095549,1.16508064191836));
#18678=CARTESIAN_POINT('Ctrl Pts',(5.03001946683071,-2.45100628429295,1.16084855225939));
#18679=CARTESIAN_POINT('Ctrl Pts',(4.94889190026816,-2.44755815532954,1.15661646260043));
#18680=CARTESIAN_POINT('Ctrl Pts',(4.8680161635081,-2.44007369682082,1.15238437294146));
#18681=CARTESIAN_POINT('Ctrl Pts',(4.78725601749221,-2.43259993539089,1.14815833194941));
#18682=CARTESIAN_POINT('Ctrl Pts',(4.70674744527386,-2.4211013444984,1.14393229095736));
#18683=CARTESIAN_POINT('Ctrl Pts',(4.62692183838578,-2.40560796367452,1.13970624996531));
#18684=CARTESIAN_POINT('Ctrl Pts',(4.54707427483165,-2.3901103212734,1.13547904656717));
#18685=CARTESIAN_POINT('Ctrl Pts',(4.46791051861151,-2.37061571435661,1.13125184316904));
#18686=CARTESIAN_POINT('Ctrl Pts',(4.38985766079624,-2.34720625437829,1.12702463977091));
#18687=CARTESIAN_POINT('Ctrl Pts',(4.31196589498755,-2.32384510879852,1.12280616082819));
#18688=CARTESIAN_POINT('Ctrl Pts',(4.23518089894569,-2.29658536317591,1.11858768188546));
#18689=CARTESIAN_POINT('Ctrl Pts',(4.15991560342905,-2.26555941502226,1.11436920294274));
#18690=CARTESIAN_POINT('Ctrl Pts',(4.08467498913727,-2.23454364099199,1.11015210733648));
#18691=CARTESIAN_POINT('Ctrl Pts',(4.01095351498968,-2.199764294038,1.10593501173021));
#18692=CARTESIAN_POINT('Ctrl Pts',(3.93914551097837,-2.16140244977957,1.10171791612395));
#18693=CARTESIAN_POINT('Ctrl Pts',(3.86733908275442,-2.12304144735082,1.09750091305954));
#18694=CARTESIAN_POINT('Ctrl Pts',(3.79744645050496,-2.08109832390305,1.09328390999513));
#18695=CARTESIAN_POINT('Ctrl Pts',(3.72983736708083,-2.03580011475001,1.08906690693073));
#18696=CARTESIAN_POINT('Ctrl Pts',(3.66194838066793,-1.9903143700842,1.08483244538734));
#18697=CARTESIAN_POINT('Ctrl Pts',(3.59636229036309,-1.9414459522043,1.08059798384396));
#18698=CARTESIAN_POINT('Ctrl Pts',(3.53342257406746,-1.88946759495649,1.07636352230058));
#18699=CARTESIAN_POINT('Ctrl Pts',(3.47065147947842,-1.83762849285346,1.07214040529724));
#18700=CARTESIAN_POINT('Ctrl Pts',(3.41051291467663,-1.78269643951463,1.0679172882939));
#18701=CARTESIAN_POINT('Ctrl Pts',(3.35331161785885,-1.72497997478028,1.06369417129057));
#18702=CARTESIAN_POINT('Ctrl Pts',(3.29587983166491,-1.6670309448299,1.05945403747716));
#18703=CARTESIAN_POINT('Ctrl Pts',(3.24140934282728,-1.6062753736399,1.05521390366376));
#18704=CARTESIAN_POINT('Ctrl Pts',(3.19016748139266,-1.54305868176037,1.05097376985035));
#18705=CARTESIAN_POINT('Ctrl Pts',(3.13892561995805,-1.47984198988085,1.04673363603695));
#18706=CARTESIAN_POINT('Ctrl Pts',(3.09091261150796,-1.41416459129448,1.04249350222354));
#18707=CARTESIAN_POINT('Ctrl Pts',(3.04635076874628,-1.34639915919387,1.03825336841014));
#18708=CARTESIAN_POINT('Ctrl Pts',(3.00187346632254,-1.27876228803632,1.03402127875118));
#18709=CARTESIAN_POINT('Ctrl Pts',(2.96066829775093,-1.20879296809767,1.02978918909222));
#18710=CARTESIAN_POINT('Ctrl Pts',(2.9229879400944,-1.1368409524031,1.02555709943326));
#18711=CARTESIAN_POINT('Ctrl Pts',(2.88536143666856,-1.06499177332402,1.02133105844122));
#18712=CARTESIAN_POINT('Ctrl Pts',(2.85124995232455,-0.991165934832547,
1.01710501744917));
#18713=CARTESIAN_POINT('Ctrl Pts',(2.82086276928575,-0.915741857301956,
1.01287897645713));
#18714=CARTESIAN_POINT('Ctrl Pts',(2.79046722801125,-0.840297033780658,
1.008651773059));
#18715=CARTESIAN_POINT('Ctrl Pts',(2.76379827099131,-0.763253495899821,
1.00442456966086));
#18716=CARTESIAN_POINT('Ctrl Pts',(2.74101913587287,-0.685014359702723,
1.00019736626273));
#18717=CARTESIAN_POINT('Ctrl Pts',(2.71828701423593,-0.606936699969137,
0.995978887320007));
#18718=CARTESIAN_POINT('Ctrl Pts',(2.69942882816898,-0.527668811345698,
0.991760408377288));
#18719=CARTESIAN_POINT('Ctrl Pts',(2.68455791009646,-0.447629258849976,
0.987541929434567));
#18720=CARTESIAN_POINT('Ctrl Pts',(2.66969186854068,-0.367615953168051,
0.983324833828307));
#18721=CARTESIAN_POINT('Ctrl Pts',(2.65881058318793,-0.286831942657926,
0.979107738222049));
#18722=CARTESIAN_POINT('Ctrl Pts',(2.65197641713918,-0.205706640135218,
0.974890642615789));
#18723=CARTESIAN_POINT('Ctrl Pts',(2.64514240106244,-0.124583117862515,
0.970673639551366));
#18724=CARTESIAN_POINT('Ctrl Pts',(2.64235536557133,-0.0431187816132713,
0.966456636486941));
#18725=CARTESIAN_POINT('Ctrl Pts',(2.64362573752005,0.0382526019873604,
0.962239633422518));
#18726=CARTESIAN_POINT('Ctrl Pts',(2.64490136883462,0.119960864780826,0.958005171879135));
#18727=CARTESIAN_POINT('Ctrl Pts',(2.65026808016463,0.201574931687601,0.953770710335755));
#18728=CARTESIAN_POINT('Ctrl Pts',(2.65968365842976,0.282658249302825,0.949536248792372));
#18729=CARTESIAN_POINT('Ctrl Pts',(2.66907401143222,0.363524336714318,0.945313131789035));
#18730=CARTESIAN_POINT('Ctrl Pts',(2.68249144681184,0.44386206065688,0.941090014785696));
#18731=CARTESIAN_POINT('Ctrl Pts',(2.6998426393241,0.5232479207169,0.93686689778236));
#18732=CARTESIAN_POINT('Ctrl Pts',(2.71726374748095,0.602953661590489,0.932626763968954));
#18733=CARTESIAN_POINT('Ctrl Pts',(2.73865024951101,0.681699398718007,0.928386630155549));
#18734=CARTESIAN_POINT('Ctrl Pts',(2.76385752974272,0.759072982832998,0.924146496342143));
#18735=CARTESIAN_POINT('Ctrl Pts',(2.78906480997443,0.836446566947988,0.919906362528737));
#18736=CARTESIAN_POINT('Ctrl Pts',(2.81809264355031,0.912447583674052,0.91566622871533));
#18737=CARTESIAN_POINT('Ctrl Pts',(2.85074906954626,0.986686855352023,0.911426094901924));
#18738=CARTESIAN_POINT('Ctrl Pts',(2.8833435415224,1.06078528426571,0.907194005242962));
#18739=CARTESIAN_POINT('Ctrl Pts',(2.91967443931081,1.13340509916211,0.902961915583999));
#18740=CARTESIAN_POINT('Ctrl Pts',(2.95958554566783,1.20414409480807,0.898729825925037));
#18741=CARTESIAN_POINT('Ctrl Pts',(2.99943960952148,1.27478198753391,0.894503784932993));
#18742=CARTESIAN_POINT('Ctrl Pts',(3.04286349264554,1.34354399861238,0.890277743940949));
#18743=CARTESIAN_POINT('Ctrl Pts',(3.08965332706236,1.41004876355166,0.886051702948905));
#18744=CARTESIAN_POINT('Ctrl Pts',(3.13645603139418,1.47657182115393,0.881824499550772));
#18745=CARTESIAN_POINT('Ctrl Pts',(3.18662632694945,1.54083597478271,0.87759729615264));
#18746=CARTESIAN_POINT('Ctrl Pts',(3.23991458832617,1.60248508368995,0.873370092754507));
#18747=CARTESIAN_POINT('Ctrl Pts',(3.29309286893867,1.66400695601759,0.869151613811782));
#18748=CARTESIAN_POINT('Ctrl Pts',(3.34937597300426,1.72292419920925,0.864933134869057));
#18749=CARTESIAN_POINT('Ctrl Pts',(3.4084741804018,1.77891416304601,0.860714655926333));
#18750=CARTESIAN_POINT('Ctrl Pts',(3.46755300813528,1.8348857664834,0.856497560320065));
#18751=CARTESIAN_POINT('Ctrl Pts',(3.52944476885911,1.88793167753747,0.852280464713795));
#18752=CARTESIAN_POINT('Ctrl Pts',(3.59382293133738,1.93776613078952,0.848063369107527));
#18753=CARTESIAN_POINT('Ctrl Pts',(3.65819968107221,1.98759949045183,0.843846366043108));
#18754=CARTESIAN_POINT('Ctrl Pts',(3.72506235591399,2.03422124889516,0.839629362978691));
#18755=CARTESIAN_POINT('Ctrl Pts',(3.79405253868528,2.07738686710156,0.835412359914272));
#18756=CARTESIAN_POINT('Ctrl Pts',(3.86332834222469,2.12073119185045,0.831177898370891));
#18757=CARTESIAN_POINT('Ctrl Pts',(3.93474891393538,2.16059043725314,0.82694343682751));
#18758=CARTESIAN_POINT('Ctrl Pts',(4.00792488348466,2.19676273314479,0.822708975284129));
#18759=CARTESIAN_POINT('Ctrl Pts',(4.08090480739543,2.23283811988869,0.818485858280795));
#18760=CARTESIAN_POINT('Ctrl Pts',(4.15563029003622,2.26524613902794,0.814262741277461));
#18761=CARTESIAN_POINT('Ctrl Pts',(4.23169513360672,2.29383491709998,0.810039624274127));
#18762=CARTESIAN_POINT('Ctrl Pts',(4.30806647614351,2.32253889202927,0.805799490460723));
#18763=CARTESIAN_POINT('Ctrl Pts',(4.38578754448091,2.34739264670183,0.801559356647321));
#18764=CARTESIAN_POINT('Ctrl Pts',(4.46443378799616,2.368293528894,0.797319222833917));
#18765=CARTESIAN_POINT('Ctrl Pts',(4.54308003151142,2.38919441108618,0.793079089020514));
#18766=CARTESIAN_POINT('Ctrl Pts',(4.62265098016665,2.40614238428662,0.788838955207109));
#18767=CARTESIAN_POINT('Ctrl Pts',(4.7027156287509,2.41908702275893,0.784598821393705));
#18768=CARTESIAN_POINT('Ctrl Pts',(4.78262838297833,2.43200710335745,0.780366731734741));
#18769=CARTESIAN_POINT('Ctrl Pts',(4.86333110127275,2.44098724308894,0.776134642075777));
#18770=CARTESIAN_POINT('Ctrl Pts',(4.94440127321378,2.44593993297403,0.771902552416813));
#18771=CARTESIAN_POINT('Ctrl Pts',(5.02535557651595,2.45088554428235,0.767676511424783));
#18772=CARTESIAN_POINT('Ctrl Pts',(5.10667583045401,2.45181511005929,0.763450470432753));
#18773=CARTESIAN_POINT('Ctrl Pts',(5.18793111540846,2.44869244592307,0.759224429440723));
#18774=CARTESIAN_POINT('Ctrl Pts',(5.26920875027372,2.44556892287331,0.754997226042588));
#18775=CARTESIAN_POINT('Ctrl Pts',(5.35042091607538,2.43839089225648,0.750770022644452));
#18776=CARTESIAN_POINT('Ctrl Pts',(5.43113299206482,2.42717428764143,0.746542819246317));
#18777=CARTESIAN_POINT('Ctrl Pts',(5.51167848773102,2.41598083279176,0.742324340303598));
#18778=CARTESIAN_POINT('Ctrl Pts',(5.59172549204092,2.40076549679287,0.73810586136088));
#18779=CARTESIAN_POINT('Ctrl Pts',(5.67084570003744,2.38159607179844,0.73388738241816));
#18780=CARTESIAN_POINT('Ctrl Pts',(5.74993996269457,2.3624329329002,0.729670286811894));
#18781=CARTESIAN_POINT('Ctrl Pts',(5.82810758131809,2.33931838934476,0.725453191205628));
#18782=CARTESIAN_POINT('Ctrl Pts',(5.90493120065128,2.31237118081487,0.721236095599362));
#18783=CARTESIAN_POINT('Ctrl Pts',(5.98175313413231,2.28542456362669,0.717019092534944));
#18784=CARTESIAN_POINT('Ctrl Pts',(6.05723068884862,2.25464560358275,0.712802089470526));
#18785=CARTESIAN_POINT('Ctrl Pts',(6.13096378062545,2.22020221392695,0.708585086406108));
#18786=CARTESIAN_POINT('Ctrl Pts',(6.20500212891083,2.18561622793326,0.704350624862723));
#18787=CARTESIAN_POINT('Ctrl Pts',(6.27728110634971,2.14733559408323,0.700116163319338));
#18788=CARTESIAN_POINT('Ctrl Pts',(6.34741961762619,2.10557740033057,0.695881701775953));
#18789=CARTESIAN_POINT('Ctrl Pts',(6.4173702209143,2.06393108089692,0.69165858477262));
#18790=CARTESIAN_POINT('Ctrl Pts',(6.48519144589893,2.0188261044308,0.687435467769287));
#18791=CARTESIAN_POINT('Ctrl Pts',(6.55053501525511,1.97052086037958,0.683212350765954));
#18792=CARTESIAN_POINT('Ctrl Pts',(6.61614188281229,1.92202097309134,0.678972216952543));
#18793=CARTESIAN_POINT('Ctrl Pts',(6.679250726288,1.87029527870244,0.674732083139132));
#18794=CARTESIAN_POINT('Ctrl Pts',(6.73954460630417,1.8156443269441,0.67049194932572));
#18795=CARTESIAN_POINT('Ctrl Pts',(6.79983848632033,1.76099337518576,0.666251815512309));
#18796=CARTESIAN_POINT('Ctrl Pts',(6.85731711672739,1.70341754074066,0.662011681698898));
#18797=CARTESIAN_POINT('Ctrl Pts',(6.91170388622064,1.64325118035374,0.657771547885487));
#18798=CARTESIAN_POINT('Ctrl Pts',(6.96540918855505,1.58383870549914,0.653584543021816));
#18799=CARTESIAN_POINT('Ctrl Pts',(7.01630972610991,1.52166769401119,0.649397538158145));
#18800=CARTESIAN_POINT('Ctrl Pts',(7.06410492824259,1.45703663236438,0.645210533294474));
#18801=CARTESIAN_POINT('Ctrl Pts',(7.11183727288974,1.3924905697518,0.641029034937438));
#18802=CARTESIAN_POINT('Ctrl Pts',(7.15647210340004,1.32549125271794,0.636847536580401));
#18803=CARTESIAN_POINT('Ctrl Pts',(7.19774685860031,1.25637260902529,0.632666038223364));
#18804=CARTESIAN_POINT('Ctrl Pts',(7.23898061525822,1.18732262143072,0.628488693381877));
#18805=CARTESIAN_POINT('Ctrl Pts',(7.27686067727665,1.11615789015537,0.62431134854039));
#18806=CARTESIAN_POINT('Ctrl Pts',(7.31116678822456,1.04324263857501,0.620134003698903));
#18807=CARTESIAN_POINT('Ctrl Pts',(7.34544985857217,0.970376358187296,0.615959464437243));
#18808=CARTESIAN_POINT('Ctrl Pts',(7.37616354180696,0.895762320608089,0.611784925175584));
#18809=CARTESIAN_POINT('Ctrl Pts',(7.40313346543961,0.819789373349364,0.607610385913924));
#18810=CARTESIAN_POINT('Ctrl Pts',(7.43010088435227,0.743823481763554,0.603436234345314));
#18811=CARTESIAN_POINT('Ctrl Pts',(7.45332506264281,0.666499374329233,0.599262082776703));
#18812=CARTESIAN_POINT('Ctrl Pts',(7.47268021978743,0.588224743025335,0.595087931208093));
#18813=CARTESIAN_POINT('Ctrl Pts',(7.49203419135605,0.509954906336266,0.590914035321927));
#18814=CARTESIAN_POINT('Ctrl Pts',(7.50751950632686,0.430735124923251,0.58674013943576));
#18815=CARTESIAN_POINT('Ctrl Pts',(7.51906109382869,0.350985176540635,0.582566243549594));
#18816=CARTESIAN_POINT('Ctrl Pts',(7.53061059387695,0.271180554122189,0.578389486172757));
#18817=CARTESIAN_POINT('Ctrl Pts',(7.5382109109335,0.190845511248738,0.574212728795923));
#18818=CARTESIAN_POINT('Ctrl Pts',(7.54183875718163,0.110405832285044,0.570035971419086));
#18819=CARTESIAN_POINT('Ctrl Pts',(7.54353131309223,0.0728770494303689,
0.568087323405428));
#18820=CARTESIAN_POINT('Ctrl Pts',(7.54435994289275,0.0353255197735597,
0.566138675391768));
#18821=CARTESIAN_POINT('Ctrl Pts',(7.54432616288253,-0.00220558096774611,
0.56419002737811));
#18822=CARTESIAN_POINT('',(7.54432706310264,0.000672762683496843,-0.235809972659579));
#18823=CARTESIAN_POINT('Ctrl Pts',(7.5443261628818,-0.00220558177831103,
0.564190027336024));
#18824=CARTESIAN_POINT('Ctrl Pts',(7.54423010976538,-0.108924846857774,
0.558649068509566));
#18825=CARTESIAN_POINT('Ctrl Pts',(7.53715829815171,-0.215335078947692,
0.553108109683107));
#18826=CARTESIAN_POINT('Ctrl Pts',(7.52325695306015,-0.320657306947822,
0.547567150856648));
#18827=CARTESIAN_POINT('Ctrl Pts',(7.50935560796858,-0.425979534947946,
0.542026192030189));
#18828=CARTESIAN_POINT('Ctrl Pts',(7.48862491996705,-0.530214102573748,
0.53648523320373));
#18829=CARTESIAN_POINT('Ctrl Pts',(7.46126409479691,-0.632607768076282,
0.530944274377271));
#18830=CARTESIAN_POINT('Ctrl Pts',(7.4403663641171,-0.710814299921907,0.526712184718308));
#18831=CARTESIAN_POINT('Ctrl Pts',(7.4155502457108,-0.788130093372859,0.522480095059343));
#18832=CARTESIAN_POINT('Ctrl Pts',(7.38690870987743,-0.864133806050284,
0.518248005400379));
#18833=CARTESIAN_POINT('Ctrl Pts',(7.35830810963951,-0.940028891269548,
0.514021964408331));
#18834=CARTESIAN_POINT('Ctrl Pts',(7.32589311339092,-1.0146151890148,0.509795923416282));
#18835=CARTESIAN_POINT('Ctrl Pts',(7.28980696566903,-1.08748467719048,0.505569882424235));
#18836=CARTESIAN_POINT('Ctrl Pts',(7.25371089216605,-1.16037420869669,0.501342679026102));
#18837=CARTESIAN_POINT('Ctrl Pts',(7.21394179334593,-1.23154554265047,0.497115475627969));
#18838=CARTESIAN_POINT('Ctrl Pts',(7.17069198614245,-1.30060859794395,0.492888272229837));
#18839=CARTESIAN_POINT('Ctrl Pts',(7.12753144150309,-1.36952911513612,0.488669793287112));
#18840=CARTESIAN_POINT('Ctrl Pts',(7.08090476714694,-1.43634964032899,0.484451314344387));
#18841=CARTESIAN_POINT('Ctrl Pts',(7.03104901840703,-1.5007070679161,0.480232835401663));
#18842=CARTESIAN_POINT('Ctrl Pts',(6.98120961851607,-1.56504339121959,0.476015739795398));
#18843=CARTESIAN_POINT('Ctrl Pts',(6.92814353145569,-1.626917853877,0.471798644189134));
#18844=CARTESIAN_POINT('Ctrl Pts',(6.87212982415058,-1.68599818164299,0.46758154858287));
#18845=CARTESIAN_POINT('Ctrl Pts',(6.81611734603551,-1.74507721292363,0.463364545518452));
#18846=CARTESIAN_POINT('Ctrl Pts',(6.75715769683451,-1.80136189479566,0.459147542454036));
#18847=CARTESIAN_POINT('Ctrl Pts',(6.69556775059078,-1.85455582711549,0.454930539389618));
#18848=CARTESIAN_POINT('Ctrl Pts',(6.63372282070953,-1.90796998340342,0.450696077846238));
#18849=CARTESIAN_POINT('Ctrl Pts',(6.56922611707182,-1.95826742595693,0.446461616302857));
#18850=CARTESIAN_POINT('Ctrl Pts',(6.50243161924799,-2.00518919670368,0.442227154759477));
#18851=CARTESIAN_POINT('Ctrl Pts',(6.43581607047058,-2.05198525939953,0.438004037756142));
#18852=CARTESIAN_POINT('Ctrl Pts',(6.36691544130841,-2.09542350017295,0.433780920752806));
#18853=CARTESIAN_POINT('Ctrl Pts',(6.29610797575104,-2.13529180187246,0.429557803749471));
#18854=CARTESIAN_POINT('Ctrl Pts',(6.22501519553347,-2.17532075062892,0.425317669936068));
#18855=CARTESIAN_POINT('Ctrl Pts',(6.152000605206,-2.21175072707879,0.421077536122665));
#18856=CARTESIAN_POINT('Ctrl Pts',(6.07746810223484,-2.24441545570653,0.416837402309262));
#18857=CARTESIAN_POINT('Ctrl Pts',(6.0029355992637,-2.27708018433426,0.41259726849586));
#18858=CARTESIAN_POINT('Ctrl Pts',(5.9268856425996,-2.30597955728391,0.408357134682459));
#18859=CARTESIAN_POINT('Ctrl Pts',(5.84973648336748,-2.33099792749201,0.404117000869056));
#18860=CARTESIAN_POINT('Ctrl Pts',(5.77273368738216,-2.35596883419008,0.399884911210094));
#18861=CARTESIAN_POINT('Ctrl Pts',(5.69434857887907,-2.3771666268737,0.395652821551131));
#18862=CARTESIAN_POINT('Ctrl Pts',(5.61498535135581,-2.39444030722076,0.391420731892169));
#18863=CARTESIAN_POINT('Ctrl Pts',(5.53573555283973,-2.41168929935297,0.387194690900119));
#18864=CARTESIAN_POINT('Ctrl Pts',(5.45551086207904,-2.42502522022467,0.38296864990807));
#18865=CARTESIAN_POINT('Ctrl Pts',(5.37473162020496,-2.43434651019169,0.37874260891602));
#18866=CARTESIAN_POINT('Ctrl Pts',(5.29393015935994,-2.44367036405342,0.374515405517887));
#18867=CARTESIAN_POINT('Ctrl Pts',(5.21257429382919,-2.448977259706,0.370288202119756));
#18868=CARTESIAN_POINT('Ctrl Pts',(5.1310959806596,-2.45021657913494,0.366060998721624));
#18869=CARTESIAN_POINT('Ctrl Pts',(5.04978582923741,-2.45145334075294,0.3618425197789));
#18870=CARTESIAN_POINT('Ctrl Pts',(4.968354199392,-2.4486392673208,0.357624040836176));
#18871=CARTESIAN_POINT('Ctrl Pts',(4.88723472502712,-2.44177595567052,0.353405561893452));
#18872=CARTESIAN_POINT('Ctrl Pts',(4.80614185160729,-2.4349148946583,0.349188466287189));
#18873=CARTESIAN_POINT('Ctrl Pts',(4.72536139306099,-2.4240072715402,0.344971370680927));
#18874=CARTESIAN_POINT('Ctrl Pts',(4.64532394146638,-2.40910670520083,0.340754275074664));
#18875=CARTESIAN_POINT('Ctrl Pts',(4.56528824624972,-2.3942064658462,0.336537272010249));
#18876=CARTESIAN_POINT('Ctrl Pts',(4.48599598219529,-2.37531354366744,0.332320268945834));
#18877=CARTESIAN_POINT('Ctrl Pts',(4.40786818142602,-2.35253279168468,0.32810326588142));
#18878=CARTESIAN_POINT('Ctrl Pts',(4.32941692996307,-2.32965772692261,0.323868804338038));
#18879=CARTESIAN_POINT('Ctrl Pts',(4.25214026067396,-2.30286269210011,0.319634342794656));
#18880=CARTESIAN_POINT('Ctrl Pts',(4.17644794826881,-2.27230403780522,0.315399881251274));
#18881=CARTESIAN_POINT('Ctrl Pts',(4.10095842303284,-2.24182725315866,0.311176764247939));
#18882=CARTESIAN_POINT('Ctrl Pts',(4.02704518323412,-2.20760722330935,0.306953647244604));
#18883=CARTESIAN_POINT('Ctrl Pts',(3.9550918770022,-2.16984612717385,0.30273053024127));
#18884=CARTESIAN_POINT('Ctrl Pts',(3.88284863901013,-2.13193287484648,0.298490396427865));
#18885=CARTESIAN_POINT('Ctrl Pts',(3.812581564407,-2.09045020603706,0.29425026261446));
#18886=CARTESIAN_POINT('Ctrl Pts',(3.74464976856326,-2.04564675071359,0.290010128801055));
#18887=CARTESIAN_POINT('Ctrl Pts',(3.67671797271953,-2.00084329539013,0.285769994987649));
#18888=CARTESIAN_POINT('Ctrl Pts',(3.6111217956416,-1.95271938014768,0.281529861174244));
#18889=CARTESIAN_POINT('Ctrl Pts',(3.54818565973068,-1.90156320344629,0.277289727360839));
#18890=CARTESIAN_POINT('Ctrl Pts',(3.48536892288111,-1.85050407749949,0.273057637701877));
#18891=CARTESIAN_POINT('Ctrl Pts',(3.42496777694521,-1.79623370603101,0.268825548042916));
#18892=CARTESIAN_POINT('Ctrl Pts',(3.36732867519252,-1.73900927187232,0.264593458383954));
#18893=CARTESIAN_POINT('Ctrl Pts',(3.30977195348276,-1.68186662509753,0.260367417391908));
#18894=CARTESIAN_POINT('Ctrl Pts',(3.25496976256562,-1.62177862576476,0.256141376399862));
#18895=CARTESIAN_POINT('Ctrl Pts',(3.20323583655671,-1.55904288424455,0.251915335407816));
#18896=CARTESIAN_POINT('Ctrl Pts',(3.1514876807212,-1.49628988676115,0.247688132009683));
#18897=CARTESIAN_POINT('Ctrl Pts',(3.10280982282825,-1.43088800491758,0.243460928611549));
#18898=CARTESIAN_POINT('Ctrl Pts',(3.05747955297212,-1.36317228987018,0.239233725213416));
#18899=CARTESIAN_POINT('Ctrl Pts',(3.0122428395127,-1.29559633217082,0.235015246270693));
#18900=CARTESIAN_POINT('Ctrl Pts',(2.97034018911734,-1.22571645496426,0.230796767327972));
#18901=CARTESIAN_POINT('Ctrl Pts',(2.93200597649514,-1.15389749987109,0.22657828838525));
#18902=CARTESIAN_POINT('Ctrl Pts',(2.89368433454466,-1.08210209586836,0.222361192778988));
#18903=CARTESIAN_POINT('Ctrl Pts',(2.85892902515504,-1.00836928638529,0.218144097172723));
#18904=CARTESIAN_POINT('Ctrl Pts',(2.82792910448838,-0.933089638048898,
0.213927001566462));
#18905=CARTESIAN_POINT('Ctrl Pts',(2.79692986409794,-0.85781164168302,0.209709998502045));
#18906=CARTESIAN_POINT('Ctrl Pts',(2.76968602445696,-0.780987304074721,
0.205492995437632));
#18907=CARTESIAN_POINT('Ctrl Pts',(2.74633844139471,-0.703027017523819,
0.201275992373215));
#18908=CARTESIAN_POINT('Ctrl Pts',(2.72289419886089,-0.624743973791531,
0.197041530829833));
#18909=CARTESIAN_POINT('Ctrl Pts',(2.7033786904847,-0.545316003652663,0.192807069286448));
#18910=CARTESIAN_POINT('Ctrl Pts',(2.68788342794357,-0.465172043503821,
0.188572607743065));
#18911=CARTESIAN_POINT('Ctrl Pts',(2.67242967873884,-0.385242796927489,
0.184349490739732));
#18912=CARTESIAN_POINT('Ctrl Pts',(2.66097468660251,-0.304601860576383,
0.180126373736401));
#18913=CARTESIAN_POINT('Ctrl Pts',(2.65355729498284,-0.223681152716059,
0.175903256733068));
#18914=CARTESIAN_POINT('Ctrl Pts',(2.64611001540497,-0.142434379460049,
0.17166312291966));
#18915=CARTESIAN_POINT('Ctrl Pts',(2.64273295449464,-0.0609060466888589,
0.167422989106253));
#18916=CARTESIAN_POINT('Ctrl Pts',(2.64341263115474,0.0204672691777126,
0.163182855292845));
#18917=CARTESIAN_POINT('Ctrl Pts',(2.64409230781484,0.101840585044284,0.158942721479438));
#18918=CARTESIAN_POINT('Ctrl Pts',(2.64882863273646,0.183058421088749,0.15470258766603));
#18919=CARTESIAN_POINT('Ctrl Pts',(2.65755605430675,0.263691812006178,0.150462453852623));
#18920=CARTESIAN_POINT('Ctrl Pts',(2.66626691868095,0.344172229579254,0.146230364193661));
#18921=CARTESIAN_POINT('Ctrl Pts',(2.67898623277376,0.424370675316747,0.141998274534699));
#18922=CARTESIAN_POINT('Ctrl Pts',(2.69568645370933,0.503856551649249,0.137766184875736));
#18923=CARTESIAN_POINT('Ctrl Pts',(2.7123628060405,0.583228823680029,0.13354014388369));
#18924=CARTESIAN_POINT('Ctrl Pts',(2.73300867017065,0.661890098062354,0.129314102891644));
#18925=CARTESIAN_POINT('Ctrl Pts',(2.75754478458903,0.739415264644778,0.125088061899598));
#18926=CARTESIAN_POINT('Ctrl Pts',(2.78208764786025,0.816961755139046,0.120860858501465));
#18927=CARTESIAN_POINT('Ctrl Pts',(2.81052282522853,0.893371052255047,0.116633655103332));
#18928=CARTESIAN_POINT('Ctrl Pts',(2.8427198187342,0.968228283293912,0.112406451705199));
#18929=CARTESIAN_POINT('Ctrl Pts',(2.87485036139572,1.04293101772762,0.108187972762477));
#18930=CARTESIAN_POINT('Ctrl Pts',(2.9107270471507,1.11608764946936,0.103969493819754));
#18931=CARTESIAN_POINT('Ctrl Pts',(2.95017104523237,1.18730313362396,0.0997510148770315));
#18932=CARTESIAN_POINT('Ctrl Pts',(2.98960210871808,1.25849526458015,0.0955339192707685));
#18933=CARTESIAN_POINT('Ctrl Pts',(3.03259793643195,1.32774710588591,0.0913168236645044));
#18934=CARTESIAN_POINT('Ctrl Pts',(3.07893347085776,1.39468766746458,0.0870997280582415));
#18935=CARTESIAN_POINT('Ctrl Pts',(3.12526798847574,1.46162676006941,0.0828827249938237));
#18936=CARTESIAN_POINT('Ctrl Pts',(3.1749418016699,1.52625429236095,0.078665721929407));
#18937=CARTESIAN_POINT('Ctrl Pts',(3.22768701133789,1.58822895469187,0.0744487188649892));
#18938=CARTESIAN_POINT('Ctrl Pts',(3.28065058725305,1.6504601933928,0.0702142573216073));
#18939=CARTESIAN_POINT('Ctrl Pts',(3.33671074912355,1.710016181829,0.0659797957782236));
#18940=CARTESIAN_POINT('Ctrl Pts',(3.39555721020267,1.76658694749482,0.0617453342348417));
#18941=CARTESIAN_POINT('Ctrl Pts',(3.45424601580953,1.8230061545008,0.0575222172315082));
#18942=CARTESIAN_POINT('Ctrl Pts',(3.51570583031406,1.87645583795634,0.0532991002281749));
#18943=CARTESIAN_POINT('Ctrl Pts',(3.57959523468432,1.92666861191147,0.0490759832248413));
#18944=CARTESIAN_POINT('Ctrl Pts',(3.64374207778028,1.97708371538693,0.0448358494114354));
#18945=CARTESIAN_POINT('Ctrl Pts',(3.71033774211444,2.0242355030172,0.0405957155980312));
#18946=CARTESIAN_POINT('Ctrl Pts',(3.77900845618789,2.06789797573829,0.0363555817846253));
#18947=CARTESIAN_POINT('Ctrl Pts',(3.84767917026135,2.11156044845939,0.0321154479712191));
#18948=CARTESIAN_POINT('Ctrl Pts',(3.91842449697453,2.15173342960033,0.0278753141578127));
#18949=CARTESIAN_POINT('Ctrl Pts',(3.99084874874298,2.18823876309949,0.0236351803444066));
#18950=CARTESIAN_POINT('Ctrl Pts',(4.06313560110558,2.22467484063797,0.019403090685444));
#18951=CARTESIAN_POINT('Ctrl Pts',(4.13736469436463,2.25759312375906,0.0151710010264822));
#18952=CARTESIAN_POINT('Ctrl Pts',(4.21315963169909,2.28678266623765,0.0109389113675196));
#18953=CARTESIAN_POINT('Ctrl Pts',(4.28884623996522,2.31593048988839,0.00671287037547256));
#18954=CARTESIAN_POINT('Ctrl Pts',(4.36609381744558,2.34135999178187,0.00248682938342509));
#18955=CARTESIAN_POINT('Ctrl Pts',(4.44450245996956,2.362906618941,-0.00173921160862189));
#18956=CARTESIAN_POINT('Ctrl Pts',(4.52293266941243,2.38445917267079,-0.0059664150067547));
#18957=CARTESIAN_POINT('Ctrl Pts',(4.60252415455784,2.4021265292946,-0.010193618404886));
#18958=CARTESIAN_POINT('Ctrl Pts',(4.68285775296697,2.41579270638442,-0.0144208218030188));
#18959=CARTESIAN_POINT('Ctrl Pts',(4.7630255521866,2.42943067807664,-0.018639300745742));
#18960=CARTESIAN_POINT('Ctrl Pts',(4.84393195051431,2.43908386709367,-0.0228577796884664));
#18961=CARTESIAN_POINT('Ctrl Pts',(4.92514815533413,2.44468763749459,-0.0270762586311895));
#18962=CARTESIAN_POINT('Ctrl Pts',(5.00633772748878,2.45028957029004,-0.031293354237453));
#18963=CARTESIAN_POINT('Ctrl Pts',(5.08783644115347,2.45184468959132,-0.0355104498437151));
#18964=CARTESIAN_POINT('Ctrl Pts',(5.16921056632157,2.44934023593412,-0.0397275454499786));
#18965=CARTESIAN_POINT('Ctrl Pts',(5.25058290577918,2.44683583723579,-0.0439445485143945));
#18966=CARTESIAN_POINT('Ctrl Pts',(5.33183019774275,2.44027205814737,-0.0481615515788123));
#18967=CARTESIAN_POINT('Ctrl Pts',(5.41252033681973,2.42968823229451,-0.0523785546432283));
#18968=CARTESIAN_POINT('Ctrl Pts',(5.4935445347234,2.41906058918607,-0.0566130161866101));
#18969=CARTESIAN_POINT('Ctrl Pts',(5.57400648719356,2.40437959084643,-0.0608474777299928));
#18970=CARTESIAN_POINT('Ctrl Pts',(5.65347735077864,2.38573718352883,-0.0650819392733748));
#18971=CARTESIAN_POINT('Ctrl Pts',(5.73273530408329,2.36714472105883,-0.0693050562767073));
#18972=CARTESIAN_POINT('Ctrl Pts',(5.81100703423365,2.344612217432,-0.0735281732800393));
#18973=CARTESIAN_POINT('Ctrl Pts',(5.88788252018853,2.31828089923005,-0.0777512902833717));
#18974=CARTESIAN_POINT('Ctrl Pts',(5.96506777154723,2.29184348047714,-0.0819914240967782));
#18975=CARTESIAN_POINT('Ctrl Pts',(6.04084506816538,2.26157675118435,-0.0862315579101823));
#18976=CARTESIAN_POINT('Ctrl Pts',(6.1148215411939,2.22767159031258,-0.0904716917235886));
#18977=CARTESIAN_POINT('Ctrl Pts',(6.18879801422243,2.19376642944081,-0.0947118255369952));
#18978=CARTESIAN_POINT('Ctrl Pts',(6.26097327777241,2.15622310783766,-0.0989519593504032));
#18979=CARTESIAN_POINT('Ctrl Pts',(6.33098270718824,2.11527690641461,-0.10319209316381));
#18980=CARTESIAN_POINT('Ctrl Pts',(6.40085931846967,2.07440838592866,-0.107424182822774));
#18981=CARTESIAN_POINT('Ctrl Pts',(6.46883900936567,2.02999742697265,-0.111656272481739));
#18982=CARTESIAN_POINT('Ctrl Pts',(6.53454011865696,1.98224529452245,-0.115888362140703));
#18983=CARTESIAN_POINT('Ctrl Pts',(6.60014732537095,1.93456141127468,-0.120114403132748));
#18984=CARTESIAN_POINT('Ctrl Pts',(6.66348204576312,1.88354610978608,-0.124340444124791));
#18985=CARTESIAN_POINT('Ctrl Pts',(6.72418878096599,1.82944560456303,-0.128566485116836));
#18986=CARTESIAN_POINT('Ctrl Pts',(6.7849122140378,1.77533021856699,-0.132793688514969));
#18987=CARTESIAN_POINT('Ctrl Pts',(6.84300582713177,1.71812818962209,-0.137020891913102));
#18988=CARTESIAN_POINT('Ctrl Pts',(6.89814442098349,1.65812829880832,-0.141248095311235));
#18989=CARTESIAN_POINT('Ctrl Pts',(6.95316921520028,1.59825224078014,-0.145466574253956));
#18990=CARTESIAN_POINT('Ctrl Pts',(7.00525084276438,1.53559018352991,-0.149685053196679));
#18991=CARTESIAN_POINT('Ctrl Pts',(7.05410196766166,1.47046690225272,-0.153903532139401));
#18992=CARTESIAN_POINT('Ctrl Pts',(7.10293707314934,1.4053649764002,-0.158120627745664));
#18993=CARTESIAN_POINT('Ctrl Pts',(7.14854350112589,1.33780380077203,-0.162337723351927));
#18994=CARTESIAN_POINT('Ctrl Pts',(7.19067477458605,1.2681404938478,-0.166554818958191));
#18995=CARTESIAN_POINT('Ctrl Pts',(7.23280512349857,1.19847871564653,-0.170771822022609));
#18996=CARTESIAN_POINT('Ctrl Pts',(7.27146023002617,1.12671529608835,-0.174988825087027));
#18997=CARTESIAN_POINT('Ctrl Pts',(7.30643822496742,1.05323430682007,-0.179205828151446));
#18998=CARTESIAN_POINT('Ctrl Pts',(7.34156102952335,0.979449104752861,-0.183440289694827));
#18999=CARTESIAN_POINT('Ctrl Pts',(7.37297599659099,0.903932501600326,-0.187674751238211));
#19000=CARTESIAN_POINT('Ctrl Pts',(7.40052719086964,0.827094430285556,-0.191909212781592));
#19001=CARTESIAN_POINT('Ctrl Pts',(7.42800457278192,0.750462215741043,-0.196132329784928));
#19002=CARTESIAN_POINT('Ctrl Pts',(7.45163876205086,0.672516064084704,-0.200355446788263));
#19003=CARTESIAN_POINT('Ctrl Pts',(7.47132541865902,0.593676897354868,-0.204578563791598));
#19004=CARTESIAN_POINT('Ctrl Pts',(7.49109140153166,0.514520052681181,-0.208818697605003));
#19005=CARTESIAN_POINT('Ctrl Pts',(7.50687788911849,0.434463445243041,-0.213058831418408));
#19006=CARTESIAN_POINT('Ctrl Pts',(7.51863154107017,0.353940590342874,-0.217298965231812));
#19007=CARTESIAN_POINT('Ctrl Pts',(7.53038519302186,0.2734177354427,-0.221539099045217));
#19008=CARTESIAN_POINT('Ctrl Pts',(7.53810602691446,0.192429104206554,-0.225779232858622));
#19009=CARTESIAN_POINT('Ctrl Pts',(7.54179332448114,0.111408641021281,-0.230019366672027));
#19010=CARTESIAN_POINT('Ctrl Pts',(7.54347186327011,0.0745263477708464,
-0.231949568655315));
#19011=CARTESIAN_POINT('Ctrl Pts',(7.54431692344925,0.0376058353287048,
-0.233879770638604));
#19012=CARTESIAN_POINT('Ctrl Pts',(7.54432706310245,0.000672763404615103,
-0.235809972621892));
#19013=CARTESIAN_POINT('',(7.54432655273177,0.00171870210940699,-1.03580994220875));
#19014=CARTESIAN_POINT('Ctrl Pts',(7.54432706310264,0.000672762683487049,
-0.235809972659579));
#19015=CARTESIAN_POINT('Ctrl Pts',(7.54434913504306,-0.0797230281083711,
-0.240011630056277));
#19016=CARTESIAN_POINT('Ctrl Pts',(7.54041051570088,-0.160277450484104,
-0.244213287452976));
#19017=CARTESIAN_POINT('Ctrl Pts',(7.53249050506246,-0.2405645802526,-0.248414944849674));
#19018=CARTESIAN_POINT('Ctrl Pts',(7.52458159021619,-0.320739229199403,
-0.252610715800091));
#19019=CARTESIAN_POINT('Ctrl Pts',(7.51270240427678,-0.400646863270127,
-0.256806486750507));
#19020=CARTESIAN_POINT('Ctrl Pts',(7.496884261858,-0.479861223018667,-0.261002257700924));
#19021=CARTESIAN_POINT('Ctrl Pts',(7.48108343481782,-0.55898887052289,-0.265193435737671));
#19022=CARTESIAN_POINT('Ctrl Pts',(7.46135230928154,-0.637424290794586,
-0.269384613774418));
#19023=CARTESIAN_POINT('Ctrl Pts',(7.43777386554803,-0.714747556998403,
-0.273575791811165));
#19024=CARTESIAN_POINT('Ctrl Pts',(7.41420923082477,-0.792025537865028,
-0.277764515232116));
#19025=CARTESIAN_POINT('Ctrl Pts',(7.38680188651064,-0.868192206759783,
-0.281953238653067));
#19026=CARTESIAN_POINT('Ctrl Pts',(7.35568533976997,-0.942840285540893,
-0.286141962074018));
#19027=CARTESIAN_POINT('Ctrl Pts',(7.32457715080191,-1.01746831416433,-0.290329560421606));
#19028=CARTESIAN_POINT('Ctrl Pts',(7.2897619191426,-1.09057812712337,-0.294517158769195));
#19029=CARTESIAN_POINT('Ctrl Pts',(7.25142167462247,-1.16178145141431,-0.298704757116783));
#19030=CARTESIAN_POINT('Ctrl Pts',(7.21307957177671,-1.23298822688205,-0.302892558434421));
#19031=CARTESIAN_POINT('Ctrl Pts',(7.17121234244279,-1.30228791558973,-0.307080359752057));
#19032=CARTESIAN_POINT('Ctrl Pts',(7.12604771747784,-1.3693172887552,-0.311268161069695));
#19033=CARTESIAN_POINT('Ctrl Pts',(7.08083722339339,-1.43641473684281,-0.315460215511524));
#19034=CARTESIAN_POINT('Ctrl Pts',(7.03232291287187,-1.50123687440294,-0.319652269953352));
#19035=CARTESIAN_POINT('Ctrl Pts',(6.98077516759411,-1.56345049473181,-0.323844324395181));
#19036=CARTESIAN_POINT('Ctrl Pts',(6.92919923522328,-1.62569813441685,-0.328038671116295));
#19037=CARTESIAN_POINT('Ctrl Pts',(6.87458688596316,-1.6853340702272,-0.332233017837412));
#19038=CARTESIAN_POINT('Ctrl Pts',(6.81724628663476,-1.74206106330321,-0.336427364558526));
#19039=CARTESIAN_POINT('Ctrl Pts',(6.75980868398242,-1.79888402166297,-0.340628806872962));
#19040=CARTESIAN_POINT('Ctrl Pts',(6.69963396885148,-1.85278789833906,-0.344830249187399));
#19041=CARTESIAN_POINT('Ctrl Pts',(6.6370639836603,-1.90351525921518,-0.349031691501835));
#19042=CARTESIAN_POINT('Ctrl Pts',(6.59826927250458,-1.93496729339527,-0.351636674394639));
#19043=CARTESIAN_POINT('Ctrl Pts',(6.55855437060663,-1.96519902747761,-0.354241657287441));
#19044=CARTESIAN_POINT('Ctrl Pts',(6.51800593252828,-1.99415773220894,-0.356846640180244));
#19045=CARTESIAN_POINT('Ctrl Pts',(6.45213040376664,-2.04120442689893,-0.361078729839206));
#19046=CARTESIAN_POINT('Ctrl Pts',(6.38379825808443,-2.08507115137392,-0.365310819498166));
#19047=CARTESIAN_POINT('Ctrl Pts',(6.31334926780181,-2.12549195893388,-0.369542909157127));
#19048=CARTESIAN_POINT('Ctrl Pts',(6.24300096595243,-2.16585499550567,-0.373768950149169));
#19049=CARTESIAN_POINT('Ctrl Pts',(6.17054222811684,-2.20278166749751,-0.377994991141211));
#19050=CARTESIAN_POINT('Ctrl Pts',(6.096343142351,-2.2360482879433,-0.382221032133253));
#19051=CARTESIAN_POINT('Ctrl Pts',(6.02212364753813,-2.26932405863688,-0.386448235531387));
#19052=CARTESIAN_POINT('Ctrl Pts',(5.94616324199017,-2.29893751481338,-0.390675438929521));
#19053=CARTESIAN_POINT('Ctrl Pts',(5.86885846270999,-2.32471002982559,-0.394902642327654));
#19054=CARTESIAN_POINT('Ctrl Pts',(5.79171323148945,-2.35042935336891,-0.399121121270377));
#19055=CARTESIAN_POINT('Ctrl Pts',(5.7132296032131,-2.37232340372829,-0.4033396002131));
#19056=CARTESIAN_POINT('Ctrl Pts',(5.63382147251977,-2.3902628281291,-0.407558079155823));
#19057=CARTESIAN_POINT('Ctrl Pts',(5.5544393815825,-2.40819636977922,-0.411775174762083));
#19058=CARTESIAN_POINT('Ctrl Pts',(5.47413384320326,-2.42217775850318,-0.415992270368343));
#19059=CARTESIAN_POINT('Ctrl Pts',(5.39333155282869,-2.43212815574194,-0.420209365974603));
#19060=CARTESIAN_POINT('Ctrl Pts',(5.31253103561598,-2.4420783346247,-0.424426369039018));
#19061=CARTESIAN_POINT('Ctrl Pts',(5.23123424942722,-2.4479976422455,-0.428643372103433));
#19062=CARTESIAN_POINT('Ctrl Pts',(5.14987423853903,-2.44985897032412,-0.432860375167848));
#19063=CARTESIAN_POINT('Ctrl Pts',(5.06817739554108,-2.45172800433907,-0.437094836711232));
#19064=CARTESIAN_POINT('Ctrl Pts',(4.98641727461081,-2.44950536333501,-0.441329298254615));
#19065=CARTESIAN_POINT('Ctrl Pts',(4.90503173005962,-2.44321643276859,-0.445563759798));
#19066=CARTESIAN_POINT('Ctrl Pts',(4.823864225408,-2.43694435086733,-0.449786876801334));
#19067=CARTESIAN_POINT('Ctrl Pts',(4.74306975123904,-2.42662783962602,-0.45400999380467));
#19068=CARTESIAN_POINT('Ctrl Pts',(4.66307508507545,-2.41234386103336,-0.458233110808004));
#19069=CARTESIAN_POINT('Ctrl Pts',(4.58275808494858,-2.39800232596035,-0.462473244621414));
#19070=CARTESIAN_POINT('Ctrl Pts',(4.50324780944176,-2.37966139703956,-0.466713378434822));
#19071=CARTESIAN_POINT('Ctrl Pts',(4.42496166673162,-2.35744972544429,-0.470953512248231));
#19072=CARTESIAN_POINT('Ctrl Pts',(4.34667552402147,-2.33523805384901,-0.47519364606164));
#19073=CARTESIAN_POINT('Ctrl Pts',(4.26961393682897,-2.30915584832712,-0.47943377987505));
#19074=CARTESIAN_POINT('Ctrl Pts',(4.19417318033833,-2.27937995407966,-0.48367391368846));
#19075=CARTESIAN_POINT('Ctrl Pts',(4.11887554600458,-2.2496605490617,-0.487906003347422));
#19076=CARTESIAN_POINT('Ctrl Pts',(4.04491167209826,-2.21615059522003,-0.492138093006385));
#19077=CARTESIAN_POINT('Ctrl Pts',(3.97268947649545,-2.17899071930594,-0.496370182665347));
#19078=CARTESIAN_POINT('Ctrl Pts',(3.90057050365971,-2.1418839537298,-0.500596223657394));
#19079=CARTESIAN_POINT('Ctrl Pts',(3.83018867490804,-2.10113783766085,-0.50482226464944));
#19080=CARTESIAN_POINT('Ctrl Pts',(3.76193291616568,-2.05694141514846,-0.509048305641486));
#19081=CARTESIAN_POINT('Ctrl Pts',(3.69365838313564,-2.0127328360596,-0.513275509039619));
#19082=CARTESIAN_POINT('Ctrl Pts',(3.62751151362544,-1.96507224802579,-0.517502712437752));
#19083=CARTESIAN_POINT('Ctrl Pts',(3.56385778900744,-1.9141953891225,-0.521729915835885));
#19084=CARTESIAN_POINT('Ctrl Pts',(3.50033543826238,-1.86342353412962,-0.525948394778608));
#19085=CARTESIAN_POINT('Ctrl Pts',(3.4392963301879,-1.80944894164363,-0.530166873721331));
#19086=CARTESIAN_POINT('Ctrl Pts',(3.3810740230668,-1.75254870331779,-0.534385352664054));
#19087=CARTESIAN_POINT('Ctrl Pts',(3.32287080838197,-1.6956671238914,-0.538602448270314));
#19088=CARTESIAN_POINT('Ctrl Pts',(3.26748289235775,-1.63586212841842,-0.542819543876574));
#19089=CARTESIAN_POINT('Ctrl Pts',(3.21520839209312,-1.5734490115513,-0.547036639482834));
#19090=CARTESIAN_POINT('Ctrl Pts',(3.16293503896367,-1.51103726430574,-0.551253642547249));
#19091=CARTESIAN_POINT('Ctrl Pts',(3.11377526324356,-1.44601786644264,-0.555470645611663));
#19092=CARTESIAN_POINT('Ctrl Pts',(3.06798721296626,-1.37873956112997,-0.559687648676078));
#19093=CARTESIAN_POINT('Ctrl Pts',(3.02200959922396,-1.31118272225676,-0.563922110219461));
#19094=CARTESIAN_POINT('Ctrl Pts',(2.97943196451938,-1.24134861504167,-0.568156571762844));
#19095=CARTESIAN_POINT('Ctrl Pts',(2.94047101054731,-1.16961855457087,-0.572391033306228));
#19096=CARTESIAN_POINT('Ctrl Pts',(2.90161443681301,-1.09808066600562,-0.576614150309561));
#19097=CARTESIAN_POINT('Ctrl Pts',(2.8663553549631,-1.02465740942075,-0.580837267312894));
#19098=CARTESIAN_POINT('Ctrl Pts',(2.83486115444521,-0.949748838530668,
-0.585060384316227));
#19099=CARTESIAN_POINT('Ctrl Pts',(2.80324004983532,-0.874538427809293,
-0.589300518129635));
#19100=CARTESIAN_POINT('Ctrl Pts',(2.7754143840211,-0.797831153663746,-0.593540651943045));
#19101=CARTESIAN_POINT('Ctrl Pts',(2.75150306778021,-0.720047302826222,
-0.597780785756453));
#19102=CARTESIAN_POINT('Ctrl Pts',(2.72759175153932,-0.642263451988699,
-0.602020919569861));
#19103=CARTESIAN_POINT('Ctrl Pts',(2.70759483944076,-0.563403492744268,
-0.606261053383269));
#19104=CARTESIAN_POINT('Ctrl Pts',(2.69157930278517,-0.48389617104529,-0.610501187196677));
#19105=CARTESIAN_POINT('Ctrl Pts',(2.67559414994672,-0.404539686372571,
-0.614733276855639));
#19106=CARTESIAN_POINT('Ctrl Pts',(2.66351562688312,-0.324242233546837,
-0.618965366514602));
#19107=CARTESIAN_POINT('Ctrl Pts',(2.65544743384368,-0.243422643243998,
-0.623197456173564));
#19108=CARTESIAN_POINT('Ctrl Pts',(2.64739077217912,-0.162718563438931,
-0.627423497165596));
#19109=CARTESIAN_POINT('Ctrl Pts',(2.64333310249612,-0.0814942868349896,
-0.631649538157628));
#19110=CARTESIAN_POINT('Ctrl Pts',(2.64332716199235,-0.00017902179174532,
-0.63587557914966));
#19111=CARTESIAN_POINT('Ctrl Pts',(2.6433212198546,0.0811586096602686,-0.640102782547795));
#19112=CARTESIAN_POINT('Ctrl Pts',(2.64736930210408,0.162586817474471,-0.644329985945929));
#19113=CARTESIAN_POINT('Ctrl Pts',(2.65547220897854,0.243670689667399,-0.648557189344064));
#19114=CARTESIAN_POINT('Ctrl Pts',(2.66355839239706,0.324587214193079,-0.652775668286786));
#19115=CARTESIAN_POINT('Ctrl Pts',(2.67568265845103,0.405160358113423,-0.656994147229508));
#19116=CARTESIAN_POINT('Ctrl Pts',(2.69179374419152,0.48495952530394,-0.66121262617223));
#19117=CARTESIAN_POINT('Ctrl Pts',(2.70789954673575,0.564732524508723,-0.6654297217785));
#19118=CARTESIAN_POINT('Ctrl Pts',(2.72798948075679,0.643731595870925,-0.66964681738477));
#19119=CARTESIAN_POINT('Ctrl Pts',(2.75196095221086,0.721535124655565,-0.67386391299104));
#19120=CARTESIAN_POINT('Ctrl Pts',(2.77593189762414,0.799336946084448,-0.678080916055461));
#19121=CARTESIAN_POINT('Ctrl Pts',(2.80378407319052,0.875942833348865,-0.682297919119882));
#19122=CARTESIAN_POINT('Ctrl Pts',(2.835365083211,0.950946538057679,-0.686514922184302));
#19123=CARTESIAN_POINT('Ctrl Pts',(2.86707683925908,1.02626075963848,-0.690749383727684));
#19124=CARTESIAN_POINT('Ctrl Pts',(2.90254819921196,1.09995906444025,-0.694983845271068));
#19125=CARTESIAN_POINT('Ctrl Pts',(2.94157689847623,1.17165228687651,-0.69921830681445));
#19126=CARTESIAN_POINT('Ctrl Pts',(2.98050103600642,1.24315343609995,-0.703441423817783));
#19127=CARTESIAN_POINT('Ctrl Pts',(3.02296319736942,1.31265985532011,-0.707664540821115));
#19128=CARTESIAN_POINT('Ctrl Pts',(3.06871858438887,1.37981358356922,-0.711887657824448));
#19129=CARTESIAN_POINT('Ctrl Pts',(3.11465834014121,1.44723790395171,-0.716127791637856));
#19130=CARTESIAN_POINT('Ctrl Pts',(3.16391762583028,1.51229016262306,-0.720367925451264));
#19131=CARTESIAN_POINT('Ctrl Pts',(3.21620830848705,1.57464209124418,-0.724608059264671));
#19132=CARTESIAN_POINT('Ctrl Pts',(3.26849899114382,1.6369940198653,-0.728848193078079));
#19133=CARTESIAN_POINT('Ctrl Pts',(3.32382070737263,1.69664531808261,-0.733088326891487));
#19134=CARTESIAN_POINT('Ctrl Pts',(3.38184999060225,1.75330671504709,-0.737328460704894));
#19135=CARTESIAN_POINT('Ctrl Pts',(3.43976918378819,1.80986061704834,-0.741560550363855));
#19136=CARTESIAN_POINT('Ctrl Pts',(3.50060175364413,1.86364695448099,-0.745792640022815));
#19137=CARTESIAN_POINT('Ctrl Pts',(3.56405252120228,1.91435101755209,-0.750024729681776));
#19138=CARTESIAN_POINT('Ctrl Pts',(3.62741260245896,1.96498261240688,-0.754250770673819));
#19139=CARTESIAN_POINT('Ctrl Pts',(3.69338308935504,2.01254039464928,-0.758476811665862));
#19140=CARTESIAN_POINT('Ctrl Pts',(3.76163238981095,2.05674678956736,-0.762702852657904));
#19141=CARTESIAN_POINT('Ctrl Pts',(3.82990046277823,2.10096534380495,-0.766930056056037));
#19142=CARTESIAN_POINT('Ctrl Pts',(3.90044825105633,2.14183036022238,-0.771157259454171));
#19143=CARTESIAN_POINT('Ctrl Pts',(3.97291114326049,2.17910475737404,-0.775384462852305));
#19144=CARTESIAN_POINT('Ctrl Pts',(4.04522448049597,2.21630222451189,-0.77960294179503));
#19145=CARTESIAN_POINT('Ctrl Pts',(4.11944462263436,2.24992364401679,-0.783821420737755));
#19146=CARTESIAN_POINT('Ctrl Pts',(4.19518228029349,2.27977798005625,-0.78803989968048));
#19147=CARTESIAN_POINT('Ctrl Pts',(4.2708951018292,2.30962252617089,-0.792256995286739));
#19148=CARTESIAN_POINT('Ctrl Pts',(4.34812401866058,2.3357022717617,-0.796474090892998));
#19149=CARTESIAN_POINT('Ctrl Pts',(4.4264593774043,2.35787414821533,-0.800691186499257));
#19150=CARTESIAN_POINT('Ctrl Pts',(4.50479301712181,2.38004553811938,-0.804908189563682));
#19151=CARTESIAN_POINT('Ctrl Pts',(4.58423260303908,2.39830910394468,-0.809125192628107));
#19152=CARTESIAN_POINT('Ctrl Pts',(4.66435430840104,2.4125719312893,-0.813342195692531));
#19153=CARTESIAN_POINT('Ctrl Pts',(4.74480771926232,2.42689380703092,-0.817576657235913));
#19154=CARTESIAN_POINT('Ctrl Pts',(4.82594844733252,2.43718165208201,-0.821811118779293));
#19155=CARTESIAN_POINT('Ctrl Pts',(4.9073398966582,2.44339369572469,-0.826045580322675));
#19156=CARTESIAN_POINT('Ctrl Pts',(4.98851329026488,2.44958909668986,-0.830268697326008));
#19157=CARTESIAN_POINT('Ctrl Pts',(5.06993559493242,2.45173053617133,-0.834491814329344));
#19158=CARTESIAN_POINT('Ctrl Pts',(5.15117328608491,2.44982890653645,-0.838714931332677));
#19159=CARTESIAN_POINT('Ctrl Pts',(5.23273831989921,2.44791961439297,-0.842955065146082));
#19160=CARTESIAN_POINT('Ctrl Pts',(5.31411677973302,2.44193464489328,-0.847195198959485));
#19161=CARTESIAN_POINT('Ctrl Pts',(5.39487650776651,2.43193740410227,-0.851435332772891));
#19162=CARTESIAN_POINT('Ctrl Pts',(5.47563623579999,2.42194016331125,-0.855675466586296));
#19163=CARTESIAN_POINT('Ctrl Pts',(5.55577678239443,2.40793079298116,-0.859915600399702));
#19164=CARTESIAN_POINT('Ctrl Pts',(5.63487951587856,2.39002355496301,-0.864155734213107));
#19165=CARTESIAN_POINT('Ctrl Pts',(5.71383217989943,2.37215028959638,-0.868387823872063));
#19166=CARTESIAN_POINT('Ctrl Pts',(5.79204552480634,2.35032726670422,-0.872619913531017));
#19167=CARTESIAN_POINT('Ctrl Pts',(5.86909494316994,2.32463117662322,-0.876852003189972));
#19168=CARTESIAN_POINT('Ctrl Pts',(5.94603423951238,2.29897181239214,-0.881078044182022));
#19169=CARTESIAN_POINT('Ctrl Pts',(6.02181247612417,2.26945052093748,-0.885304085174071));
#19170=CARTESIAN_POINT('Ctrl Pts',(6.096016421698,2.23619474210623,-0.88953012616612));
#19171=CARTESIAN_POINT('Ctrl Pts',(6.17024077765544,2.20292981600931,-0.893757329564254));
#19172=CARTESIAN_POINT('Ctrl Pts',(6.2428895277158,2.16592847667684,-0.897984532962389));
#19173=CARTESIAN_POINT('Ctrl Pts',(6.31356548021765,2.12536789029584,-0.902211736360522));
#19174=CARTESIAN_POINT('Ctrl Pts',(6.38409556578601,2.08489101624055,-0.906430215303235));
#19175=CARTESIAN_POINT('Ctrl Pts',(6.45266057340775,2.04086978183757,-0.910648694245948));
#19176=CARTESIAN_POINT('Ctrl Pts',(6.51888854564184,1.99352709642818,-0.914867173188661));
#19177=CARTESIAN_POINT('Ctrl Pts',(6.58509480019769,1.94619993577629,-0.919084268794919));
#19178=CARTESIAN_POINT('Ctrl Pts',(6.64896516356175,1.8955537571567,-0.923301364401177));
#19179=CARTESIAN_POINT('Ctrl Pts',(6.71015687043186,1.84185463663035,-0.927518460007435));
#19180=CARTESIAN_POINT('Ctrl Pts',(6.77134723448354,1.78815669450173,-0.931735463071845));
#19181=CARTESIAN_POINT('Ctrl Pts',(6.82985871040158,1.73140625103906,-0.935952466136255));
#19182=CARTESIAN_POINT('Ctrl Pts',(6.88538292579639,1.67190854168214,-0.940169469200665));
#19183=CARTESIAN_POINT('Ctrl Pts',(6.94113701257911,1.612164510591,-0.944403930744053));
#19184=CARTESIAN_POINT('Ctrl Pts',(6.9938787201965,1.54965075382351,-0.948638392287441));
#19185=CARTESIAN_POINT('Ctrl Pts',(7.04333566297374,1.48471102545401,-0.952872853830829));
#19186=CARTESIAN_POINT('Ctrl Pts',(7.09266010572405,1.41994527702087,-0.957095970834159));
#19187=CARTESIAN_POINT('Ctrl Pts',(7.13871713113911,1.35276694814664,-0.961319087837489));
#19188=CARTESIAN_POINT('Ctrl Pts',(7.18128022621014,1.28354584156043,-0.965542204840819));
#19189=CARTESIAN_POINT('Ctrl Pts',(7.22401482685513,1.21404581245705,-0.969782338654237));
#19190=CARTESIAN_POINT('Ctrl Pts',(7.26322706153343,1.14248692596204,-0.974022472467655));
#19191=CARTESIAN_POINT('Ctrl Pts',(7.29873523791343,1.0692663830408,-0.978262606281072));
#19192=CARTESIAN_POINT('Ctrl Pts',(7.33424341429343,0.996045840119555,-0.98250274009449));
#19193=CARTESIAN_POINT('Ctrl Pts',(7.36604740694091,0.921164095233241,-0.986742873907906));
#19194=CARTESIAN_POINT('Ctrl Pts',(7.39401556223305,0.845034640304858,-0.990983007721324));
#19195=CARTESIAN_POINT('Ctrl Pts',(7.42616850853459,0.757514163866223,-0.995857580012206));
#19196=CARTESIAN_POINT('Ctrl Pts',(7.45335219664486,0.668075732514126,-1.00073215230309));
#19197=CARTESIAN_POINT('Ctrl Pts',(7.47536636025791,0.577253207853991,-1.00560672459397));
#19198=CARTESIAN_POINT('Ctrl Pts',(7.49809992997903,0.483462672228753,-1.01064059419644));
#19199=CARTESIAN_POINT('Ctrl Pts',(7.51532012506383,0.388196137853416,-1.0156744637989));
#19200=CARTESIAN_POINT('Ctrl Pts',(7.52685978595101,0.292065864031482,-1.02070833340136));
#19201=CARTESIAN_POINT('Ctrl Pts',(7.53839944683819,0.195935590209548,-1.02574220300383));
#19202=CARTESIAN_POINT('Ctrl Pts',(7.54425836357575,0.098941766422127,-1.03077607260629));
#19203=CARTESIAN_POINT('Ctrl Pts',(7.54432655273177,0.00171870210940699,
-1.03580994220875));
#19204=CARTESIAN_POINT('',(7.54195689531145,-0.00183542994100908,-1.83580997262189));
#19205=CARTESIAN_POINT('Ctrl Pts',(7.54168867809974,0.00171626522762203,
-1.03580997262189));
#19206=CARTESIAN_POINT('Ctrl Pts',(7.53826864661413,-0.525630169298386,
-1.06314340882444));
#19207=CARTESIAN_POINT('Ctrl Pts',(7.11247511815589,-1.87364194780338,-1.13275260286306));
#19208=CARTESIAN_POINT('Ctrl Pts',(4.8932778873185,-2.88797071625038,-1.24463755473777));
#19209=CARTESIAN_POINT('Ctrl Pts',(2.56077426740912,-1.4015127303073,-1.37146482824597));
#19210=CARTESIAN_POINT('Ctrl Pts',(2.54053909816163,1.36430017347163,-1.4982921017542));
#19211=CARTESIAN_POINT('Ctrl Pts',(4.85104382313895,2.88472721769187,-1.62511937526241));
#19212=CARTESIAN_POINT('Ctrl Pts',(7.09724317847486,1.89752826528236,-1.7376253322183));
#19213=CARTESIAN_POINT('Ctrl Pts',(7.53818940518866,0.537343417442344,-1.80785553133814));
#19214=CARTESIAN_POINT('Ctrl Pts',(7.54195689531145,-0.00183542994100908,
-1.83580997262189));
#19215=CARTESIAN_POINT('',(7.54821176704488,-0.000461678752230058,-2.63580997262189));
#19216=CARTESIAN_POINT('Ctrl Pts',(7.54195689531145,-0.00183542994100908,
-1.83580997262189));
#19217=CARTESIAN_POINT('Ctrl Pts',(7.5438870150412,-0.278061696576387,-1.85013128917421));
#19218=CARTESIAN_POINT('Ctrl Pts',(7.37337369192932,-1.3673806984397,-1.90672836356257));
#19219=CARTESIAN_POINT('Ctrl Pts',(5.77424896835661,-2.81382675798286,-2.00560119578708));
#19220=CARTESIAN_POINT('Ctrl Pts',(3.10188638839217,-2.10065866965814,-2.13242846929526));
#19221=CARTESIAN_POINT('Ctrl Pts',(2.24784422830493,0.530071735913177,-2.2592557428035));
#19222=CARTESIAN_POINT('Ctrl Pts',(3.99172513773674,2.67693220178668,-2.38608301631169));
#19223=CARTESIAN_POINT('Ctrl Pts',(6.71326075235729,2.38324884212861,-2.51160109291785));
#19224=CARTESIAN_POINT('Ctrl Pts',(7.54617393712679,0.784506871056184,-2.5948434116879));
#19225=CARTESIAN_POINT('Ctrl Pts',(7.54821176704488,-0.000461678752230058,
-2.63580997262189));
#19226=CARTESIAN_POINT('',(7.54432619404611,0.00217068071508165,-3.43580997262189));
#19227=CARTESIAN_POINT('Ctrl Pts',(7.54821176704488,-0.000461678752230058,
-2.63580997262189));
#19228=CARTESIAN_POINT('Ctrl Pts',(7.54827689139399,-0.0255474650670082,
-2.63711916952397));
#19229=CARTESIAN_POINT('Ctrl Pts',(7.53657731044435,-0.86062535690245,-2.68070412426241));
#19230=CARTESIAN_POINT('Ctrl Pts',(6.59176122330639,-2.4772542092338,-2.7665648368361));
#19231=CARTESIAN_POINT('Ctrl Pts',(3.82877477306649,-2.60388887691698,-2.8933921103447));
#19232=CARTESIAN_POINT('Ctrl Pts',(2.22057696198272,-0.353593302260975,
-3.02021938385273));
#19233=CARTESIAN_POINT('Ctrl Pts',(3.23519284446952,2.21947595045414,-3.14704665736103));
#19234=CARTESIAN_POINT('Ctrl Pts',(5.94644184717804,2.76652176454744,-3.27387393086921));
#19235=CARTESIAN_POINT('Ctrl Pts',(7.41343420069762,1.26507933464666,-3.37012820241141));
#19236=CARTESIAN_POINT('Ctrl Pts',(7.54521044087543,0.227592873628459,-3.42410671611751));
#19237=CARTESIAN_POINT('Ctrl Pts',(7.54327308142312,0.00217939078736114,
-3.43580947198754));
#19238=CARTESIAN_POINT('',(7.54432691509248,-0.00108536048784296,-4.23580997266998));
#19239=CARTESIAN_POINT('Ctrl Pts',(7.54432619404611,0.00217068071508165,
-3.43580997262189));
#19240=CARTESIAN_POINT('Ctrl Pts',(7.54439758870441,-0.078427327229146,
-3.43999260303891));
#19241=CARTESIAN_POINT('Ctrl Pts',(7.54048835863658,-0.159110489756147,
-3.44417523345593));
#19242=CARTESIAN_POINT('Ctrl Pts',(7.53260002672682,-0.239451732796754,
-3.44835786387295));
#19243=CARTESIAN_POINT('Ctrl Pts',(7.52471552022917,-0.319754014702473,
-3.45253846594161));
#19244=CARTESIAN_POINT('Ctrl Pts',(7.51285578731776,-0.399714235521038,
-3.45671906801028));
#19245=CARTESIAN_POINT('Ctrl Pts',(7.49707436664272,-0.478908229110086,
-3.46089967007895));
#19246=CARTESIAN_POINT('Ctrl Pts',(7.48129555875154,-0.558089111282113,
-3.465079580004));
#19247=CARTESIAN_POINT('Ctrl Pts',(7.46159644547567,-0.636503553768053,
-3.46925948992905));
#19248=CARTESIAN_POINT('Ctrl Pts',(7.43808179801882,-0.713736940902685,
-3.4734393998541));
#19249=CARTESIAN_POINT('Ctrl Pts',(7.41456353334558,-0.79098220871184,-3.47761995276726));
#19250=CARTESIAN_POINT('Ctrl Pts',(7.38722870964907,-0.867045608132491,
-3.48180050568042));
#19251=CARTESIAN_POINT('Ctrl Pts',(7.35623167916053,-0.941528555652031,
-3.48598105859357));
#19252=CARTESIAN_POINT('Ctrl Pts',(7.32520084589774,-1.01609272805733,-3.4901661704688));
#19253=CARTESIAN_POINT('Ctrl Pts',(7.29050002102054,-1.08907257242188,-3.49435128234403));
#19254=CARTESIAN_POINT('Ctrl Pts',(7.25233103441385,-1.1600910544054,-3.49853639421926));
#19255=CARTESIAN_POINT('Ctrl Pts',(7.21413743471517,-1.23115533232395,-3.50272420484426));
#19256=CARTESIAN_POINT('Ctrl Pts',(7.17247146990418,-1.30025532754648,-3.50691201546925));
#19257=CARTESIAN_POINT('Ctrl Pts',(7.12757876976536,-1.36704228950033,-3.51109982609424));
#19258=CARTESIAN_POINT('Ctrl Pts',(7.08261342757628,-1.43393732118115,-3.51529441312496));
#19259=CARTESIAN_POINT('Ctrl Pts',(7.034411218612,-1.49851147622434,-3.51948900015567));
#19260=CARTESIAN_POINT('Ctrl Pts',(6.98325807161719,-1.56044899405375,-3.52368358718638));
#19261=CARTESIAN_POINT('Ctrl Pts',(6.96762854260127,-1.57937362115806,-3.52496521741947));
#19262=CARTESIAN_POINT('Ctrl Pts',(6.95172377923429,-1.59805236380879,-3.52624684765256));
#19263=CARTESIAN_POINT('Ctrl Pts',(6.93555258953373,-1.61647693316687,-3.52752847788565));
#19264=CARTESIAN_POINT('Ctrl Pts',(6.88215346160043,-1.67731697984777,-3.53176056829132));
#19265=CARTESIAN_POINT('Ctrl Pts',(6.82563677564708,-1.73562167328497,-3.53599265869699));
#19266=CARTESIAN_POINT('Ctrl Pts',(6.7662726377776,-1.7910545381569,-3.54022474910266));
#19267=CARTESIAN_POINT('Ctrl Pts',(6.70699334571578,-1.8464081759675,-3.54445079082066));
#19268=CARTESIAN_POINT('Ctrl Pts',(6.64487502140792,-1.89889782278366,-3.54867683253866));
#19269=CARTESIAN_POINT('Ctrl Pts',(6.58022693169389,-1.94822122850342,-3.55290287425666));
#19270=CARTESIAN_POINT('Ctrl Pts',(6.51556107393455,-1.99755819039339,-3.55713007747071));
#19271=CARTESIAN_POINT('Ctrl Pts',(6.4483643874204,-2.04372683776174,-3.56135728068476));
#19272=CARTESIAN_POINT('Ctrl Pts',(6.37898217397017,-2.08646275509064,-3.56558448389881));
#19273=CARTESIAN_POINT('Ctrl Pts',(6.3097431432978,-2.12911047910524,-3.56980296351255));
#19274=CARTESIAN_POINT('Ctrl Pts',(6.23832797971304,-2.16833936204582,-3.5740214431263));
#19275=CARTESIAN_POINT('Ctrl Pts',(6.16511013077376,-2.20392899994263,-3.57823992274004));
#19276=CARTESIAN_POINT('Ctrl Pts',(6.0919162920328,-2.23950696699311,-3.5824570189953));
#19277=CARTESIAN_POINT('Ctrl Pts',(6.01692135951845,-2.27144785601514,-3.58667411525056));
#19278=CARTESIAN_POINT('Ctrl Pts',(5.94052277285294,-2.29957752238882,-3.59089121150582));
#19279=CARTESIAN_POINT('Ctrl Pts',(5.8641258631243,-2.32770657132079,-3.59510821519649));
#19280=CARTESIAN_POINT('Ctrl Pts',(5.78632579696908,-2.3520244044536,-3.59932521888716));
#19281=CARTESIAN_POINT('Ctrl Pts',(5.70753800193967,-2.37240579305159,-3.60354222257783));
#19282=CARTESIAN_POINT('Ctrl Pts',(5.62842405068523,-2.39287155406746,-3.6077766833125));
#19283=CARTESIAN_POINT('Ctrl Pts',(5.548314628918,-2.40936807926592,-3.61201114404717));
#19284=CARTESIAN_POINT('Ctrl Pts',(5.46764182775742,-2.42182015037658,-3.61624560478184));
#19285=CARTESIAN_POINT('Ctrl Pts',(5.38718513085923,-2.43423886519361,-3.62046872235003));
#19286=CARTESIAN_POINT('Ctrl Pts',(5.30616853837484,-2.44263475937152,-3.62469183991823));
#19287=CARTESIAN_POINT('Ctrl Pts',(5.22502512900846,-2.44698535789141,-3.62891495748642));
#19288=CARTESIAN_POINT('Ctrl Pts',(5.14355479651501,-2.45135348477601,-3.63315508980433));
#19289=CARTESIAN_POINT('Ctrl Pts',(5.06195709457774,-2.45164365752016,-3.63739522212224));
#19290=CARTESIAN_POINT('Ctrl Pts',(4.98066777652398,-2.44788586436549,-3.64163535444015));
#19291=CARTESIAN_POINT('Ctrl Pts',(4.89937845847021,-2.44412807121081,-3.64587548675806));
#19292=CARTESIAN_POINT('Ctrl Pts',(4.81839798350605,-2.43632241891511,-3.65011561907597));
#19293=CARTESIAN_POINT('Ctrl Pts',(4.73815252936359,-2.42455064091392,-3.65435575139387));
#19294=CARTESIAN_POINT('Ctrl Pts',(4.65805914462597,-2.41280117105832,-3.65858784843546));
#19295=CARTESIAN_POINT('Ctrl Pts',(4.5783991872543,-2.39705677532944,-3.66281994547704));
#19296=CARTESIAN_POINT('Ctrl Pts',(4.49960190571245,-2.37736126883792,-3.66705204251862));
#19297=CARTESIAN_POINT('Ctrl Pts',(4.42091724336842,-2.35769391169493,-3.67127809093308));
#19298=CARTESIAN_POINT('Ctrl Pts',(4.34309325511306,-2.3340867711541,-3.67550413934755));
#19299=CARTESIAN_POINT('Ctrl Pts',(4.26655174911285,-2.30663513631102,-3.67973018776201));
#19300=CARTESIAN_POINT('Ctrl Pts',(4.18998935775338,-2.27917601092737,-3.68395738930952));
#19301=CARTESIAN_POINT('Ctrl Pts',(4.11471060589362,-2.24787038687307,-3.68818459085702));
#19302=CARTESIAN_POINT('Ctrl Pts',(4.04112513035319,-2.21286436465287,-3.69241179240452));
#19303=CARTESIAN_POINT('Ctrl Pts',(3.96769136457852,-2.1779305136783,-3.69663027881155));
#19304=CARTESIAN_POINT('Ctrl Pts',(3.89594433049418,-2.13931168443951,-3.70084876521857));
#19305=CARTESIAN_POINT('Ctrl Pts',(3.82627202538661,-2.09720152637797,-3.7050672516256));
#19306=CARTESIAN_POINT('Ctrl Pts',(3.75662256740782,-2.05510517719219,-3.70928435469527));
#19307=CARTESIAN_POINT('Ctrl Pts',(3.68904688467489,-2.00952001300304,-3.71350145776494));
#19308=CARTESIAN_POINT('Ctrl Pts',(3.62390718793589,-1.96068496681496,-3.71771856083461));
#19309=CARTESIAN_POINT('Ctrl Pts',(3.55876892081949,-1.9118509924109,-3.72193557135141));
#19310=CARTESIAN_POINT('Ctrl Pts',(3.49606690451329,-1.85976755748095,-3.72615258186821));
#19311=CARTESIAN_POINT('Ctrl Pts',(3.4361320697381,-1.8047152830284,-3.73036959238501));
#19312=CARTESIAN_POINT('Ctrl Pts',(3.37594933542629,-1.74943530404681,-3.73460404509476));
#19313=CARTESIAN_POINT('Ctrl Pts',(3.3185570784769,-1.69116218383102,-3.73883849780452));
#19314=CARTESIAN_POINT('Ctrl Pts',(3.26425330789796,-1.63021771133253,-3.74307295051428));
#19315=CARTESIAN_POINT('Ctrl Pts',(3.21009481524181,-1.56943628250992,-3.74729607486714));
#19316=CARTESIAN_POINT('Ctrl Pts',(3.1590085661019,-1.50599816639619,-3.75151919922));
#19317=CARTESIAN_POINT('Ctrl Pts',(3.11124883911793,-1.44025465442662,-3.75574232357287));
#19318=CARTESIAN_POINT('Ctrl Pts',(3.06329694188728,-1.37424661106816,-3.75998244046107));
#19319=CARTESIAN_POINT('Ctrl Pts',(3.01869864343333,-1.30591497987846,-3.76422255734928));
#19320=CARTESIAN_POINT('Ctrl Pts',(2.97766563770153,-1.23564180925838,-3.76846267423748));
#19321=CARTESIAN_POINT('Ctrl Pts',(2.93663263196972,-1.16536863863829,-3.77270279112568));
#19322=CARTESIAN_POINT('Ctrl Pts',(2.89916507896408,-1.09315437204353,-3.77694290801389));
#19323=CARTESIAN_POINT('Ctrl Pts',(2.86542603589723,-1.01940114791091,-3.78118302490209));
#19324=CARTESIAN_POINT('Ctrl Pts',(2.83175100953722,-0.945787863684691,
-3.78541509656153));
#19325=CARTESIAN_POINT('Ctrl Pts',(2.80166470736299,-0.870366825716182,
-3.78964716822096));
#19326=CARTESIAN_POINT('Ctrl Pts',(2.7753636846141,-0.793522138560183,-3.7938792398804));
#19327=CARTESIAN_POINT('Ctrl Pts',(2.74910025251282,-0.716787281412822,
-3.79810526286576));
#19328=CARTESIAN_POINT('Ctrl Pts',(2.72661150401748,-0.638633252283635,
-3.80233128585113));
#19329=CARTESIAN_POINT('Ctrl Pts',(2.708046745083,-0.559465891269729,-3.80655730883649));
#19330=CARTESIAN_POINT('Ctrl Pts',(2.68947678086819,-0.480276332913594,
-3.8107845167354));
#19331=CARTESIAN_POINT('Ctrl Pts',(2.67483317674379,-0.400073309224773,
-3.81501172463431));
#19332=CARTESIAN_POINT('Ctrl Pts',(2.664215975812,-0.31928007417146,-3.81923893253322));
#19333=CARTESIAN_POINT('Ctrl Pts',(2.65362074377035,-0.23865401479058,-3.82345739358194));
#19334=CARTESIAN_POINT('Ctrl Pts',(2.64703535420249,-0.157440641622429,
-3.82767585463066));
#19335=CARTESIAN_POINT('Ctrl Pts',(2.64450817442951,-0.0760708827182392,
-3.83189431567939));
#19336=CARTESIAN_POINT('Ctrl Pts',(2.64198182333156,0.00527219463054879,
-3.8361113934734));
#19337=CARTESIAN_POINT('Ctrl Pts',(2.64351105377966,0.086771091768486,-3.84032847126741));
#19338=CARTESIAN_POINT('Ctrl Pts',(2.64909220696122,0.167991909395576,-3.84454554906143));
#19339=CARTESIAN_POINT('Ctrl Pts',(2.6546732378064,0.249210946698602,-3.84876253441898));
#19340=CARTESIAN_POINT('Ctrl Pts',(2.66430598179138,0.330151453089001,-3.85297951977653));
#19341=CARTESIAN_POINT('Ctrl Pts',(2.67793478577229,0.410383123578419,-3.85719650513408));
#19342=CARTESIAN_POINT('Ctrl Pts',(2.69162013935566,0.490947697019378,-3.8614309879071));
#19343=CARTESIAN_POINT('Ctrl Pts',(2.70933471895357,0.5707970723659,-3.86566547068012));
#19344=CARTESIAN_POINT('Ctrl Pts',(2.73097041667715,0.649506183204621,-3.86989995345314));
#19345=CARTESIAN_POINT('Ctrl Pts',(2.75254795380765,0.728003709992476,-3.87412305318538));
#19346=CARTESIAN_POINT('Ctrl Pts',(2.7780253693176,0.80536666366508,-3.87834615291761));
#19347=CARTESIAN_POINT('Ctrl Pts',(2.80724602517311,0.881190663050533,-3.88256925264985));
#19348=CARTESIAN_POINT('Ctrl Pts',(2.83658482407696,0.957321229080808,-3.88680942694326));
#19349=CARTESIAN_POINT('Ctrl Pts',(2.86969699717403,1.03189994260836,-3.89104960123667));
#19350=CARTESIAN_POINT('Ctrl Pts',(2.906376929941,1.10454142561836,-3.89528977553008));
#19351=CARTESIAN_POINT('Ctrl Pts',(2.94305686270798,1.17718290862836,-3.89952994982349));
#19352=CARTESIAN_POINT('Ctrl Pts',(2.98330426986581,1.24788678572931,-3.90377012411689));
#19353=CARTESIAN_POINT('Ctrl Pts',(3.02687023321737,1.31629758475116,-3.9080102984103));
#19354=CARTESIAN_POINT('Ctrl Pts',(3.07035323817815,1.38457811579862,-3.91224239855571));
#19355=CARTESIAN_POINT('Ctrl Pts',(3.11730439187291,1.45082905363251,-3.91647449870111));
#19356=CARTESIAN_POINT('Ctrl Pts',(3.16750813305921,1.51467662356142,-3.92070659884652));
#19357=CARTESIAN_POINT('Ctrl Pts',(3.21764011974826,1.57843293833338,-3.92493265019534));
#19358=CARTESIAN_POINT('Ctrl Pts',(3.27101517605462,1.63979234535314,-3.92915870154416));
#19359=CARTESIAN_POINT('Ctrl Pts',(3.32737381319896,1.69840891414263,-3.93338475289298));
#19360=CARTESIAN_POINT('Ctrl Pts',(3.38374777933176,1.7570414260555,-3.93761195368571));
#19361=CARTESIAN_POINT('Ctrl Pts',(3.44310667674929,1.81292922866238,-3.94183915447844));
#19362=CARTESIAN_POINT('Ctrl Pts',(3.50514962968871,1.86575828261088,-3.94606635527117));
#19363=CARTESIAN_POINT('Ctrl Pts',(3.56706471771255,1.91847846065643,-3.95028484418533));
#19364=CARTESIAN_POINT('Ctrl Pts',(3.63165247150197,1.96815216474818,-3.95450333309948));
#19365=CARTESIAN_POINT('Ctrl Pts',(3.69857747673012,2.01450455050948,-3.95872182201364));
#19366=CARTESIAN_POINT('Ctrl Pts',(3.76548053312411,2.06084173446654,-3.96293892742527));
#19367=CARTESIAN_POINT('Ctrl Pts',(3.83471893698654,2.10385949889893,-3.9671560328369));
#19368=CARTESIAN_POINT('Ctrl Pts',(3.90592649960958,2.1433250527735,-3.97137313824853));
#19369=CARTESIAN_POINT('Ctrl Pts',(3.97713249661538,2.18278973893191,-3.97559015094005));
#19370=CARTESIAN_POINT('Ctrl Pts',(4.05030715930537,2.21870214556278,-3.97980716363158));
#19371=CARTESIAN_POINT('Ctrl Pts',(4.12505905264289,2.25087507715943,-3.9840241763231));
#19372=CARTESIAN_POINT('Ctrl Pts',(4.20012003786161,2.28318104073035,-3.98825862595605));
#19373=CARTESIAN_POINT('Ctrl Pts',(4.27677089659107,2.31171634042401,-3.992493075589));
#19374=CARTESIAN_POINT('Ctrl Pts',(4.35459609502854,2.33634066208324,-3.99672752522195));
#19375=CARTESIAN_POINT('Ctrl Pts',(4.43221317760941,2.36089913473858,-4.00095065132307));
#19376=CARTESIAN_POINT('Ctrl Pts',(4.51099786449122,2.38156744087855,-4.00517377742418));
#19377=CARTESIAN_POINT('Ctrl Pts',(4.59052558621481,2.39825723816322,-4.00939690352529));
#19378=CARTESIAN_POINT('Ctrl Pts',(4.67037316626169,2.41501416135643,-4.01363701492416));
#19379=CARTESIAN_POINT('Ctrl Pts',(4.7509693036795,2.42776044027575,-4.01787712632303));
#19380=CARTESIAN_POINT('Ctrl Pts',(4.83187878361868,2.43645917275322,-4.0221172377219));
#19381=CARTESIAN_POINT('Ctrl Pts',(4.91278826355786,2.44515790523068,-4.02635734912078));
#19382=CARTESIAN_POINT('Ctrl Pts',(4.99401061591388,2.4498091266479,-4.03059746051965));
#19383=CARTESIAN_POINT('Ctrl Pts',(5.07511218746176,2.45042853394525,-4.03483757191852));
#19384=CARTESIAN_POINT('Ctrl Pts',(5.15606115943214,2.45104677577454,-4.03906970518336));
#19385=CARTESIAN_POINT('Ctrl Pts',(5.23719177755503,2.44765068438233,-4.0433018384482));
#19386=CARTESIAN_POINT('Ctrl Pts',(5.3180731298665,2.44021802160368,-4.04753397171304));
#19387=CARTESIAN_POINT('Ctrl Pts',(5.39883889022776,2.43279598124864,-4.0517600566055));
#19388=CARTESIAN_POINT('Ctrl Pts',(5.47935563344585,2.42134886931261,-4.05598614149796));
#19389=CARTESIAN_POINT('Ctrl Pts',(5.55919194146204,2.40590645411306,-4.06021222639042));
#19390=CARTESIAN_POINT('Ctrl Pts',(5.6390491728845,2.39045999178338,-4.06443941885027));
#19391=CARTESIAN_POINT('Ctrl Pts',(5.71822514618863,2.37101615488072,-4.06866661131011));
#19392=CARTESIAN_POINT('Ctrl Pts',(5.79629272765714,2.34765678280878,-4.07289380376996));
#19393=CARTESIAN_POINT('Ctrl Pts',(5.8742002062599,2.32434531669652,-4.07711232700227));
#19394=CARTESIAN_POINT('Ctrl Pts',(5.95100338236365,2.29713446878585,-4.08133085023458));
#19395=CARTESIAN_POINT('Ctrl Pts',(6.02628923398334,2.26615637635691,-4.08554937346689));
#19396=CARTESIAN_POINT('Ctrl Pts',(6.10155039873976,2.23518844190474,-4.08976651340999));
#19397=CARTESIAN_POINT('Ctrl Pts',(6.17529479769941,2.20045589283366,-4.09398365335309));
#19398=CARTESIAN_POINT('Ctrl Pts',(6.24712797868544,2.16213955634959,-4.09820079329619));
#19399=CARTESIAN_POINT('Ctrl Pts',(6.31895958312151,2.12382406080865,-4.10241784068413));
#19400=CARTESIAN_POINT('Ctrl Pts',(6.38887964352791,2.08192515395072,-4.10663488807207));
#19401=CARTESIAN_POINT('Ctrl Pts',(6.45651825550695,2.03666963836407,-4.11085193546));
#19402=CARTESIAN_POINT('Ctrl Pts',(6.52443533872885,1.99122780376078,-4.1150863446239));
#19403=CARTESIAN_POINT('Ctrl Pts',(6.59005174893046,1.94240191503448,-4.11932075378779));
#19404=CARTESIAN_POINT('Ctrl Pts',(6.6530238504446,1.89046447105668,-4.12355516295168));
#19405=CARTESIAN_POINT('Ctrl Pts',(6.71582867230475,1.83866499416985,-4.12777832379318));
#19406=CARTESIAN_POINT('Ctrl Pts',(6.77600289862874,1.78377081761753,-4.13200148463468));
#19407=CARTESIAN_POINT('Ctrl Pts',(6.83324158643299,1.72609028943997,-4.13622464547618));
#19408=CARTESIAN_POINT('Ctrl Pts',(6.8907089557526,1.66817931449472,-4.14046467880127));
#19409=CARTESIAN_POINT('Ctrl Pts',(6.94521697288551,1.60746003379095,-4.14470471212637));
#19410=CARTESIAN_POINT('Ctrl Pts',(6.99649810553022,1.54427766471339,-4.14894474545146));
#19411=CARTESIAN_POINT('Ctrl Pts',(7.04777923817494,1.48109529563584,-4.15318477877655));
#19412=CARTESIAN_POINT('Ctrl Pts',(7.09583326051984,1.41545025193801,-4.15742481210164));
#19413=CARTESIAN_POINT('Ctrl Pts',(7.14043763352947,1.3477150296068,-4.16166484542674));
#19414=CARTESIAN_POINT('Ctrl Pts',(7.18580626204348,1.27881922563271,-4.1659775278799));
#19415=CARTESIAN_POINT('Ctrl Pts',(7.22777065721584,1.20751131754,-4.17029021033307));
#19416=CARTESIAN_POINT('Ctrl Pts',(7.26607126314968,1.13415421639984,-4.17460289278624));
#19417=CARTESIAN_POINT('Ctrl Pts',(7.3043109779799,1.06091373991189,-4.17890871884673));
#19418=CARTESIAN_POINT('Ctrl Pts',(7.33889827743594,0.985630932960405,-4.18321454490722));
#19419=CARTESIAN_POINT('Ctrl Pts',(7.36961702068705,0.908697275938748,-4.18752037096771));
#19420=CARTESIAN_POINT('Ctrl Pts',(7.40028604549749,0.831888136428436,-4.19181922802703));
#19421=CARTESIAN_POINT('Ctrl Pts',(7.42709881131217,0.753433871284795,-4.19611808508636));
#19422=CARTESIAN_POINT('Ctrl Pts',(7.44988591003959,0.673748762474872,-4.20041694214568));
#19423=CARTESIAN_POINT('Ctrl Pts',(7.47265125497041,0.594139725378565,-4.20471169528361));
#19424=CARTESIAN_POINT('Ctrl Pts',(7.49139844954934,0.513302602208026,-4.20900644842154));
#19425=CARTESIAN_POINT('Ctrl Pts',(7.50600706974429,0.431669214897464,-4.21330120155947));
#19426=CARTESIAN_POINT('Ctrl Pts',(7.52060499624227,0.350095584271307,-4.21759281088313));
#19427=CARTESIAN_POINT('Ctrl Pts',(7.53107029486122,0.267727281947792,-4.22188442020678));
#19428=CARTESIAN_POINT('Ctrl Pts',(7.53733333112178,0.185007620029785,-4.22617602953044));
#19429=CARTESIAN_POINT('Ctrl Pts',(7.54201981975292,0.123110364605593,-4.22938734389426));
#19430=CARTESIAN_POINT('Ctrl Pts',(7.54435442092451,0.0610166722415663,
-4.23259865825807));
#19431=CARTESIAN_POINT('Ctrl Pts',(7.54432691509289,-0.00108535955790657,
-4.23580997262189));
#19432=CARTESIAN_POINT('Ctrl Pts',(7.54432691509248,-0.00108536048783975,
-4.23580997266998));
#19433=CARTESIAN_POINT('Ctrl Pts',(7.54428737107733,-0.0903668487108589,
-4.24042674473442));
#19434=CARTESIAN_POINT('Ctrl Pts',(7.539364321265,-0.179489948314284,-4.24504351679887));
#19435=CARTESIAN_POINT('Ctrl Pts',(7.52963449131211,-0.267941920153354,
-4.24966028886331));
#19436=CARTESIAN_POINT('Ctrl Pts',(7.5198755875487,-0.35665819628985,-4.25429085635449));
#19437=CARTESIAN_POINT('Ctrl Pts',(7.50528126099808,-0.44469903253678,-4.25892142384567));
#19438=CARTESIAN_POINT('Ctrl Pts',(7.4859791683996,-0.531562787407136,-4.26355199133684));
#19439=CARTESIAN_POINT('Ctrl Pts',(7.46659045105702,-0.618816373095013,
-4.26820334008383));
#19440=CARTESIAN_POINT('Ctrl Pts',(7.44245175280597,-0.704882000402029,
-4.27285468883082));
#19441=CARTESIAN_POINT('Ctrl Pts',(7.41374111740686,-0.789271473659132,
-4.27750603757781));
#19442=CARTESIAN_POINT('Ctrl Pts',(7.39113710915984,-0.855711673360351,
-4.28116806469686));
#19443=CARTESIAN_POINT('Ctrl Pts',(7.3657001849672,-0.921113270048054,-4.28483009181591));
#19444=CARTESIAN_POINT('Ctrl Pts',(7.33753740143156,-0.98524848748491,-4.28849211893496));
#19445=CARTESIAN_POINT('Ctrl Pts',(7.30498972995338,-1.05936942743657,-4.29272431620567));
#19446=CARTESIAN_POINT('Ctrl Pts',(7.26870453158392,-1.13201406130332,-4.29695651347637));
#19447=CARTESIAN_POINT('Ctrl Pts',(7.22883777657832,-1.20278007037137,-4.30118871074708));
#19448=CARTESIAN_POINT('Ctrl Pts',(7.18902800658851,-1.27344492743585,-4.30541485857062));
#19449=CARTESIAN_POINT('Ctrl Pts',(7.14564707388499,-1.3422360915104,-4.30964100639415));
#19450=CARTESIAN_POINT('Ctrl Pts',(7.09889861254965,-1.40877205464076,-4.31386715421769));
#19451=CARTESIAN_POINT('Ctrl Pts',(7.05213877125819,-1.47532421458958,-4.31809433081042));
#19452=CARTESIAN_POINT('Ctrl Pts',(7.00200997354623,-1.53961965964256,-4.32232150740315));
#19453=CARTESIAN_POINT('Ctrl Pts',(6.94876160275957,-1.60130210959577,-4.32654868399587));
#19454=CARTESIAN_POINT('Ctrl Pts',(6.89562148097813,-1.6628591648421,-4.33076726713017));
#19455=CARTESIAN_POINT('Ctrl Pts',(6.83937474176338,-1.72181347026048,-4.33498585026446));
#19456=CARTESIAN_POINT('Ctrl Pts',(6.78031090742075,-1.77784217644569,-4.33920443339876));
#19457=CARTESIAN_POINT('Ctrl Pts',(6.72126645803511,-1.83385249381359,-4.34342163197932));
#19458=CARTESIAN_POINT('Ctrl Pts',(6.65940708651111,-1.88693879926115,-4.34763883055987));
#19459=CARTESIAN_POINT('Ctrl Pts',(6.59505915027523,-1.93681510416519,-4.35185602914043));
#19460=CARTESIAN_POINT('Ctrl Pts',(6.53071264666796,-1.9866902986339,-4.35607313383019));
#19461=CARTESIAN_POINT('Ctrl Pts',(6.4638780564703,-2.03335535089688,-4.36029023851994));
#19462=CARTESIAN_POINT('Ctrl Pts',(6.39491365015738,-2.07656547772955,-4.3645073432097));
#19463=CARTESIAN_POINT('Ctrl Pts',(6.32566742818896,-2.1199521781147,-4.36874168064582));
#19464=CARTESIAN_POINT('Ctrl Pts',(6.2542743400458,-2.15985539631951,-4.37297601808194));
#19465=CARTESIAN_POINT('Ctrl Pts',(6.18112357533096,-2.19607302823035,-4.37721035551806));
#19466=CARTESIAN_POINT('Ctrl Pts',(6.10816496908693,-2.23219552067421,-4.38143356984686));
#19467=CARTESIAN_POINT('Ctrl Pts',(6.03345835416626,-2.26465161685163,-4.38565678417567));
#19468=CARTESIAN_POINT('Ctrl Pts',(5.95740984230358,-2.29328916470909,-4.38987999850447));
#19469=CARTESIAN_POINT('Ctrl Pts',(5.88106088543859,-2.32203985098204,-4.39411989749425));
#19470=CARTESIAN_POINT('Ctrl Pts',(5.80335985837994,-2.34694161948083,-4.39835979648404));
#19471=CARTESIAN_POINT('Ctrl Pts',(5.72473115985107,-2.3678915488752,-4.40259969547382));
#19472=CARTESIAN_POINT('Ctrl Pts',(5.64610246132221,-2.38884147826957,-4.4068395944636));
#19473=CARTESIAN_POINT('Ctrl Pts',(5.56654656112702,-2.40583953172261,-4.41107949345339));
#19474=CARTESIAN_POINT('Ctrl Pts',(5.48649434772001,-2.41883499356968,-4.41531939244317));
#19475=CARTESIAN_POINT('Ctrl Pts',(5.40658499139273,-2.43180726438117,-4.41955172512639));
#19476=CARTESIAN_POINT('Ctrl Pts',(5.32588318725199,-2.4408395937733,-4.42378405780961));
#19477=CARTESIAN_POINT('Ctrl Pts',(5.24481144096651,-2.44584422961235,-4.42801639049282));
#19478=CARTESIAN_POINT('Ctrl Pts',(5.16385551824722,-2.45084171555273,-4.43224267663224));
#19479=CARTESIAN_POINT('Ctrl Pts',(5.08253116295906,-2.45182290803043,-4.43646896277166));
#19480=CARTESIAN_POINT('Ctrl Pts',(5.00126931782718,-2.44875137502647,-4.44069524891108));
#19481=CARTESIAN_POINT('Ctrl Pts',(4.91999100920527,-2.44567921973595,-4.44492239128776));
#19482=CARTESIAN_POINT('Ctrl Pts',(4.83877570024038,-2.43855264889365,-4.44914953366444));
#19483=CARTESIAN_POINT('Ctrl Pts',(4.75805796902285,-2.42738734104056,-4.45337667604112));
#19484=CARTESIAN_POINT('Ctrl Pts',(4.67750092251725,-2.41624425995536,-4.45759540344943));
#19485=CARTESIAN_POINT('Ctrl Pts',(4.59743993829805,-2.40107854452902,-4.46181413085774));
#19486=CARTESIAN_POINT('Ctrl Pts',(4.5183034039012,-2.3819577371145,-4.46603285826605));
#19487=CARTESIAN_POINT('Ctrl Pts',(4.43919280575068,-2.36284319636271,-4.47025020302658));
#19488=CARTESIAN_POINT('Ctrl Pts',(4.3610065070123,-2.33977624689354,-4.47446754778712));
#19489=CARTESIAN_POINT('Ctrl Pts',(4.28416197600715,-2.31287538514135,-4.47868489254765));
#19490=CARTESIAN_POINT('Ctrl Pts',(4.20731912492323,-2.28597511147693,-4.48290214511155));
#19491=CARTESIAN_POINT('Ctrl Pts',(4.13181842140342,-2.25524124677705,-4.48711939767545));
#19492=CARTESIAN_POINT('Ctrl Pts',(4.05806009290624,-2.22084147163705,-4.49133665023935));
#19493=CARTESIAN_POINT('Ctrl Pts',(3.98400591954238,-2.18630371890053,-4.49557081821536));
#19494=CARTESIAN_POINT('Ctrl Pts',(3.91170855971481,-2.14807077559741,-4.49980498619136));
#19495=CARTESIAN_POINT('Ctrl Pts',(3.84154913832487,-2.10635942275229,-4.50403915416736));
#19496=CARTESIAN_POINT('Ctrl Pts',(3.77156872390866,-2.06475449357623,-4.50826251895285));
#19497=CARTESIAN_POINT('Ctrl Pts',(3.70371571876488,-2.01968917518783,-4.51248588373834));
#19498=CARTESIAN_POINT('Ctrl Pts',(3.63833860513962,-1.97142165198274,-4.51670924852383));
#19499=CARTESIAN_POINT('Ctrl Pts',(3.57271064363016,-1.92296892931868,-4.52094881809509));
#19500=CARTESIAN_POINT('Ctrl Pts',(3.50957796964361,-1.87128968515863,-4.52518838766635));
#19501=CARTESIAN_POINT('Ctrl Pts',(3.44925757793471,-1.81668410977279,-4.52942795723761));
#19502=CARTESIAN_POINT('Ctrl Pts',(3.38893718622581,-1.76207853438695,-4.53366752680887));
#19503=CARTESIAN_POINT('Ctrl Pts',(3.33142936290843,-1.70454700184035,-4.53790709638013));
#19504=CARTESIAN_POINT('Ctrl Pts',(3.27701083001953,-1.64442351285733,-4.54214666595139));
#19505=CARTESIAN_POINT('Ctrl Pts',(3.22269977497076,-1.58441876913247,-4.54637786227633));
#19506=CARTESIAN_POINT('Ctrl Pts',(3.17126305689973,-1.52160829688815,-4.55060905860126));
#19507=CARTESIAN_POINT('Ctrl Pts',(3.12300395699217,-1.45629879159744,-4.5548402549262));
#19508=CARTESIAN_POINT('Ctrl Pts',(3.07481386315022,-1.3910826728808,-4.55906540103031));
#19509=CARTESIAN_POINT('Ctrl Pts',(3.02979263726867,-1.32337498893158,-4.56329054713442));
#19510=CARTESIAN_POINT('Ctrl Pts',(2.98820508344839,-1.25351742703743,-4.56751569323853));
#19511=CARTESIAN_POINT('Ctrl Pts',(2.94659507980136,-1.18362215457803,-4.5717431201644));
#19512=CARTESIAN_POINT('Ctrl Pts',(2.90842275172535,-1.11157504490533,-4.57597054709028));
#19513=CARTESIAN_POINT('Ctrl Pts',(2.873911367295,-1.03774955720847,-4.58019797401616));
#19514=CARTESIAN_POINT('Ctrl Pts',(2.83948031483959,-0.9640959127258,-4.58441556078177));
#19515=CARTESIAN_POINT('Ctrl Pts',(2.80869339990547,-0.88867257172208,-4.58863314754738));
#19516=CARTESIAN_POINT('Ctrl Pts',(2.78172676412774,-0.811875624977789,
-4.59285073431299));
#19517=CARTESIAN_POINT('Ctrl Pts',(2.75476895412816,-0.735103812730058,
-4.59706694072529));
#19518=CARTESIAN_POINT('Ctrl Pts',(2.73162909420773,-0.656959725825265,
-4.60128314713759));
#19519=CARTESIAN_POINT('Ctrl Pts',(2.71243462366512,-0.577857992541767,
-4.60549935354988));
#19520=CARTESIAN_POINT('Ctrl Pts',(2.69324055545416,-0.498757917294607,
-4.60971547158708));
#19521=CARTESIAN_POINT('Ctrl Pts',(2.6779918207041,-0.418700687646197,-4.61393158962428));
#19522=CARTESIAN_POINT('Ctrl Pts',(2.66676520413243,-0.338113197688939,
-4.61814770766147));
#19523=CARTESIAN_POINT('Ctrl Pts',(2.65548692612198,-0.257154868872812,
-4.62238322697798));
#19524=CARTESIAN_POINT('Ctrl Pts',(2.64826795247294,-0.17566185414372,-4.6266187462945));
#19525=CARTESIAN_POINT('Ctrl Pts',(2.64513349959239,-0.0940724707205781,
-4.63085426561101));
#19526=CARTESIAN_POINT('Ctrl Pts',(2.64200886573112,-0.0127386750374495,
-4.63507651669623));
#19527=CARTESIAN_POINT('Ctrl Pts',(2.64294315023596,0.0686904189995033,
-4.63929876778145));
#19528=CARTESIAN_POINT('Ctrl Pts',(2.64790901419109,0.14978216264069,-4.64352101886667));
#19529=CARTESIAN_POINT('Ctrl Pts',(2.65289828564739,0.231256146935658,-4.64776317229883));
#19530=CARTESIAN_POINT('Ctrl Pts',(2.66195718106376,0.312389122891401,-4.65200532573098));
#19531=CARTESIAN_POINT('Ctrl Pts',(2.67500575817194,0.392750936414906,-4.65624747916314));
#19532=CARTESIAN_POINT('Ctrl Pts',(2.68805433528013,0.473112749938412,-4.66048963259529));
#19533=CARTESIAN_POINT('Ctrl Pts',(2.70509243458295,0.55270295544313,-4.66473178602745));
#19534=CARTESIAN_POINT('Ctrl Pts',(2.7259896763458,0.631106902620107,-4.6689739394596));
#19535=CARTESIAN_POINT('Ctrl Pts',(2.74684211988583,0.709342772232802,-4.6732069988239));
#19536=CARTESIAN_POINT('Ctrl Pts',(2.77161505289539,0.786689742421022,-4.67744005818819));
#19537=CARTESIAN_POINT('Ctrl Pts',(2.80021567526547,0.862726276377071,-4.68167311755248));
#19538=CARTESIAN_POINT('Ctrl Pts',(2.82877539968435,0.938654080585398,-4.68590012378083));
#19539=CARTESIAN_POINT('Ctrl Pts',(2.8611517802724,1.01327473923382,-4.69012713000918));
#19540=CARTESIAN_POINT('Ctrl Pts',(2.89720173634656,1.08618001184655,-4.69435413623753));
#19541=CARTESIAN_POINT('Ctrl Pts',(2.9332513112152,1.15908451353207,-4.69858109776796));
#19542=CARTESIAN_POINT('Ctrl Pts',(2.97297423605483,1.23027322347637,-4.70280805929839));
#19543=CARTESIAN_POINT('Ctrl Pts',(3.01617851871151,1.29935614526803,-4.70703502082882));
#19544=CARTESIAN_POINT('Ctrl Pts',(3.05930578486468,1.36831591896504,-4.71125444732389));
#19545=CARTESIAN_POINT('Ctrl Pts',(3.10590178478073,1.43517699764488,-4.71547387381895));
#19546=CARTESIAN_POINT('Ctrl Pts',(3.15572961509238,1.49957599809002,-4.71969330031402));
#19547=CARTESIAN_POINT('Ctrl Pts',(3.20554100646591,1.56395375235252,-4.72391133475789));
#19548=CARTESIAN_POINT('Ctrl Pts',(3.25858182676458,1.62587067445297,-4.72812936920175));
#19549=CARTESIAN_POINT('Ctrl Pts',(3.31457314015658,1.68499418368467,-4.73234740364562));
#19550=CARTESIAN_POINT('Ctrl Pts',(3.37056309323716,1.74411625650811,-4.73656533561215));
#19551=CARTESIAN_POINT('Ctrl Pts',(3.42950307669267,1.80044471494321,-4.74078326757868));
#19552=CARTESIAN_POINT('Ctrl Pts',(3.49107632108868,1.85368282425665,-4.74500119954521));
#19553=CARTESIAN_POINT('Ctrl Pts',(3.5528744105041,1.90711534144708,-4.7492345339971));
#19554=CARTESIAN_POINT('Ctrl Pts',(3.61732467862498,1.95743458243436,-4.75346786844898));
#19555=CARTESIAN_POINT('Ctrl Pts',(3.68407373946097,2.00438158944311,-4.75770120290087));
#19556=CARTESIAN_POINT('Ctrl Pts',(3.75067581467381,2.05122521619462,-4.76192521528448));
#19557=CARTESIAN_POINT('Ctrl Pts',(3.81956615421436,2.09471122721534,-4.76614922766808));
#19558=CARTESIAN_POINT('Ctrl Pts',(3.89036656291258,2.13462709909764,-4.77037324005169));
#19559=CARTESIAN_POINT('Ctrl Pts',(3.96140134814094,2.17467510783792,-4.77461123553771));
#19560=CARTESIAN_POINT('Ctrl Pts',(4.03435844437011,2.21112910154888,-4.77884923102374));
#19561=CARTESIAN_POINT('Ctrl Pts',(4.10883482557177,2.24382271137337,-4.78308722650976));
#19562=CARTESIAN_POINT('Ctrl Pts',(4.18331120677344,2.27651632119785,-4.78732522199578));
#19563=CARTESIAN_POINT('Ctrl Pts',(4.2593064159903,2.30544943910065,-4.7915632174818));
#19564=CARTESIAN_POINT('Ctrl Pts',(4.33640305275022,2.3305061636144,-4.79580121296782));
#19565=CARTESIAN_POINT('Ctrl Pts',(4.41341477979149,2.35553529211985,-4.80003454097392));
#19566=CARTESIAN_POINT('Ctrl Pts',(4.49181135896812,2.37678947487168,-4.80426786898002));
#19567=CARTESIAN_POINT('Ctrl Pts',(4.57118839547999,2.39411757785071,-4.80850119698611));
#19568=CARTESIAN_POINT('Ctrl Pts',(4.65045229706855,2.41142098333929,-4.81272849129203));
#19569=CARTESIAN_POINT('Ctrl Pts',(4.73069343056475,2.42480932489246,-4.81695578559795));
#19570=CARTESIAN_POINT('Ctrl Pts',(4.81149125040211,2.43418090673619,-4.82118307990387));
#19571=CARTESIAN_POINT('Ctrl Pts',(4.89228137968239,2.44355159656718,-4.82540997184438));
#19572=CARTESIAN_POINT('Ctrl Pts',(4.97362763800656,2.4489061761921,-4.82963686378488));
#19573=CARTESIAN_POINT('Ctrl Pts',(5.05509834107404,2.45019393700515,-4.83386375572539));
#19574=CARTESIAN_POINT('Ctrl Pts',(5.13643156187334,2.4514795247146,-4.83808351476205));
#19575=CARTESIAN_POINT('Ctrl Pts',(5.21788834432283,2.44871197281434,-4.84230327379871));
#19576=CARTESIAN_POINT('Ctrl Pts',(5.29903483032702,2.44189272085668,-4.84652303283537));
#19577=CARTESIAN_POINT('Ctrl Pts',(5.38015485222368,2.43507569284519,-4.85074141569221));
#19578=CARTESIAN_POINT('Ctrl Pts',(5.46096431626495,2.42420962781349,-4.85495979854904));
#19579=CARTESIAN_POINT('Ctrl Pts',(5.5410323879996,2.40934798856102,-4.85917818140588));
#19580=CARTESIAN_POINT('Ctrl Pts',(5.62109880477188,2.39448665649035,-4.86339647707109));
#19581=CARTESIAN_POINT('Ctrl Pts',(5.70042340335079,2.37563000029033,-4.86761477273631));
#19582=CARTESIAN_POINT('Ctrl Pts',(5.77858488702693,2.35288272105727,-4.87183306840152));
#19583=CARTESIAN_POINT('Ctrl Pts',(5.85701793115484,2.33005640978523,-4.87606601990773));
#19584=CARTESIAN_POINT('Ctrl Pts',(5.93427931019796,2.30331251641365,-4.88029897141394));
#19585=CARTESIAN_POINT('Ctrl Pts',(6.00995976488316,2.27280691919461,-4.88453192292015));
#19586=CARTESIAN_POINT('Ctrl Pts',(6.08548749420368,2.24236288316041,-4.88875633220677));
#19587=CARTESIAN_POINT('Ctrl Pts',(6.15944026498193,2.20817253964699,-4.89298074149339));
#19588=CARTESIAN_POINT('Ctrl Pts',(6.23143409427271,2.17043790575762,-4.89720515078002));
#19589=CARTESIAN_POINT('Ctrl Pts',(6.30364629270944,2.13258881650649,-4.90144237339602));
#19590=CARTESIAN_POINT('Ctrl Pts',(6.37388725118885,2.09117415365666,-4.90567959601202));
#19591=CARTESIAN_POINT('Ctrl Pts',(6.44179853445689,2.04644164622074,-4.90991681862802));
#19592=CARTESIAN_POINT('Ctrl Pts',(6.50970981772493,2.00170913878482,-4.91415404124403));
#19593=CARTESIAN_POINT('Ctrl Pts',(6.57529108735771,1.95365911117781,-4.91839126386003));
#19594=CARTESIAN_POINT('Ctrl Pts',(6.63821842469443,1.90257873884136,-4.92262848647603));
#19595=CARTESIAN_POINT('Ctrl Pts',(6.70017391982866,1.85228724560987,-4.92680026993739));
#19596=CARTESIAN_POINT('Ctrl Pts',(6.75980233382613,1.79885885488646,-4.93097205339874));
#19597=CARTESIAN_POINT('Ctrl Pts',(6.81676205169122,1.74253998327872,-4.9351438368601));
#19598=CARTESIAN_POINT('Ctrl Pts',(6.87403087073743,1.68591548814638,-4.93933825918351));
#19599=CARTESIAN_POINT('Ctrl Pts',(6.92860151443369,1.62636928924725,-4.94353268150691));
#19600=CARTESIAN_POINT('Ctrl Pts',(6.98015822822778,1.5641947877054,-4.94772710383032));
#19601=CARTESIAN_POINT('Ctrl Pts',(7.03130380679619,1.50251609215742,-4.95188807804112));
#19602=CARTESIAN_POINT('Ctrl Pts',(7.07948302343086,1.43825122094879,-4.95604905225193));
#19603=CARTESIAN_POINT('Ctrl Pts',(7.12442395388076,1.37172405833512,-4.96021002646273));
#19604=CARTESIAN_POINT('Ctrl Pts',(7.16933776961209,1.305237034305,-4.96436849018602));
#19605=CARTESIAN_POINT('Ctrl Pts',(7.21101690765184,1.23649082270111,-4.96852695390931));
#19606=CARTESIAN_POINT('Ctrl Pts',(7.24923098070076,1.16584072673234,-4.9726854176326));
#19607=CARTESIAN_POINT('Ctrl Pts',(7.28743447585925,1.09521018714463,-4.97684273026755));
#19608=CARTESIAN_POINT('Ctrl Pts',(7.32217458279344,1.0226772308401,-4.98100004290251));
#19609=CARTESIAN_POINT('Ctrl Pts',(7.35326619168597,0.948622944876998,-4.98515735553747));
#19610=CARTESIAN_POINT('Ctrl Pts',(7.3848344886857,0.873433278704817,-4.98937840696117));
#19611=CARTESIAN_POINT('Ctrl Pts',(7.41264123776607,0.79667569270143,-4.99359945838487));
#19612=CARTESIAN_POINT('Ctrl Pts',(7.43654358952192,0.718769754193858,-4.99782050980857));
#19613=CARTESIAN_POINT('Ctrl Pts',(7.46010728211529,0.64196762171163,-5.00198175549623));
#19614=CARTESIAN_POINT('Ctrl Pts',(7.47987644130325,0.564049955605879,-5.00614300118389));
#19615=CARTESIAN_POINT('Ctrl Pts',(7.4957652064418,0.485431611262245,-5.01030424687154));
#19616=CARTESIAN_POINT('Ctrl Pts',(7.51199650337201,0.405118403780354,-5.01455520116327));
#19617=CARTESIAN_POINT('Ctrl Pts',(7.52417805709933,0.32407447512187,-5.01880615545499));
#19618=CARTESIAN_POINT('Ctrl Pts',(7.53227411923112,0.242748130459943,-5.02305710974672));
#19619=CARTESIAN_POINT('Ctrl Pts',(7.54037018136291,0.161421785798016,-5.02730806403844));
#19620=CARTESIAN_POINT('Ctrl Pts',(7.5443807895523,0.0798135539581412,-5.03155901833017));
#19621=CARTESIAN_POINT('Ctrl Pts',(7.54432661329192,-0.00163007106614652,
-5.03580997262189));
#19622=CARTESIAN_POINT('Origin',(5.09382715545311,0.,-6.77268258743872));
#19623=CARTESIAN_POINT('',(6.2322445509742,-1.63799676314545,12.7063625311661));
#19624=CARTESIAN_POINT('Ctrl Pts',(6.2322445509742,-1.63799676314545,12.7063625311661));
#19625=CARTESIAN_POINT('Ctrl Pts',(6.18723751963155,-1.66927691494676,12.7026454909915));
#19626=CARTESIAN_POINT('Ctrl Pts',(6.14095921641945,-1.69868960221159,12.6988580646124));
#19627=CARTESIAN_POINT('Ctrl Pts',(5.93503956423552,-1.81794739040668,12.6823136378186));
#19628=CARTESIAN_POINT('Ctrl Pts',(5.76462383730148,-1.88749318531041,12.6695051840078));
#19629=CARTESIAN_POINT('Ctrl Pts',(5.56341161226874,-1.93884377134319,12.6559190568223));
#19630=CARTESIAN_POINT('Ctrl Pts',(5.5396236298541,-1.94445116206349,12.6543338775543));
#19631=CARTESIAN_POINT('Ctrl Pts',(5.50499088329774,-1.95194591492976,12.6520553073756));
#19632=CARTESIAN_POINT('Ctrl Pts',(5.49422482639037,-1.95418273937355,12.651351047854));
#19633=CARTESIAN_POINT('Ctrl Pts',(5.47532410946914,-1.95794691645816,12.6501216010108));
#19634=CARTESIAN_POINT('Ctrl Pts',(5.46719749484511,-1.95951285950553,12.6495952228125));
#19635=CARTESIAN_POINT('Ctrl Pts',(5.45032734667706,-1.96265486105093,12.6485070419849));
#19636=CARTESIAN_POINT('Ctrl Pts',(5.44158254368898,-1.96422317569687,12.6479454902952));
#19637=CARTESIAN_POINT('Ctrl Pts',(5.41897191528525,-1.96812248926442,12.646499853696));
#19638=CARTESIAN_POINT('Ctrl Pts',(5.40509124865864,-1.97036542993468,12.6456184974278));
#19639=CARTESIAN_POINT('Ctrl Pts',(5.34912562121874,-1.97880258950332,12.6420882725356));
#19640=CARTESIAN_POINT('Ctrl Pts',(5.30686941728698,-1.98379695924688,12.6394760781965));
#19641=CARTESIAN_POINT('Ctrl Pts',(5.11806873338589,-2.00000880851574,12.6279896156928));
#19642=CARTESIAN_POINT('Ctrl Pts',(4.97071634581146,-1.99636377597456,12.6195567854678));
#19643=CARTESIAN_POINT('Ctrl Pts',(4.73572640100998,-1.96441495345043,12.6056334717768));
#19644=CARTESIAN_POINT('Ctrl Pts',(4.64729381143923,-1.94621841789028,12.600269460508));
#19645=CARTESIAN_POINT('Ctrl Pts',(4.54986226646271,-1.91917939090682,12.5939245573538));
#19646=CARTESIAN_POINT('Ctrl Pts',(4.5393412980253,-1.91616616098604,12.5932335632078));
#19647=CARTESIAN_POINT('Ctrl Pts',(4.52349276982025,-1.91148565433896,12.5921830685969));
#19648=CARTESIAN_POINT('Ctrl Pts',(4.518146344896,-1.90988227929641,12.5918270316851));
#19649=CARTESIAN_POINT('Ctrl Pts',(4.51277827934583,-1.90824782640071,12.59146781953));
#19650=CARTESIAN_POINT('Ctrl Pts',(4.51274976313558,-1.90823914316996,12.5914659112757));
#19651=CARTESIAN_POINT('Ctrl Pts',(4.51269202440837,-1.9082215602227,12.5914620474027));
#19652=CARTESIAN_POINT('Ctrl Pts',(4.51266280188701,-1.90821266046981,12.5914600917812));
#19653=CARTESIAN_POINT('Ctrl Pts',(4.51260362535662,-1.90819463670315,12.5914561314808));
#19654=CARTESIAN_POINT('Ctrl Pts',(4.51257367136493,-1.90818551265747,12.5914541268006));
#19655=CARTESIAN_POINT('Ctrl Pts',(4.51251300550165,-1.90816703215337,12.5914500666086));
#19656=CARTESIAN_POINT('Ctrl Pts',(4.51248229364932,-1.90815767566129,12.5914480110954));
#19657=CARTESIAN_POINT('Ctrl Pts',(4.51242008440394,-1.90813872171764,12.5914438473776));
#19658=CARTESIAN_POINT('Ctrl Pts',(4.5123885870135,-1.90812912422485,12.5914417391702));
#19659=CARTESIAN_POINT('Ctrl Pts',(4.51232477765905,-1.90810967930591,12.591437468112));
#19660=CARTESIAN_POINT('Ctrl Pts',(4.51229246569785,-1.90809983183592,12.5914353052581));
#19661=CARTESIAN_POINT('Ctrl Pts',(4.51222699669508,-1.90807987752981,12.5914309228552));
#19662=CARTESIAN_POINT('Ctrl Pts',(4.51219383968033,-1.90806977065429,12.5914287033046));
#19663=CARTESIAN_POINT('Ctrl Pts',(4.51212664853273,-1.90804928762717,12.5914242053533));
#19664=CARTESIAN_POINT('Ctrl Pts',(4.51209261441863,-1.90803891143063,12.5914219269504));
#19665=CARTESIAN_POINT('Ctrl Pts',(4.5120236354109,-1.90801787934526,12.5914173090301));
#19666=CARTESIAN_POINT('Ctrl Pts',(4.51198869051462,-1.90800722340161,12.5914149695088));
#19667=CARTESIAN_POINT('Ctrl Pts',(4.51191785450351,-1.90798562085157,12.5914102269676));
#19668=CARTESIAN_POINT('Ctrl Pts',(4.51188196341328,-1.90797467419506,12.5914078239452));
#19669=CARTESIAN_POINT('Ctrl Pts',(4.51180919772279,-1.90795247867071,12.5914029518929));
#19670=CARTESIAN_POINT('Ctrl Pts',(4.51177232313178,-1.90794122974416,12.5914004828591));
#19671=CARTESIAN_POINT('Ctrl Pts',(4.51169755113618,-1.90791841750315,12.5913954761388));
#19672=CARTESIAN_POINT('Ctrl Pts',(4.51165965378225,-1.90790685413838,12.5913929384511));
#19673=CARTESIAN_POINT('Ctrl Pts',(4.5115827948851,-1.9078834001967,12.5913877916382));
#19674=CARTESIAN_POINT('Ctrl Pts',(4.51154383333025,-1.9078715095459,12.5913851825073));
#19675=CARTESIAN_POINT('Ctrl Pts',(4.51146480235348,-1.90784738748869,12.591379889868));
#19676=CARTESIAN_POINT('Ctrl Pts',(4.51142473296251,-1.90783515601643,12.5913772063563));
#19677=CARTESIAN_POINT('Ctrl Pts',(4.51134344021335,-1.90781033801536,12.5913717618517));
#19678=CARTESIAN_POINT('Ctrl Pts',(4.51130221687445,-1.90779775141175,12.5913690008544));
#19679=CARTESIAN_POINT('Ctrl Pts',(4.50696216130483,-1.90647246093234,12.5910783079931));
#19680=CARTESIAN_POINT('Ctrl Pts',(4.5026679041137,-1.90514527129782,12.5907895540963));
#19681=CARTESIAN_POINT('Ctrl Pts',(4.49303084428502,-1.90213110618786,12.5901389583457));
#19682=CARTESIAN_POINT('Ctrl Pts',(4.48769074418875,-1.9004361609251,12.5897766755344));
#19683=CARTESIAN_POINT('Ctrl Pts',(4.47199469809999,-1.89538135804588,12.5887067416442));
#19684=CARTESIAN_POINT('Ctrl Pts',(4.46165923216744,-1.89195924946562,12.5879956852284));
#19685=CARTESIAN_POINT('Ctrl Pts',(4.36404925557136,-1.85875114981835,12.5812216900391));
#19686=CARTESIAN_POINT('Ctrl Pts',(4.27892038465484,-1.82303445481991,12.5748729694351));
#19687=CARTESIAN_POINT('Ctrl Pts',(4.07991571698058,-1.72280969877737,12.5593908680569));
#19688=CARTESIAN_POINT('Ctrl Pts',(3.96929305990238,-1.65273095111793,12.5502534644303));
#19689=CARTESIAN_POINT('Ctrl Pts',(3.81805608485066,-1.53466072923676,12.53732382093));
#19690=CARTESIAN_POINT('Ctrl Pts',(3.77155685309105,-1.49478357640746,12.5332730538595));
#19691=CARTESIAN_POINT('Ctrl Pts',(3.71588647170828,-1.44240710531632,12.5283236466226));
#19692=CARTESIAN_POINT('Ctrl Pts',(3.70493080994919,-1.43186093873175,12.5273444003053));
#19693=CARTESIAN_POINT('Ctrl Pts',(3.68763813144638,-1.41482937616726,12.5257899741617));
#19694=CARTESIAN_POINT('Ctrl Pts',(3.68122305381124,-1.4084244358007,12.5252113539758));
#19695=CARTESIAN_POINT('Ctrl Pts',(3.66916162512141,-1.39621675777233,12.524119583994));
#19696=CARTESIAN_POINT('Ctrl Pts',(3.66350652545945,-1.39042295958586,12.5236060583568));
#19697=CARTESIAN_POINT('Ctrl Pts',(3.65075984945893,-1.37720359293777,12.5224447172042));
#19698=CARTESIAN_POINT('Ctrl Pts',(3.6436899808946,-1.36975733883143,12.5217978416863));
#19699=CARTESIAN_POINT('Ctrl Pts',(3.62555380862095,-1.35035782979332,12.520130996751));
#19700=CARTESIAN_POINT('Ctrl Pts',(3.61457572156844,-1.33832287180318,12.5191147470155));
#19701=CARTESIAN_POINT('Ctrl Pts',(3.51656816852848,-1.2282005562993,12.5099708012622));
#19702=CARTESIAN_POINT('Ctrl Pts',(3.43925665749271,-1.1218848075501,12.5022693904214));
#19703=CARTESIAN_POINT('Ctrl Pts',(3.32540327515749,-0.927651995339202,
12.4891855523885));
#19704=CARTESIAN_POINT('Ctrl Pts',(3.28366670373308,-0.843314085038435,
12.4837723108124));
#19705=CARTESIAN_POINT('Ctrl Pts',(3.23300736711884,-0.719685733890782,
12.4758239730855));
#19706=CARTESIAN_POINT('Ctrl Pts',(3.21907889568554,-0.682580702392783,
12.4734360065092));
#19707=CARTESIAN_POINT('Ctrl Pts',(3.19860980746405,-0.622687060603674,
12.4695414513147));
#19708=CARTESIAN_POINT('Ctrl Pts',(3.19135390953321,-0.600152817296067,
12.4680673079187));
#19709=CARTESIAN_POINT('Ctrl Pts',(3.18231918289361,-0.570282065938907,
12.4660950865986));
#19710=CARTESIAN_POINT('Ctrl Pts',(3.18017820016021,-0.563055978985791,
12.4656165954773));
#19711=CARTESIAN_POINT('Ctrl Pts',(3.17673380241601,-0.551184106655632,
12.4648279389091));
#19712=CARTESIAN_POINT('Ctrl Pts',(3.1754061811022,-0.546545339072591,12.464519150038));
#19713=CARTESIAN_POINT('Ctrl Pts',(3.17285136171797,-0.537494682097194,
12.4639153617674));
#19714=CARTESIAN_POINT('Ctrl Pts',(3.17162251456136,-0.533083342655446,
12.4636204581332));
#19715=CARTESIAN_POINT('Ctrl Pts',(3.16863876911263,-0.522227773975677,
12.4628932957496));
#19716=CARTESIAN_POINT('Ctrl Pts',(3.16690103708571,-0.515778927514173,
12.4624600653469));
#19717=CARTESIAN_POINT('Ctrl Pts',(3.16105405416527,-0.493638348530498,
12.4609686707115));
#19718=CARTESIAN_POINT('Ctrl Pts',(3.15710396446798,-0.477905766142753,
12.4599020482814));
#19719=CARTESIAN_POINT('Ctrl Pts',(3.13039713457844,-0.365763327402304,
12.4522588648364));
#19720=CARTESIAN_POINT('Ctrl Pts',(3.11466022664813,-0.26783309454235,12.4453805421707));
#19721=CARTESIAN_POINT('Ctrl Pts',(3.09619549174484,-0.0508676684509539,
12.4301977354646));
#19722=CARTESIAN_POINT('Ctrl Pts',(3.09670693678055,0.0680909993364611,
12.4219194855569));
#19723=CARTESIAN_POINT('Ctrl Pts',(3.11338612636969,0.245891031721891,12.4098909324857));
#19724=CARTESIAN_POINT('Ctrl Pts',(3.12165462170422,0.305197996803086,12.4059332340362));
#19725=CARTESIAN_POINT('Ctrl Pts',(3.13531309294309,0.378780583618809,12.401089088398));
#19726=CARTESIAN_POINT('Ctrl Pts',(3.13821356534267,0.393481346636533,12.4001245546047));
#19727=CARTESIAN_POINT('Ctrl Pts',(3.14310968073674,0.416903953167463,12.3985926660017));
#19728=CARTESIAN_POINT('Ctrl Pts',(3.14499878804879,0.425647237797762,12.3980219300497));
#19729=CARTESIAN_POINT('Ctrl Pts',(3.14868775248628,0.44218117563066,12.396944614798));
#19730=CARTESIAN_POINT('Ctrl Pts',(3.15047575830151,0.449974265149608,12.396437667005));
#19731=CARTESIAN_POINT('Ctrl Pts',(3.15463928449656,0.467633337781124,12.3952907195161));
#19732=CARTESIAN_POINT('Ctrl Pts',(3.15704334351841,0.477492418203566,12.3946516515278));
#19733=CARTESIAN_POINT('Ctrl Pts',(3.16345856869421,0.502955505473551,12.3930041633034));
#19734=CARTESIAN_POINT('Ctrl Pts',(3.16758377758906,0.518530225055481,12.3919994293147));
#19735=CARTESIAN_POINT('Ctrl Pts',(3.20654119372476,0.658728544150087,12.3829776374736));
#19736=CARTESIAN_POINT('Ctrl Pts',(3.25323521727404,0.779743135453562,12.3753793957891));
#19737=CARTESIAN_POINT('Ctrl Pts',(3.35289618582782,0.978141931426943,12.3624883358535));
#19738=CARTESIAN_POINT('Ctrl Pts',(3.40017137634611,1.0578897922908,12.3571622729389));
#19739=CARTESIAN_POINT('Ctrl Pts',(3.48778134483719,1.18466360433034,12.3480200883196));
#19740=CARTESIAN_POINT('Ctrl Pts',(3.52506920610242,1.23361577413524,12.3443007546343));
#19741=CARTESIAN_POINT('Ctrl Pts',(3.57096387177269,1.28841555581908,12.3398099546415));
#19742=CARTESIAN_POINT('Ctrl Pts',(3.57743090723702,1.29602069188735,12.3391790086005));
#19743=CARTESIAN_POINT('Ctrl Pts',(3.58743845899392,1.30761197525262,12.3382048798982));
#19744=CARTESIAN_POINT('Ctrl Pts',(3.59093843681843,1.31163313485098,12.3378646075071));
#19745=CARTESIAN_POINT('Ctrl Pts',(3.59741173006245,1.31901044025377,12.3372359172888));
#19746=CARTESIAN_POINT('Ctrl Pts',(3.60038028502556,1.32237064037352,12.3369478499126));
#19747=CARTESIAN_POINT('Ctrl Pts',(3.6071076499983,1.32993400961694,12.3362955972534));
#19748=CARTESIAN_POINT('Ctrl Pts',(3.61087297425112,1.33413127255403,12.3359309324031));
#19749=CARTESIAN_POINT('Ctrl Pts',(3.62060707019488,1.344889891772,12.3349893639296));
#19750=CARTESIAN_POINT('Ctrl Pts',(3.62660182826597,1.3514274205184,12.3344106091692));
#19751=CARTESIAN_POINT('Ctrl Pts',(3.66443928092342,1.39214220329821,12.3307657816568));
#19752=CARTESIAN_POINT('Ctrl Pts',(3.69742815539956,1.42522934092756,12.327624001904));
#19753=CARTESIAN_POINT('Ctrl Pts',(3.74617306669238,1.47080149990933,12.3230692513813));
#19754=CARTESIAN_POINT('Ctrl Pts',(3.76100628899616,1.48425641121027,12.3216940853168));
#19755=CARTESIAN_POINT('Ctrl Pts',(3.88677879421587,1.59493628545549,12.3101392768706));
#19756=CARTESIAN_POINT('Ctrl Pts',(4.00800176840245,1.67981488847997,12.299722688753));
#19757=CARTESIAN_POINT('Ctrl Pts',(4.2008405366079,1.78516543736933,12.2848115688193));
#19758=CARTESIAN_POINT('Ctrl Pts',(4.26604209303637,1.81631901648813,12.2800110676617));
#19759=CARTESIAN_POINT('Ctrl Pts',(4.34751462023686,1.84994558677418,12.2742990684326));
#19760=CARTESIAN_POINT('Ctrl Pts',(4.36230490152697,1.85584382168861,12.2732731313827));
#19761=CARTESIAN_POINT('Ctrl Pts',(4.38575737200205,1.86487252204341,12.271663242785));
#19762=CARTESIAN_POINT('Ctrl Pts',(4.39437308076907,1.86812107310452,12.2710753834234));
#19763=CARTESIAN_POINT('Ctrl Pts',(4.41056577820019,1.87409879784304,12.2699770900376));
#19764=CARTESIAN_POINT('Ctrl Pts',(4.41813737017176,1.876841956819,12.2694662022758));
#19765=CARTESIAN_POINT('Ctrl Pts',(4.43513750058359,1.88288482938028,12.2683249895967));
#19766=CARTESIAN_POINT('Ctrl Pts',(4.4445746745822,1.88615973979641,12.2676954906258));
#19767=CARTESIAN_POINT('Ctrl Pts',(4.46863667263551,1.89430780001674,12.2661003878841));
#19768=CARTESIAN_POINT('Ctrl Pts',(4.48329428160301,1.89908262370223,12.265137995578));
#19769=CARTESIAN_POINT('Ctrl Pts',(4.57630408552551,1.92819307903178,12.2590869040561));
#19770=CARTESIAN_POINT('Ctrl Pts',(4.65604460436796,1.94784687925749,12.2541525791783));
#19771=CARTESIAN_POINT('Ctrl Pts',(4.87062024860056,1.98688529734874,12.2412754013749));
#19772=CARTESIAN_POINT('Ctrl Pts',(5.00659553874558,1.99747901975286,12.2335393632787));
#19773=CARTESIAN_POINT('Ctrl Pts',(5.20669153551384,1.9925865806146,12.2216712890258));
#19774=CARTESIAN_POINT('Ctrl Pts',(5.27067835883385,1.98792895377555,12.2177979524977));
#19775=CARTESIAN_POINT('Ctrl Pts',(5.34441016464217,1.97897422467048,12.2131319487659));
#19776=CARTESIAN_POINT('Ctrl Pts',(5.3544881651005,1.97767202898286,12.2124897462396));
#19777=CARTESIAN_POINT('Ctrl Pts',(5.36991655704566,1.97555852478028,12.2114991972189));
#19778=CARTESIAN_POINT('Ctrl Pts',(5.37527450285379,1.97480232719358,12.211153829856));
#19779=CARTESIAN_POINT('Ctrl Pts',(5.38509282836015,1.97337584219566,12.2105183265323));
#19780=CARTESIAN_POINT('Ctrl Pts',(5.38955406899058,1.97271221883778,12.2102285642118));
#19781=CARTESIAN_POINT('Ctrl Pts',(5.3995884364275,1.97118477234887,12.2095745560146));
#19782=CARTESIAN_POINT('Ctrl Pts',(5.40516011362618,1.9703124510988,12.2092098486817));
#19783=CARTESIAN_POINT('Ctrl Pts',(5.42155091597614,1.96767499074004,12.2081324942697));
#19784=CARTESIAN_POINT('Ctrl Pts',(5.43235906903729,1.965844312991,12.207416360505));
#19785=CARTESIAN_POINT('Ctrl Pts',(5.53867668276732,1.94693355315497,12.200319058902));
#19786=CARTESIAN_POINT('Ctrl Pts',(5.63282436823093,1.9229973877585,12.1936192697975));
#19787=CARTESIAN_POINT('Ctrl Pts',(5.84595090681782,1.85192737131336,12.1779824887464));
#19788=CARTESIAN_POINT('Ctrl Pts',(5.96291472946638,1.80000517724095,12.1690571620422));
#19789=CARTESIAN_POINT('Ctrl Pts',(6.12688048745212,1.70748305145927,12.1563727763964));
#19790=CARTESIAN_POINT('Ctrl Pts',(6.17826131600852,1.6753212809606,12.1523654154912));
#19791=CARTESIAN_POINT('Ctrl Pts',(6.24053571284764,1.63227310121271,12.1474643296516));
#19792=CARTESIAN_POINT('Ctrl Pts',(6.25287049849402,1.62353766271917,12.1464912115559));
#19793=CARTESIAN_POINT('Ctrl Pts',(6.27240458806707,1.60936761433364,12.1449460107085));
#19794=CARTESIAN_POINT('Ctrl Pts',(6.27966818607189,1.60402304759612,12.1443705138342));
#19795=CARTESIAN_POINT('Ctrl Pts',(6.29335347991602,1.59380961724399,12.143284356848));
#19796=CARTESIAN_POINT('Ctrl Pts',(6.29978238016489,1.5889507538589,12.1427733245512));
#19797=CARTESIAN_POINT('Ctrl Pts',(6.31430179991397,1.57783831950005,12.1416172706325));
#19798=CARTESIAN_POINT('Ctrl Pts',(6.32237407443138,1.57156119650483,12.1409731868925));
#19799=CARTESIAN_POINT('Ctrl Pts',(6.34313511373106,1.55515937638821,12.1393128586219));
#19800=CARTESIAN_POINT('Ctrl Pts',(6.35574935547309,1.54494124349367,12.1383003251915));
#19801=CARTESIAN_POINT('Ctrl Pts',(6.46689292308435,1.45264011801318,12.1293409610452));
#19802=CARTESIAN_POINT('Ctrl Pts',(6.5574229852202,1.36138401169962,12.1218012028334));
#19803=CARTESIAN_POINT('Ctrl Pts',(6.69624716482366,1.1914642308639,12.109044984281));
#19804=CARTESIAN_POINT('Ctrl Pts',(6.74901103184418,1.11700573473798,12.1037947930387));
#19805=CARTESIAN_POINT('Ctrl Pts',(6.82926078749395,0.985521692073947,12.0946578200157));
#19806=CARTESIAN_POINT('Ctrl Pts',(6.85946477614059,0.930325206395275,12.0908566646311));
#19807=CARTESIAN_POINT('Ctrl Pts',(6.89142762493263,0.864732262928983,12.0862723767022));
#19808=CARTESIAN_POINT('Ctrl Pts',(6.89577779887109,0.855630295769165,12.0856347756757));
#19809=CARTESIAN_POINT('Ctrl Pts',(6.90234160229976,0.841624619315283,12.0846508354907));
#19810=CARTESIAN_POINT('Ctrl Pts',(6.90460481827666,0.836744141583591,12.0843074444435));
#19811=CARTESIAN_POINT('Ctrl Pts',(6.90872239383953,0.827769915867824,12.0836749510917));
#19812=CARTESIAN_POINT('Ctrl Pts',(6.91058268539381,0.8236790049598,12.0833862156832));
#19813=CARTESIAN_POINT('Ctrl Pts',(6.91474172076468,0.814450359628221,12.0827339330049));
#19814=CARTESIAN_POINT('Ctrl Pts',(6.91703253430751,0.809309203643577,12.0823699206554));
#19815=CARTESIAN_POINT('Ctrl Pts',(6.9237146727944,0.794140461947037,12.081294202982));
#19816=CARTESIAN_POINT('Ctrl Pts',(6.92804516097314,0.784086535218607,12.0805790113496));
#19817=CARTESIAN_POINT('Ctrl Pts',(6.97014991853022,0.684075727522825,12.0734465813574));
#19818=CARTESIAN_POINT('Ctrl Pts',(7.00135464276814,0.591507502141149,12.0667064368498));
#19819=CARTESIAN_POINT('Ctrl Pts',(7.05741340275238,0.373625754207483,12.051043138094));
#19820=CARTESIAN_POINT('Ctrl Pts',(7.07727084328638,0.247436917017078,12.0421331004315));
#19821=CARTESIAN_POINT('Ctrl Pts',(7.08736833456825,0.0801813959388592,
12.030843681731));
#19822=CARTESIAN_POINT('Ctrl Pts',(7.0885771551553,0.0400941634017856,12.0281742241702));
#19823=CARTESIAN_POINT('Ctrl Pts',(7.08857715545311,1.48164940157807E-8,
12.0255409243712));
#19824=CARTESIAN_POINT('',(3.93347817078409,-1.62253437445176,12.7063625311661));
#19825=CARTESIAN_POINT('Origin',(5.09382715545311,0.,12.7063625311661));
#19826=CARTESIAN_POINT('Ctrl Pts',(7.08857671409759,0.0013269467482341,
12.1854076497708));
#19827=CARTESIAN_POINT('Ctrl Pts',(7.08852952443368,0.0722654085738397,
12.1899562455583));
#19828=CARTESIAN_POINT('Ctrl Pts',(7.08469842768434,0.143085755684006,12.1945048413457));
#19829=CARTESIAN_POINT('Ctrl Pts',(7.07711961581017,0.213491403084141,12.1990534371332));
#19830=CARTESIAN_POINT('Ctrl Pts',(7.0696816549397,0.282588572814277,12.2035174979971));
#19831=CARTESIAN_POINT('Ctrl Pts',(7.05861405494534,0.351430098961739,12.2079815588611));
#19832=CARTESIAN_POINT('Ctrl Pts',(7.04394472965862,0.419605778409722,12.212445619725));
#19833=CARTESIAN_POINT('Ctrl Pts',(7.0292973878188,0.487679289802924,12.2169029907485));
#19834=CARTESIAN_POINT('Ctrl Pts',(7.01105913665847,0.555088462726542,12.2213603617721));
#19835=CARTESIAN_POINT('Ctrl Pts',(6.98930956850293,0.621428985740803,12.2258177327956));
#19836=CARTESIAN_POINT('Ctrl Pts',(6.96758580705325,0.687690793152414,12.2302698149756));
#19837=CARTESIAN_POINT('Ctrl Pts',(6.94235915592093,0.75288600875125,12.2347218971556));
#19838=CARTESIAN_POINT('Ctrl Pts',(6.91375968328197,0.816623019912162,12.2391739793356));
#19839=CARTESIAN_POINT('Ctrl Pts',(6.88517841785667,0.880319454332546,12.2436232271972));
#19840=CARTESIAN_POINT('Ctrl Pts',(6.85322879026267,0.942559082802846,12.2480724750588));
#19841=CARTESIAN_POINT('Ctrl Pts',(6.81808935639918,1.002969304061,12.2525217229204));
#19842=CARTESIAN_POINT('Ctrl Pts',(6.78296049682802,1.0633613464452,12.2569696318973));
#19843=CARTESIAN_POINT('Ctrl Pts',(6.74464398165632,1.12192465379024,12.2614175408743));
#19844=CARTESIAN_POINT('Ctrl Pts',(6.70336394796837,1.17831187554046,12.2658654498513));
#19845=CARTESIAN_POINT('Ctrl Pts',(6.66208247919094,1.23470105757758,12.2703135134587));
#19846=CARTESIAN_POINT('Ctrl Pts',(6.61783757702986,1.28891361215761,12.274761577066));
#19847=CARTESIAN_POINT('Ctrl Pts',(6.57089523458937,1.34063322802947,12.2792096406734));
#19848=CARTESIAN_POINT('Ctrl Pts',(6.52390530755207,1.39240527113313,12.2836622132017));
#19849=CARTESIAN_POINT('Ctrl Pts',(6.47421281053821,1.44167897015133,12.2881147857301));
#19850=CARTESIAN_POINT('Ctrl Pts',(6.42212171514428,1.48817375504167,12.2925673582585));
#19851=CARTESIAN_POINT('Ctrl Pts',(6.370001166536,1.53469482889475,12.297022448349));
#19852=CARTESIAN_POINT('Ctrl Pts',(6.31547969951562,1.57843355534781,12.3014775384396));
#19853=CARTESIAN_POINT('Ctrl Pts',(6.25889346380344,1.61915041291627,12.3059326285302));
#19854=CARTESIAN_POINT('Ctrl Pts',(6.20221252669866,1.65993541325949,12.3103951745547));
#19855=CARTESIAN_POINT('Ctrl Pts',(6.14346033266793,1.69768818583729,12.3148577205792));
#19856=CARTESIAN_POINT('Ctrl Pts',(6.08300030721383,1.73221362375885,12.3193202666037));
#19857=CARTESIAN_POINT('Ctrl Pts',(6.05337263044726,1.74913238135581,12.3215070812829));
#19858=CARTESIAN_POINT('Ctrl Pts',(6.02333518917303,1.76527685320593,12.3236938959622));
#19859=CARTESIAN_POINT('Ctrl Pts',(5.99293249614417,1.78062830170724,12.3258807106414));
#19860=CARTESIAN_POINT('Ctrl Pts',(5.93089953607057,1.81195104640785,12.3303426373384));
#19861=CARTESIAN_POINT('Ctrl Pts',(5.86710968920218,1.84008796029356,12.3348045640354));
#19862=CARTESIAN_POINT('Ctrl Pts',(5.80192264234284,1.86484003173098,12.3392664907323));
#19863=CARTESIAN_POINT('Ctrl Pts',(5.7368312905586,1.88955576694135,12.3437218672874));
#19864=CARTESIAN_POINT('Ctrl Pts',(5.67034726249248,1.91089635161925,12.3481772438424));
#19865=CARTESIAN_POINT('Ctrl Pts',(5.60285331167373,1.92870939614636,12.3526326203974));
#19866=CARTESIAN_POINT('Ctrl Pts',(5.53543625303222,1.94650214724332,12.3570829211849));
#19867=CARTESIAN_POINT('Ctrl Pts',(5.46701202615253,1.96077521685046,12.3615332219724));
#19868=CARTESIAN_POINT('Ctrl Pts',(5.39798009560142,1.9714255125414,12.3659835227599));
#19869=CARTESIAN_POINT('Ctrl Pts',(5.32899007130282,1.98206934290569,12.3704311219653));
#19870=CARTESIAN_POINT('Ctrl Pts',(5.25939355597442,1.98909468865264,12.3748787211707));
#19871=CARTESIAN_POINT('Ctrl Pts',(5.18960031806416,1.99244951349425,12.3793263203761));
#19872=CARTESIAN_POINT('Ctrl Pts',(5.11982598868202,1.99580342943979,12.3837727146288));
#19873=CARTESIAN_POINT('Ctrl Pts',(5.04985552917746,1.9954887755675,12.3882191088814));
#19874=CARTESIAN_POINT('Ctrl Pts',(4.98010218929287,1.99150550955097,12.392665503134));
#19875=CARTESIAN_POINT('Ctrl Pts',(4.91034430162017,1.98752198383289,12.3971121872833));
#19876=CARTESIAN_POINT('Ctrl Pts',(4.84080404815237,1.97986940126113,12.4015588714326));
#19877=CARTESIAN_POINT('Ctrl Pts',(4.77189127271463,1.96859971804971,12.4060055555819));
#19878=CARTESIAN_POINT('Ctrl Pts',(4.70290534783468,1.95731807230978,12.4104569597916));
#19879=CARTESIAN_POINT('Ctrl Pts',(4.63454871228637,1.94241174169231,12.4149083640013));
#19880=CARTESIAN_POINT('Ctrl Pts',(4.56722176774901,1.92398397294287,12.419359768211));
#19881=CARTESIAN_POINT('Ctrl Pts',(4.49985495273736,1.90554529141719,12.4238138085064));
#19882=CARTESIAN_POINT('Ctrl Pts',(4.43351950537399,1.88358117388198,12.4282678488019));
#19883=CARTESIAN_POINT('Ctrl Pts',(4.36859875255737,1.85824415137874,12.4327218890973));
#19884=CARTESIAN_POINT('Ctrl Pts',(4.30356652679628,1.83286362364212,12.4371835772552));
#19885=CARTESIAN_POINT('Ctrl Pts',(4.23995428840741,1.80409883119403,12.4416452654131));
#19886=CARTESIAN_POINT('Ctrl Pts',(4.17812281934862,1.77214929713595,12.4461069535709));
#19887=CARTESIAN_POINT('Ctrl Pts',(4.14762977101178,1.7563929403616,12.4483072970972));
#19888=CARTESIAN_POINT('Ctrl Pts',(4.1175694080126,1.73986270713659,12.4505076406234));
#19889=CARTESIAN_POINT('Ctrl Pts',(4.08798234152434,1.72258636149036,12.4527079841497));
#19890=CARTESIAN_POINT('Ctrl Pts',(4.02872379827553,1.68798438173463,12.4571149486611));
#19891=CARTESIAN_POINT('Ctrl Pts',(3.97112187864988,1.65024433874099,12.4615219131726));
#19892=CARTESIAN_POINT('Ctrl Pts',(3.91553427760012,1.60955070019584,12.4659288776841));
#19893=CARTESIAN_POINT('Ctrl Pts',(3.86003112086898,1.56891888023099,12.4703291474811));
#19894=CARTESIAN_POINT('Ctrl Pts',(3.80653661376772,1.52534265688757,12.4747294172781));
#19895=CARTESIAN_POINT('Ctrl Pts',(3.75538257227053,1.47905160837924,12.4791296870752));
#19896=CARTESIAN_POINT('Ctrl Pts',(3.70428711683655,1.43281357641103,12.4835249173));
#19897=CARTESIAN_POINT('Ctrl Pts',(3.65552717687369,1.38386722368545,12.4879201475249));
#19898=CARTESIAN_POINT('Ctrl Pts',(3.60940280615803,1.33248336339328,12.4923153777497));
#19899=CARTESIAN_POINT('Ctrl Pts',(3.56330634682053,1.2811305971699,12.4967079482758));
#19900=CARTESIAN_POINT('Ctrl Pts',(3.51984262916518,1.22734361880134,12.5011005188019));
#19901=CARTESIAN_POINT('Ctrl Pts',(3.47927478295544,1.1714299803924,12.5054930893279));
#19902=CARTESIAN_POINT('Ctrl Pts',(3.43871700971986,1.11553022530949,12.5098845691811));
#19903=CARTESIAN_POINT('Ctrl Pts',(3.40105397551522,1.05750526279527,12.5142760490343));
#19904=CARTESIAN_POINT('Ctrl Pts',(3.36650723192758,0.997694063474245,12.5186675288875));
#19905=CARTESIAN_POINT('Ctrl Pts',(3.33195673872641,0.937876372401497,12.5230594853805));
#19906=CARTESIAN_POINT('Ctrl Pts',(3.30052345541993,0.876272494759972,12.5274514418734));
#19907=CARTESIAN_POINT('Ctrl Pts',(3.27238348676533,0.813246902420903,12.5318433983664));
#19908=CARTESIAN_POINT('Ctrl Pts',(3.24420912633263,0.750144282199782,12.5362407225694));
#19909=CARTESIAN_POINT('Ctrl Pts',(3.2193363165379,0.68561693831397,12.5406380467725));
#19910=CARTESIAN_POINT('Ctrl Pts',(3.19789297972795,0.620049323697209,12.5450353709755));
#19911=CARTESIAN_POINT('Ctrl Pts',(3.17643544802973,0.554438305156324,12.549435606084));
#19912=CARTESIAN_POINT('Ctrl Pts',(3.15841203243788,0.48778613016387,12.5538358411925));
#19913=CARTESIAN_POINT('Ctrl Pts',(3.14389992929858,0.420489447193765,12.558236076301));
#19914=CARTESIAN_POINT('Ctrl Pts',(3.12935926600675,0.353060322804765,12.5626449711733));
#19915=CARTESIAN_POINT('Ctrl Pts',(3.11834378409934,0.284984653093198,12.5670538660456));
#19916=CARTESIAN_POINT('Ctrl Pts',(3.11087893255167,0.216665428234485,12.5714627609179));
#19917=CARTESIAN_POINT('Ctrl Pts',(3.10632299192651,0.17496890821315,12.5741535931646));
#19918=CARTESIAN_POINT('Ctrl Pts',(3.10308859917712,0.133181711858857,12.5768444254112));
#19919=CARTESIAN_POINT('Ctrl Pts',(3.10117201157415,0.0913949674364949,
12.5795352576578));
#19920=CARTESIAN_POINT('Ctrl Pts',(3.09790982357712,0.0202705294624338,
12.5841152730161));
#19921=CARTESIAN_POINT('Ctrl Pts',(3.09845473118738,-0.0511425087401567,
12.5886952883743));
#19922=CARTESIAN_POINT('Ctrl Pts',(3.10283697426873,-0.122415934123722,
12.5932753037325));
#19923=CARTESIAN_POINT('Ctrl Pts',(3.10734547188689,-0.195742781269199,
12.5979872715423));
#19924=CARTESIAN_POINT('Ctrl Pts',(3.11591592914825,-0.26892136795584,12.602699239352));
#19925=CARTESIAN_POINT('Ctrl Pts',(3.12852366695523,-0.341481713416793,
12.6074112071617));
#19926=CARTESIAN_POINT('Ctrl Pts',(3.14073779752797,-0.411776761381121,
12.611976069706));
#19927=CARTESIAN_POINT('Ctrl Pts',(3.15674076481258,-0.481491110343606,
12.6165409322502));
#19928=CARTESIAN_POINT('Ctrl Pts',(3.17645751882798,-0.550201089646342,
12.6211057947944));
#19929=CARTESIAN_POINT('Ctrl Pts',(3.19615568536413,-0.618846294325737,
12.6256663539281));
#19930=CARTESIAN_POINT('Ctrl Pts',(3.21956055507191,-0.686488574425669,
12.6302269130617));
#19931=CARTESIAN_POINT('Ctrl Pts',(3.24654635307994,-0.752715882444068,
12.6347874721954));
#19932=CARTESIAN_POINT('Ctrl Pts',(3.27351392811627,-0.818898468480926,
12.6393449516743));
#19933=CARTESIAN_POINT('Ctrl Pts',(3.30405745206538,-0.883667560659087,
12.6439024311533));
#19934=CARTESIAN_POINT('Ctrl Pts',(3.33800223095384,-0.946628964804647,
12.6484599106322));
#19935=CARTESIAN_POINT('Ctrl Pts',(3.37193315718283,-1.00956467478106,12.6530155302313));
#19936=CARTESIAN_POINT('Ctrl Pts',(3.40926236073151,-1.0706937633267,12.6575711498303));
#19937=CARTESIAN_POINT('Ctrl Pts',(3.44976881160282,-1.12964584030406,12.6621267694294));
#19938=CARTESIAN_POINT('Ctrl Pts',(3.49028059898438,-1.18860568390513,12.6666829892072));
#19939=CARTESIAN_POINT('Ctrl Pts',(3.53397021691296,-1.24538756331038,12.671239208985));
#19940=CARTESIAN_POINT('Ctrl Pts',(3.58057339540124,-1.29965019147034,12.6757954287628));
#19941=CARTESIAN_POINT('Ctrl Pts',(3.62717973921168,-1.3539165051879,12.6803519580024));
#19942=CARTESIAN_POINT('Ctrl Pts',(3.67669973409684,-1.40566288633933,12.684908487242));
#19943=CARTESIAN_POINT('Ctrl Pts',(3.72883010209269,-1.45458262289131,12.6894650164816));
#19944=CARTESIAN_POINT('Ctrl Pts',(3.78099529562535,-1.50353504012734,12.694024589697));
#19945=CARTESIAN_POINT('Ctrl Pts',(3.83577400428353,-1.54965673795645,12.6985841629123));
#19946=CARTESIAN_POINT('Ctrl Pts',(3.89282823149158,-1.59267986335712,12.7031437361277));
#19947=CARTESIAN_POINT('Ctrl Pts',(3.90625389326459,-1.60280380961513,12.7042166678072));
#19948=CARTESIAN_POINT('Ctrl Pts',(3.91980542131159,-1.61275636221494,12.7052895994866));
#19949=CARTESIAN_POINT('Ctrl Pts',(3.93347817078409,-1.62253437445176,12.7063625311661));
#19950=CARTESIAN_POINT('Ctrl Pts',(5.96741924226898,-1.78935549366613,-5.55880302681794));
#19951=CARTESIAN_POINT('Ctrl Pts',(6.5615443607172,-1.49929406993443,-5.51652726898187));
#19952=CARTESIAN_POINT('Ctrl Pts',(7.42803687527648,-0.286026890556653,
-5.43197575330973));
#19953=CARTESIAN_POINT('Ctrl Pts',(6.60117793883817,1.80796350105253,-5.30514847980151));
#19954=CARTESIAN_POINT('Ctrl Pts',(4.3963971709158,2.24586678413418,-5.17832120629329));
#19955=CARTESIAN_POINT('Ctrl Pts',(2.82926100857112,0.636515102147664,-5.05149393278508));
#19956=CARTESIAN_POINT('Ctrl Pts',(3.32878390476465,-1.5553570121133,-4.92466665927686));
#19957=CARTESIAN_POINT('Ctrl Pts',(5.43978137117777,-2.32666155138565,-4.79783938576864));
#19958=CARTESIAN_POINT('Ctrl Pts',(7.2348341668827,-0.974507642748168,-4.67101211226043));
#19959=CARTESIAN_POINT('Ctrl Pts',(7.07556887268865,1.26742862746759,-4.54418483875221));
#19960=CARTESIAN_POINT('Ctrl Pts',(5.10725347901043,2.35229469782244,-4.417357565244));
#19961=CARTESIAN_POINT('Ctrl Pts',(3.12670289415786,1.2899543892979,-4.29053029173577));
#19962=CARTESIAN_POINT('Ctrl Pts',(2.94180830639893,-0.949937059360794,
-4.16370301822756));
#19963=CARTESIAN_POINT('Ctrl Pts',(4.72136534354493,-2.3226730290144,-4.03687574471934));
#19964=CARTESIAN_POINT('Ctrl Pts',(6.84091687949711,-1.57519194182562,-3.91004847121113));
#19965=CARTESIAN_POINT('Ctrl Pts',(7.36565906395742,0.610189633448571,-3.78322119770291));
#19966=CARTESIAN_POINT('Ctrl Pts',(5.81658455864063,2.23856420545701,-3.65639392419469));
#19967=CARTESIAN_POINT('Ctrl Pts',(3.60774963453304,1.82349219851761,-3.52956665068648));
#19968=CARTESIAN_POINT('Ctrl Pts',(2.75546340395978,-0.256134521428759,
-3.40273937717826));
#19969=CARTESIAN_POINT('Ctrl Pts',(4.03772598570737,-2.10195142318311,-3.27591210367005));
#19970=CARTESIAN_POINT('Ctrl Pts',(6.28403841692564,-2.02902611036282,-3.14908483016182));
#19971=CARTESIAN_POINT('Ctrl Pts',(7.44388010034515,-0.103927350902949,
-3.02225755665361));
#19972=CARTESIAN_POINT('Ctrl Pts',(6.45850272749029,1.91604025675891,-2.89543028314539));
#19973=CARTESIAN_POINT('Ctrl Pts',(4.22739682589132,2.18697238579333,-2.76860300963718));
#19974=CARTESIAN_POINT('Ctrl Pts',(2.78720196805409,0.461551691566315,-2.64177573612896));
#19975=CARTESIAN_POINT('Ctrl Pts',(3.45258361826661,-1.6851911952421,-2.51494846262075));
#19976=CARTESIAN_POINT('Ctrl Pts',(5.61615571900432,-2.2936265153134,-2.38812118911253));
#19977=CARTESIAN_POINT('Ctrl Pts',(7.30292614602958,-0.808351017512908,
-2.26129391560431));
#19978=CARTESIAN_POINT('Ctrl Pts',(6.97314574407777,1.41481848995056,-2.13446664209609));
#19979=CARTESIAN_POINT('Ctrl Pts',(4.92785079394974,2.34648706910725,-2.00763936858788));
#19980=CARTESIAN_POINT('Ctrl Pts',(3.03406547309841,1.13619167817969,-1.88081209507966));
#19981=CARTESIAN_POINT('Ctrl Pts',(3.02051012162903,-1.11126333281937,-1.75398482157145));
#19982=CARTESIAN_POINT('Ctrl Pts',(4.89955858751159,-2.34431427954153,-1.62715754806323));
#19983=CARTESIAN_POINT('Ctrl Pts',(6.95594290088628,-1.43738466260644,-1.50033027455501));
#19984=CARTESIAN_POINT('Ctrl Pts',(7.31251608517135,0.781645156597075,-1.3735030010468));
#19985=CARTESIAN_POINT('Ctrl Pts',(5.6437843742328,2.28715910579401,-1.24667572753858));
#19986=CARTESIAN_POINT('Ctrl Pts',(3.47303048594182,1.70486594012406,-1.11984845403036));
#19987=CARTESIAN_POINT('Ctrl Pts',(2.78180235944796,-0.433694662582063,
-0.993021180522151));
#19988=CARTESIAN_POINT('Ctrl Pts',(4.20107970964125,-2.17636203690783,-0.866193907013934));
#19989=CARTESIAN_POINT('Ctrl Pts',(6.43529138793569,-1.93236213755744,-0.739366633505718));
#19990=CARTESIAN_POINT('Ctrl Pts',(7.44496273503322,0.0755725090779332,
-0.612539359997501));
#19991=CARTESIAN_POINT('Ctrl Pts',(6.308426772541,2.01452165236963,-0.485712086489285));
#19992=CARTESIAN_POINT('Ctrl Pts',(4.06315739668914,2.11453767194281,-0.358884812981069));
#19993=CARTESIAN_POINT('Ctrl Pts',(2.75872315992675,0.284322084567546,-0.232057539472851));
#19994=CARTESIAN_POINT('Ctrl Pts',(3.58586198401954,-1.80543367627818,-0.105230265964635));
#19995=CARTESIAN_POINT('Ctrl Pts',(5.78952962322882,-2.24711988866344,0.0215970075435808));
#19996=CARTESIAN_POINT('Ctrl Pts',(7.35813319611717,-0.637548329076448,
0.148424281051797));
#19997=CARTESIAN_POINT('Ctrl Pts',(6.85979081411103,1.55400195430878,0.275251554560013));
#19998=CARTESIAN_POINT('Ctrl Pts',(4.74940863924933,2.32699927017435,0.402078828068231));
#19999=CARTESIAN_POINT('Ctrl Pts',(2.95342498034503,0.975821831324032,0.528906101576446));
#20000=CARTESIAN_POINT('Ctrl Pts',(3.11128304523419,-1.26612344134854,0.655733375084663));
#20001=CARTESIAN_POINT('Ctrl Pts',(5.07888389905091,-2.35230236508492,0.782560648592879));
#20002=CARTESIAN_POINT('Ctrl Pts',(7.06012553411309,-1.29120889238538,0.909387922101095));
#20003=CARTESIAN_POINT('Ctrl Pts',(7.24645411109106,0.948549897241488,1.03621519560932));
#20004=CARTESIAN_POINT('Ctrl Pts',(5.46778171273805,2.32243572715841,1.16304246911752));
#20005=CARTESIAN_POINT('Ctrl Pts',(3.34774916005368,1.57631258057466,1.28986974262575));
#20006=CARTESIAN_POINT('Ctrl Pts',(2.82160399922678,-0.608729534362231,
1.41669701613396));
#20007=CARTESIAN_POINT('Ctrl Pts',(4.36963184197595,-2.23809983370575,1.54352428964218));
#20008=CARTESIAN_POINT('Ctrl Pts',(6.57873312041059,-1.82444621541158,1.6703515631504));
#20009=CARTESIAN_POINT('Ctrl Pts',(7.43235491747289,0.254632330937633,1.7971788366586));
#20010=CARTESIAN_POINT('Ctrl Pts',(6.15127830746928,2.10127265693809,1.92400611016684));
#20011=CARTESIAN_POINT('Ctrl Pts',(3.90491946886846,2.02979019370868,2.05083338367504));
#20012=CARTESIAN_POINT('Ctrl Pts',(2.74384145776938,0.105436892869242,2.17766065718327));
#20013=CARTESIAN_POINT('Ctrl Pts',(3.72792109968031,-1.91516327358771,2.30448793069147));
#20014=CARTESIAN_POINT('Ctrl Pts',(5.95885251252833,-2.18752847965755,2.4313152041997));
#20015=CARTESIAN_POINT('Ctrl Pts',(7.40015538993177,-0.463033252091554,
2.55814247770792));
#20016=CARTESIAN_POINT('Ctrl Pts',(6.73615283189305,1.68413660081422,2.68496975121613));
#20017=CARTESIAN_POINT('Ctrl Pts',(4.57297200352591,2.29396155774392,2.81179702472434));
#20018=CARTESIAN_POINT('Ctrl Pts',(2.88524786256229,0.80976985910186,2.93862429823255));
#20019=CARTESIAN_POINT('Ctrl Pts',(3.21360015010372,-1.41361102360262,3.06545157174077));
#20020=CARTESIAN_POINT('Ctrl Pts',(5.25829622386344,-2.34659319934927,3.19227884524899));
#20021=CARTESIAN_POINT('Ctrl Pts',(7.15285858356203,-1.13751452551417,3.31910611875722));
#20022=CARTESIAN_POINT('Ctrl Pts',(7.16785757819435,1.10993131464959,3.44593339226543));
#20023=CARTESIAN_POINT('Ctrl Pts',(5.28960154650705,2.34418900805874,3.57276066577364));
#20024=CARTESIAN_POINT('Ctrl Pts',(3.23263509388115,1.43858049049663,3.69958793928185));
#20025=CARTESIAN_POINT('Ctrl Pts',(2.87463659605508,-0.780219827211948,
3.82641521279009));
#20026=CARTESIAN_POINT('Ctrl Pts',(4.54240090039093,-2.28680537058231,3.95324248629829));
#20027=CARTESIAN_POINT('Ctrl Pts',(6.71352837509979,-1.70590670224695,4.08006975980651));
#20028=CARTESIAN_POINT('Ctrl Pts',(7.40613005693279,0.432209450966328,4.20689703331472));
#20029=CARTESIAN_POINT('Ctrl Pts',(5.98797239666618,2.17578813428881,4.33372430682294));
#20030=CARTESIAN_POINT('Ctrl Pts',(3.7536044467024,1.93322342439896,4.46055158033115));
#20031=CARTESIAN_POINT('Ctrl Pts',(2.74264351715072,-0.07406224865045,4.58737885383938));
#20032=CARTESIAN_POINT('Ctrl Pts',(3.87793376704564,-2.0137410423694,4.71420612734759));
#20033=CARTESIAN_POINT('Ctrl Pts',(6.12313843469951,-2.11519928330928,4.8410334008558));
#20034=CARTESIAN_POINT('Ctrl Pts',(7.42874803580416,-0.285821972907499,
4.96786067436402));
#20035=CARTESIAN_POINT('Ctrl Pts',(6.60295173065374,1.80446466693628,5.09468794787225));
#20036=CARTESIAN_POINT('Ctrl Pts',(4.39956826187594,2.24756630745012,5.22151522138046));
#20037=CARTESIAN_POINT('Ctrl Pts',(2.82993110916943,0.639002667691711,5.34834249488867));
#20038=CARTESIAN_POINT('Ctrl Pts',(3.32686565266144,-1.55286727228962,5.47516976839688));
#20039=CARTESIAN_POINT('Ctrl Pts',(5.43675085965053,-2.3272200262965,5.6019970419051));
#20040=CARTESIAN_POINT('Ctrl Pts',(7.23360207278054,-0.977196510878107,
5.72882431541332));
#20041=CARTESIAN_POINT('Ctrl Pts',(7.07718414723108,1.26484969892137,5.85565158892153));
#20042=CARTESIAN_POINT('Ctrl Pts',(5.11028140309013,2.35229228103794,5.98247886242977));
#20043=CARTESIAN_POINT('Ctrl Pts',(3.12835858658117,1.29247167182591,6.10930613593796));
#20044=CARTESIAN_POINT('Ctrl Pts',(2.94059134575166,-0.947166968129349,
6.23613340944619));
#20045=CARTESIAN_POINT('Ctrl Pts',(4.71838086574373,-2.32219503944855,6.36296068295439));
#20046=CARTESIAN_POINT('Ctrl Pts',(6.83889225100422,-1.57743384329904,6.48978795646262));
#20047=CARTESIAN_POINT('Ctrl Pts',(7.36644085848617,0.60726985309855,6.61661522997083));
#20048=CARTESIAN_POINT('Ctrl Pts',(5.81945995619197,2.23763418730316,6.74344250347906));
#20049=CARTESIAN_POINT('Ctrl Pts',(3.61009342435358,1.82539966388007,6.87026977698727));
#20050=CARTESIAN_POINT('Ctrl Pts',(2.75513631357441,-0.253130132162693,
6.99709705049549));
#20051=CARTESIAN_POINT('Ctrl Pts',(4.03502647545116,-2.1005929728825,7.1239243240037));
#20052=CARTESIAN_POINT('Ctrl Pts',(6.28143076716157,-2.03055346621384,7.25075159751192));
#20053=CARTESIAN_POINT('Ctrl Pts',(7.44374464125381,-0.106946377330505,
7.37757887102014));
#20054=CARTESIAN_POINT('Ctrl Pts',(6.46096312877579,1.91428549285182,7.50440614452834));
#20055=CARTESIAN_POINT('Ctrl Pts',(4.23020712914702,2.18808367478468,7.63123341803657));
#20056=CARTESIAN_POINT('Ctrl Pts',(2.78779682479175,0.464514619539295,7.75806069154478));
#20057=CARTESIAN_POINT('Ctrl Pts',(3.45042001777526,-1.6830813104319,7.88488796505301));
#20058=CARTESIAN_POINT('Ctrl Pts',(5.61320868064904,-2.29429565422208,8.0117152385612));
#20059=CARTESIAN_POINT('Ctrl Pts',(7.30188583948063,-0.811188366278425,
8.13854251206945));
#20060=CARTESIAN_POINT('Ctrl Pts',(6.97496180167311,1.41240297383033,8.26536978557763));
#20061=CARTESIAN_POINT('Ctrl Pts',(4.93086544802557,2.34669836144671,8.39219705908588));
#20062=CARTESIAN_POINT('Ctrl Pts',(3.03552683115188,1.13883690345341,8.51902433259408));
#20063=CARTESIAN_POINT('Ctrl Pts',(3.01908419956648,-1.10859883848275,8.64585160610229));
#20064=CARTESIAN_POINT('Ctrl Pts',(4.89654702206317,-2.34406276936477,8.77267887961052));
#20065=CARTESIAN_POINT('Ctrl Pts',(6.95409476521605,-1.4397757247852,8.89950615311873));
#20066=CARTESIAN_POINT('Ctrl Pts',(7.31351842887804,0.778794175853053,9.02633342662694));
#20067=CARTESIAN_POINT('Ctrl Pts',(5.64672221925978,2.28645069189862,9.15316070013516));
#20068=CARTESIAN_POINT('Ctrl Pts',(3.47522205400328,1.70694676033461,9.27998797364338));
#20069=CARTESIAN_POINT('Ctrl Pts',(2.78124710252401,-0.430724060710163,
9.4068152471516));
#20070=CARTESIAN_POINT('Ctrl Pts',(4.1982844878738,-2.17521333450196,9.53364252065981));
#20071=CARTESIAN_POINT('Ctrl Pts',(6.43280778728865,-1.93408391246274,9.66046979416803));
#20072=CARTESIAN_POINT('Ctrl Pts',(7.44505788272711,0.0725519555479146,
9.78729706767624));
#20073=CARTESIAN_POINT('Ctrl Pts',(6.31101381278495,2.01295960551136,9.91412434118447));
#20074=CARTESIAN_POINT('Ctrl Pts',(4.06587478177254,2.11586001424485,10.0409516146927));
#20075=CARTESIAN_POINT('Ctrl Pts',(2.75909035112716,0.287321757942756,10.1677788882009));
#20076=CARTESIAN_POINT('Ctrl Pts',(3.5835438040437,-1.80349494092047,10.2946061617091));
#20077=CARTESIAN_POINT('Ctrl Pts',(5.78664217907986,-2.24801174578714,10.4214334352174));
#20078=CARTESIAN_POINT('Ctrl Pts',(7.35731229095528,-0.640456843765642,
10.5482607087256));
#20079=CARTESIAN_POINT('Ctrl Pts',(6.86178573958764,1.55173214216356,10.6750879822338));
#20080=CARTESIAN_POINT('Ctrl Pts',(4.75239846900008,2.32743945525609,10.801915255742));
#20081=CARTESIAN_POINT('Ctrl Pts',(2.95468025641726,0.978571486204148,10.9287425292502));
#20082=CARTESIAN_POINT('Ctrl Pts',(3.10965833359497,-1.26357676609641,11.0555698027584));
#20083=CARTESIAN_POINT('Ctrl Pts',(5.07586147928159,-2.35227869001964,11.1823970762667));
#20084=CARTESIAN_POINT('Ctrl Pts',(7.05846594952206,-1.29373874962098,11.3092243497749));
#20085=CARTESIAN_POINT('Ctrl Pts',(7.24766931928765,0.945792852126664,11.4360516232831));
#20086=CARTESIAN_POINT('Ctrl Pts',(5.47076809243279,2.32193586078442,11.5628788967913));
#20087=CARTESIAN_POINT('Ctrl Pts',(3.34976983211822,1.57858785389917,11.6897061702995));
#20088=CARTESIAN_POINT('Ctrl Pts',(2.82083498267555,-0.605873543948998,
11.8165334438077));
#20089=CARTESIAN_POINT('Ctrl Pts',(4.36673594724824,-2.23704641637698,11.943360717316));
#20090=CARTESIAN_POINT('Ctrl Pts',(6.57642846184293,-1.82658327984848,12.0701879908242));
#20091=CARTESIAN_POINT('Ctrl Pts',(7.43260311629662,0.252068073834375,12.1970152643324));
#20092=CARTESIAN_POINT('Ctrl Pts',(6.15412356552886,2.09907067965551,12.3238425378406));
#20093=CARTESIAN_POINT('Ctrl Pts',(3.90724904943681,2.03294633564993,12.4506698113488));
#20094=CARTESIAN_POINT('Ctrl Pts',(2.74435016673355,0.104853876027658,12.5775143854051));
#20095=CARTESIAN_POINT('Ctrl Pts',(3.39801752208532,-1.23561899131413,12.6620832016253));
#20096=CARTESIAN_POINT('Ctrl Pts',(3.93619204088349,-1.62013490387918,12.7043762600095));
#20097=CARTESIAN_POINT('Ctrl Pts',(6.03504684936144,-1.92787532700788,-5.46980632749697));
#20098=CARTESIAN_POINT('Ctrl Pts',(6.67516512718069,-1.61535930427873,-5.4275305696609));
#20099=CARTESIAN_POINT('Ctrl Pts',(7.60873564783407,-0.308169163208136,
-5.34297905398876));
#20100=CARTESIAN_POINT('Ctrl Pts',(6.7178668695963,1.94792384081748,-5.21615178048054));
#20101=CARTESIAN_POINT('Ctrl Pts',(4.3424068455905,2.4197266424727,-5.08932450697231));
#20102=CARTESIAN_POINT('Ctrl Pts',(2.65395357169351,0.685789808141594,-4.96249723346412));
#20103=CARTESIAN_POINT('Ctrl Pts',(3.19214616129121,-1.67576226130358,-4.83566995995589));
#20104=CARTESIAN_POINT('Ctrl Pts',(5.46656281314146,-2.50677599565422,-4.70884268644769));
#20105=CARTESIAN_POINT('Ctrl Pts',(7.40057648888444,-1.04994745151819,-4.58201541293946));
#20106=CARTESIAN_POINT('Ctrl Pts',(7.22898194983825,1.36554440315936,-4.45518813943125));
#20107=CARTESIAN_POINT('Ctrl Pts',(5.10829285442139,2.53439348739581,-4.32836086592303));
#20108=CARTESIAN_POINT('Ctrl Pts',(2.97442140185426,1.38981395753714,-4.20153359241481));
#20109=CARTESIAN_POINT('Ctrl Pts',(2.77521352220177,-1.02347477929045,-4.0747063189066));
#20110=CARTESIAN_POINT('Ctrl Pts',(4.69253186227509,-2.50247870878307,-3.94787904539838));
#20111=CARTESIAN_POINT('Ctrl Pts',(6.97616478203201,-1.69713267749013,-3.82105177189016));
#20112=CARTESIAN_POINT('Ctrl Pts',(7.54152896709318,0.657426399217776,-3.69422449838195));
#20113=CARTESIAN_POINT('Ctrl Pts',(5.87253556188757,2.41185874740932,-3.56739722487373));
#20114=CARTESIAN_POINT('Ctrl Pts',(3.49270753626949,1.96465466530119,-3.44056995136552));
#20115=CARTESIAN_POINT('Ctrl Pts',(2.57444305428872,-0.275962728482613,
-3.3137426778573));
#20116=CARTESIAN_POINT('Ctrl Pts',(3.95596975641528,-2.26467032496782,-3.18691540434908));
#20117=CARTESIAN_POINT('Ctrl Pts',(6.3761765449635,-2.18609962630105,-3.06008813084087));
#20118=CARTESIAN_POINT('Ctrl Pts',(7.62580534852698,-0.111972705432947,
-2.93326085733265));
#20119=CARTESIAN_POINT('Ctrl Pts',(6.56414670571223,2.0643671699865,-2.80643358382443));
#20120=CARTESIAN_POINT('Ctrl Pts',(4.1603236337403,2.35627303704761,-2.67960631031622));
#20121=CARTESIAN_POINT('Ctrl Pts',(2.60863860394261,0.497281910419246,-2.552779036808));
#20122=CARTESIAN_POINT('Ctrl Pts',(3.32552961359897,-1.81564733117496,-2.42595176329978));
#20123=CARTESIAN_POINT('Ctrl Pts',(5.65659087335395,-2.47118360990644,-2.29912448979157));
#20124=CARTESIAN_POINT('Ctrl Pts',(7.47393968978501,-0.870928101062764,
-2.17229721628335));
#20125=CARTESIAN_POINT('Ctrl Pts',(7.11862991344148,1.52434419466967,-2.04546994277514));
#20126=CARTESIAN_POINT('Ctrl Pts',(4.91500202353184,2.52813627123722,-1.91864266926692));
#20127=CARTESIAN_POINT('Ctrl Pts',(2.87461261648416,1.22414797443433,-1.7918153957587));
#20128=CARTESIAN_POINT('Ctrl Pts',(2.86000790113313,-1.19728984471475,-1.66498812225048));
#20129=CARTESIAN_POINT('Ctrl Pts',(4.88451962529862,-2.52579527895851,-1.53816084874227));
#20130=CARTESIAN_POINT('Ctrl Pts',(7.10009534216109,-1.54865728820657,-1.41133357523405));
#20131=CARTESIAN_POINT('Ctrl Pts',(7.48427201733219,0.842154852522489,-1.28450630172584));
#20132=CARTESIAN_POINT('Ctrl Pts',(5.68635835271843,2.46421553716391,-1.15767902821762));
#20133=CARTESIAN_POINT('Ctrl Pts',(3.34755933985805,1.83684516210202,-1.0308517547094));
#20134=CARTESIAN_POINT('Ctrl Pts',(2.60282099405786,-0.467268378143176,
-0.904024481201181));
#20135=CARTESIAN_POINT('Ctrl Pts',(4.1319692238558,-2.34484130651688,-0.777197207692966));
#20136=CARTESIAN_POINT('Ctrl Pts',(6.53913850080685,-2.08195258070742,-0.650369934184749));
#20137=CARTESIAN_POINT('Ctrl Pts',(7.62697179349039,0.0814228230036674,
-0.523542660676532));
#20138=CARTESIAN_POINT('Ctrl Pts',(6.40245288257421,2.17047233100077,-0.396715387168316));
#20139=CARTESIAN_POINT('Ctrl Pts',(3.98336989570362,2.27823091621384,-0.2698881136601));
#20140=CARTESIAN_POINT('Ctrl Pts',(2.57795515857602,0.306332382638052,-0.143060840151882));
#20141=CARTESIAN_POINT('Ctrl Pts',(3.46912549148267,-1.94519817407244,-0.0162335666436664));
#20142=CARTESIAN_POINT('Ctrl Pts',(5.84338621585831,-2.42107675390258,0.11059370686455));
#20143=CARTESIAN_POINT('Ctrl Pts',(7.53342049732578,-0.686903020530217,
0.237420980372767));
#20144=CARTESIAN_POINT('Ctrl Pts',(6.99649980936145,1.67430230406352,0.364248253880983));
#20145=CARTESIAN_POINT('Ctrl Pts',(4.72274608078444,2.50713985835369,0.491075527389199));
#20146=CARTESIAN_POINT('Ctrl Pts',(2.78772948069178,1.05136337570955,0.617902800897417));
#20147=CARTESIAN_POINT('Ctrl Pts',(2.95780785223184,-1.36413817833427,0.744730074405631));
#20148=CARTESIAN_POINT('Ctrl Pts',(5.07772709293065,-2.53440174820603,0.87155734791385));
#20149=CARTESIAN_POINT('Ctrl Pts',(7.21234309215354,-1.39116557579219,0.998384621422065));
#20150=CARTESIAN_POINT('Ctrl Pts',(7.41309597079834,1.0219802324361,1.12521189493028));
#20151=CARTESIAN_POINT('Ctrl Pts',(5.49673075228657,2.50222303661797,1.2520391684385));
#20152=CARTESIAN_POINT('Ctrl Pts',(3.21257957872646,1.69834006853254,1.37886644194671));
#20153=CARTESIAN_POINT('Ctrl Pts',(2.6457038083313,-0.655853269108355,1.50569371545493));
#20154=CARTESIAN_POINT('Ctrl Pts',(4.3135695254129,-2.41135842712921,1.63252098896314));
#20155=CARTESIAN_POINT('Ctrl Pts',(6.69368452471353,-1.96568253574837,1.75934826247136));
#20156=CARTESIAN_POINT('Ctrl Pts',(7.61338796373266,0.274344248535754,1.88617553597958));
#20157=CARTESIAN_POINT('Ctrl Pts',(6.23313904328329,2.2639390132183,2.01300280948779));
#20158=CARTESIAN_POINT('Ctrl Pts',(3.81288225480597,2.1869228598259,2.13983008299601));
#20159=CARTESIAN_POINT('Ctrl Pts',(2.56192141541284,0.113599105956597,2.26665735650423));
#20160=CARTESIAN_POINT('Ctrl Pts',(3.62218186570703,-2.06342229669333,2.39348463001244));
#20161=CARTESIAN_POINT('Ctrl Pts',(6.02581694118578,-2.35687217994802,2.52031190352066));
#20162=CARTESIAN_POINT('Ctrl Pts',(7.57869576595109,-0.49887816336741,2.64713917702888));
#20163=CARTESIAN_POINT('Ctrl Pts',(6.86329060848278,1.81451109715958,2.77396645053709));
#20164=CARTESIAN_POINT('Ctrl Pts',(4.53265091076624,2.4715445890621,2.90079372404531));
#20165=CARTESIAN_POINT('Ctrl Pts',(2.71427455029638,0.872456779797623,3.02762099755352));
#20166=CARTESIAN_POINT('Ctrl Pts',(3.06804565724436,-1.52304325442127,3.15444827106175));
#20167=CARTESIAN_POINT('Ctrl Pts',(5.27102830981658,-2.52825061736673,3.28127554456996));
#20168=CARTESIAN_POINT('Ctrl Pts',(7.31225490881806,-1.22557322768701,3.40810281807818));
#20169=CARTESIAN_POINT('Ctrl Pts',(7.32841502444848,1.19585471068256,3.53493009158639));
#20170=CARTESIAN_POINT('Ctrl Pts',(5.30475707938881,2.52566030980246,3.66175736509461));
#20171=CARTESIAN_POINT('Ctrl Pts',(3.08855415798074,1.54994568902632,3.78858463860283));
#20172=CARTESIAN_POINT('Ctrl Pts',(2.70284183110785,-0.840619183750031,
3.91541191211104));
#20173=CARTESIAN_POINT('Ctrl Pts',(4.49971319902478,-2.46383441815802,4.04223918561925));
#20174=CARTESIAN_POINT('Ctrl Pts',(6.83891471884371,-1.83796649300864,4.16906645912748));
#20175=CARTESIAN_POINT('Ctrl Pts',(7.58513295137294,0.465668191461714,4.29589373263569));
#20176=CARTESIAN_POINT('Ctrl Pts',(6.05719109034367,2.34422297622799,4.42272100614391));
#20177=CARTESIAN_POINT('Ctrl Pts',(3.64985344422461,2.08288054256695,4.54954827965212));
#20178=CARTESIAN_POINT('Ctrl Pts',(2.56063073831145,-0.0797956484004017,
4.67637555316034));
#20179=CARTESIAN_POINT('Ctrl Pts',(3.78380750196318,-2.16963129143944,4.80320282666856));
#20180=CARTESIAN_POINT('Ctrl Pts',(6.20282077136359,-2.27894374506981,4.93003010017677));
#20181=CARTESIAN_POINT('Ctrl Pts',(7.60950186161309,-0.307948382216727,
5.056857373685));
#20182=CARTESIAN_POINT('Ctrl Pts',(6.71977797641024,1.94415415056313,5.18368464719321));
#20183=CARTESIAN_POINT('Ctrl Pts',(4.34582342102416,2.42155773142069,5.31051192070143));
#20184=CARTESIAN_POINT('Ctrl Pts',(2.65467554696042,0.688469944231741,5.43733919420963));
#20185=CARTESIAN_POINT('Ctrl Pts',(3.19007941104852,-1.67307978261573,5.56416646771786));
#20186=CARTESIAN_POINT('Ctrl Pts',(5.46329769985222,-2.50737770392584,5.69099374122607));
#20187=CARTESIAN_POINT('Ctrl Pts',(7.39924901436718,-1.05284447368267,5.81782101473429));
#20188=CARTESIAN_POINT('Ctrl Pts',(7.23072226804094,1.36276583135963,5.94464828824251));
#20189=CARTESIAN_POINT('Ctrl Pts',(5.11155517996038,2.53439088352015,6.07147556175072));
#20190=CARTESIAN_POINT('Ctrl Pts',(2.97620526681754,1.39252611109973,6.19830283525895));
#20191=CARTESIAN_POINT('Ctrl Pts',(2.77390235266945,-1.02049024627978,6.32513010876715));
#20192=CARTESIAN_POINT('Ctrl Pts',(4.68931634633245,-2.50196371648903,6.45195738227537));
#20193=CARTESIAN_POINT('Ctrl Pts',(6.97398342045709,-1.69954813185427,6.5787846557836));
#20194=CARTESIAN_POINT('Ctrl Pts',(7.54237128288121,0.654280589166612,6.7056119292918));
#20195=CARTESIAN_POINT('Ctrl Pts',(5.87563355332317,2.41085673352286,6.83243920280003));
#20196=CARTESIAN_POINT('Ctrl Pts',(3.49523276648935,1.96670979376639,6.95926647630824));
#20197=CARTESIAN_POINT('Ctrl Pts',(2.57409064277192,-0.272725759663801,
7.08609374981645));
#20198=CARTESIAN_POINT('Ctrl Pts',(3.95306126828289,-2.26320671260751,7.21292102332467));
#20199=CARTESIAN_POINT('Ctrl Pts',(6.37336702854295,-2.18774521974024,7.33974829683289));
#20200=CARTESIAN_POINT('Ctrl Pts',(7.62565940310645,-0.115225444523568,
7.46657557034111));
#20201=CARTESIAN_POINT('Ctrl Pts',(6.56679757467015,2.06247656409339,7.59340284384931));
#20202=CARTESIAN_POINT('Ctrl Pts',(4.16335149171894,2.35747035453718,7.72023011735755));
#20203=CARTESIAN_POINT('Ctrl Pts',(2.60927951047665,0.500474208291315,7.84705739086575));
#20204=CARTESIAN_POINT('Ctrl Pts',(3.3231985217508,-1.81337411331366,7.97388466437398));
#20205=CARTESIAN_POINT('Ctrl Pts',(5.6534156951666,-2.47190454903617,8.10071193788218));
#20206=CARTESIAN_POINT('Ctrl Pts',(7.47281884971977,-0.873985098232146,
8.2275392113904));
#20207=CARTESIAN_POINT('Ctrl Pts',(7.12058655796674,1.52174168558375,8.35436648489863));
#20208=CARTESIAN_POINT('Ctrl Pts',(4.91825005179277,2.52836392040445,8.48119375840682));
#20209=CARTESIAN_POINT('Ctrl Pts',(2.87618710302144,1.22699797520702,8.60802103191507));
#20210=CARTESIAN_POINT('Ctrl Pts',(2.85847159380217,-1.19441908319826,8.73484830542326));
#20211=CARTESIAN_POINT('Ctrl Pts',(4.88127492476582,-2.52552429856026,8.86167557893149));
#20212=CARTESIAN_POINT('Ctrl Pts',(7.09810413629271,-1.55123345029179,8.98850285243972));
#20213=CARTESIAN_POINT('Ctrl Pts',(7.48535195572798,0.839083168078771,9.11533012594791));
#20214=CARTESIAN_POINT('Ctrl Pts',(5.689523625892,2.46345228264291,9.24215739945616));
#20215=CARTESIAN_POINT('Ctrl Pts',(3.34992056433698,1.8390870653784,9.36898467296433));
#20216=CARTESIAN_POINT('Ctrl Pts',(2.60222275288801,-0.464067812310691,
9.4958119464726));
#20217=CARTESIAN_POINT('Ctrl Pts',(4.12895761487251,-2.34360367931858,9.62263921998077));
#20218=CARTESIAN_POINT('Ctrl Pts',(6.53646263654931,-2.08380764381274,9.74946649348901));
#20219=CARTESIAN_POINT('Ctrl Pts',(7.62707430687696,0.0781684385926071,
9.87629376699721));
#20220=CARTESIAN_POINT('Ctrl Pts',(6.40524019402461,2.16878936101054,10.0031210405055));
#20221=CARTESIAN_POINT('Ctrl Pts',(3.98629764241174,2.27965562533786,10.1299483140136));
#20222=CARTESIAN_POINT('Ctrl Pts',(2.57835077524251,0.309564270493552,10.2567755875219));
#20223=CARTESIAN_POINT('Ctrl Pts',(3.46662785364894,-1.94310935489986,10.3836028610301));
#20224=CARTESIAN_POINT('Ctrl Pts',(5.8402752452588,-2.42203765258933,10.5104301345384));
#20225=CARTESIAN_POINT('Ctrl Pts',(7.53253604322313,-0.690036692809079,
10.6372574080466));
#20226=CARTESIAN_POINT('Ctrl Pts',(6.99864916851293,1.67185677837162,10.7640846815548));
#20227=CARTESIAN_POINT('Ctrl Pts',(4.72596736298847,2.50761411959545,10.890911955063));
#20228=CARTESIAN_POINT('Ctrl Pts',(2.78908193177085,1.05432589032441,11.0177392285712));
#20229=CARTESIAN_POINT('Ctrl Pts',(2.95605736637601,-1.36139435666112,11.1445665020794));
#20230=CARTESIAN_POINT('Ctrl Pts',(5.07447069780861,-2.53437624037689,11.2713937755877));
#20231=CARTESIAN_POINT('Ctrl Pts',(7.21055503371717,-1.39389127751139,11.3982210490959));
#20232=CARTESIAN_POINT('Ctrl Pts',(7.41440525221706,1.0190097554844,11.5250483226041));
#20233=CARTESIAN_POINT('Ctrl Pts',(5.49994831735453,2.50168447396085,11.6518755961123));
#20234=CARTESIAN_POINT('Ctrl Pts',(3.21475667759305,1.70079147817141,11.7787028696205));
#20235=CARTESIAN_POINT('Ctrl Pts',(2.6448752597056,-0.652776187180628,11.9055301431287));
#20236=CARTESIAN_POINT('Ctrl Pts',(4.31044945004781,-2.41022346133601,12.0323574166369));
#20237=CARTESIAN_POINT('Ctrl Pts',(6.69120145502419,-1.96798503729974,12.1591846901452));
#20238=CARTESIAN_POINT('Ctrl Pts',(7.61365537643526,0.27158148394315,12.2860119636534));
#20239=CARTESIAN_POINT('Ctrl Pts',(6.23620456203093,2.26156657370656,12.4128392371616));
#20240=CARTESIAN_POINT('Ctrl Pts',(3.81539217578921,2.19032332898847,12.5396665106698));
#20241=CARTESIAN_POINT('Ctrl Pts',(2.56246950519383,0.112970955883516,12.666511084726));
#20242=CARTESIAN_POINT('Ctrl Pts',(3.2667393782928,-1.3312722795269,12.7510799009463));
#20243=CARTESIAN_POINT('Ctrl Pts',(3.84657573841683,-1.74555482053124,12.7933729593303));
#20244=CARTESIAN_POINT('Ctrl Pts',(6.10267445645391,-2.06639516034963,-5.38080962817601));
#20245=CARTESIAN_POINT('Ctrl Pts',(6.78878589364418,-1.73142453862302,-5.33853387033994));
#20246=CARTESIAN_POINT('Ctrl Pts',(7.78943442039165,-0.330311435859617,
-5.25398235466779));
#20247=CARTESIAN_POINT('Ctrl Pts',(6.83455580035441,2.08788418058241,-5.12715508115958));
#20248=CARTESIAN_POINT('Ctrl Pts',(4.28841652026521,2.59358650081123,-5.00032780765136));
#20249=CARTESIAN_POINT('Ctrl Pts',(2.47864613481591,0.73506451413552,-4.87350053414315));
#20250=CARTESIAN_POINT('Ctrl Pts',(3.05550841781776,-1.79616751049385,-4.74667326063492));
#20251=CARTESIAN_POINT('Ctrl Pts',(5.49334425510517,-2.6868904399228,-4.61984598712671));
#20252=CARTESIAN_POINT('Ctrl Pts',(7.56631881088614,-1.12538726028821,-4.49301871361849));
#20253=CARTESIAN_POINT('Ctrl Pts',(7.38239502698786,1.46366017885112,-4.36619144011028));
#20254=CARTESIAN_POINT('Ctrl Pts',(5.10933222983235,2.71649227696918,-4.23936416660206));
#20255=CARTESIAN_POINT('Ctrl Pts',(2.82213990955064,1.48967352577638,-4.11253689309384));
#20256=CARTESIAN_POINT('Ctrl Pts',(2.60861873800462,-1.0970124992201,-3.98570961958563));
#20257=CARTESIAN_POINT('Ctrl Pts',(4.66369838100526,-2.68228438855176,-3.85888234607741));
#20258=CARTESIAN_POINT('Ctrl Pts',(7.11141268456692,-1.81907341315463,-3.7320550725692));
#20259=CARTESIAN_POINT('Ctrl Pts',(7.71739887022894,0.704663164986982,-3.60522779906098));
#20260=CARTESIAN_POINT('Ctrl Pts',(5.92848656513453,2.58515328936164,-3.47840052555276));
#20261=CARTESIAN_POINT('Ctrl Pts',(3.37766543800594,2.10581713208477,-3.35157325204455));
#20262=CARTESIAN_POINT('Ctrl Pts',(2.39342270461766,-0.295790935536472,
-3.22474597853633));
#20263=CARTESIAN_POINT('Ctrl Pts',(3.87421352712319,-2.42738922675253,-3.09791870502811));
#20264=CARTESIAN_POINT('Ctrl Pts',(6.46831467300135,-2.34317314223929,-2.9710914315199));
#20265=CARTESIAN_POINT('Ctrl Pts',(7.80773059670882,-0.12001805996294,-2.84426415801168));
#20266=CARTESIAN_POINT('Ctrl Pts',(6.66979068393416,2.21269408321409,-2.71743688450346));
#20267=CARTESIAN_POINT('Ctrl Pts',(4.09325044158931,2.5255736883019,-2.59060961099524));
#20268=CARTESIAN_POINT('Ctrl Pts',(2.43007523983111,0.533012129272175,-2.46378233748703));
#20269=CARTESIAN_POINT('Ctrl Pts',(3.19847560893134,-1.94610346710782,-2.33695506397881));
#20270=CARTESIAN_POINT('Ctrl Pts',(5.69702602770357,-2.64874070449948,-2.2101277904706));
#20271=CARTESIAN_POINT('Ctrl Pts',(7.64495323354044,-0.933505184612618,
-2.08330051696238));
#20272=CARTESIAN_POINT('Ctrl Pts',(7.26411408280514,1.63386989938877,-1.95647324345417));
#20273=CARTESIAN_POINT('Ctrl Pts',(4.90215325311397,2.70978547336718,-1.82964596994594));
#20274=CARTESIAN_POINT('Ctrl Pts',(2.71515975986988,1.31210427068896,-1.70281869643773));
#20275=CARTESIAN_POINT('Ctrl Pts',(2.69950568063724,-1.28331635661013,-1.57599142292951));
#20276=CARTESIAN_POINT('Ctrl Pts',(4.86948066308565,-2.70727627837548,-1.4491641494213));
#20277=CARTESIAN_POINT('Ctrl Pts',(7.2442477834359,-1.6599299138067,-1.32233687591308));
#20278=CARTESIAN_POINT('Ctrl Pts',(7.65602794949304,0.9026645484479,-1.19550960240486));
#20279=CARTESIAN_POINT('Ctrl Pts',(5.72893233120405,2.64127196853383,-1.06868232889665));
#20280=CARTESIAN_POINT('Ctrl Pts',(3.22208819377429,1.96882438407996,-0.941855055388429));
#20281=CARTESIAN_POINT('Ctrl Pts',(2.42383962866776,-0.50084209370429,-0.815027781880213));
#20282=CARTESIAN_POINT('Ctrl Pts',(4.06285873807033,-2.51332057612591,-0.688200508371996));
#20283=CARTESIAN_POINT('Ctrl Pts',(6.64298561367803,-2.23154302385742,-0.561373234863779));
#20284=CARTESIAN_POINT('Ctrl Pts',(7.80898085194752,0.0872731369294008,
-0.434545961355562));
#20285=CARTESIAN_POINT('Ctrl Pts',(6.49647899260744,2.32642300963191,-0.307718687847347));
#20286=CARTESIAN_POINT('Ctrl Pts',(3.90358239471807,2.44192416048487,-0.18089141433913));
#20287=CARTESIAN_POINT('Ctrl Pts',(2.3971871572253,0.328342680708558,-0.0540641408309133));
#20288=CARTESIAN_POINT('Ctrl Pts',(3.3523889989458,-2.08496267186669,0.0727631326773033));
#20289=CARTESIAN_POINT('Ctrl Pts',(5.89724280848781,-2.59503361914173,0.199590406185519));
#20290=CARTESIAN_POINT('Ctrl Pts',(7.70870779853437,-0.736257711983984,
0.326417679693737));
#20291=CARTESIAN_POINT('Ctrl Pts',(7.13320880461186,1.79460265381826,0.453244953201953));
#20292=CARTESIAN_POINT('Ctrl Pts',(4.69608352231956,2.68728044653302,0.580072226710167));
#20293=CARTESIAN_POINT('Ctrl Pts',(2.62203398103853,1.12690492009508,0.706899500218388));
#20294=CARTESIAN_POINT('Ctrl Pts',(2.80433265922951,-1.46215291532002,0.8337267737266));
#20295=CARTESIAN_POINT('Ctrl Pts',(5.07657028681036,-2.71650113132714,0.960554047234819));
#20296=CARTESIAN_POINT('Ctrl Pts',(7.36456065019403,-1.49112225919901,1.08738132074303));
#20297=CARTESIAN_POINT('Ctrl Pts',(7.5797378305056,1.0954105676307,1.21420859425125));
#20298=CARTESIAN_POINT('Ctrl Pts',(5.52567979183511,2.68201034607753,1.34103586775946));
#20299=CARTESIAN_POINT('Ctrl Pts',(3.07740999739923,1.82036755649042,1.46786314126768));
#20300=CARTESIAN_POINT('Ctrl Pts',(2.46980361743582,-0.70297700385448,1.5946904147759));
#20301=CARTESIAN_POINT('Ctrl Pts',(4.25750720884985,-2.58461702055266,1.72151768828412));
#20302=CARTESIAN_POINT('Ctrl Pts',(6.80863592901645,-2.10691885608516,1.84834496179233));
#20303=CARTESIAN_POINT('Ctrl Pts',(7.79442100999245,0.294056166133873,1.97517223530055));
#20304=CARTESIAN_POINT('Ctrl Pts',(6.31499977909728,2.42660536949851,2.10199950880876));
#20305=CARTESIAN_POINT('Ctrl Pts',(3.7208450407435,2.34405552594312,2.22882678231698));
#20306=CARTESIAN_POINT('Ctrl Pts',(2.38000137305629,0.121761319043953,2.3556540558252));
#20307=CARTESIAN_POINT('Ctrl Pts',(3.51644263173374,-2.21168131979895,2.48248132933342));
#20308=CARTESIAN_POINT('Ctrl Pts',(6.09278136984322,-2.52621588023851,2.60930860284163));
#20309=CARTESIAN_POINT('Ctrl Pts',(7.75723614197039,-0.534723074643263,
2.73613587634985));
#20310=CARTESIAN_POINT('Ctrl Pts',(6.99042838507253,1.94488559350494,2.86296314985806));
#20311=CARTESIAN_POINT('Ctrl Pts',(4.49232981800657,2.64912762038029,2.98979042336628));
#20312=CARTESIAN_POINT('Ctrl Pts',(2.54330123803048,0.935143700493388,3.1166176968745));
#20313=CARTESIAN_POINT('Ctrl Pts',(2.92249116438501,-1.63247548523992,3.24344497038271));
#20314=CARTESIAN_POINT('Ctrl Pts',(5.2837603957697,-2.70990803538419,3.37027224389094));
#20315=CARTESIAN_POINT('Ctrl Pts',(7.47165123407409,-1.31363192985983,3.49709951739914));
#20316=CARTESIAN_POINT('Ctrl Pts',(7.48897247070264,1.28177810671553,3.62392679090736));
#20317=CARTESIAN_POINT('Ctrl Pts',(5.31991261227054,2.70713161154618,3.75075406441558));
#20318=CARTESIAN_POINT('Ctrl Pts',(2.94447322208036,1.66131088755599,3.8775813379238));
#20319=CARTESIAN_POINT('Ctrl Pts',(2.53104706616061,-0.901018540288114,
4.00440861143202));
#20320=CARTESIAN_POINT('Ctrl Pts',(4.45702549765863,-2.64086346573374,4.13123588494022));
#20321=CARTESIAN_POINT('Ctrl Pts',(6.96430106258761,-1.97002628377034,4.25806315844845));
#20322=CARTESIAN_POINT('Ctrl Pts',(7.7641358458131,0.499126931957104,4.38489043195666));
#20323=CARTESIAN_POINT('Ctrl Pts',(6.12640978402113,2.51265781816716,4.51171770546489));
#20324=CARTESIAN_POINT('Ctrl Pts',(3.54610244174684,2.23253766073493,4.63854497897309));
#20325=CARTESIAN_POINT('Ctrl Pts',(2.37861795947216,-0.0855290481503543,
4.76537225248131));
#20326=CARTESIAN_POINT('Ctrl Pts',(3.68968123688074,-2.32552154050947,4.89219952598953));
#20327=CARTESIAN_POINT('Ctrl Pts',(6.28250310802764,-2.44268820683033,5.01902679949774));
#20328=CARTESIAN_POINT('Ctrl Pts',(7.79025568742204,-0.330074791525955,
5.14585407300597));
#20329=CARTESIAN_POINT('Ctrl Pts',(6.83660422216671,2.08384363418999,5.27268134651417));
#20330=CARTESIAN_POINT('Ctrl Pts',(4.29207858017239,2.59554915539126,5.39950862002241));
#20331=CARTESIAN_POINT('Ctrl Pts',(2.47941998475138,0.737937220771773,5.5263358935306));
#20332=CARTESIAN_POINT('Ctrl Pts',(3.05329316943561,-1.79329229294183,5.65316316703884));
#20333=CARTESIAN_POINT('Ctrl Pts',(5.4898445400539,-2.68753538155518,5.77999044054704));
#20334=CARTESIAN_POINT('Ctrl Pts',(7.56489595595383,-1.12849243648723,5.90681771405526));
#20335=CARTESIAN_POINT('Ctrl Pts',(7.38426038885078,1.46068196379789,6.03364498756347));
#20336=CARTESIAN_POINT('Ctrl Pts',(5.11282895683061,2.71648948600237,6.1604722610717));
#20337=CARTESIAN_POINT('Ctrl Pts',(2.8240519470539,1.49258055037353,6.28729953457991));
#20338=CARTESIAN_POINT('Ctrl Pts',(2.60721335958723,-1.09381352443021,6.41412680808813));
#20339=CARTESIAN_POINT('Ctrl Pts',(4.66025182692117,-2.68173239352949,6.54095408159633));
#20340=CARTESIAN_POINT('Ctrl Pts',(7.10907458990993,-1.8216624204095,6.66778135510457));
#20341=CARTESIAN_POINT('Ctrl Pts',(7.7183017072763,0.701291325234671,6.79460862861277));
#20342=CARTESIAN_POINT('Ctrl Pts',(5.93180715045433,2.58407927974254,6.921435902121));
#20343=CARTESIAN_POINT('Ctrl Pts',(3.38037210862516,2.10801992365272,7.04826317562921));
#20344=CARTESIAN_POINT('Ctrl Pts',(2.3930449719694,-0.292321387164904,7.17509044913742));
#20345=CARTESIAN_POINT('Ctrl Pts',(3.87109606111463,-2.42582045233252,7.30191772264565));
#20346=CARTESIAN_POINT('Ctrl Pts',(6.46530328992434,-2.34493697326663,7.42874499615385));
#20347=CARTESIAN_POINT('Ctrl Pts',(7.8075741649591,-0.123504511716634,7.55557226966209));
#20348=CARTESIAN_POINT('Ctrl Pts',(6.67263202056451,2.21066763533496,7.68239954317029));
#20349=CARTESIAN_POINT('Ctrl Pts',(4.09649585429084,2.52685703428968,7.80922681667851));
#20350=CARTESIAN_POINT('Ctrl Pts',(2.43076219616156,0.536433797043339,7.93605409018673));
#20351=CARTESIAN_POINT('Ctrl Pts',(3.19597702572634,-1.94366691619542,8.06288136369493));
#20352=CARTESIAN_POINT('Ctrl Pts',(5.69362270968416,-2.64951344385026,8.18970863720316));
#20353=CARTESIAN_POINT('Ctrl Pts',(7.64375185995891,-0.936781830185868,
8.31653591071137));
#20354=CARTESIAN_POINT('Ctrl Pts',(7.26621131426039,1.63108039733716,8.4433631842196));
#20355=CARTESIAN_POINT('Ctrl Pts',(4.90563465555995,2.71002947936219,8.5701904577278));
#20356=CARTESIAN_POINT('Ctrl Pts',(2.716847374891,1.31515904696063,8.69701773123603));
#20357=CARTESIAN_POINT('Ctrl Pts',(2.69785898803786,-1.28023932791378,8.82384500474423));
#20358=CARTESIAN_POINT('Ctrl Pts',(4.86600282746846,-2.70698582775575,8.95067227825246));
#20359=CARTESIAN_POINT('Ctrl Pts',(7.24211350736936,-1.66269117579839,9.07749955176067));
#20360=CARTESIAN_POINT('Ctrl Pts',(7.65718548257792,0.899372160304488,9.20432682526889));
#20361=CARTESIAN_POINT('Ctrl Pts',(5.73232503252422,2.64045387338719,9.33115409877711));
#20362=CARTESIAN_POINT('Ctrl Pts',(3.22461907467068,1.97122737042217,9.45798137228532));
#20363=CARTESIAN_POINT('Ctrl Pts',(2.42319840325199,-0.497411563911216,
9.58480864579354));
#20364=CARTESIAN_POINT('Ctrl Pts',(4.05963074187124,-2.51199402413522,9.71163591930176));
#20365=CARTESIAN_POINT('Ctrl Pts',(6.64011748580997,-2.23353137516274,9.83846319280997));
#20366=CARTESIAN_POINT('Ctrl Pts',(7.80909073102681,0.0837849216372962,
9.96529046631819));
#20367=CARTESIAN_POINT('Ctrl Pts',(6.49946657526425,2.32461911650972,10.0921177398264));
#20368=CARTESIAN_POINT('Ctrl Pts',(3.90672050305093,2.44345123643088,10.2189450133346));
#20369=CARTESIAN_POINT('Ctrl Pts',(2.39761119935786,0.331806783044349,10.3457722868428));
#20370=CARTESIAN_POINT('Ctrl Pts',(3.34971190325417,-2.08272376887925,10.472599560351));
#20371=CARTESIAN_POINT('Ctrl Pts',(5.89390831143774,-2.59606355939153,10.5994268338592));
#20372=CARTESIAN_POINT('Ctrl Pts',(7.70775979549099,-0.739616541852521,
10.7262541073675));
#20373=CARTESIAN_POINT('Ctrl Pts',(7.13551259743823,1.79198141457968,10.8530813808757));
#20374=CARTESIAN_POINT('Ctrl Pts',(4.69953625697684,2.68778878393482,10.9799086543839));
#20375=CARTESIAN_POINT('Ctrl Pts',(2.62348360712445,1.13008029444468,11.1067359278921));
#20376=CARTESIAN_POINT('Ctrl Pts',(2.80245639915702,-1.45921194722585,11.2335632014003));
#20377=CARTESIAN_POINT('Ctrl Pts',(5.07307991633565,-2.71647379073412,11.3603904749085));
#20378=CARTESIAN_POINT('Ctrl Pts',(7.36264411791226,-1.49404380540182,11.4872177484168));
#20379=CARTESIAN_POINT('Ctrl Pts',(7.5811411851465,1.09222665884215,11.614045021925));
#20380=CARTESIAN_POINT('Ctrl Pts',(5.52912854227627,2.68143308713726,11.7408722954332));
#20381=CARTESIAN_POINT('Ctrl Pts',(3.07974352306788,1.82299510244365,11.8676995689414));
#20382=CARTESIAN_POINT('Ctrl Pts',(2.46891553673564,-0.699678830412259,
11.9945268424496));
#20383=CARTESIAN_POINT('Ctrl Pts',(4.25416295284739,-2.58340050629504,12.1213541159578));
#20384=CARTESIAN_POINT('Ctrl Pts',(6.80597444820543,-2.109386794751,12.2481813894661));
#20385=CARTESIAN_POINT('Ctrl Pts',(7.7947076365739,0.291094894051927,12.3750086629743));
#20386=CARTESIAN_POINT('Ctrl Pts',(6.318285558533,2.42406246775762,12.5018359364825));
#20387=CARTESIAN_POINT('Ctrl Pts',(3.72353530214159,2.34770032232699,12.6286632099907));
#20388=CARTESIAN_POINT('Ctrl Pts',(2.38058884365411,0.121088035739373,12.755507784047));
#20389=CARTESIAN_POINT('Ctrl Pts',(3.13546123450027,-1.42692556773965,12.8400766002673));
#20390=CARTESIAN_POINT('Ctrl Pts',(3.75695943595017,-1.87097473718329,12.8823696586513));
#20391=CARTESIAN_POINT('Ctrl Pts',(6.17030206354638,-2.20491499369139,-5.29181292885504));
#20392=CARTESIAN_POINT('Ctrl Pts',(6.90240666010767,-1.84748977296731,-5.24953717101897));
#20393=CARTESIAN_POINT('Ctrl Pts',(7.97013319294923,-0.352453708511098,
-5.16498565534682));
#20394=CARTESIAN_POINT('Ctrl Pts',(6.95124473111254,2.22784452034734,-5.0381583818386));
#20395=CARTESIAN_POINT('Ctrl Pts',(4.23442619493992,2.76744635914975,-4.91133110833039));
#20396=CARTESIAN_POINT('Ctrl Pts',(2.3033386979383,0.784339220129447,-4.78450383482217));
#20397=CARTESIAN_POINT('Ctrl Pts',(2.91887067434431,-1.91657275968413,-4.65767656131396));
#20398=CARTESIAN_POINT('Ctrl Pts',(5.52012569706886,-2.86700488419138,-4.53084928780574));
#20399=CARTESIAN_POINT('Ctrl Pts',(7.73206113288786,-1.20082706905823,-4.40402201429753));
#20400=CARTESIAN_POINT('Ctrl Pts',(7.53580810413746,1.56177595454288,-4.2771947407893));
#20401=CARTESIAN_POINT('Ctrl Pts',(5.11037160524329,2.89859106654255,-4.1503674672811));
#20402=CARTESIAN_POINT('Ctrl Pts',(2.66985841724704,1.58953309401564,-4.02354019377287));
#20403=CARTESIAN_POINT('Ctrl Pts',(2.44202395380747,-1.17055021914974,-3.89671292026466));
#20404=CARTESIAN_POINT('Ctrl Pts',(4.63486489973541,-2.86209006832044,-3.76988564675644));
#20405=CARTESIAN_POINT('Ctrl Pts',(7.24666058710183,-1.94101414881913,-3.64305837324822));
#20406=CARTESIAN_POINT('Ctrl Pts',(7.89326877336469,0.75189993075619,-3.51623109974001));
#20407=CARTESIAN_POINT('Ctrl Pts',(5.98443756838148,2.75844783131394,-3.38940382623179));
#20408=CARTESIAN_POINT('Ctrl Pts',(3.26262333974239,2.24697959886835,-3.26257655272358));
#20409=CARTESIAN_POINT('Ctrl Pts',(2.21240235494661,-0.315619142590331,
-3.13574927921536));
#20410=CARTESIAN_POINT('Ctrl Pts',(3.79245729783111,-2.59010812853723,-3.00892200570714));
#20411=CARTESIAN_POINT('Ctrl Pts',(6.56045280103919,-2.50024665817753,-2.88209473219892));
#20412=CARTESIAN_POINT('Ctrl Pts',(7.98965584489067,-0.128063414492935,
-2.75526745869071));
#20413=CARTESIAN_POINT('Ctrl Pts',(6.77543466215609,2.36102099644168,-2.62844018518249));
#20414=CARTESIAN_POINT('Ctrl Pts',(4.0261772494383,2.6948743395562,-2.50161291167428));
#20415=CARTESIAN_POINT('Ctrl Pts',(2.25151187571962,0.568742348125107,-2.37478563816606));
#20416=CARTESIAN_POINT('Ctrl Pts',(3.07142160426369,-2.07655960304068,-2.24795836465784));
#20417=CARTESIAN_POINT('Ctrl Pts',(5.7374611820532,-2.8262977990925,-2.12113109114962));
#20418=CARTESIAN_POINT('Ctrl Pts',(7.81596677729586,-0.996082268162477,
-1.99430381764141));
#20419=CARTESIAN_POINT('Ctrl Pts',(7.40959825216883,1.74339560410787,-1.86747654413319));
#20420=CARTESIAN_POINT('Ctrl Pts',(4.88930448269607,2.89143467549714,-1.74064927062498));
#20421=CARTESIAN_POINT('Ctrl Pts',(2.55570690325562,1.4000605669436,-1.61382199711676));
#20422=CARTESIAN_POINT('Ctrl Pts',(2.53900346014134,-1.3693428685055,-1.48699472360854));
#20423=CARTESIAN_POINT('Ctrl Pts',(4.85444170087268,-2.88875727779245,-1.36016745010033));
#20424=CARTESIAN_POINT('Ctrl Pts',(7.38840022471071,-1.77120253940683,-1.23334017659211));
#20425=CARTESIAN_POINT('Ctrl Pts',(7.8277838816539,0.963174244373312,-1.10651290308389));
#20426=CARTESIAN_POINT('Ctrl Pts',(5.77150630968967,2.81832839990373,-0.979685629575677));
#20427=CARTESIAN_POINT('Ctrl Pts',(3.09661704769054,2.10080360605791,-0.852858356067459));
#20428=CARTESIAN_POINT('Ctrl Pts',(2.24485826327766,-0.534415809265402,
-0.726031082559243));
#20429=CARTESIAN_POINT('Ctrl Pts',(3.99374825228489,-2.68179984573495,-0.599203809051027));
#20430=CARTESIAN_POINT('Ctrl Pts',(6.74683272654919,-2.3811334670074,-0.47237653554281));
#20431=CARTESIAN_POINT('Ctrl Pts',(7.99098991040469,0.0931234508551305,
-0.345549262034593));
#20432=CARTESIAN_POINT('Ctrl Pts',(6.59050510264064,2.48237368826305,-0.218721988526377));
#20433=CARTESIAN_POINT('Ctrl Pts',(3.82379489373254,2.60561740475589,-0.0918947150181613));
#20434=CARTESIAN_POINT('Ctrl Pts',(2.21641915587456,0.350352978779065,0.0349325584900565));
#20435=CARTESIAN_POINT('Ctrl Pts',(3.23565250640894,-2.22472716966094,0.161759831998273));
#20436=CARTESIAN_POINT('Ctrl Pts',(5.9510994011173,-2.76899048438087,0.288587105506489));
#20437=CARTESIAN_POINT('Ctrl Pts',(7.88399509974297,-0.785612403437753,
0.415414379014706));
#20438=CARTESIAN_POINT('Ctrl Pts',(7.26991779986226,1.91490300357299,0.542241652522922));
#20439=CARTESIAN_POINT('Ctrl Pts',(4.66942096385466,2.86742103471235,0.669068926031139));
#20440=CARTESIAN_POINT('Ctrl Pts',(2.45633848138528,1.2024464644806,0.795896199539355));
#20441=CARTESIAN_POINT('Ctrl Pts',(2.65085746622716,-1.56016765230576,0.922723473047572));
#20442=CARTESIAN_POINT('Ctrl Pts',(5.07541348069008,-2.89860051444825,1.04955074655579));
#20443=CARTESIAN_POINT('Ctrl Pts',(7.51677820823447,-1.59107894260581,1.176378020064));
#20444=CARTESIAN_POINT('Ctrl Pts',(7.74637969021288,1.16884090282531,1.30320529357222));
#20445=CARTESIAN_POINT('Ctrl Pts',(5.55462883138362,2.86179765553708,1.43003256708044));
#20446=CARTESIAN_POINT('Ctrl Pts',(2.94224041607201,1.94239504444831,1.55685984058865));
#20447=CARTESIAN_POINT('Ctrl Pts',(2.29390342654034,-0.750100738600607,
1.68368711409687));
#20448=CARTESIAN_POINT('Ctrl Pts',(4.20144489228679,-2.75787561397612,1.81051438760508));
#20449=CARTESIAN_POINT('Ctrl Pts',(6.92358733331937,-2.24815517642194,1.93734166111331));
#20450=CARTESIAN_POINT('Ctrl Pts',(7.97545405625221,0.313768083731995,2.06416893462152));
#20451=CARTESIAN_POINT('Ctrl Pts',(6.39686051491129,2.58927172577871,2.19099620812974));
#20452=CARTESIAN_POINT('Ctrl Pts',(3.62880782668101,2.50118819206035,2.31782348163795));
#20453=CARTESIAN_POINT('Ctrl Pts',(2.19808133069975,0.129923532131306,2.44465075514617));
#20454=CARTESIAN_POINT('Ctrl Pts',(3.41070339776045,-2.35994034290457,2.57147802865439));
#20455=CARTESIAN_POINT('Ctrl Pts',(6.15974579850069,-2.69555958052898,2.6983053021626));
#20456=CARTESIAN_POINT('Ctrl Pts',(7.93577651798969,-0.570567985919117,
2.82513257567082));
#20457=CARTESIAN_POINT('Ctrl Pts',(7.11756616166227,2.0752600898503,2.95195984917904));
#20458=CARTESIAN_POINT('Ctrl Pts',(4.4520087252469,2.82671065169848,3.07878712268725));
#20459=CARTESIAN_POINT('Ctrl Pts',(2.37232792576459,0.997830621189154,3.20561439619547));
#20460=CARTESIAN_POINT('Ctrl Pts',(2.77693667152565,-1.74190771605857,3.33244166970368));
#20461=CARTESIAN_POINT('Ctrl Pts',(5.29649248172284,-2.89156545340167,3.45926894321191));
#20462=CARTESIAN_POINT('Ctrl Pts',(7.63104755933012,-1.40169063203266,3.58609621672012));
#20463=CARTESIAN_POINT('Ctrl Pts',(7.64952991695677,1.3677015027485,3.71292349022833));
#20464=CARTESIAN_POINT('Ctrl Pts',(5.33506814515229,2.88860291328989,3.83975076373655));
#20465=CARTESIAN_POINT('Ctrl Pts',(2.80039228617996,1.77267608608568,3.96657803724477));
#20466=CARTESIAN_POINT('Ctrl Pts',(2.35925230121338,-0.961417896826199,
4.09340531075299));
#20467=CARTESIAN_POINT('Ctrl Pts',(4.41433779629248,-2.81789251330945,4.2202325842612));
#20468=CARTESIAN_POINT('Ctrl Pts',(7.08968740633153,-2.10208607453204,4.34705985776942));
#20469=CARTESIAN_POINT('Ctrl Pts',(7.94313874025325,0.532585672452493,4.47388713127763));
#20470=CARTESIAN_POINT('Ctrl Pts',(6.1956284776986,2.68109266010633,4.60071440478585));
#20471=CARTESIAN_POINT('Ctrl Pts',(3.44235143926906,2.38219477890292,4.72754167829407));
#20472=CARTESIAN_POINT('Ctrl Pts',(2.19660518063288,-0.0912624479003074,
4.85436895180227));
#20473=CARTESIAN_POINT('Ctrl Pts',(3.59555497179828,-2.48141178957951,4.98119622531051));
#20474=CARTESIAN_POINT('Ctrl Pts',(6.3621854446917,-2.60643266859086,5.10802349881871));
#20475=CARTESIAN_POINT('Ctrl Pts',(7.97100951323098,-0.352201200835182,
5.23485077232694));
#20476=CARTESIAN_POINT('Ctrl Pts',(6.95343046792319,2.22353311781684,5.36167804583515));
#20477=CARTESIAN_POINT('Ctrl Pts',(4.23833373932061,2.76954057936184,5.48850531934335));
#20478=CARTESIAN_POINT('Ctrl Pts',(2.30416442254237,0.787404497311804,5.61533259285159));
#20479=CARTESIAN_POINT('Ctrl Pts',(2.9165069278227,-1.91350480326794,5.74215986635979));
#20480=CARTESIAN_POINT('Ctrl Pts',(5.51639138025557,-2.86769305918452,5.86898713986803));
#20481=CARTESIAN_POINT('Ctrl Pts',(7.73054289754047,-1.20414039929179,5.99581441337622));
#20482=CARTESIAN_POINT('Ctrl Pts',(7.53779850966063,1.55859809623616,6.12264168688445));
#20483=CARTESIAN_POINT('Ctrl Pts',(5.11410273370085,2.89858808848458,6.24946896039267));
#20484=CARTESIAN_POINT('Ctrl Pts',(2.67189862729027,1.59263498964734,6.37629623390088));
#20485=CARTESIAN_POINT('Ctrl Pts',(2.44052436650502,-1.16713680258064,6.5031235074091));
#20486=CARTESIAN_POINT('Ctrl Pts',(4.63118730750988,-2.86150107056997,6.6299507809173));
#20487=CARTESIAN_POINT('Ctrl Pts',(7.24416575936279,-1.94377670896474,6.75677805442554));
#20488=CARTESIAN_POINT('Ctrl Pts',(7.89423213167136,0.748302061302728,6.88360532793373));
#20489=CARTESIAN_POINT('Ctrl Pts',(5.98798074758552,2.75730182596224,7.01043260144197));
#20490=CARTESIAN_POINT('Ctrl Pts',(3.26551145076094,2.24933005353904,7.13725987495017));
#20491=CARTESIAN_POINT('Ctrl Pts',(2.21199930116691,-0.311917014666013,
7.2640871484584));
#20492=CARTESIAN_POINT('Ctrl Pts',(3.78913085394635,-2.58843419205753,7.39091442196661));
#20493=CARTESIAN_POINT('Ctrl Pts',(6.55723955130574,-2.50212872679302,7.51774169547482));
#20494=CARTESIAN_POINT('Ctrl Pts',(7.98948892681172,-0.131783578909695,
7.64456896898306));
#20495=CARTESIAN_POINT('Ctrl Pts',(6.77846646645888,2.35885870657652,7.77139624249124));
#20496=CARTESIAN_POINT('Ctrl Pts',(4.02964021686276,2.69624371404217,7.8982235159995));
#20497=CARTESIAN_POINT('Ctrl Pts',(2.25224488184646,0.57239338579536,8.02505078950768));
#20498=CARTESIAN_POINT('Ctrl Pts',(3.06875552970189,-2.07395971907718,8.15187806301592));
#20499=CARTESIAN_POINT('Ctrl Pts',(5.73382972420172,-2.82712233866435,8.27870533652413));
#20500=CARTESIAN_POINT('Ctrl Pts',(7.81468487019807,-0.999578562139587,
8.40553261003235));
#20501=CARTESIAN_POINT('Ctrl Pts',(7.41183607055402,1.74041910909059,8.53235988354056));
#20502=CARTESIAN_POINT('Ctrl Pts',(4.89301925932717,2.89169503831994,8.65918715704877));
#20503=CARTESIAN_POINT('Ctrl Pts',(2.55750764676054,1.40332011871425,8.786014430557));
#20504=CARTESIAN_POINT('Ctrl Pts',(2.53724638227356,-1.3660595726293,8.91284170406521));
#20505=CARTESIAN_POINT('Ctrl Pts',(4.8507307301711,-2.88844735695125,9.03966897757343));
#20506=CARTESIAN_POINT('Ctrl Pts',(7.38612287844602,-1.77414890130498,9.16649625108164));
#20507=CARTESIAN_POINT('Ctrl Pts',(7.82901900942787,0.959661152530205,9.29332352458986));
#20508=CARTESIAN_POINT('Ctrl Pts',(5.77512643915643,2.81745546413148,9.42015079809808));
#20509=CARTESIAN_POINT('Ctrl Pts',(3.09931758500439,2.10336767546596,9.54697807160629));
#20510=CARTESIAN_POINT('Ctrl Pts',(2.24417405361598,-0.530755315511743,
9.67380534511451));
#20511=CARTESIAN_POINT('Ctrl Pts',(3.99030386886996,-2.68038436895184,9.80063261862273));
#20512=CARTESIAN_POINT('Ctrl Pts',(6.74377233507061,-2.38325510651274,9.92745989213094));
#20513=CARTESIAN_POINT('Ctrl Pts',(7.99110715517667,0.0894014046819865,
10.0542871656391));
#20514=CARTESIAN_POINT('Ctrl Pts',(6.59369295650387,2.48044887200891,10.1811144391474));
#20515=CARTESIAN_POINT('Ctrl Pts',(3.82714336369014,2.60724684752389,10.3079417126556));
#20516=CARTESIAN_POINT('Ctrl Pts',(2.2168716234732,0.354049295595143,10.4347689861638));
#20517=CARTESIAN_POINT('Ctrl Pts',(3.23279595285942,-2.22233818285863,10.561596259672));
#20518=CARTESIAN_POINT('Ctrl Pts',(5.94754137761666,-2.77008946619374,10.6884235331802));
#20519=CARTESIAN_POINT('Ctrl Pts',(7.88298354775886,-0.789196390895958,
10.8152508066884));
#20520=CARTESIAN_POINT('Ctrl Pts',(7.2723760263635,1.91210605078773,10.9420780801967));
#20521=CARTESIAN_POINT('Ctrl Pts',(4.67310515096523,2.86796344827419,11.0689053537049));
#20522=CARTESIAN_POINT('Ctrl Pts',(2.45788528247802,1.20583469856495,11.1957326272131));
#20523=CARTESIAN_POINT('Ctrl Pts',(2.64885543193806,-1.55702953779058,11.3225599007213));
#20524=CARTESIAN_POINT('Ctrl Pts',(5.07168913486267,-2.89857134109138,11.4493871742295));
#20525=CARTESIAN_POINT('Ctrl Pts',(7.51473320210737,-1.59419633329225,11.5762144477377));
#20526=CARTESIAN_POINT('Ctrl Pts',(7.74787711807591,1.16544356219989,11.703041721246));
#20527=CARTESIAN_POINT('Ctrl Pts',(5.558308767198,2.86118170031369,11.8298689947542));
#20528=CARTESIAN_POINT('Ctrl Pts',(2.94473036854272,1.94519872671588,11.9566962682624));
#20529=CARTESIAN_POINT('Ctrl Pts',(2.29295581376568,-0.746581473643887,
12.0835235417706));
#20530=CARTESIAN_POINT('Ctrl Pts',(4.19787645564695,-2.75657755125406,12.2103508152788));
#20531=CARTESIAN_POINT('Ctrl Pts',(6.9207474413867,-2.25078855220226,12.3371780887871));
#20532=CARTESIAN_POINT('Ctrl Pts',(7.97575989671253,0.310608304160704,12.4640053622953));
#20533=CARTESIAN_POINT('Ctrl Pts',(6.40036655503507,2.58655836180867,12.5908326358035));
#20534=CARTESIAN_POINT('Ctrl Pts',(3.63167842849399,2.50507731566553,12.7176599093117));
#20535=CARTESIAN_POINT('Ctrl Pts',(2.19870818211441,0.129205115595229,12.844504483368));
#20536=CARTESIAN_POINT('Ctrl Pts',(3.00418309070775,-1.52257885595242,12.9290732995882));
#20537=CARTESIAN_POINT('Ctrl Pts',(3.66734313348352,-1.99639465383534,12.9713663579723));
#20538=CARTESIAN_POINT('Ctrl Pts',(4.01617654290848,2.20524431464374,12.706362531166));
#20539=CARTESIAN_POINT('Ctrl Pts',(3.96412481280005,2.1740903404473,12.706362531166));
#20540=CARTESIAN_POINT('Ctrl Pts',(3.91342899343042,2.14094354517164,12.706362531166));
#20541=CARTESIAN_POINT('Ctrl Pts',(3.8642154788866,2.10580426985646,12.706362531166));
#20542=CARTESIAN_POINT('Ctrl Pts',(3.7955725456219,2.05679206349834,12.706362531166));
#20543=CARTESIAN_POINT('Ctrl Pts',(3.72981155181425,2.00390483037292,12.706362531166));
#20544=CARTESIAN_POINT('Ctrl Pts',(3.66707598254363,1.94750832456937,12.706362531166));
#20545=CARTESIAN_POINT('Ctrl Pts',(3.60356184354373,1.89041191896788,12.706362531166));
#20546=CARTESIAN_POINT('Ctrl Pts',(3.54314820656414,1.82971763964448,12.706362531166));
#20547=CARTESIAN_POINT('Ctrl Pts',(3.48602767856145,1.76577476703768,12.706362531166));
#20548=CARTESIAN_POINT('Ctrl Pts',(3.43577223874705,1.7095169329767,12.706362531166));
#20549=CARTESIAN_POINT('Ctrl Pts',(3.38806637215777,1.65074357121809,12.706362531166));
#20550=CARTESIAN_POINT('Ctrl Pts',(3.34307309132191,1.58968252285634,12.706362531166));
#20551=CARTESIAN_POINT('Ctrl Pts',(3.33502299263552,1.57875761460171,12.706362531166));
#20552=CARTESIAN_POINT('Ctrl Pts',(3.32705953936463,1.56775894682874,12.706362531166));
#20553=CARTESIAN_POINT('Ctrl Pts',(3.31919274731376,1.55670083255366,12.706362531166));
#20554=CARTESIAN_POINT('Ctrl Pts',(3.27051921520694,1.48828190438977,12.706362531166));
#20555=CARTESIAN_POINT('Ctrl Pts',(3.22545495269274,1.41747248052991,12.706362531166));
#20556=CARTESIAN_POINT('Ctrl Pts',(3.18414803610741,1.34462167953958,12.706362531166));
#20557=CARTESIAN_POINT('Ctrl Pts',(3.14298608776046,1.27202655128295,12.706362531166));
#20558=CARTESIAN_POINT('Ctrl Pts',(3.10555484108553,1.19740334531551,12.706362531166));
#20559=CARTESIAN_POINT('Ctrl Pts',(3.07204921526324,1.12108015481246,12.706362531166));
#20560=CARTESIAN_POINT('Ctrl Pts',(3.0393754946111,1.04665197910837,12.706362531166));
#20561=CARTESIAN_POINT('Ctrl Pts',(3.01043477138293,0.970606298836382,12.706362531166));
#20562=CARTESIAN_POINT('Ctrl Pts',(2.98545673362889,0.893244772984474,12.706362531166));
#20563=CARTESIAN_POINT('Ctrl Pts',(2.97373044481661,0.856926323792001,12.706362531166));
#20564=CARTESIAN_POINT('Ctrl Pts',(2.9628782381547,0.820317910312545,12.706362531166));
#20565=CARTESIAN_POINT('Ctrl Pts',(2.95292784475094,0.783451362266065,12.706362531166));
#20566=CARTESIAN_POINT('Ctrl Pts',(2.94898502933406,0.768843096230084,12.706362531166));
#20567=CARTESIAN_POINT('Ctrl Pts',(2.94518353990657,0.754192671177584,12.706362531166));
#20568=CARTESIAN_POINT('Ctrl Pts',(2.94153002573792,0.739522721976762,12.706362531166));
#20569=CARTESIAN_POINT('Ctrl Pts',(2.92212297738889,0.661597633890026,12.706362531166));
#20570=CARTESIAN_POINT('Ctrl Pts',(2.90685063396446,0.582991787835282,12.706362531166));
#20571=CARTESIAN_POINT('Ctrl Pts',(2.89588468653661,0.504004912306211,12.706362531166));
#20572=CARTESIAN_POINT('Ctrl Pts',(2.88523725179527,0.427312259149472,12.706362531166));
#20573=CARTESIAN_POINT('Ctrl Pts',(2.87864967603292,0.350259608145263,12.706362531166));
#20574=CARTESIAN_POINT('Ctrl Pts',(2.87632731099095,0.273124066218685,12.706362531166));
#20575=CARTESIAN_POINT('Ctrl Pts',(2.87460628536994,0.215961543726355,12.706362531166));
#20576=CARTESIAN_POINT('Ctrl Pts',(2.87522858516988,0.158753502861158,12.706362531166));
#20577=CARTESIAN_POINT('Ctrl Pts',(2.87829576895771,0.101617392022989,12.706362531166));
#20578=CARTESIAN_POINT('Ctrl Pts',(2.88063481507154,0.0580451748816736,
12.706362531166));
#20579=CARTESIAN_POINT('Ctrl Pts',(2.88439617502459,0.0145148557028028,
12.706362531166));
#20580=CARTESIAN_POINT('Ctrl Pts',(2.88955511502261,-0.0289182870924016,
12.706362531166));
#20581=CARTESIAN_POINT('Ctrl Pts',(2.891997784775,-0.0494831364989744,12.706362531166));
#20582=CARTESIAN_POINT('Ctrl Pts',(2.89475382668687,-0.0700261632891898,
12.7063625311661));
#20583=CARTESIAN_POINT('Ctrl Pts',(2.89782089320795,-0.0905412794435463,
12.7063625311661));
#20584=CARTESIAN_POINT('Ctrl Pts',(2.89963471943402,-0.10267367222214,12.706362531166));
#20585=CARTESIAN_POINT('Ctrl Pts',(2.90155583066391,-0.114786297038073,
12.7063625311661));
#20586=CARTESIAN_POINT('Ctrl Pts',(2.90358323488813,-0.126877932230494,
12.706362531166));
#20587=CARTESIAN_POINT('Ctrl Pts',(2.91645442833662,-0.203642976818655,
12.7063625311661));
#20588=CARTESIAN_POINT('Ctrl Pts',(2.93360576650297,-0.279564944346245,
12.7063625311661));
#20589=CARTESIAN_POINT('Ctrl Pts',(2.95481919736294,-0.354355451724281,
12.7063625311661));
#20590=CARTESIAN_POINT('Ctrl Pts',(2.97622105807171,-0.429810291245941,
12.7063625311661));
#20591=CARTESIAN_POINT('Ctrl Pts',(3.00175809900175,-0.504114372604786,
12.7063625311661));
#20592=CARTESIAN_POINT('Ctrl Pts',(3.03125399139832,-0.576948215175514,
12.7063625311661));
#20593=CARTESIAN_POINT('Ctrl Pts',(3.06045458320581,-0.649052875651101,
12.7063625311661));
#20594=CARTESIAN_POINT('Ctrl Pts',(3.09353584953513,-0.719717347631348,
12.7063625311661));
#20595=CARTESIAN_POINT('Ctrl Pts',(3.13036322612031,-0.788596670847388,
12.7063625311661));
#20596=CARTESIAN_POINT('Ctrl Pts',(3.13841107268683,-0.803648794464367,
12.7063625311661));
#20597=CARTESIAN_POINT('Ctrl Pts',(3.14663793160898,-0.818615510215626,
12.7063625311661));
#20598=CARTESIAN_POINT('Ctrl Pts',(3.15504258425979,-0.833492938132457,
12.7063625311661));
#20599=CARTESIAN_POINT('Ctrl Pts',(3.16198740923832,-0.84578626390163,12.7063625311661));
#20600=CARTESIAN_POINT('Ctrl Pts',(3.16905363004956,-0.85801862357911,12.7063625311661));
#20601=CARTESIAN_POINT('Ctrl Pts',(3.17624058869617,-0.870187770193119,
12.7063625311661));
#20602=CARTESIAN_POINT('Ctrl Pts',(3.18310939201618,-0.881818207875329,
12.7063625311661));
#20603=CARTESIAN_POINT('Ctrl Pts',(3.1900833958179,-0.893382290911527,12.7063625311661));
#20604=CARTESIAN_POINT('Ctrl Pts',(3.19716136682681,-0.904877975358936,
12.7063625311661));
#20605=CARTESIAN_POINT('Ctrl Pts',(3.2371698418621,-0.969857727840078,12.7063625311661));
#20606=CARTESIAN_POINT('Ctrl Pts',(3.28050020814543,-1.03265978440192,12.7063625311661));
#20607=CARTESIAN_POINT('Ctrl Pts',(3.3269982826191,-1.09297461243398,12.7063625311661));
#20608=CARTESIAN_POINT('Ctrl Pts',(3.36850332953163,-1.14681275079408,12.7063625311661));
#20609=CARTESIAN_POINT('Ctrl Pts',(3.41253311578195,-1.1986690627602,12.7063625311661));
#20610=CARTESIAN_POINT('Ctrl Pts',(3.45899756854344,-1.2482942239992,12.7063625311661));
#20611=CARTESIAN_POINT('Ctrl Pts',(3.47176322594664,-1.26192825537815,12.7063625311661));
#20612=CARTESIAN_POINT('Ctrl Pts',(3.4847127467252,-1.27539369266552,12.7063625311661));
#20613=CARTESIAN_POINT('Ctrl Pts',(3.49784445064999,-1.28868493357174,12.7063625311661));
#20614=CARTESIAN_POINT('Ctrl Pts',(3.50919570582733,-1.30017409507081,12.7063625311661));
#20615=CARTESIAN_POINT('Ctrl Pts',(3.52068411570671,-1.31153392785575,12.7063625311661));
#20616=CARTESIAN_POINT('Ctrl Pts',(3.53229553060125,-1.32274849072851,12.7063625311661));
#20617=CARTESIAN_POINT('Ctrl Pts',(3.58532462221074,-1.3739651673645,12.7063625311661));
#20618=CARTESIAN_POINT('Ctrl Pts',(3.64097669980664,-1.42221694716149,12.7063625311661));
#20619=CARTESIAN_POINT('Ctrl Pts',(3.69912395167213,-1.4671959866198,12.7063625311661));
#20620=CARTESIAN_POINT('Ctrl Pts',(3.75558706950963,-1.51087228642202,12.7063625311661));
#20621=CARTESIAN_POINT('Ctrl Pts',(3.81440352439144,-1.5514630336865,12.7063625311661));
#20622=CARTESIAN_POINT('Ctrl Pts',(3.87547414029406,-1.58864064437125,12.7063625311661));
#20623=CARTESIAN_POINT('Ctrl Pts',(3.89458882478181,-1.60027698187568,12.7063625311661));
#20624=CARTESIAN_POINT('Ctrl Pts',(3.91392443695495,-1.61157858690491,12.7063625311661));
#20625=CARTESIAN_POINT('Ctrl Pts',(3.93347817078409,-1.62253437445176,12.7063625311661));
#20626=CARTESIAN_POINT('',(6.25533269723243,1.62367305565468,-5.29454830118707));
#20627=CARTESIAN_POINT('Ctrl Pts',(6.25666079319718,1.62473242747262,-5.29363746883395));
#20628=CARTESIAN_POINT('Ctrl Pts',(6.30029936923465,1.60060502024658,-5.29363746883395));
#20629=CARTESIAN_POINT('Ctrl Pts',(6.34288879700294,1.57478294270003,-5.29363746883395));
#20630=CARTESIAN_POINT('Ctrl Pts',(6.38431760724696,1.54728805898193,-5.29363746883395));
#20631=CARTESIAN_POINT('Ctrl Pts',(6.44434588998498,1.50744934181971,-5.29363746883395));
#20632=CARTESIAN_POINT('Ctrl Pts',(6.50193891059609,1.46410113537834,-5.29363746883395));
#20633=CARTESIAN_POINT('Ctrl Pts',(6.55701390975331,1.4175919904065,-5.29363746883395));
#20634=CARTESIAN_POINT('Ctrl Pts',(6.58791321965453,1.3914984723726,-5.29363746883395));
#20635=CARTESIAN_POINT('Ctrl Pts',(6.61801962391498,1.36440905786912,-5.29363746883395));
#20636=CARTESIAN_POINT('Ctrl Pts',(6.64731552654543,1.33637883922313,-5.29363746883395));
#20637=CARTESIAN_POINT('Ctrl Pts',(6.65793035597894,1.32622260701332,-5.29363746883395));
#20638=CARTESIAN_POINT('Ctrl Pts',(6.66843905008924,1.31594252779162,-5.29363746883395));
#20639=CARTESIAN_POINT('Ctrl Pts',(6.67883979765888,1.30554198152458,-5.29363746883395));
#20640=CARTESIAN_POINT('Ctrl Pts',(6.731109861527,1.2532729293241,-5.29363746883395));
#20641=CARTESIAN_POINT('Ctrl Pts',(6.78048306833212,1.19813763446167,-5.29363746883395));
#20642=CARTESIAN_POINT('Ctrl Pts',(6.82687614202416,1.1405003640249,-5.29363746883395));
#20643=CARTESIAN_POINT('Ctrl Pts',(6.87457429265904,1.0812417077495,-5.29363746883395));
#20644=CARTESIAN_POINT('Ctrl Pts',(6.9191229398719,1.01933778227313,-5.29363746883395));
#20645=CARTESIAN_POINT('Ctrl Pts',(6.96040442051302,0.95513715488343,-5.29363746883395));
#20646=CARTESIAN_POINT('Ctrl Pts',(6.97007751070159,0.940093642653284,-5.29363746883395));
#20647=CARTESIAN_POINT('Ctrl Pts',(6.97957107437076,0.924923849450251,-5.29363746883395));
#20648=CARTESIAN_POINT('Ctrl Pts',(6.98888332827715,0.9096319518153,-5.29363746883395));
#20649=CARTESIAN_POINT('Ctrl Pts',(6.99596956207693,0.89799546048109,-5.29363746883395));
#20650=CARTESIAN_POINT('Ctrl Pts',(7.00295080503329,0.886288261447592,-5.29363746883395));
#20651=CARTESIAN_POINT('Ctrl Pts',(7.00982622720321,0.87451215610694,-5.29363746883395));
#20652=CARTESIAN_POINT('Ctrl Pts',(7.01689812932228,0.862399523274394,-5.29363746883395));
#20653=CARTESIAN_POINT('Ctrl Pts',(7.02385346834336,0.850221843496349,-5.29363746883395));
#20654=CARTESIAN_POINT('Ctrl Pts',(7.03069026763827,0.837984069217663,-5.29363746883395));
#20655=CARTESIAN_POINT('Ctrl Pts',(7.0688520410006,0.769675033316855,-5.29363746883395));
#20656=CARTESIAN_POINT('Ctrl Pts',(7.10333816565241,0.699471189973925,-5.29363746883395));
#20657=CARTESIAN_POINT('Ctrl Pts',(7.1340509191707,0.627756354610849,-5.29363746883395));
#20658=CARTESIAN_POINT('Ctrl Pts',(7.16512437454675,0.555199273881231,-5.29363746883395));
#20659=CARTESIAN_POINT('Ctrl Pts',(7.19233595085917,0.481094685903242,-5.29363746883395));
#20660=CARTESIAN_POINT('Ctrl Pts',(7.21554881768624,0.405800158113758,-5.29363746883395));
#20661=CARTESIAN_POINT('Ctrl Pts',(7.2386023964655,0.331022305771233,-5.29363746883395));
#20662=CARTESIAN_POINT('Ctrl Pts',(7.25771249741322,0.2550698512193,-5.29363746883395));
#20663=CARTESIAN_POINT('Ctrl Pts',(7.27270144705816,0.178267214732533,-5.29363746883395));
#20664=CARTESIAN_POINT('Ctrl Pts',(7.2773482629243,0.154457160109444,-5.29363746883395));
#20665=CARTESIAN_POINT('Ctrl Pts',(7.28159864515951,0.130565261658507,-5.29363746883395));
#20666=CARTESIAN_POINT('Ctrl Pts',(7.28544631241327,0.106600894764324,-5.29363746883395));
#20667=CARTESIAN_POINT('Ctrl Pts',(7.28782821378857,0.0917657349911405,
-5.29363746883395));
#20668=CARTESIAN_POINT('Ctrl Pts',(7.29005592416018,0.0769009007266584,
-5.29363746883395));
#20669=CARTESIAN_POINT('Ctrl Pts',(7.2921251510253,0.0620305370594762,-5.29363746883395));
#20670=CARTESIAN_POINT('Ctrl Pts',(7.30329430528889,-0.0182358602865081,
-5.29363746883395));
#20671=CARTESIAN_POINT('Ctrl Pts',(7.30987324050768,-0.0988001668559794,
-5.29363746883395));
#20672=CARTESIAN_POINT('Ctrl Pts',(7.31173319533953,-0.179285772036483,
-5.29363746883395));
#20673=CARTESIAN_POINT('Ctrl Pts',(7.31242671300975,-0.209296280052594,
-5.29363746883395));
#20674=CARTESIAN_POINT('Ctrl Pts',(7.31246371580651,-0.239296136201682,
-5.29363746883395));
#20675=CARTESIAN_POINT('Ctrl Pts',(7.31183589213809,-0.269266694326119,
-5.29363746883395));
#20676=CARTESIAN_POINT('Ctrl Pts',(7.3101929237976,-0.347697439488371,-5.29363746883395));
#20677=CARTESIAN_POINT('Ctrl Pts',(7.30400105115064,-0.425927024337316,
-5.29363746883395));
#20678=CARTESIAN_POINT('Ctrl Pts',(7.29350020192805,-0.503697173141665,
-5.29363746883395));
#20679=CARTESIAN_POINT('Ctrl Pts',(7.28299935270546,-0.581467321946014,
-5.29363746883395));
#20680=CARTESIAN_POINT('Ctrl Pts',(7.26818923120758,-0.65877879964822,-5.29363746883395));
#20681=CARTESIAN_POINT('Ctrl Pts',(7.24925749796867,-0.735375178179596,
-5.29363746883395));
#20682=CARTESIAN_POINT('Ctrl Pts',(7.24622536278699,-0.747642970631759,
-5.29363746883395));
#20683=CARTESIAN_POINT('Ctrl Pts',(7.24308680695059,-0.759894624142244,
-5.29363746883395));
#20684=CARTESIAN_POINT('Ctrl Pts',(7.2398444115817,-0.772121842590014,-5.29363746883395));
#20685=CARTESIAN_POINT('Ctrl Pts',(7.21915333483621,-0.850148821568037,
-5.29363746883395));
#20686=CARTESIAN_POINT('Ctrl Pts',(7.19429464267757,-0.926973379788445,
-5.29363746883395));
#20687=CARTESIAN_POINT('Ctrl Pts',(7.16554718013261,-1.00232735033283,-5.29363746883395));
#20688=CARTESIAN_POINT('Ctrl Pts',(7.13626789340404,-1.07907535917899,-5.29363746883395));
#20689=CARTESIAN_POINT('Ctrl Pts',(7.10295442700467,-1.15429867121524,-5.29363746883395));
#20690=CARTESIAN_POINT('Ctrl Pts',(7.06584639520479,-1.22771683525656,-5.29363746883395));
#20691=CARTESIAN_POINT('Ctrl Pts',(7.02829731740499,-1.30200760789503,-5.29363746883395));
#20692=CARTESIAN_POINT('Ctrl Pts',(6.98686265169164,-1.37445097862862,-5.29363746883395));
#20693=CARTESIAN_POINT('Ctrl Pts',(6.94173861538553,-1.44474621559212,-5.29363746883395));
#20694=CARTESIAN_POINT('Ctrl Pts',(6.9137828184364,-1.48829638379319,-5.29363746883395));
#20695=CARTESIAN_POINT('Ctrl Pts',(6.88440995680354,-1.53102180418571,-5.29363746883395));
#20696=CARTESIAN_POINT('Ctrl Pts',(6.85365761921674,-1.57284665132636,-5.29363746883395));
#20697=CARTESIAN_POINT('Ctrl Pts',(6.84595894636615,-1.58331726398313,-5.29363746883395));
#20698=CARTESIAN_POINT('Ctrl Pts',(6.83817934135279,-1.59372384382491,-5.29363746883395));
#20699=CARTESIAN_POINT('Ctrl Pts',(6.83032080761261,-1.60406400041825,-5.29363746883395));
#20700=CARTESIAN_POINT('Ctrl Pts',(6.77836195742938,-1.67243078041412,-5.29363746883395));
#20701=CARTESIAN_POINT('Ctrl Pts',(6.72294242113773,-1.73791443631007,-5.29363746883395));
#20702=CARTESIAN_POINT('Ctrl Pts',(6.66431733044397,-1.80021839569566,-5.29363746883395));
#20703=CARTESIAN_POINT('Ctrl Pts',(6.60562811837204,-1.86259050023369,-5.29363746883395));
#20704=CARTESIAN_POINT('Ctrl Pts',(6.54372589764592,-1.92177688286241,-5.29363746883395));
#20705=CARTESIAN_POINT('Ctrl Pts',(6.47881773090058,-1.97746203272859,-5.29363746883395));
#20706=CARTESIAN_POINT('Ctrl Pts',(6.41530242565524,-2.03195223740901,-5.29363746883395));
#20707=CARTESIAN_POINT('Ctrl Pts',(6.348908239579,-2.08309064270886,-5.29363746883395));
#20708=CARTESIAN_POINT('Ctrl Pts',(6.27979002010412,-2.1305519155269,-5.29363746883395));
#20709=CARTESIAN_POINT('Ctrl Pts',(6.24357415776808,-2.1554201910081,-5.29363746883395));
#20710=CARTESIAN_POINT('Ctrl Pts',(6.20660982183934,-2.17927836310074,-5.29363746883395));
#20711=CARTESIAN_POINT('Ctrl Pts',(6.1689156158044,-2.20207516956608,-5.29363746883395));
#20712=CARTESIAN_POINT('Ctrl Pts',(6.25440237736867,1.62237255794581,-5.29454830118707));
#20713=CARTESIAN_POINT('Ctrl Pts',(6.24705183310046,1.62763081968323,-5.29424469040269));
#20714=CARTESIAN_POINT('Ctrl Pts',(6.23966555258041,1.63283912556818,-5.29394107961832));
#20715=CARTESIAN_POINT('Ctrl Pts',(6.2322442180908,1.63799699450132,-5.29363746883395));
#20716=CARTESIAN_POINT('Ctrl Pts',(3.66734314315846,1.99639467351756,-5.55864130264131));
#20717=CARTESIAN_POINT('Ctrl Pts',(3.00418308807966,1.52257887569804,-5.5163482439231));
#20718=CARTESIAN_POINT('Ctrl Pts',(2.19870851602258,-0.129205714733684,
-5.4317794273688));
#20719=CARTESIAN_POINT('Ctrl Pts',(3.63167818438598,-2.50507698344247,-5.30493485297845));
#20720=CARTESIAN_POINT('Ctrl Pts',(6.40036668721888,-2.58655864996601,-5.17810757947023));
#20721=CARTESIAN_POINT('Ctrl Pts',(7.97575989825059,-0.310608158848719,
-5.05128030596201));
#20722=CARTESIAN_POINT('Ctrl Pts',(6.92074750039589,2.25078850093184,-4.92445303245379));
#20723=CARTESIAN_POINT('Ctrl Pts',(4.19787642714988,2.7565776590141,-4.79762575894558));
#20724=CARTESIAN_POINT('Ctrl Pts',(2.29295576704817,0.74658145406325,-4.67079848543737));
#20725=CARTESIAN_POINT('Ctrl Pts',(2.94473032594405,-1.94519874334173,-4.54397121192914));
#20726=CARTESIAN_POINT('Ctrl Pts',(5.55830877699676,-2.86118176505069,-4.41714393842093));
#20727=CARTESIAN_POINT('Ctrl Pts',(7.7478771670619,-1.16544357738298,-4.29031666491272));
#20728=CARTESIAN_POINT('Ctrl Pts',(7.51473324745422,1.59419635928178,-4.16348939140448));
#20729=CARTESIAN_POINT('Ctrl Pts',(5.07168913436726,2.89857139725113,-4.03666211789627));
#20730=CARTESIAN_POINT('Ctrl Pts',(2.64885538638093,1.55702956562814,-3.90983484438807));
#20731=CARTESIAN_POINT('Ctrl Pts',(2.45788523332366,-1.20583472037831,-3.78300757087985));
#20732=CARTESIAN_POINT('Ctrl Pts',(4.67310514312105,-2.86796350212083,-3.65618029737162));
#20733=CARTESIAN_POINT('Ctrl Pts',(7.27237606698426,-1.91210608623046,-3.52935302386342));
#20734=CARTESIAN_POINT('Ctrl Pts',(7.88298359976007,0.789196405494946,-3.4025257503552));
#20735=CARTESIAN_POINT('Ctrl Pts',(5.94754139353568,2.7700895179055,-3.27569847684697));
#20736=CARTESIAN_POINT('Ctrl Pts',(3.23279591815959,2.22233822425849,-3.14887120333877));
#20737=CARTESIAN_POINT('Ctrl Pts',(2.21687156983362,-0.354049302176947,
-3.02204392983055));
#20738=CARTESIAN_POINT('Ctrl Pts',(3.82714334007257,-2.60724689614626,-2.89521665632232));
#20739=CARTESIAN_POINT('Ctrl Pts',(6.59369298446895,-2.4804489182506,-2.76838938281411));
#20740=CARTESIAN_POINT('Ctrl Pts',(7.9911072091958,-0.089401406352042,-2.6415621093059));
#20741=CARTESIAN_POINT('Ctrl Pts',(6.74377236583368,2.3832551509499,-2.51473483579769));
#20742=CARTESIAN_POINT('Ctrl Pts',(3.99030384829488,2.6803844189262,-2.38790756228946));
#20743=CARTESIAN_POINT('Ctrl Pts',(2.2441740004847,0.530755325408102,-2.26108028878124));
#20744=CARTESIAN_POINT('Ctrl Pts',(3.09931754781707,-2.10336771468319,-2.13425301527302));
#20745=CARTESIAN_POINT('Ctrl Pts',(5.77512645185915,-2.81745551666232,-2.00742574176481));
#20746=CARTESIAN_POINT('Ctrl Pts',(7.82901906042506,-0.959661170423007,
-1.88059846825659));
#20747=CARTESIAN_POINT('Ctrl Pts',(7.3861229211855,1.77414893438375,-1.75377119474838));
#20748=CARTESIAN_POINT('Ctrl Pts',(4.85073072563859,2.88844741080586,-1.62694392124016));
#20749=CARTESIAN_POINT('Ctrl Pts',(2.53724633460654,1.36605959809925,-1.50011664773194));
#20750=CARTESIAN_POINT('Ctrl Pts',(2.55750759947128,-1.40332014487893,-1.37328937422373));
#20751=CARTESIAN_POINT('Ctrl Pts',(4.89301925558316,-2.89169509223513,-1.24646210071551));
#20752=CARTESIAN_POINT('Ctrl Pts',(7.4118361137729,-1.74041914154042,-1.11963482720729));
#20753=CARTESIAN_POINT('Ctrl Pts',(7.81468492092802,0.99957858077657,-0.992807553699079));
#20754=CARTESIAN_POINT('Ctrl Pts',(5.73382973613445,2.82712239137559,-0.865980280190864));
#20755=CARTESIAN_POINT('Ctrl Pts',(3.06875549194474,2.0739597577458,-0.739153006682644));
#20756=CARTESIAN_POINT('Ctrl Pts',(2.25224482886564,-0.57239339646756,-0.612325733174432));
#20757=CARTESIAN_POINT('Ctrl Pts',(4.02964019702116,-2.69624376431319,-0.485498459666212));
#20758=CARTESIAN_POINT('Ctrl Pts',(6.77846649786872,-2.35885875055705,-0.358671186157998));
#20759=CARTESIAN_POINT('Ctrl Pts',(7.98948898080085,0.131783581366781,-0.23184391264978));
#20760=CARTESIAN_POINT('Ctrl Pts',(6.55723957859082,2.50212877344481,-0.105016639141564));
#20761=CARTESIAN_POINT('Ctrl Pts',(3.7891308296205,2.58843424031846,0.021810634366653));
#20762=CARTESIAN_POINT('Ctrl Pts',(2.21199924743569,0.311917020481634,0.148637907874869));
#20763=CARTESIAN_POINT('Ctrl Pts',(3.26551141667232,-2.24933009547745,0.275465181383086));
#20764=CARTESIAN_POINT('Ctrl Pts',(5.98798076425687,-2.75730187737167,0.402292454891301));
#20765=CARTESIAN_POINT('Ctrl Pts',(7.89423218388447,-0.748302075254695,
0.529119728399519));
#20766=CARTESIAN_POINT('Ctrl Pts',(7.24416579945549,1.94377674520614,0.655947001907735));
#20767=CARTESIAN_POINT('Ctrl Pts',(4.63118729888403,2.86150112392219,0.782774275415952));
#20768=CARTESIAN_POINT('Ctrl Pts',(2.44052431703461,1.1671368243417,0.909601548924168));
#20769=CARTESIAN_POINT('Ctrl Pts',(2.67189858213383,-1.59263501934178,1.03642882243239));
#20770=CARTESIAN_POINT('Ctrl Pts',(5.11410273407891,-2.89858814252828,1.16325609594061));
#20771=CARTESIAN_POINT('Ctrl Pts',(7.53779855522807,-1.55859812529596,1.29008336944882));
#20772=CARTESIAN_POINT('Ctrl Pts',(7.73054294670161,1.20414042174279,1.41691064295704));
#20773=CARTESIAN_POINT('Ctrl Pts',(5.51639138813421,2.8676931126522,1.54373791646525));
#20774=CARTESIAN_POINT('Ctrl Pts',(2.91650688722692,1.91350483894491,1.67056518997347));
#20775=CARTESIAN_POINT('Ctrl Pts',(2.30416437052955,-0.787404511992841,
1.79739246348169));
#20776=CARTESIAN_POINT('Ctrl Pts',(4.23833372337011,-2.76954063099948,1.92421973698991));
#20777=CARTESIAN_POINT('Ctrl Pts',(6.9534305025952,-2.22353315927424,2.05104701049812));
#20778=CARTESIAN_POINT('Ctrl Pts',(7.97100956687557,0.352201207401914,2.17787428400634));
#20779=CARTESIAN_POINT('Ctrl Pts',(6.36218546834003,2.60643271718737,2.30470155751455));
#20780=CARTESIAN_POINT('Ctrl Pts',(3.59555494386324,2.48141183584503,2.43152883102277));
#20781=CARTESIAN_POINT('Ctrl Pts',(2.19660512661465,0.0912624496018655,
2.55835610453099));
#20782=CARTESIAN_POINT('Ctrl Pts',(3.44235140847758,-2.38219482331856,2.6851833780392));
#20783=CARTESIAN_POINT('Ctrl Pts',(6.19562849824152,-2.68109271009487,2.81201065154742));
#20784=CARTESIAN_POINT('Ctrl Pts',(7.9431387933782,-0.532585682382451,2.93883792505564));
#20785=CARTESIAN_POINT('Ctrl Pts',(7.08968744354401,2.10208611372509,3.06566519856385));
#20786=CARTESIAN_POINT('Ctrl Pts',(4.41433778362352,2.81789256584859,3.19249247207207));
#20787=CARTESIAN_POINT('Ctrl Pts',(2.35925225022766,0.96141791475166,3.31931974558028));
#20788=CARTESIAN_POINT('Ctrl Pts',(2.80039224341925,-1.77267611913694,3.4461470190885));
#20789=CARTESIAN_POINT('Ctrl Pts',(5.3350681496502,-2.88860296714743,3.57297429259672));
#20790=CARTESIAN_POINT('Ctrl Pts',(7.64952996460744,-1.36770152824906,3.69980156610494));
#20791=CARTESIAN_POINT('Ctrl Pts',(7.63104760663617,1.40169065816697,3.82662883961315));
#20792=CARTESIAN_POINT('Ctrl Pts',(5.29649248550149,2.89156550731442,3.95345611312137));
#20793=CARTESIAN_POINT('Ctrl Pts',(2.77693662832761,1.74190774853615,4.08028338662959));
#20794=CARTESIAN_POINT('Ctrl Pts',(2.37232787502268,-0.997830639793556,
4.2071106601378));
#20795=CARTESIAN_POINT('Ctrl Pts',(4.45200871328031,-2.82671070440203,4.33393793364602));
#20796=CARTESIAN_POINT('Ctrl Pts',(7.11756619939457,-2.07526012854318,4.46076520715423));
#20797=CARTESIAN_POINT('Ctrl Pts',(7.93577657097738,0.570567996557279,4.58759248066245));
#20798=CARTESIAN_POINT('Ctrl Pts',(6.15974581837457,2.69555963078725,4.71441975417067));
#20799=CARTESIAN_POINT('Ctrl Pts',(3.41070336637887,2.35994038690525,4.84124702767889));
#20800=CARTESIAN_POINT('Ctrl Pts',(2.19808127670905,-0.129923534553724,
4.9680743011871));
#20801=CARTESIAN_POINT('Ctrl Pts',(3.62880779936598,-2.5011882386946,5.09490157469532));
#20802=CARTESIAN_POINT('Ctrl Pts',(6.39686053920616,-2.58927177405525,5.22172884820352));
#20803=CARTESIAN_POINT('Ctrl Pts',(7.97545410997968,-0.31376808958212,5.34855612171176));
#20804=CARTESIAN_POINT('Ctrl Pts',(6.92358736743495,2.24815521833844,5.47538339521996));
#20805=CARTESIAN_POINT('Ctrl Pts',(4.20144487564846,2.75787566539626,5.60221066872819));
#20806=CARTESIAN_POINT('Ctrl Pts',(2.29390337433622,0.750100752586105,5.72903794223639));
#20807=CARTESIAN_POINT('Ctrl Pts',(2.94224037595603,-1.94239508066396,5.85586521574462));
#20808=CARTESIAN_POINT('Ctrl Pts',(5.55462883997521,-2.86179770889484,5.98269248925282));
#20809=CARTESIAN_POINT('Ctrl Pts',(7.7463797396693,-1.16884092461813,6.10951976276106));
#20810=CARTESIAN_POINT('Ctrl Pts',(7.51677825340999,1.59107897227123,6.23634703626926));
#20811=CARTESIAN_POINT('Ctrl Pts',(5.07541348034676,2.89860056849218,6.36317430977749));
#20812=CARTESIAN_POINT('Ctrl Pts',(2.6508574206784,1.56016768139483,6.4900015832857));
#20813=CARTESIAN_POINT('Ctrl Pts',(2.45633843220973,-1.20244648690003,6.61682885679392));
#20814=CARTESIAN_POINT('Ctrl Pts',(4.66942095594169,-2.86742108817495,6.74365613030213));
#20815=CARTESIAN_POINT('Ctrl Pts',(7.26991784043513,-1.91490303927604,6.87048340381035));
#20816=CARTESIAN_POINT('Ctrl Pts',(7.8839951517652,0.785612418085389,6.99731067731856));
#20817=CARTESIAN_POINT('Ctrl Pts',(5.95109941710099,2.76899053600824,7.12413795082678));
#20818=CARTESIAN_POINT('Ctrl Pts',(3.23565247176357,2.22472721114061,7.250965224335));
#20819=CARTESIAN_POINT('Ctrl Pts',(2.21641910222577,-0.350352985311341,
7.37779249784321));
#20820=CARTESIAN_POINT('Ctrl Pts',(3.823794870053,-2.6056174533372,7.50461977135142));
#20821=CARTESIAN_POINT('Ctrl Pts',(6.59050513054598,-2.4823737345465,7.63144704485966));
#20822=CARTESIAN_POINT('Ctrl Pts',(7.9909899644218,-0.0931234525913811,
7.75827431836786));
#20823=CARTESIAN_POINT('Ctrl Pts',(6.74683275736921,2.38113351140325,7.88510159187608));
#20824=CARTESIAN_POINT('Ctrl Pts',(3.99374823177407,2.68179989573667,8.0119288653843));
#20825=CARTESIAN_POINT('Ctrl Pts',(2.2448582101591,0.534415819229491,8.13875613889251));
#20826=CARTESIAN_POINT('Ctrl Pts',(3.09661701045288,-2.10080364522705,8.26558341240074));
#20827=CARTESIAN_POINT('Ctrl Pts',(5.7715063223249,-2.818328452451,8.39241068590894));
#20828=CARTESIAN_POINT('Ctrl Pts',(7.82778393262807,-0.963174262331539,
8.51923795941717));
#20829=CARTESIAN_POINT('Ctrl Pts',(7.38840026749263,1.77120257243064,8.64606523292537));
#20830=CARTESIAN_POINT('Ctrl Pts',(4.85444169640936,2.88875733165284,8.7728925064336));
#20831=CARTESIAN_POINT('Ctrl Pts',(2.53900341250707,1.3693428940367,8.89971977994182));
#20832=CARTESIAN_POINT('Ctrl Pts',(2.55570685593279,-1.40006059304758,9.02654705345002));
#20833=CARTESIAN_POINT('Ctrl Pts',(4.88930447888277,-2.89143472940734,9.15337432695825));
#20834=CARTESIAN_POINT('Ctrl Pts',(7.40959829534611,-1.74339563661343,9.28020160046646));
#20835=CARTESIAN_POINT('Ctrl Pts',(7.81596682804957,0.996082286734809,9.40702887397467));
#20836=CARTESIAN_POINT('Ctrl Pts',(5.73746119405384,2.82629785178745,9.53385614748291));
#20837=CARTESIAN_POINT('Ctrl Pts',(3.07142156655589,2.07655964175948,9.6606834209911));
#20838=CARTESIAN_POINT('Ctrl Pts',(2.25151182272583,-0.568742358732331,
9.78751069449933));
#20839=CARTESIAN_POINT('Ctrl Pts',(4.02617722953086,-2.69487438979598,9.91433796800753));
#20840=CARTESIAN_POINT('Ctrl Pts',(6.77543469351166,-2.36102104047297,10.0411652415158));
#20841=CARTESIAN_POINT('Ctrl Pts',(7.98965589887894,0.128063416899711,10.1679925150239));
#20842=CARTESIAN_POINT('Ctrl Pts',(6.56045282839116,2.50024670475965,10.2948197885321));
#20843=CARTESIAN_POINT('Ctrl Pts',(3.79245727355498,2.59010817689208,10.4216470620404));
#20844=CARTESIAN_POINT('Ctrl Pts',(2.21240230124421,0.315619148361449,10.5484743355487));
#20845=CARTESIAN_POINT('Ctrl Pts',(3.26262330556337,-2.24697964055797,10.6753016090568));
#20846=CARTESIAN_POINT('Ctrl Pts',(5.98443758504871,-2.75844788311353,10.802128882565));
#20847=CARTESIAN_POINT('Ctrl Pts',(7.8932688254564,-0.751899944113938,10.9289561560733));
#20848=CARTESIAN_POINT('Ctrl Pts',(7.24666062741032,1.94101418382779,11.0557834295814));
#20849=CARTESIAN_POINT('Ctrl Pts',(4.63486489090856,2.86209012378437,11.1826107030897));
#20850=CARTESIAN_POINT('Ctrl Pts',(2.4420239047778,1.17055023725741,11.3094379765979));
#20851=CARTESIAN_POINT('Ctrl Pts',(2.66985837145817,-1.58953311711393,11.4362652501061));
#20852=CARTESIAN_POINT('Ctrl Pts',(5.11037160631846,-2.89859113200809,11.5630925236143));
#20853=CARTESIAN_POINT('Ctrl Pts',(7.53580814890384,-1.56177596387239,11.6899197971225));
#20854=CARTESIAN_POINT('Ctrl Pts',(7.73206118220609,1.20082705749807,11.8167470706307));
#20855=CARTESIAN_POINT('Ctrl Pts',(5.52012570729668,2.86700499518553,11.9435743441391));
#20856=CARTESIAN_POINT('Ctrl Pts',(2.9188706246569,1.91657269933589,12.0704016176473));
#20857=CARTESIAN_POINT('Ctrl Pts',(2.30333867231827,-0.784339077085607,
12.1972288911554));
#20858=CARTESIAN_POINT('Ctrl Pts',(4.23442611238473,-2.76744666524104,12.3240561646636));
#20859=CARTESIAN_POINT('Ctrl Pts',(6.95124491673232,-2.22784415223559,12.4508834381719));
#20860=CARTESIAN_POINT('Ctrl Pts',(7.97013296042037,0.352453055628561,12.57771071168));
#20861=CARTESIAN_POINT('Ctrl Pts',(6.9024066677663,1.84748978079073,12.6622622273523));
#20862=CARTESIAN_POINT('Ctrl Pts',(6.17030206810482,2.20491500302837,12.7045379851883));
#20863=CARTESIAN_POINT('Ctrl Pts',(3.75695945986218,1.87097473485327,-5.46964458820123));
#20864=CARTESIAN_POINT('Ctrl Pts',(3.13546125378344,1.42692557039988,-5.42735152948301));
#20865=CARTESIAN_POINT('Ctrl Pts',(2.38058918671353,-0.121088595893445,
-5.34278271292872));
#20866=CARTESIAN_POINT('Ctrl Pts',(3.72353508858527,-2.34769998490586,-5.21593813853836));
#20867=CARTESIAN_POINT('Ctrl Pts',(6.31828566881595,-2.42406271089463,-5.08911086503014));
#20868=CARTESIAN_POINT('Ctrl Pts',(7.79470760802413,-0.29109475463651,-4.96228359152192));
#20869=CARTESIAN_POINT('Ctrl Pts',(6.80597448449539,2.10938672327844,-4.83545631801371));
#20870=CARTESIAN_POINT('Ctrl Pts',(4.25416293546439,2.58340057859856,-4.70862904450549));
#20871=CARTESIAN_POINT('Ctrl Pts',(2.46891552210067,0.699678804292331,-4.58180177099727));
#20872=CARTESIAN_POINT('Ctrl Pts',(3.07974350551026,-1.82299509778206,-4.45497449748906));
#20873=CARTESIAN_POINT('Ctrl Pts',(5.52912854662575,-2.68143311803203,-4.32814722398084));
#20874=CARTESIAN_POINT('Ctrl Pts',(7.58114120343533,-1.09222666094304,-4.20131995047263));
#20875=CARTESIAN_POINT('Ctrl Pts',(7.36264413521682,1.49404381316841,-4.0744926769644));
#20876=CARTESIAN_POINT('Ctrl Pts',(5.07307991610174,2.7164738132014,-3.94766540345619));
#20877=CARTESIAN_POINT('Ctrl Pts',(2.80245638190584,1.45921195711113,-3.82083812994798));
#20878=CARTESIAN_POINT('Ctrl Pts',(2.62348358848939,-1.13008030233899,-3.69401085643976));
#20879=CARTESIAN_POINT('Ctrl Pts',(4.69953625400377,-2.68778880455282,-3.56718358293154));
#20880=CARTESIAN_POINT('Ctrl Pts',(7.13551261283571,-1.79198142789719,-3.44035630942333));
#20881=CARTESIAN_POINT('Ctrl Pts',(7.7077598151996,0.739616547321491,-3.31352903591511));
#20882=CARTESIAN_POINT('Ctrl Pts',(5.89390831747238,2.59606357902733,-3.1867017624069));
#20883=CARTESIAN_POINT('Ctrl Pts',(3.34971189010135,2.08272378455118,-3.05987448889867));
#20884=CARTESIAN_POINT('Ctrl Pts',(2.3976111790275,-0.331806785528213,-2.93304721539046));
#20885=CARTESIAN_POINT('Ctrl Pts',(3.906720494099,-2.443451254866,-2.80621994188224));
#20886=CARTESIAN_POINT('Ctrl Pts',(6.49946658586394,-2.32461913403326,-2.67939266837402));
#20887=CARTESIAN_POINT('Ctrl Pts',(7.80909075150137,-0.0837849222720541,
-2.55256539486581));
#20888=CARTESIAN_POINT('Ctrl Pts',(6.64011749747002,2.23353139200658,-2.42573812135759));
#20889=CARTESIAN_POINT('Ctrl Pts',(4.05963073407268,2.51199404307626,-2.29891084784938));
#20890=CARTESIAN_POINT('Ctrl Pts',(2.42319838311386,0.497411567662471,-2.17208357434116));
#20891=CARTESIAN_POINT('Ctrl Pts',(3.22461906057571,-1.97122738528671,-2.04525630083294));
#20892=CARTESIAN_POINT('Ctrl Pts',(5.7323250373389,-2.64045389329767,-1.91842902732473));
#20893=CARTESIAN_POINT('Ctrl Pts',(7.65718550190721,-0.899372167086362,
-1.79160175381651));
#20894=CARTESIAN_POINT('Ctrl Pts',(7.24211352356873,1.66269118833614,-1.66477448030829));
#20895=CARTESIAN_POINT('Ctrl Pts',(4.86600282575051,2.70698584816805,-1.53794720680008));
#20896=CARTESIAN_POINT('Ctrl Pts',(2.6978589699708,1.28023933756755,-1.41111993329186));
#20897=CARTESIAN_POINT('Ctrl Pts',(2.71684735696714,-1.31515905687775,-1.28429265978365));
#20898=CARTESIAN_POINT('Ctrl Pts',(4.90563465414091,-2.71002949979746,-1.15746538627543));
#20899=CARTESIAN_POINT('Ctrl Pts',(7.26621133064149,-1.63108040963648,-1.03063811276721));
#20900=CARTESIAN_POINT('Ctrl Pts',(7.64375187918689,0.936781837249784,-0.903810839258996));
#20901=CARTESIAN_POINT('Ctrl Pts',(5.69362271420696,2.64951346382921,-0.776983565750779));
#20902=CARTESIAN_POINT('Ctrl Pts',(3.19597701141537,1.94366693085183,-0.650156292242562));
#20903=CARTESIAN_POINT('Ctrl Pts',(2.43076217608045,-0.536433801088405,
-0.523329018734348));
#20904=CARTESIAN_POINT('Ctrl Pts',(4.09649584677037,-2.52685705334372,-0.39650174522613));
#20905=CARTESIAN_POINT('Ctrl Pts',(6.67263203246968,-2.21066765200472,-0.269674471717914));
#20906=CARTESIAN_POINT('Ctrl Pts',(7.80757418542239,0.123504512647947,-0.142847198209698));
#20907=CARTESIAN_POINT('Ctrl Pts',(6.4653033002661,2.34493699094889,-0.0160199247014798));
#20908=CARTESIAN_POINT('Ctrl Pts',(3.87109605189446,2.42582047062467,0.110807348806736));
#20909=CARTESIAN_POINT('Ctrl Pts',(2.39304495160387,0.292321389369155,0.237634622314952));
#20910=CARTESIAN_POINT('Ctrl Pts',(3.3803720957047,-2.10801993954849,0.364461895823169));
#20911=CARTESIAN_POINT('Ctrl Pts',(5.93180715677322,-2.58407929922806,0.491289169331385));
#20912=CARTESIAN_POINT('Ctrl Pts',(7.71830172706644,-0.701291330522815,
0.618116442839602));
#20913=CARTESIAN_POINT('Ctrl Pts',(7.10907460510611,1.82166243414596,0.744943716347819));
#20914=CARTESIAN_POINT('Ctrl Pts',(4.66025182365174,2.68173241375138,0.871770989856034));
#20915=CARTESIAN_POINT('Ctrl Pts',(2.60721334083663,1.09381353267821,0.998598263364254));
#20916=CARTESIAN_POINT('Ctrl Pts',(2.82405192993845,-1.49258056162853,1.12542553687247));
#20917=CARTESIAN_POINT('Ctrl Pts',(5.11282895697391,-2.71648950648634,1.25225281038069));
#20918=CARTESIAN_POINT('Ctrl Pts',(7.38426040612206,-1.46068197481231,1.3790800838889));
#20919=CARTESIAN_POINT('Ctrl Pts',(7.56489597458717,1.12849244499676,1.50590735739712));
#20920=CARTESIAN_POINT('Ctrl Pts',(5.4898445430401,2.68753540182084,1.63273463090533));
#20921=CARTESIAN_POINT('Ctrl Pts',(3.05329315404872,1.79329230646433,1.75956190441355));
#20922=CARTESIAN_POINT('Ctrl Pts',(2.47941996503718,-0.737937226336289,
1.88638917792177));
#20923=CARTESIAN_POINT('Ctrl Pts',(4.29207857412674,-2.59554917496329,2.01321645142998));
#20924=CARTESIAN_POINT('Ctrl Pts',(6.83660423530834,-2.08384364990342,2.1400437249382));
#20925=CARTESIAN_POINT('Ctrl Pts',(7.79025570775473,0.330074794014927,2.26687099844642));
#20926=CARTESIAN_POINT('Ctrl Pts',(6.28250311699098,2.4426882252497,2.39369827195463));
#20927=CARTESIAN_POINT('Ctrl Pts',(3.6896812262926,2.32552155804531,2.52052554546285));
#20928=CARTESIAN_POINT('Ctrl Pts',(2.37861793899785,0.0855290487952711,
2.64735281897107));
#20929=CARTESIAN_POINT('Ctrl Pts',(3.54610243007606,-2.23253767756964,2.77418009247928));
#20930=CARTESIAN_POINT('Ctrl Pts',(6.12640979180747,-2.51265783711412,2.9010073659875));
#20931=CARTESIAN_POINT('Ctrl Pts',(7.76413586594884,-0.499126935720797,
3.02783463949572));
#20932=CARTESIAN_POINT('Ctrl Pts',(6.96430107669211,1.97002629862555,3.15466191300393));
#20933=CARTESIAN_POINT('Ctrl Pts',(4.45702549285675,2.64086348564745,3.28148918651215));
#20934=CARTESIAN_POINT('Ctrl Pts',(2.53104704683569,0.901018547082313,3.40831646002037));
#20935=CARTESIAN_POINT('Ctrl Pts',(2.94447320587293,-1.66131090008331,3.53514373352858));
#20936=CARTESIAN_POINT('Ctrl Pts',(5.3199126139754,-2.7071316319596,3.6619710070368));
#20937=CARTESIAN_POINT('Ctrl Pts',(7.48897248876349,-1.2817781163809,3.78879828054501));
#20938=CARTESIAN_POINT('Ctrl Pts',(7.47165125200432,1.31363193976544,3.91562555405324));
#20939=CARTESIAN_POINT('Ctrl Pts',(5.28376039720189,2.70990805581855,4.04245282756144));
#20940=CARTESIAN_POINT('Ctrl Pts',(2.92249114801181,1.63247549754976,4.16928010106968));
#20941=CARTESIAN_POINT('Ctrl Pts',(2.54330121879797,-0.935143707544964,
4.29610737457787));
#20942=CARTESIAN_POINT('Ctrl Pts',(4.49232981347094,-2.64912764035633,4.4229346480861));
#20943=CARTESIAN_POINT('Ctrl Pts',(6.99042839937408,-1.94488560817054,4.54976192159431));
#20944=CARTESIAN_POINT('Ctrl Pts',(7.75723616205411,0.534723078675424,4.67658919510254));
#20945=CARTESIAN_POINT('Ctrl Pts',(6.09278137737594,2.52621589928772,4.80341646861074));
#20946=CARTESIAN_POINT('Ctrl Pts',(3.51644261983928,2.21168133647635,4.93024374211896));
#20947=CARTESIAN_POINT('Ctrl Pts',(2.38000135259241,-0.121761319962131,
5.05707101562718));
#20948=CARTESIAN_POINT('Ctrl Pts',(3.7208450303904,-2.34405554361875,5.1838982891354));
#20949=CARTESIAN_POINT('Ctrl Pts',(6.3149997883057,-2.42660538779657,5.31072556264361));
#20950=CARTESIAN_POINT('Ctrl Pts',(7.79442103035657,-0.294056168351199,
5.43755283615183));
#20951=CARTESIAN_POINT('Ctrl Pts',(6.80863594194712,2.10691887197262,5.56438010966004));
#20952=CARTESIAN_POINT('Ctrl Pts',(4.25750720254346,2.58461704004224,5.69120738316827));
#20953=CARTESIAN_POINT('Ctrl Pts',(2.46980359764909,0.702977009155337,5.81803465667647));
#20954=CARTESIAN_POINT('Ctrl Pts',(3.07740998219424,-1.82036757021712,5.9448619301847));
#20955=CARTESIAN_POINT('Ctrl Pts',(5.52567979509156,-2.68201036630151,6.07168920369291));
#20956=CARTESIAN_POINT('Ctrl Pts',(7.5797378492509,-1.09541057589074,6.19851647720112));
#20957=CARTESIAN_POINT('Ctrl Pts',(7.36456066731672,1.49112227044299,6.32534375070935));
#20958=CARTESIAN_POINT('Ctrl Pts',(5.07657028668021,2.71650115181121,6.45217102421755));
#20959=CARTESIAN_POINT('Ctrl Pts',(2.80433264196533,1.46215292634553,6.57899829772579));
#20960=CARTESIAN_POINT('Ctrl Pts',(2.62203396239971,-1.12690492859264,6.70582557123398));
#20961=CARTESIAN_POINT('Ctrl Pts',(4.69608351932035,-2.68728046679675,6.83265284474222));
#20962=CARTESIAN_POINT('Ctrl Pts',(7.13320881999005,-1.79460266735062,6.95948011825042));
#20963=CARTESIAN_POINT('Ctrl Pts',(7.70870781825216,0.736257717535846,7.08630739175865));
#20964=CARTESIAN_POINT('Ctrl Pts',(5.89724281454603,2.59503363870986,7.21313466526686));
#20965=CARTESIAN_POINT('Ctrl Pts',(3.35238898581429,2.08496268758856,7.33996193877508));
#20966=CARTESIAN_POINT('Ctrl Pts',(2.39718713689099,-0.328342683184473,
7.4667892122833));
#20967=CARTESIAN_POINT('Ctrl Pts',(3.90358238574292,-2.44192417889846,7.59361648579151));
#20968=CARTESIAN_POINT('Ctrl Pts',(6.4964790031843,-2.32642302717454,7.72044375929973));
#20969=CARTESIAN_POINT('Ctrl Pts',(7.80898087242143,-0.0872731375874623,
7.84727103280795));
#20970=CARTESIAN_POINT('Ctrl Pts',(6.6429856253596,2.23154304068462,7.97409830631615));
#20971=CARTESIAN_POINT('Ctrl Pts',(4.06285873029619,2.51332059507786,8.10092557982439));
#20972=CARTESIAN_POINT('Ctrl Pts',(2.42383960853443,0.500842097480926,8.22775285333259));
#20973=CARTESIAN_POINT('Ctrl Pts',(3.22208817966025,-1.9688243989261,8.35458012684081));
#20974=CARTESIAN_POINT('Ctrl Pts',(5.72893233599315,-2.64127198845061,8.48140740034902));
#20975=CARTESIAN_POINT('Ctrl Pts',(7.65602796881361,-0.902664555254527,
8.60823467385724));
#20976=CARTESIAN_POINT('Ctrl Pts',(7.24424779965137,1.65992992632361,8.73506194736546));
#20977=CARTESIAN_POINT('Ctrl Pts',(4.86948066139391,2.70727629878997,8.86188922087367));
#20978=CARTESIAN_POINT('Ctrl Pts',(2.69950566258259,1.28331636628713,8.9887164943819));
#20979=CARTESIAN_POINT('Ctrl Pts',(2.71515974193331,-1.31210428058311,9.11554376789009));
#20980=CARTESIAN_POINT('Ctrl Pts',(4.90215325166861,-2.70978549380048,9.24237104139833));
#20981=CARTESIAN_POINT('Ctrl Pts',(7.26411409917053,-1.63386991170937,9.36919831490655));
#20982=CARTESIAN_POINT('Ctrl Pts',(7.64495325277734,0.933505191652339,9.49602558841475));
#20983=CARTESIAN_POINT('Ctrl Pts',(5.69702603225222,2.64874072447172,9.62285286192299));
#20984=CARTESIAN_POINT('Ctrl Pts',(3.19847559463885,1.9461034817842,9.74968013543118));
#20985=CARTESIAN_POINT('Ctrl Pts',(2.43007521974548,-0.533012133294348,
9.87650740893942));
#20986=CARTESIAN_POINT('Ctrl Pts',(4.09325043404316,-2.52557370734091,10.0033346824476));
#20987=CARTESIAN_POINT('Ctrl Pts',(6.66979069582002,-2.21269409990892,10.1301619559558));
#20988=CARTESIAN_POINT('Ctrl Pts',(7.80773061716958,0.12001806088582,10.256989229464));
#20989=CARTESIAN_POINT('Ctrl Pts',(6.46831468337235,2.34317315987586,10.3838165029722));
#20990=CARTESIAN_POINT('Ctrl Pts',(3.87421351791502,2.42738924511528,10.5106437764805));
#20991=CARTESIAN_POINT('Ctrl Pts',(2.39342268427494,0.295790937660488,10.6374710499887));
#20992=CARTESIAN_POINT('Ctrl Pts',(3.37766542503081,-2.10581714777185,10.7642983234969));
#20993=CARTESIAN_POINT('Ctrl Pts',(5.92848657148644,-2.58515330920086,10.8911255970051));
#20994=CARTESIAN_POINT('Ctrl Pts',(7.71739888991534,-0.704663169680801,
11.0179528705133));
#20995=CARTESIAN_POINT('Ctrl Pts',(7.11141269993937,1.81907342576453,11.1447801440215));
#20996=CARTESIAN_POINT('Ctrl Pts',(4.66369837750916,2.68228441074656,11.2716074175298));
#20997=CARTESIAN_POINT('Ctrl Pts',(2.60861871965148,1.09701250400869,11.398434691038));
#20998=CARTESIAN_POINT('Ctrl Pts',(2.82213989186371,-1.48967353088191,11.5252619645462));
#20999=CARTESIAN_POINT('Ctrl Pts',(5.10933223066781,-2.71649230815741,11.6520892380544));
#21000=CARTESIAN_POINT('Ctrl Pts',(7.38239504352909,-1.46366017134169,11.7789165115626));
#21001=CARTESIAN_POINT('Ctrl Pts',(7.56631882965092,1.12538723695775,11.9057437850708));
#21002=CARTESIAN_POINT('Ctrl Pts',(5.49334426025409,2.68689051410809,12.0325710585791));
#21003=CARTESIAN_POINT('Ctrl Pts',(3.05550839388582,1.79616743399183,12.1593983320873));
#21004=CARTESIAN_POINT('Ctrl Pts',(2.47864613984498,-0.735064371915841,
12.2862256055955));
#21005=CARTESIAN_POINT('Ctrl Pts',(4.28841645183988,-2.5935867588731,12.4130528791037));
#21006=CARTESIAN_POINT('Ctrl Pts',(6.83455595498352,-2.08788381241227,12.5398801526119));
#21007=CARTESIAN_POINT('Ctrl Pts',(7.78943417253837,0.330310820325419,12.6667074261201));
#21008=CARTESIAN_POINT('Ctrl Pts',(6.78878588200046,1.73142452672881,12.7512589417923));
#21009=CARTESIAN_POINT('Ctrl Pts',(6.10267444952349,2.0663951461543,12.7935346996283));
#21010=CARTESIAN_POINT('Ctrl Pts',(3.8465757765659,1.74555479618898,-5.38064787376115));
#21011=CARTESIAN_POINT('Ctrl Pts',(3.2667394194872,1.33127226510172,-5.33835481504293));
#21012=CARTESIAN_POINT('Ctrl Pts',(2.56246985740446,-0.112971477053206,
-5.25378599848864));
#21013=CARTESIAN_POINT('Ctrl Pts',(3.81539199278459,-2.19032298636925,-5.12694142409827));
#21014=CARTESIAN_POINT('Ctrl Pts',(6.236204650413,-2.26156677182326,-5.00011415059006));
#21015=CARTESIAN_POINT('Ctrl Pts',(7.61365531779766,-0.271581350424303,
-4.87328687708184));
#21016=CARTESIAN_POINT('Ctrl Pts',(6.69120146859492,1.96798494562505,-4.74645960357363));
#21017=CARTESIAN_POINT('Ctrl Pts',(4.31044944377891,2.41022349818302,-4.61963233006541));
#21018=CARTESIAN_POINT('Ctrl Pts',(2.6448752771532,0.652776154521415,-4.4928050565572));
#21019=CARTESIAN_POINT('Ctrl Pts',(3.21475668507646,-1.70079145222239,-4.36597778304898));
#21020=CARTESIAN_POINT('Ctrl Pts',(5.49994831625476,-2.50168447101337,-4.23915050954076));
#21021=CARTESIAN_POINT('Ctrl Pts',(7.41440523980874,-1.01900974450311,-4.11232323603255));
#21022=CARTESIAN_POINT('Ctrl Pts',(7.21055502297941,1.39389126705505,-3.98549596252432));
#21023=CARTESIAN_POINT('Ctrl Pts',(5.07447069783619,2.53437622915167,-3.85866868901612));
#21024=CARTESIAN_POINT('Ctrl Pts',(2.95605737743077,1.36139434859413,-3.73184141550789));
#21025=CARTESIAN_POINT('Ctrl Pts',(2.78908194365509,-1.05432588429969,-3.60501414199968));
#21026=CARTESIAN_POINT('Ctrl Pts',(4.7259673648865,-2.50761410698481,-3.47818686849146));
#21027=CARTESIAN_POINT('Ctrl Pts',(6.99864915868715,-1.67185676956393,-3.35135959498325));
#21028=CARTESIAN_POINT('Ctrl Pts',(7.53253603063915,0.690036689148038,-3.22453232147503));
#21029=CARTESIAN_POINT('Ctrl Pts',(5.84027524140905,2.42203764014914,-3.09770504796681));
#21030=CARTESIAN_POINT('Ctrl Pts',(3.46662786204312,1.94310934484386,-2.9708777744586));
#21031=CARTESIAN_POINT('Ctrl Pts',(2.57835078822135,-0.309564268879482,
-2.84405050095038));
#21032=CARTESIAN_POINT('Ctrl Pts',(3.98629764812545,-2.27965561358574,-2.71722322744216));
#21033=CARTESIAN_POINT('Ctrl Pts',(6.40524018725889,-2.16878934981591,-2.59039595393395));
#21034=CARTESIAN_POINT('Ctrl Pts',(7.62707429380696,-0.0781684381920649,
-2.46356868042573));
#21035=CARTESIAN_POINT('Ctrl Pts',(6.53646262910636,2.08380763306326,-2.33674140691751));
#21036=CARTESIAN_POINT('Ctrl Pts',(4.1289576198505,2.34360366722632,-2.2099141334093));
#21037=CARTESIAN_POINT('Ctrl Pts',(2.60222276574302,0.464067809916839,-2.08308685990108));
#21038=CARTESIAN_POINT('Ctrl Pts',(3.34992057333436,-1.83908705589022,-1.95625958639286));
#21039=CARTESIAN_POINT('Ctrl Pts',(5.68952362281864,-2.46345226993301,-1.82943231288465));
#21040=CARTESIAN_POINT('Ctrl Pts',(7.48535194338934,-0.839083163749716,
-1.70260503937643));
#21041=CARTESIAN_POINT('Ctrl Pts',(7.09810412595198,1.55123344228854,-1.57577776586821));
#21042=CARTESIAN_POINT('Ctrl Pts',(4.88127492586239,2.52552428553024,-1.44895049236));
#21043=CARTESIAN_POINT('Ctrl Pts',(2.85847160533509,1.19441907703585,-1.32212321885178));
#21044=CARTESIAN_POINT('Ctrl Pts',(2.87618711446296,-1.22699796887657,-1.19529594534357));
#21045=CARTESIAN_POINT('Ctrl Pts',(4.91825005269867,-2.52836390735981,-1.06846867183535));
#21046=CARTESIAN_POINT('Ctrl Pts',(7.12058654751004,-1.52174167773256,-0.94164139832713));
#21047=CARTESIAN_POINT('Ctrl Pts',(7.47281883744579,0.873985093723001,-0.814814124818913));
#21048=CARTESIAN_POINT('Ctrl Pts',(5.65341569227946,2.47190453628283,-0.687986851310695));
#21049=CARTESIAN_POINT('Ctrl Pts',(3.32319853088602,1.81337410395784,-0.561159577802478));
#21050=CARTESIAN_POINT('Ctrl Pts',(2.60927952329525,-0.500474205709249,
-0.434332304294264));
#21051=CARTESIAN_POINT('Ctrl Pts',(4.16335149651959,-2.35747034237424,-0.307505030786045));
#21052=CARTESIAN_POINT('Ctrl Pts',(6.56679756707065,-2.06247655345239,-0.18067775727783));
#21053=CARTESIAN_POINT('Ctrl Pts',(7.62565939004391,0.115225443929111,-0.0538504837696133));
#21054=CARTESIAN_POINT('Ctrl Pts',(6.37336702194138,2.18774520845296,0.0729767897386032));
#21055=CARTESIAN_POINT('Ctrl Pts',(3.95306127416843,2.26320670093089,0.199804063246821));
#21056=CARTESIAN_POINT('Ctrl Pts',(2.57409065577204,0.272725758256677,0.326631336755036));
#21057=CARTESIAN_POINT('Ctrl Pts',(3.49523277473707,-1.96670978361953,0.453458610263254));
#21058=CARTESIAN_POINT('Ctrl Pts',(5.8756335492896,-2.41085672108445,0.580285883771469));
#21059=CARTESIAN_POINT('Ctrl Pts',(7.54237127024841,-0.65428058579094,0.707113157279686));
#21060=CARTESIAN_POINT('Ctrl Pts',(6.97398341075674,1.69954812308578,0.833940430787902));
#21061=CARTESIAN_POINT('Ctrl Pts',(4.68931634841942,2.50196370358057,0.960767704296119));
#21062=CARTESIAN_POINT('Ctrl Pts',(2.77390236463867,1.02049024101471,1.08759497780433));
#21063=CARTESIAN_POINT('Ctrl Pts',(2.97620527774305,-1.39252610391526,1.21442225131255));
#21064=CARTESIAN_POINT('Ctrl Pts',(5.11155517986895,-2.53439087044442,1.34124952482077));
#21065=CARTESIAN_POINT('Ctrl Pts',(7.23072225701601,-1.36276582432866,1.46807679832898));
#21066=CARTESIAN_POINT('Ctrl Pts',(7.39924900247276,1.05284446825073,1.5949040718372));
#21067=CARTESIAN_POINT('Ctrl Pts',(5.46329769794598,2.50737769098948,1.72173134534542));
#21068=CARTESIAN_POINT('Ctrl Pts',(3.19007942087056,1.67307977398374,1.84855861885363));
#21069=CARTESIAN_POINT('Ctrl Pts',(2.65467555954479,-0.688469940679736,
1.97538589236185));
#21070=CARTESIAN_POINT('Ctrl Pts',(4.34582342488339,-2.42155771892711,2.10221316587007));
#21071=CARTESIAN_POINT('Ctrl Pts',(6.71977796802145,-1.94415414053259,2.22904043937828));
#21072=CARTESIAN_POINT('Ctrl Pts',(7.6095018486339,0.307948380627944,2.3558677128865));
#21073=CARTESIAN_POINT('Ctrl Pts',(6.20282076564191,2.27894373331201,2.48269498639471));
#21074=CARTESIAN_POINT('Ctrl Pts',(3.78380750872197,2.16963128024559,2.60952225990293));
#21075=CARTESIAN_POINT('Ctrl Pts',(2.56063075138103,0.0797956479886741,
2.73634953341115));
#21076=CARTESIAN_POINT('Ctrl Pts',(3.64985345167457,-2.08288053182072,2.86317680691936));
#21077=CARTESIAN_POINT('Ctrl Pts',(6.05719108537339,-2.34422296413337,2.99000408042758));
#21078=CARTESIAN_POINT('Ctrl Pts',(7.5851329385195,-0.465668189059147,3.11683135393579));
#21079=CARTESIAN_POINT('Ctrl Pts',(6.8389147098402,1.837966483526,3.24365862744402));
#21080=CARTESIAN_POINT('Ctrl Pts',(4.49971320208998,2.4638344054463,3.37048590095223));
#21081=CARTESIAN_POINT('Ctrl Pts',(2.70284184344369,0.840619179412967,3.49731317446045));
#21082=CARTESIAN_POINT('Ctrl Pts',(3.08855416832663,-1.54994568102967,3.62414044796866));
#21083=CARTESIAN_POINT('Ctrl Pts',(5.30475707830057,-2.52566029677176,3.75096772147688));
#21084=CARTESIAN_POINT('Ctrl Pts',(7.32841501291955,-1.19585470451273,3.87779499498509));
#21085=CARTESIAN_POINT('Ctrl Pts',(7.31225489737246,1.22557322136391,4.00462226849332));
#21086=CARTESIAN_POINT('Ctrl Pts',(5.2710283089023,2.52825060432267,4.13144954200153));
#21087=CARTESIAN_POINT('Ctrl Pts',(3.06804566769601,1.52304324656336,4.25827681550975));
#21088=CARTESIAN_POINT('Ctrl Pts',(2.71427456257327,-0.872456775296374,
4.38510408901796));
#21089=CARTESIAN_POINT('Ctrl Pts',(4.53265091366157,-2.47154457631062,4.51193136252618));
#21090=CARTESIAN_POINT('Ctrl Pts',(6.86329059935359,-1.81451108779791,4.63875863603439));
#21091=CARTESIAN_POINT('Ctrl Pts',(7.57869575313083,0.498878160793571,4.76558590954261));
#21092=CARTESIAN_POINT('Ctrl Pts',(6.02581693637731,2.35687216778819,4.89241318305083));
#21093=CARTESIAN_POINT('Ctrl Pts',(3.62218187329969,2.06342228604745,5.01924045655905));
#21094=CARTESIAN_POINT('Ctrl Pts',(2.56192142847576,-0.113599105370537,
5.14606773006726));
#21095=CARTESIAN_POINT('Ctrl Pts',(3.81288226141482,-2.18692284854289,5.27289500357548));
#21096=CARTESIAN_POINT('Ctrl Pts',(6.23313903740525,-2.26393900153788,5.3997222770837));
#21097=CARTESIAN_POINT('Ctrl Pts',(7.61338795073345,-0.274344247120272,
5.52654955059191));
#21098=CARTESIAN_POINT('Ctrl Pts',(6.69368451645931,1.9656825256068,5.65337682410013));
#21099=CARTESIAN_POINT('Ctrl Pts',(4.31356952943847,2.41135841468822,5.78020409760834));
#21100=CARTESIAN_POINT('Ctrl Pts',(2.64570382096195,0.655853265724565,5.90703137111657));
#21101=CARTESIAN_POINT('Ctrl Pts',(3.21257958843244,-1.69834005977028,6.03385864462477));
#21102=CARTESIAN_POINT('Ctrl Pts',(5.49673075020791,-2.50222302370819,6.160685918133));
#21103=CARTESIAN_POINT('Ctrl Pts',(7.4130959588325,-1.02198022716333,6.2875131916412));
#21104=CARTESIAN_POINT('Ctrl Pts',(7.21234308122342,1.39116556861474,6.41434046514944));
#21105=CARTESIAN_POINT('Ctrl Pts',(5.07772709301368,2.53440173513023,6.54116773865764));
#21106=CARTESIAN_POINT('Ctrl Pts',(2.95780786325225,1.36413817129623,6.66799501216586));
#21107=CARTESIAN_POINT('Ctrl Pts',(2.78772949258969,-1.05136337028526,6.79482228567407));
#21108=CARTESIAN_POINT('Ctrl Pts',(4.72274608269899,-2.50713984541855,6.9216495591823));
#21109=CARTESIAN_POINT('Ctrl Pts',(6.99649979954498,-1.67430229542522,7.04847683269051));
#21110=CARTESIAN_POINT('Ctrl Pts',(7.53342048473911,0.686903016986302,7.17530410619872));
#21111=CARTESIAN_POINT('Ctrl Pts',(5.84338621199107,2.42107674141147,7.30213137970695));
#21112=CARTESIAN_POINT('Ctrl Pts',(3.469125499865,1.94519816403651,7.42895865321516));
#21113=CARTESIAN_POINT('Ctrl Pts',(2.57795517155622,-0.306332381057607,
7.55578592672338));
#21114=CARTESIAN_POINT('Ctrl Pts',(3.98336990143284,-2.27823090445972,7.68261320023158));
#21115=CARTESIAN_POINT('Ctrl Pts',(6.40245287582263,-2.17047231980259,7.80944047373982));
#21116=CARTESIAN_POINT('Ctrl Pts',(7.62697178042107,-0.0814228225835379,
7.93626774724802));
#21117=CARTESIAN_POINT('Ctrl Pts',(6.53913849334999,2.08195256996599,8.06309502075624));
#21118=CARTESIAN_POINT('Ctrl Pts',(4.1319692288183,2.34484129441906,8.18992229426447));
#21119=CARTESIAN_POINT('Ctrl Pts',(2.60282100690976,0.467268375732359,8.31674956777266));
#21120=CARTESIAN_POINT('Ctrl Pts',(3.34755934886763,-1.83684515262515,8.44357684128091));
#21121=CARTESIAN_POINT('Ctrl Pts',(5.6863583496614,-2.46421552445023,8.57040411478909));
#21122=CARTESIAN_POINT('Ctrl Pts',(7.48427200499913,-0.842154848177517,
8.69723138829734));
#21123=CARTESIAN_POINT('Ctrl Pts',(7.1000953318101,1.54865728021659,8.82405866180553));
#21124=CARTESIAN_POINT('Ctrl Pts',(4.88451962637846,2.52579526592709,8.95088593531377));
#21125=CARTESIAN_POINT('Ctrl Pts',(2.86000791265811,1.19728983853755,9.07771320882196));
#21126=CARTESIAN_POINT('Ctrl Pts',(2.87461262793382,-1.22414796811865,9.20454048233019));
#21127=CARTESIAN_POINT('Ctrl Pts',(4.91500202445447,-2.52813625819363,9.33136775583841));
#21128=CARTESIAN_POINT('Ctrl Pts',(7.11862990299495,-1.52434418680528,9.45819502934663));
#21129=CARTESIAN_POINT('Ctrl Pts',(7.47393967750512,0.870928096569864,9.58502230285483));
#21130=CARTESIAN_POINT('Ctrl Pts',(5.65659087045061,2.47118359715601,9.71184957636306));
#21131=CARTESIAN_POINT('Ctrl Pts',(3.32552962272182,1.81564732180891,9.83867684987128));
#21132=CARTESIAN_POINT('Ctrl Pts',(2.60863861676512,-0.497281907856358,
9.9655041233795));
#21133=CARTESIAN_POINT('Ctrl Pts',(4.16032363855547,-2.35627302488586,10.0923313968877));
#21134=CARTESIAN_POINT('Ctrl Pts',(6.56414669812838,-2.06436715934487,10.2191586703959));
#21135=CARTESIAN_POINT('Ctrl Pts',(7.62580533546022,0.111972704871926,10.3459859439041));
#21136=CARTESIAN_POINT('Ctrl Pts',(6.37617653835352,2.18609961499206,10.4728132174123));
#21137=CARTESIAN_POINT('Ctrl Pts',(3.95596976227508,2.26467031333847,10.5996404909206));
#21138=CARTESIAN_POINT('Ctrl Pts',(2.57444306730565,0.275962726959528,10.7264677644287));
#21139=CARTESIAN_POINT('Ctrl Pts',(3.49270754449826,-1.96465465498572,10.853295037937));
#21140=CARTESIAN_POINT('Ctrl Pts',(5.87253555792415,-2.4118587352882,10.9801223114452));
#21141=CARTESIAN_POINT('Ctrl Pts',(7.54152895437427,-0.657426395247666,
11.1069495849534));
#21142=CARTESIAN_POINT('Ctrl Pts',(6.97616477246841,1.69713266770127,11.2337768584616));
#21143=CARTESIAN_POINT('Ctrl Pts',(4.69253186410977,2.50247869770875,11.3606041319699));
#21144=CARTESIAN_POINT('Ctrl Pts',(2.77521353452516,1.02347477075997,11.487431405478));
#21145=CARTESIAN_POINT('Ctrl Pts',(2.97442141226926,-1.38981394464989,11.6142586789863));
#21146=CARTESIAN_POINT('Ctrl Pts',(5.10829285501715,-2.53439348430674,11.7410859524945));
#21147=CARTESIAN_POINT('Ctrl Pts',(7.22898193815433,-1.36554437881099,11.8679132260027));
#21148=CARTESIAN_POINT('Ctrl Pts',(7.40057647709575,1.04994741641743,11.9947404995109));
#21149=CARTESIAN_POINT('Ctrl Pts',(5.46656281321151,2.50677603303065,12.1215677730191));
#21150=CARTESIAN_POINT('Ctrl Pts',(3.19214616311474,1.67576216864776,12.2483950465273));
#21151=CARTESIAN_POINT('Ctrl Pts',(2.6539536073717,-0.685789666746076,12.3752223200356));
#21152=CARTESIAN_POINT('Ctrl Pts',(4.34240679129502,-2.41972685250515,12.5020495935438));
#21153=CARTESIAN_POINT('Ctrl Pts',(6.71786699323475,-1.94792347258894,12.628876867052));
#21154=CARTESIAN_POINT('Ctrl Pts',(7.60873538465635,0.30816858502228,12.7557041405602));
#21155=CARTESIAN_POINT('Ctrl Pts',(6.67516509623461,1.6153592726669,12.8402556562324));
#21156=CARTESIAN_POINT('Ctrl Pts',(6.03504683094217,1.92787528928025,12.8825314140684));
#21157=CARTESIAN_POINT('Ctrl Pts',(3.93619209326963,1.62013485752469,-5.29165115932106));
#21158=CARTESIAN_POINT('Ctrl Pts',(3.39801758519098,1.23561895980355,-5.24935810060285));
#21159=CARTESIAN_POINT('Ctrl Pts',(2.74435052809542,-0.104854358212967,
-5.16478928404856));
#21160=CARTESIAN_POINT('Ctrl Pts',(3.90724889698388,-2.03294598783264,-5.03794470965818));
#21161=CARTESIAN_POINT('Ctrl Pts',(6.15412363201007,-2.09907083275189,-4.91111743614997));
#21162=CARTESIAN_POINT('Ctrl Pts',(7.43260302757121,-0.252067946212096,
-4.78429016264175));
#21163=CARTESIAN_POINT('Ctrl Pts',(6.57642845269443,1.82658316797167,-4.65746288913354));
#21164=CARTESIAN_POINT('Ctrl Pts',(4.36673595209344,2.23704641776749,-4.53063561562533));
#21165=CARTESIAN_POINT('Ctrl Pts',(2.82083503220571,0.605873504750498,-4.4038083421171));
#21166=CARTESIAN_POINT('Ctrl Pts',(3.34976986464268,-1.57858780666272,-4.2769810686089));
#21167=CARTESIAN_POINT('Ctrl Pts',(5.47076808588375,-2.32193582399472,-4.15015379510067));
#21168=CARTESIAN_POINT('Ctrl Pts',(7.24766927618217,-0.94579282806317,-4.02332652159245));
#21169=CARTESIAN_POINT('Ctrl Pts',(7.05846591074198,1.29373872094169,-3.89649924808424));
#21170=CARTESIAN_POINT('Ctrl Pts',(5.07586147957067,2.35227864510194,-3.76967197457603));
#21171=CARTESIAN_POINT('Ctrl Pts',(3.10965837295569,1.26357674007712,-3.6428447010678));
#21172=CARTESIAN_POINT('Ctrl Pts',(2.95468029882081,-0.97857146626037,-3.51601742755959));
#21173=CARTESIAN_POINT('Ctrl Pts',(4.75239847576922,-2.32743940941681,-3.38919015405137));
#21174=CARTESIAN_POINT('Ctrl Pts',(6.86178570453861,-1.55173211123067,-3.26236288054317));
#21175=CARTESIAN_POINT('Ctrl Pts',(7.35731224607869,0.640456830974584,-3.13553560703494));
#21176=CARTESIAN_POINT('Ctrl Pts',(5.78664216534575,2.24801170127096,-3.00870833352674));
#21177=CARTESIAN_POINT('Ctrl Pts',(3.58354383398488,1.80349490513657,-2.8818810600185));
#21178=CARTESIAN_POINT('Ctrl Pts',(2.75909039741521,-0.28732175223075,-2.7550537865103));
#21179=CARTESIAN_POINT('Ctrl Pts',(4.0658748021519,-2.11585997230547,-2.62822651300207));
#21180=CARTESIAN_POINT('Ctrl Pts',(6.31101378865387,-2.01295956559857,-2.50139923949386));
#21181=CARTESIAN_POINT('Ctrl Pts',(7.44505783611255,-0.0725519541120768,
-2.37457196598564));
#21182=CARTESIAN_POINT('Ctrl Pts',(6.43280776074269,1.93408387411994,-2.24774469247742));
#21183=CARTESIAN_POINT('Ctrl Pts',(4.19828450562832,2.17521329137638,-2.12091741896921));
#21184=CARTESIAN_POINT('Ctrl Pts',(2.78124714837218,0.430724052171207,-1.99409014546099));
#21185=CARTESIAN_POINT('Ctrl Pts',(3.47522208609301,-1.70694672649373,-1.86726287195277));
#21186=CARTESIAN_POINT('Ctrl Pts',(5.64672220829838,-2.28645064656837,-1.74043559844456));
#21187=CARTESIAN_POINT('Ctrl Pts',(7.31351838487148,-0.778794160413069,
-1.61360832493634));
#21188=CARTESIAN_POINT('Ctrl Pts',(6.95409472833523,1.43977569624093,-1.48678105142812));
#21189=CARTESIAN_POINT('Ctrl Pts',(4.89654702597431,2.34406272289244,-1.35995377791991));
#21190=CARTESIAN_POINT('Ctrl Pts',(3.01908424069936,1.10859881650414,-1.23312650441169));
#21191=CARTESIAN_POINT('Ctrl Pts',(3.03552687195881,-1.1388368808754,-1.10629923090347));
#21192=CARTESIAN_POINT('Ctrl Pts',(4.93086545125642,-2.34669831492216,-0.979471957395263));
#21193=CARTESIAN_POINT('Ctrl Pts',(6.97496176437862,-1.41240294582864,-0.852644683887045));
#21194=CARTESIAN_POINT('Ctrl Pts',(7.30188579570467,0.811188350196216,-0.725817410378829));
#21195=CARTESIAN_POINT('Ctrl Pts',(5.61320867035197,2.29429560873646,-0.598990136870612));
#21196=CARTESIAN_POINT('Ctrl Pts',(3.45042005035666,1.68308127706386,-0.472162863362396));
#21197=CARTESIAN_POINT('Ctrl Pts',(2.78779687051006,-0.464514610330093,
-0.34533558985418));
#21198=CARTESIAN_POINT('Ctrl Pts',(4.2302071462688,-2.18808363140476,-0.218508316345962));
#21199=CARTESIAN_POINT('Ctrl Pts',(6.46096310167163,-1.91428545490006,-0.0916810428377464));
#21200=CARTESIAN_POINT('Ctrl Pts',(7.44374459466541,0.106946375210275,0.0351462306704699));
#21201=CARTESIAN_POINT('Ctrl Pts',(6.28143074361666,2.03055342595704,0.161973504178687));
#21202=CARTESIAN_POINT('Ctrl Pts',(4.0350264964424,2.1005929312371,0.288800777686904));
#21203=CARTESIAN_POINT('Ctrl Pts',(2.75513635994022,0.253130127144199,0.415628051195119));
#21204=CARTESIAN_POINT('Ctrl Pts',(3.61009345376945,-1.82539962769057,0.542455324703337));
#21205=CARTESIAN_POINT('Ctrl Pts',(5.81945994180594,-2.23763414294083,0.669282598211551));
#21206=CARTESIAN_POINT('Ctrl Pts',(7.36644081343039,-0.607269841059064,
0.79610987171977));
#21207=CARTESIAN_POINT('Ctrl Pts',(6.83889221640734,1.5774338120256,0.922937145227985));
#21208=CARTESIAN_POINT('Ctrl Pts',(4.71838087318712,2.32219499340978,1.04976441873621));
#21209=CARTESIAN_POINT('Ctrl Pts',(2.9405913884407,0.947166949351214,1.17659169224442));
#21210=CARTESIAN_POINT('Ctrl Pts',(3.12835862554768,-1.29247164620201,1.30341896575264));
#21211=CARTESIAN_POINT('Ctrl Pts',(5.11028140276398,-2.35229223440248,1.43024623926085));
#21212=CARTESIAN_POINT('Ctrl Pts',(7.07718410790996,-1.26484967384501,1.55707351276907));
#21213=CARTESIAN_POINT('Ctrl Pts',(7.23360203035833,0.977196491504692,1.68390078627729));
#21214=CARTESIAN_POINT('Ctrl Pts',(5.43675085285186,2.32721998015813,1.8107280597855));
#21215=CARTESIAN_POINT('Ctrl Pts',(3.32686568769237,1.55286724150316,1.93755533329372));
#21216=CARTESIAN_POINT('Ctrl Pts',(2.82993115405241,-0.639002655023184,
2.06438260680194));
#21217=CARTESIAN_POINT('Ctrl Pts',(4.39956827564003,-2.24756626289093,2.19120988031016));
#21218=CARTESIAN_POINT('Ctrl Pts',(6.60295170073458,-1.80446463116177,2.31803715381837));
#21219=CARTESIAN_POINT('Ctrl Pts',(7.42874798951307,0.285821967240959,2.44486442732659));
#21220=CARTESIAN_POINT('Ctrl Pts',(6.12313841429284,2.11519924137433,2.5716917008348));
#21221=CARTESIAN_POINT('Ctrl Pts',(3.87793379115134,2.01374100244589,2.69851897434302));
#21222=CARTESIAN_POINT('Ctrl Pts',(2.7426435637642,0.0740622471820766,2.82534624785124));
#21223=CARTESIAN_POINT('Ctrl Pts',(3.75360447327307,-1.93322338607179,2.95217352135945));
#21224=CARTESIAN_POINT('Ctrl Pts',(5.98797237893932,-2.17578809115262,3.07900079486767));
#21225=CARTESIAN_POINT('Ctrl Pts',(7.40613001109016,-0.432209442397493,
3.20582806837589));
#21226=CARTESIAN_POINT('Ctrl Pts',(6.71352834298829,1.70590666842646,3.3326553418841));
#21227=CARTESIAN_POINT('Ctrl Pts',(4.54240091132322,2.28680532524515,3.45948261539232));
#21228=CARTESIAN_POINT('Ctrl Pts',(2.8746366400517,0.780219811743623,3.58630988890054));
#21229=CARTESIAN_POINT('Ctrl Pts',(3.23263513078033,-1.43858046197604,3.71313716240875));
#21230=CARTESIAN_POINT('Ctrl Pts',(5.28960154262576,-2.34418896158393,3.83996443591697));
#21231=CARTESIAN_POINT('Ctrl Pts',(7.16785753707561,-1.10993129264456,3.96679170942518));
#21232=CARTESIAN_POINT('Ctrl Pts',(7.15285854274059,1.13751450296238,4.09361898293341));
#21233=CARTESIAN_POINT('Ctrl Pts',(5.25829622060271,2.3465931528268,4.22044625644161));
#21234=CARTESIAN_POINT('Ctrl Pts',(3.2136001873802,1.41361099557698,4.34727352994984));
#21235=CARTESIAN_POINT('Ctrl Pts',(2.88524790634857,-0.809769843047783,
4.47410080345805));
#21236=CARTESIAN_POINT('Ctrl Pts',(4.57297201385219,-2.2939615122649,4.60092807696627));
#21237=CARTESIAN_POINT('Ctrl Pts',(6.73615279933309,-1.68413656742527,4.72775535047449));
#21238=CARTESIAN_POINT('Ctrl Pts',(7.40015534420757,0.463033242911717,4.8545826239827));
#21239=CARTESIAN_POINT('Ctrl Pts',(5.95885249537868,2.18752843628864,4.98140989749092));
#21240=CARTESIAN_POINT('Ctrl Pts',(3.7279211267601,1.91516323561854,5.10823717099913));
#21241=CARTESIAN_POINT('Ctrl Pts',(2.74384150435911,-0.105436890778946,
5.23506444450736));
#21242=CARTESIAN_POINT('Ctrl Pts',(3.90491949243924,-2.02979015346703,5.36189171801556));
#21243=CARTESIAN_POINT('Ctrl Pts',(6.15127828650479,-2.10127261527921,5.48871899152379));
#21244=CARTESIAN_POINT('Ctrl Pts',(7.43235487111032,-0.25463232588935,5.61554626503199));
#21245=CARTESIAN_POINT('Ctrl Pts',(6.5787330909715,1.82444617924099,5.74237353854023));
#21246=CARTESIAN_POINT('Ctrl Pts',(4.36963185633347,2.23809978933421,5.86920081204843));
#21247=CARTESIAN_POINT('Ctrl Pts',(2.82160404427482,0.608729522293797,5.99602808555666));
#21248=CARTESIAN_POINT('Ctrl Pts',(3.34774919467065,-1.57631254932345,6.12285535906485));
#21249=CARTESIAN_POINT('Ctrl Pts',(5.46778170532425,-2.32243568111486,6.2496826325731));
#21250=CARTESIAN_POINT('Ctrl Pts',(7.2464540684141,-0.948549878435926,6.37650990608129));
#21251=CARTESIAN_POINT('Ctrl Pts',(7.06012549513016,1.2912088667865,6.50333717958953));
#21252=CARTESIAN_POINT('Ctrl Pts',(5.07888389934713,2.35230231844925,6.63016445309772));
#21253=CARTESIAN_POINT('Ctrl Pts',(3.11128308453918,1.26612341624693,6.75699172660596));
#21254=CARTESIAN_POINT('Ctrl Pts',(2.95342502277967,-0.975821811977877,
6.88381900011415));
#21255=CARTESIAN_POINT('Ctrl Pts',(4.74940864607765,-2.32699922404035,7.01064627362239));
#21256=CARTESIAN_POINT('Ctrl Pts',(6.85979077909989,-1.55400192349981,7.13747354713059));
#21257=CARTESIAN_POINT('Ctrl Pts',(7.35813315122608,0.637548316436762,7.26430082063883));
#21258=CARTESIAN_POINT('Ctrl Pts',(5.78952960943609,2.24711984411309,7.39112809414702));
#21259=CARTESIAN_POINT('Ctrl Pts',(3.58586201391573,1.80543364048445,7.51795536765526));
#21260=CARTESIAN_POINT('Ctrl Pts',(2.75872320622145,-0.284322078930742,
7.64478264116346));
#21261=CARTESIAN_POINT('Ctrl Pts',(4.06315741712276,-2.11453763002099,7.77160991467167));
#21262=CARTESIAN_POINT('Ctrl Pts',(6.30842674846097,-2.01452161243064,7.89843718817991));
#21263=CARTESIAN_POINT('Ctrl Pts',(7.44496268842068,-0.0755725075796159,
8.0252644616881));
#21264=CARTESIAN_POINT('Ctrl Pts',(6.4352913613404,1.93236209924735,8.15209173519635));
#21265=CARTESIAN_POINT('Ctrl Pts',(4.20107972734041,2.17636199376026,8.27891900870454));
#21266=CARTESIAN_POINT('Ctrl Pts',(2.78180240528509,0.433694653983792,8.40574628221277));
#21267=CARTESIAN_POINT('Ctrl Pts',(3.47303051807501,-1.7048659063242,8.53257355572097));
#21268=CARTESIAN_POINT('Ctrl Pts',(5.64378436332965,-2.28715906044984,8.6594008292292));
#21269=CARTESIAN_POINT('Ctrl Pts',(7.31251604118465,-0.781645141100505,
8.78622810273741));
#21270=CARTESIAN_POINT('Ctrl Pts',(6.95594286396882,1.43738463410957,8.91305537624562));
#21271=CARTESIAN_POINT('Ctrl Pts',(4.89955859136301,2.34431423306421,9.03988264975386));
#21272=CARTESIAN_POINT('Ctrl Pts',(3.02051016273363,1.11126331078796,9.16670992326206));
#21273=CARTESIAN_POINT('Ctrl Pts',(3.03406551393433,-1.13619165565418,9.29353719677028));
#21274=CARTESIAN_POINT('Ctrl Pts',(4.92785079724033,-2.34648702258678,9.42036447027849));
#21275=CARTESIAN_POINT('Ctrl Pts',(6.9731457068194,-1.4148184619012,9.54719174378672));
#21276=CARTESIAN_POINT('Ctrl Pts',(7.30292610223287,0.808351001487389,9.67401901729492));
#21277=CARTESIAN_POINT('Ctrl Pts',(5.61615570864899,2.29362646984029,9.80084629080315));
#21278=CARTESIAN_POINT('Ctrl Pts',(3.45258365080479,1.68519116183362,9.92767356431137));
#21279=CARTESIAN_POINT('Ctrl Pts',(2.78720201378478,-0.461551682418371,
10.0545008378195));
#21280=CARTESIAN_POINT('Ctrl Pts',(4.22739684306776,-2.1869723424308,10.1813281113278));
#21281=CARTESIAN_POINT('Ctrl Pts',(6.45850270043673,-1.91604021878082,10.308155384836));
#21282=CARTESIAN_POINT('Ctrl Pts',(7.44388005375085,0.103927348858032,10.4349826583442));
#21283=CARTESIAN_POINT('Ctrl Pts',(6.28403839333469,2.02902607010827,10.5618099318524));
#21284=CARTESIAN_POINT('Ctrl Pts',(4.03772600663513,2.10195138156167,10.6886372053606));
#21285=CARTESIAN_POINT('Ctrl Pts',(2.75546345033636,0.25613451625857,10.8154644788688));
#21286=CARTESIAN_POINT('Ctrl Pts',(3.60774966396572,-1.82349216219961,10.9422917523771));
#21287=CARTESIAN_POINT('Ctrl Pts',(5.81658454436188,-2.23856416137554,11.0691190258853));
#21288=CARTESIAN_POINT('Ctrl Pts',(7.3656590188332,-0.61018962081453,11.1959462993935));
#21289=CARTESIAN_POINT('Ctrl Pts',(6.84091684499746,1.57519190963801,11.3227735729017));
#21290=CARTESIAN_POINT('Ctrl Pts',(4.72136535071037,2.32267298467096,11.4496008464099));
#21291=CARTESIAN_POINT('Ctrl Pts',(2.94180834939884,0.94993703751125,11.5764281199182));
#21292=CARTESIAN_POINT('Ctrl Pts',(3.12670293267481,-1.28995435841787,11.7032553934263));
#21293=CARTESIAN_POINT('Ctrl Pts',(5.1072534793665,-2.35229466045606,11.8300826669346));
#21294=CARTESIAN_POINT('Ctrl Pts',(7.07556883277958,-1.26742858628029,11.9569099404428));
#21295=CARTESIAN_POINT('Ctrl Pts',(7.2348341245406,0.97450759587711,12.083737213951));
#21296=CARTESIAN_POINT('Ctrl Pts',(5.43978136616892,2.32666155195322,12.2105644874592));
#21297=CARTESIAN_POINT('Ctrl Pts',(3.32878393234366,1.5553569033037,12.3373917609675));
#21298=CARTESIAN_POINT('Ctrl Pts',(2.8292610748984,-0.636514961576311,12.4642190344756));
#21299=CARTESIAN_POINT('Ctrl Pts',(4.39639713075019,-2.24586694613722,12.5910463079839));
#21300=CARTESIAN_POINT('Ctrl Pts',(6.60117803148594,-1.80796313276562,12.7178735814921));
#21301=CARTESIAN_POINT('Ctrl Pts',(7.42803659677434,0.28602634971914,12.8447008550003));
#21302=CARTESIAN_POINT('Ctrl Pts',(6.56154431046876,1.49929401860499,12.9292523706725));
#21303=CARTESIAN_POINT('Ctrl Pts',(5.96741921236085,1.7893554324062,12.9715281285085));
#21304=CARTESIAN_POINT('',(6.25533271652633,-1.62367300596587,12.7072733567685));
#21305=CARTESIAN_POINT('Ctrl Pts',(6.25666084923699,-1.62473234417576,12.7063625311661));
#21306=CARTESIAN_POINT('Ctrl Pts',(6.30032205070727,-1.60059242823093,12.7063625311661));
#21307=CARTESIAN_POINT('Ctrl Pts',(6.34291068770113,-1.57476837059284,12.7063625311661));
#21308=CARTESIAN_POINT('Ctrl Pts',(6.38431766016846,-1.54728798228453,12.7063625311661));
#21309=CARTESIAN_POINT('Ctrl Pts',(6.44363247708358,-1.50792277144838,12.7063625311661));
#21310=CARTESIAN_POINT('Ctrl Pts',(6.50052383028944,-1.46516132071873,12.7063625311661));
#21311=CARTESIAN_POINT('Ctrl Pts',(6.55492121660405,-1.41935664268984,12.7063625311661));
#21312=CARTESIAN_POINT('Ctrl Pts',(6.61105831717652,-1.37208705877406,12.7063625311661));
#21313=CARTESIAN_POINT('Ctrl Pts',(6.66453998122585,-1.32157607379915,12.7063625311661));
#21314=CARTESIAN_POINT('Ctrl Pts',(6.71526745766364,-1.26816023566171,12.7063625311661));
#21315=CARTESIAN_POINT('Ctrl Pts',(6.74038993745235,-1.24170636079468,12.7063625311661));
#21316=CARTESIAN_POINT('Ctrl Pts',(6.76483652651217,-1.21453928084961,12.706362531166));
#21317=CARTESIAN_POINT('Ctrl Pts',(6.78859267017858,-1.18669594610846,12.706362531166));
#21318=CARTESIAN_POINT('Ctrl Pts',(6.80262589826627,-1.17024833269817,12.706362531166));
#21319=CARTESIAN_POINT('Ctrl Pts',(6.81641816076635,-1.1535646942934,12.7063625311661));
#21320=CARTESIAN_POINT('Ctrl Pts',(6.82996613291959,-1.13665228404755,12.7063625311661));
#21321=CARTESIAN_POINT('Ctrl Pts',(6.84137015391622,-1.122416243453,12.7063625311661));
#21322=CARTESIAN_POINT('Ctrl Pts',(6.85260488848684,-1.10801285918862,12.7063625311661));
#21323=CARTESIAN_POINT('Ctrl Pts',(6.86364697729733,-1.09347496824222,12.7063625311661));
#21324=CARTESIAN_POINT('Ctrl Pts',(6.90963170604025,-1.03293198736804,12.7063625311661));
#21325=CARTESIAN_POINT('Ctrl Pts',(6.95233668874753,-0.96999049639788,12.706362531166));
#21326=CARTESIAN_POINT('Ctrl Pts',(6.99167813852895,-0.905029924872353,
12.706362531166));
#21327=CARTESIAN_POINT('Ctrl Pts',(7.03205889091705,-0.838353257684557,
12.706362531166));
#21328=CARTESIAN_POINT('Ctrl Pts',(7.06889673727258,-0.769548784540488,
12.706362531166));
#21329=CARTESIAN_POINT('Ctrl Pts',(7.10207071012869,-0.698980285508197,
12.706362531166));
#21330=CARTESIAN_POINT('Ctrl Pts',(7.135188177495,-0.628531986357274,12.706362531166));
#21331=CARTESIAN_POINT('Ctrl Pts',(7.16465482357667,-0.556324770439544,
12.706362531166));
#21332=CARTESIAN_POINT('Ctrl Pts',(7.19031105018904,-0.482686730203765,
12.706362531166));
#21333=CARTESIAN_POINT('Ctrl Pts',(7.19984472032834,-0.455323361618091,
12.706362531166));
#21334=CARTESIAN_POINT('Ctrl Pts',(7.20885180882894,-0.427762155343313,
12.706362531166));
#21335=CARTESIAN_POINT('Ctrl Pts',(7.21732248911392,-0.400019139505833,
12.706362531166));
#21336=CARTESIAN_POINT('Ctrl Pts',(7.22131145096394,-0.386954565226427,
12.706362531166));
#21337=CARTESIAN_POINT('Ctrl Pts',(7.2251817406524,-0.373848315982475,12.706362531166));
#21338=CARTESIAN_POINT('Ctrl Pts',(7.22892749257759,-0.360719691257243,
12.706362531166));
#21339=CARTESIAN_POINT('Ctrl Pts',(7.25098092868138,-0.283423785844427,
12.706362531166));
#21340=CARTESIAN_POINT('Ctrl Pts',(7.26876312114318,-0.20521987500682,12.706362531166));
#21341=CARTESIAN_POINT('Ctrl Pts',(7.28215780080698,-0.126489502252328,
12.706362531166));
#21342=CARTESIAN_POINT('Ctrl Pts',(7.29550082974256,-0.0480627187725307,
12.706362531166));
#21343=CARTESIAN_POINT('Ctrl Pts',(7.30449066516009,0.0308874283709469,
12.706362531166));
#21344=CARTESIAN_POINT('Ctrl Pts',(7.30897015665432,0.110012229383381,12.706362531166));
#21345=CARTESIAN_POINT('Ctrl Pts',(7.31197287395277,0.163051599821535,12.706362531166));
#21346=CARTESIAN_POINT('Ctrl Pts',(7.312948053959,0.216170020118987,12.706362531166));
#21347=CARTESIAN_POINT('Ctrl Pts',(7.31183578929012,0.269266404483285,12.706362531166));
#21348=CARTESIAN_POINT('Ctrl Pts',(7.31082231252311,0.317646932491655,12.706362531166));
#21349=CARTESIAN_POINT('Ctrl Pts',(7.30807561817696,0.366009266789958,12.706362531166));
#21350=CARTESIAN_POINT('Ctrl Pts',(7.30364204599346,0.414293597553426,12.706362531166));
#21351=CARTESIAN_POINT('Ctrl Pts',(7.30239041935636,0.42792458223954,12.706362531166));
#21352=CARTESIAN_POINT('Ctrl Pts',(7.30100430601789,0.441549350536377,12.706362531166));
#21353=CARTESIAN_POINT('Ctrl Pts',(7.29948463756176,0.455166553839244,12.706362531166));
#21354=CARTESIAN_POINT('Ctrl Pts',(7.29800012491074,0.468468738597494,12.706362531166));
#21355=CARTESIAN_POINT('Ctrl Pts',(7.29638902328974,0.481755694243806,12.706362531166));
#21356=CARTESIAN_POINT('Ctrl Pts',(7.29465345449701,0.495020590754398,12.706362531166));
#21357=CARTESIAN_POINT('Ctrl Pts',(7.28453102028643,0.572386030142982,12.706362531166));
#21358=CARTESIAN_POINT('Ctrl Pts',(7.27017225257139,0.649059725150864,12.706362531166));
#21359=CARTESIAN_POINT('Ctrl Pts',(7.2518463038517,0.724789641219328,12.706362531166));
#21360=CARTESIAN_POINT('Ctrl Pts',(7.23298733911895,0.802722185842006,12.706362531166));
#21361=CARTESIAN_POINT('Ctrl Pts',(7.20992700069116,0.879655964123195,12.7063625311661));
#21362=CARTESIAN_POINT('Ctrl Pts',(7.18290443834463,0.955323585080013,12.7063625311661));
#21363=CARTESIAN_POINT('Ctrl Pts',(7.15535953714381,1.03245384077628,12.706362531166));
#21364=CARTESIAN_POINT('Ctrl Pts',(7.12369756612586,1.10826938256074,12.7063625311661));
#21365=CARTESIAN_POINT('Ctrl Pts',(7.08811837296769,1.18248233643891,12.7063625311661));
#21366=CARTESIAN_POINT('Ctrl Pts',(7.07816689635174,1.20323965018226,12.7063625311661));
#21367=CARTESIAN_POINT('Ctrl Pts',(7.06790866277265,1.22387151865158,12.7063625311661));
#21368=CARTESIAN_POINT('Ctrl Pts',(7.05734735003915,1.24437143188873,12.7063625311661));
#21369=CARTESIAN_POINT('Ctrl Pts',(7.04849952500069,1.26154539976591,12.7063625311661));
#21370=CARTESIAN_POINT('Ctrl Pts',(7.03943898195409,1.27862675491862,12.7063625311661));
#21371=CARTESIAN_POINT('Ctrl Pts',(7.03016772806532,1.29561159813897,12.7063625311661));
#21372=CARTESIAN_POINT('Ctrl Pts',(7.02341966037244,1.30797398980452,12.7063625311661));
#21373=CARTESIAN_POINT('Ctrl Pts',(7.01656466503568,1.32027661892001,12.7063625311661));
#21374=CARTESIAN_POINT('Ctrl Pts',(7.00960470932485,1.33251686759166,12.7063625311661));
#21375=CARTESIAN_POINT('Ctrl Pts',(6.96795839788621,1.40575888657079,12.7063625311661));
#21376=CARTESIAN_POINT('Ctrl Pts',(6.9225501456431,1.47678283374337,12.7063625311661));
#21377=CARTESIAN_POINT('Ctrl Pts',(6.87362331348931,1.54529429041433,12.7063625311661));
#21378=CARTESIAN_POINT('Ctrl Pts',(6.82436351863789,1.61427198939912,12.7063625311661));
#21379=CARTESIAN_POINT('Ctrl Pts',(6.77153672791292,1.68070382107673,12.7063625311661));
#21380=CARTESIAN_POINT('Ctrl Pts',(6.71534151108349,1.74427364312724,12.7063625311661));
#21381=CARTESIAN_POINT('Ctrl Pts',(6.69873238379939,1.76306241778523,12.7063625311661));
#21382=CARTESIAN_POINT('Ctrl Pts',(6.68182869401359,1.7816010220568,12.7063625311661));
#21383=CARTESIAN_POINT('Ctrl Pts',(6.66463481673223,1.79988084526421,12.7063625311661));
#21384=CARTESIAN_POINT('Ctrl Pts',(6.65367857690042,1.81152906886533,12.7063625311661));
#21385=CARTESIAN_POINT('Ctrl Pts',(6.64261103852896,1.82306524299457,12.7063625311661));
#21386=CARTESIAN_POINT('Ctrl Pts',(6.63143491401651,1.8344862619574,12.7063625311661));
#21387=CARTESIAN_POINT('Ctrl Pts',(6.57115803581338,1.89608394442874,12.7063625311661));
#21388=CARTESIAN_POINT('Ctrl Pts',(6.50771572710583,1.95434495315579,12.7063625311661));
#21389=CARTESIAN_POINT('Ctrl Pts',(6.4413306123096,2.00895641381313,12.7063625311661));
#21390=CARTESIAN_POINT('Ctrl Pts',(6.37554842109209,2.0630718816956,12.7063625311661));
#21391=CARTESIAN_POINT('Ctrl Pts',(6.30687613262566,2.11360466634069,12.7063625311661));
#21392=CARTESIAN_POINT('Ctrl Pts',(6.23548856958003,2.16022201180838,12.7063625311661));
#21393=CARTESIAN_POINT('Ctrl Pts',(6.21355277048793,2.17454647787444,12.7063625311661));
#21394=CARTESIAN_POINT('Ctrl Pts',(6.19136032543429,2.1885009958289,12.7063625311661));
#21395=CARTESIAN_POINT('Ctrl Pts',(6.16891561580437,2.2020751695661,12.7063625311661));
#21396=CARTESIAN_POINT('Ctrl Pts',(6.2322445509742,-1.63799676314545,12.7063625311661));
#21397=CARTESIAN_POINT('Ctrl Pts',(6.23966578565302,-1.63283896134468,12.7066661397002));
#21398=CARTESIAN_POINT('Ctrl Pts',(6.24705196728502,-1.62763072394165,12.7069697482344));
#21399=CARTESIAN_POINT('Ctrl Pts',(6.25440241361523,-1.62237253201659,12.7072733567685));
#21400=CARTESIAN_POINT('Ctrl Pts',(4.0161764580452,-2.20524422515229,-5.29363746883395));
#21401=CARTESIAN_POINT('Ctrl Pts',(3.96415957839439,-2.17411111039703,-5.29363746883395));
#21402=CARTESIAN_POINT('Ctrl Pts',(3.91346144812925,-2.14096669141098,-5.29363746883395));
#21403=CARTESIAN_POINT('Ctrl Pts',(3.86421540032617,-2.10580418894025,-5.29363746883395));
#21404=CARTESIAN_POINT('Ctrl Pts',(3.7946109321332,-2.05610543352749,-5.29363746883395));
#21405=CARTESIAN_POINT('Ctrl Pts',(3.72790538661327,-2.00237606934197,-5.29363746883395));
#21406=CARTESIAN_POINT('Ctrl Pts',(3.66426959291209,-1.94498134030856,-5.29363746883395));
#21407=CARTESIAN_POINT('Ctrl Pts',(3.63249149466555,-1.91631987115769,-5.29363746883395));
#21408=CARTESIAN_POINT('Ctrl Pts',(3.60147957008092,-1.88674383400354,-5.29363746883395));
#21409=CARTESIAN_POINT('Ctrl Pts',(3.57125926033597,-1.85629625244888,-5.29363746883395));
#21410=CARTESIAN_POINT('Ctrl Pts',(3.55712156398471,-1.84205223356612,-5.29363746883395));
#21411=CARTESIAN_POINT('Ctrl Pts',(3.54315715919797,-1.82761745310723,-5.29363746883395));
#21412=CARTESIAN_POINT('Ctrl Pts',(3.52936887534993,-1.81299623318088,-5.29363746883395));
#21413=CARTESIAN_POINT('Ctrl Pts',(3.51960577775136,-1.80264335687485,-5.29363746883395));
#21414=CARTESIAN_POINT('Ctrl Pts',(3.50993238971118,-1.79219841760079,-5.29363746883395));
#21415=CARTESIAN_POINT('Ctrl Pts',(3.5003555839824,-1.7816697380745,-5.29363746883395));
#21416=CARTESIAN_POINT('Ctrl Pts',(3.443365838096,-1.71901557261304,-5.29363746883395));
#21417=CARTESIAN_POINT('Ctrl Pts',(3.38973035102999,-1.65333255407641,-5.29363746883395));
#21418=CARTESIAN_POINT('Ctrl Pts',(3.3396145347394,-1.58497710192186,-5.29363746883395));
#21419=CARTESIAN_POINT('Ctrl Pts',(3.28953311945874,-1.51666857101419,-5.29363746883395));
#21420=CARTESIAN_POINT('Ctrl Pts',(3.24296617947589,-1.44569027005333,-5.29363746883395));
#21421=CARTESIAN_POINT('Ctrl Pts',(3.20012684269656,-1.37237966206277,-5.29363746883395));
#21422=CARTESIAN_POINT('Ctrl Pts',(3.19379617350613,-1.36154603945727,-5.29363746883395));
#21423=CARTESIAN_POINT('Ctrl Pts',(3.18754699922928,-1.35066146707165,-5.29363746883395));
#21424=CARTESIAN_POINT('Ctrl Pts',(3.1813801042914,-1.33972702074568,-5.29363746883395));
#21425=CARTESIAN_POINT('Ctrl Pts',(3.17376606231537,-1.32622665562688,-5.29363746883395));
#21426=CARTESIAN_POINT('Ctrl Pts',(3.1662774447426,-1.31265026282385,-5.29363746883395));
#21427=CARTESIAN_POINT('Ctrl Pts',(3.15891578258334,-1.29899986614287,-5.29363746883395));
#21428=CARTESIAN_POINT('Ctrl Pts',(3.15231892098481,-1.28676760449851,-5.29363746883395));
#21429=CARTESIAN_POINT('Ctrl Pts',(3.14582890907765,-1.27448500477395,-5.29363746883395));
#21430=CARTESIAN_POINT('Ctrl Pts',(3.13944646896944,-1.26215385852175,-5.29363746883395));
#21431=CARTESIAN_POINT('Ctrl Pts',(3.10127090708007,-1.1883970462467,-5.29363746883395));
#21432=CARTESIAN_POINT('Ctrl Pts',(3.06693869563808,-1.11290254769809,-5.29363746883394));
#21433=CARTESIAN_POINT('Ctrl Pts',(3.03661028899585,-1.03600109297847,-5.29363746883395));
#21434=CARTESIAN_POINT('Ctrl Pts',(3.00661636168852,-0.959947752297,-5.29363746883395));
#21435=CARTESIAN_POINT('Ctrl Pts',(2.98053819156754,-0.882517366186935,
-5.29363746883395));
#21436=CARTESIAN_POINT('Ctrl Pts',(2.95858073793476,-0.804021262619071,
-5.29363746883395));
#21437=CARTESIAN_POINT('Ctrl Pts',(2.9372611370858,-0.727805430662714,-5.29363746883395));
#21438=CARTESIAN_POINT('Ctrl Pts',(2.91982628590018,-0.650584114279385,
-5.29363746883395));
#21439=CARTESIAN_POINT('Ctrl Pts',(2.90651258241353,-0.572646792630231,
-5.29363746883395));
#21440=CARTESIAN_POINT('Ctrl Pts',(2.90242099371331,-0.54869496999091,-5.29363746883395));
#21441=CARTESIAN_POINT('Ctrl Pts',(2.89871899161892,-0.524675600344247,
-5.29363746883395));
#21442=CARTESIAN_POINT('Ctrl Pts',(2.89541441031052,-0.500597345162154,
-5.29363746883395));
#21443=CARTESIAN_POINT('Ctrl Pts',(2.89342273847487,-0.48608537580135,-5.29363746883395));
#21444=CARTESIAN_POINT('Ctrl Pts',(2.89157543776742,-0.471552019314399,
-5.29363746883395));
#21445=CARTESIAN_POINT('Ctrl Pts',(2.88987430653294,-0.456999201895081,
-5.29363746883395));
#21446=CARTESIAN_POINT('Ctrl Pts',(2.88843961385479,-0.444725709894666,
-5.29363746883395));
#21447=CARTESIAN_POINT('Ctrl Pts',(2.88710998374673,-0.432447681393096,
-5.29363746883395));
#21448=CARTESIAN_POINT('Ctrl Pts',(2.88588612845473,-0.420167265009195,
-5.29363746883395));
#21449=CARTESIAN_POINT('Ctrl Pts',(2.87814293320273,-0.342470447045378,
-5.29363746883395));
#21450=CARTESIAN_POINT('Ctrl Pts',(2.8746281056688,-0.264664011995165,-5.29363746883395));
#21451=CARTESIAN_POINT('Ctrl Pts',(2.8755201572915,-0.187027918273236,-5.29363746883395));
#21452=CARTESIAN_POINT('Ctrl Pts',(2.87584760148051,-0.1585301418004,-5.29363746883395));
#21453=CARTESIAN_POINT('Ctrl Pts',(2.87676932323159,-0.130055355239279,
-5.29363746883395));
#21454=CARTESIAN_POINT('Ctrl Pts',(2.87829591735836,-0.101617658814265,
-5.29363746883395));
#21455=CARTESIAN_POINT('Ctrl Pts',(2.88255816402082,-0.022219687506853,
-5.29363746883395));
#21456=CARTESIAN_POINT('Ctrl Pts',(2.89153207798952,0.0568907686398899,
-5.29363746883395));
#21457=CARTESIAN_POINT('Ctrl Pts',(2.9050288877662,0.135390588484381,-5.29363746883395));
#21458=CARTESIAN_POINT('Ctrl Pts',(2.91810519077797,0.211444667014056,-5.29363746883395));
#21459=CARTESIAN_POINT('Ctrl Pts',(2.93542774284134,0.286926220129041,-5.29363746883395));
#21460=CARTESIAN_POINT('Ctrl Pts',(2.95686365990608,0.361515460144451,-5.29363746883395));
#21461=CARTESIAN_POINT('Ctrl Pts',(2.9615370009577,0.377776997092935,-5.29363746883395));
#21462=CARTESIAN_POINT('Ctrl Pts',(2.96640746651885,0.394000351614356,-5.29363746883395));
#21463=CARTESIAN_POINT('Ctrl Pts',(2.97146478449135,0.410154161007378,-5.29363746883395));
#21464=CARTESIAN_POINT('Ctrl Pts',(2.99470377368125,0.484382873518835,-5.29363746883395));
#21465=CARTESIAN_POINT('Ctrl Pts',(3.02191236934093,0.557250909909585,-5.29363746883395));
#21466=CARTESIAN_POINT('Ctrl Pts',(3.05288579579963,0.628467523783645,-5.29363746883395));
#21467=CARTESIAN_POINT('Ctrl Pts',(3.08387954778233,0.699730871750787,-5.29363746883395));
#21468=CARTESIAN_POINT('Ctrl Pts',(3.11864373988791,0.769341465886313,-5.29363746883396));
#21469=CARTESIAN_POINT('Ctrl Pts',(3.15701609577644,0.836978638120724,-5.29363746883396));
#21470=CARTESIAN_POINT('Ctrl Pts',(3.19461969513807,0.903260758875702,-5.29363746883396));
#21471=CARTESIAN_POINT('Ctrl Pts',(3.23568904181845,0.967648362437176,-5.29363746883396));
#21472=CARTESIAN_POINT('Ctrl Pts',(3.28010225514524,1.0298008894447,-5.29363746883396));
#21473=CARTESIAN_POINT('Ctrl Pts',(3.29720451409011,1.05373405102749,-5.29363746883396));
#21474=CARTESIAN_POINT('Ctrl Pts',(3.31480287590974,1.07733533248401,-5.29363746883396));
#21475=CARTESIAN_POINT('Ctrl Pts',(3.33289130559999,1.10058341461658,-5.29363746883396));
#21476=CARTESIAN_POINT('Ctrl Pts',(3.34051062023558,1.11037610837029,-5.29363746883396));
#21477=CARTESIAN_POINT('Ctrl Pts',(3.34821707277534,1.12010621186302,-5.29363746883396));
#21478=CARTESIAN_POINT('Ctrl Pts',(3.3560008305098,1.12976079639403,-5.29363746883396));
#21479=CARTESIAN_POINT('Ctrl Pts',(3.40307483513459,1.18814904181068,-5.29363746883396));
#21480=CARTESIAN_POINT('Ctrl Pts',(3.45305491913425,1.24388420374776,-5.29363746883395));
#21481=CARTESIAN_POINT('Ctrl Pts',(3.50578778719035,1.29668117475663,-5.29363746883395));
#21482=CARTESIAN_POINT('Ctrl Pts',(3.55766743438001,1.34862388770958,-5.29363746883395));
#21483=CARTESIAN_POINT('Ctrl Pts',(3.6122121661761,1.39772327576028,-5.29363746883395));
#21484=CARTESIAN_POINT('Ctrl Pts',(3.66930278229164,1.44366593341478,-5.29363746883395));
#21485=CARTESIAN_POINT('Ctrl Pts',(3.72456640762552,1.48813835274063,-5.29363746883395));
#21486=CARTESIAN_POINT('Ctrl Pts',(3.78221616455222,1.52965316492833,-5.29363746883396));
#21487=CARTESIAN_POINT('Ctrl Pts',(3.84216013143835,1.56788041483154,-5.29363746883395));
#21488=CARTESIAN_POINT('Ctrl Pts',(3.87203299659095,1.58693083042519,-5.29363746883395));
#21489=CARTESIAN_POINT('Ctrl Pts',(3.90247582953994,1.60516403142193,-5.29363746883395));
#21490=CARTESIAN_POINT('Ctrl Pts',(3.93347817078402,1.62253437445171,-5.29363746883395));
#21491=CARTESIAN_POINT('Origin',(5.09382715545311,0.,12.7063625311661));
#21492=CARTESIAN_POINT('Origin',(1.8440744744562,0.,-5.29363746883395));
#21493=CARTESIAN_POINT('',(8.34357983645002,-3.97979921880339E-16,-5.29363746883395));
#21494=CARTESIAN_POINT('Origin',(5.09382715545311,0.,-5.29363746883395));
#21495=CARTESIAN_POINT('Origin',(5.09382715545311,0.,-5.79500850830927));
#21496=CARTESIAN_POINT('',(12.124643767714,-8.61026705959731E-16,-6.2963795477846));
#21497=CARTESIAN_POINT('Origin',(5.09382715545311,0.,-6.29637954778459));
#21498=CARTESIAN_POINT('',(10.234111802082,-6.29503313920035E-16,-5.79500850830927));
#21499=CARTESIAN_POINT('Origin',(5.09382715545311,0.,-10.2993262321375));
#21500=CARTESIAN_POINT('',(10.1694090836076,-6.21579516212456E-16,-14.3022729164904));
#21501=CARTESIAN_POINT('',(11.1470264256608,7.41303111086094E-16,-10.2993262321375));
#21502=CARTESIAN_POINT('Origin',(5.09382715545311,0.,-14.3022729164904));
#21503=CARTESIAN_POINT('Origin',(5.09382715545311,0.,-14.3022729164904));
#23561=UNCERTAINTY_MEASURE_WITH_UNIT(LENGTH_MEASURE(0.01),#23578,
'DISTANCE_ACCURACY_VALUE',
'Maximum model space distance between geometric entities at asserted c
onnectivities');
#23566=UNCERTAINTY_MEASURE_WITH_UNIT(LENGTH_MEASURE(0.01),#23578,
'DISTANCE_ACCURACY_VALUE',
'Maximum model space distance between geometric entities at asserted c
onnectivities');
#23572=(
GEOMETRIC_REPRESENTATION_CONTEXT(3)
GLOBAL_UNCERTAINTY_ASSIGNED_CONTEXT((#23561))
GLOBAL_UNIT_ASSIGNED_CONTEXT((#23578,#23580,#23581))
REPRESENTATION_CONTEXT('','3D')
);
#23577=(
GEOMETRIC_REPRESENTATION_CONTEXT(3)
GLOBAL_UNCERTAINTY_ASSIGNED_CONTEXT((#23566))
GLOBAL_UNIT_ASSIGNED_CONTEXT((#23578,#23580,#23581))
REPRESENTATION_CONTEXT('','3D')
);
#23578=(
LENGTH_UNIT()
NAMED_UNIT(*)
SI_UNIT(.MILLI.,.METRE.)
);
#23580=(
NAMED_UNIT(*)
PLANE_ANGLE_UNIT()
SI_UNIT($,.RADIAN.)
);
#23581=(
NAMED_UNIT(*)
SI_UNIT($,.STERADIAN.)
SOLID_ANGLE_UNIT()
);
#23587=SHAPE_DEFINITION_REPRESENTATION(#23597,#23616);
#23597=PRODUCT_DEFINITION_SHAPE('',$,#23627);
#23616=SHAPE_REPRESENTATION('',(#4436),#23572);
#23621=PRODUCT_DEFINITION_CONTEXT('part definition',#23653,'design');
#23627=PRODUCT_DEFINITION('Screw','Screw',#23637,#23621);
#23637=PRODUCT_DEFINITION_FORMATION('',$,#23660);
#23653=APPLICATION_CONTEXT(
'Core Data for Automotive Mechanical Design Process');
#23654=PRODUCT_CONTEXT('part definition',#23653,'mechanical');
#23660=PRODUCT('Screw','Screw',$,(#23654));
#23667=PRESENTATION_STYLE_ASSIGNMENT((#23672));
#23672=SURFACE_STYLE_USAGE(.BOTH.,#23677);
#23677=SURFACE_SIDE_STYLE('',(#23682));
#23682=SURFACE_STYLE_FILL_AREA(#23687);
#23687=FILL_AREA_STYLE('Opaque(151,151,151)',(#23692));
#23692=FILL_AREA_STYLE_COLOUR('Opaque(151,151,151)',#23697);
#23697=COLOUR_RGB('Opaque(151,151,151)', 0.72549020, 0.75294118, 0.79215686);
ENDSEC;
END-ISO-10303-21;
